ISO-10303-21;
HEADER;
FILE_DESCRIPTION (('STEP AP214'),
    '1' );
FILE_NAME ('Material Hold-Down Screw Clamp.step',
    '2026-10-06T22:16:42',
    ( '' ),
    ( '' ),
    'SwSTEP 2.0',
    'SolidWorks 2025',
    '' );
FILE_SCHEMA (( 'AUTOMOTIVE_DESIGN' ));
ENDSEC;

DATA;
#3=CARTESIAN_POINT ( 'NONE',  ( 41.64333658814960870, 63.71518717409399812, 38.42115945441014446 ) ) ;
#7=CARTESIAN_POINT ( 'NONE',  ( 40.27526882409969033, 126.5651871740940209, 37.97664729208901946 ) ) ;
#9=ORIENTED_EDGE ( 'NONE', *, *, #6823, .T. ) ;
#13=CARTESIAN_POINT ( 'NONE',  ( 41.46631938032478359, 107.1844580088725820, 29.45539723777780239 ) ) ;
#14=CARTESIAN_POINT ( 'NONE',  ( 38.58424406990786082, 153.3797705074273097, 34.21067981925357060 ) ) ;
#15=CARTESIAN_POINT ( 'NONE',  ( 44.37947211624943833, 71.47977050742731819, 30.00020018409699318 ) ) ;
#16=CARTESIAN_POINT ( 'NONE',  ( 39.42975644700377558, 122.8151871740940067, 31.60846029578754468 ) ) ;
#18=CARTESIAN_POINT ( 'NONE',  ( 39.92123440845004723, 84.26049967264872009, 29.95742577749337343 ) ) ;
#22=CARTESIAN_POINT ( 'NONE',  ( 44.37947211624943833, 79.01518717409400949, 38.42115945441014446 ) ) ;
#23=CARTESIAN_POINT ( 'NONE',  ( 39.92123440845005433, 82.16049967264872578, 38.46393386101375711 ) ) ;
#24=CARTESIAN_POINT ( 'NONE',  ( 41.46631938032478359, 133.3104996726487457, 38.96596240072933170 ) ) ;
#28=CARTESIAN_POINT ( 'NONE',  ( 44.37947211624943833, 68.47977050742731819, 30.00020018409699318 ) ) ;
#33=CARTESIAN_POINT ( 'NONE',  ( 38.58424406990786082, 150.1151871740939896, 34.21067981925357060 ) ) ;
#35=CARTESIAN_POINT ( 'NONE',  ( 43.01140435219951286, 110.6297705074273097, 29.55568802177586107 ) ) ;
#36=CARTESIAN_POINT ( 'NONE',  ( 47.05648932407426344, 153.9844580088725934, 37.14960608071593384 ) ) ;
#41=CARTESIAN_POINT ( 'NONE',  ( 45.74753988029933538, 116.3297705074272983, 30.44471234641811819 ) ) ;
#43=CARTESIAN_POINT ( 'NONE',  ( 47.43856463449117200, 157.7651871740939953, 32.77220824515698183 ) ) ;
#51=CARTESIAN_POINT ( 'NONE',  ( 43.01140435219954838, 110.9604996726487371, 29.21067981925356705 ) ) ;
#52=CARTESIAN_POINT ( 'NONE',  ( 38.58424406990786082, 90.37977050742732388, 34.21067981925357060 ) ) ;
#55=CARTESIAN_POINT ( 'NONE',  ( 38.58424406990786082, 90.11518717409400381, 34.21067981925357060 ) ) ;
#56=ADVANCED_FACE ( 'NONE', ( #2544 ), #19514, .T. ) ;
#57=ORIENTED_EDGE ( 'NONE', *, *, #21284, .T. ) ;
#60=CARTESIAN_POINT ( 'NONE',  ( 43.01140435219951286, 139.1297705074273097, 38.86567161673127657 ) ) ;
#62=MANIFOLD_SOLID_BREP ( 'Thread1', #3899 ) ;
#63=CARTESIAN_POINT ( 'NONE',  ( 43.01140435219951286, 119.0344580088725621, 29.21067981925356705 ) ) ;
#65=ORIENTED_EDGE ( 'NONE', *, *, #3046, .T. ) ;
#66=CARTESIAN_POINT ( 'NONE',  ( 45.74753988029933538, 145.4297705074273210, 37.97664729208901946 ) ) ;
#69=CARTESIAN_POINT ( 'NONE',  ( 43.01140435219951286, 94.12977050742730967, 38.86567161673127657 ) ) ;
#73=CARTESIAN_POINT ( 'NONE',  ( 45.22503871336621017, 59.11591952901361680, 30.37667785261832165 ) ) ;
#76=CARTESIAN_POINT ( 'NONE',  ( 39.92123440845005433, 122.3344580088725593, 29.95742577749336988 ) ) ;
#78=SHAPE_REPRESENTATION_RELATIONSHIP ( 'NONE' , 'NONE' ,  #6206, #4526 ) ;
#79=CARTESIAN_POINT ( 'NONE',  ( 46.10157429594899270, 144.8344580088725877, 38.46393386101376421 ) ) ;
#80=CARTESIAN_POINT ( 'NONE',  ( 39.42975644700377558, 120.6797705074273210, 36.81289934271958941 ) ) ;
#83=CARTESIAN_POINT ( 'NONE',  ( 44.37947211624943833, 121.0151871740940095, 38.42115945441014446 ) ) ;
#88=EDGE_CURVE ( 'NONE', #2955, #13896, #17623, .T. ) ;
#92=CARTESIAN_POINT ( 'NONE',  ( 41.64333658814960870, 83.77977050742732956, 30.00020018409699318 ) ) ;
#95=ADVANCED_FACE ( 'NONE', ( #19738 ), #13347, .T. ) ;
#97=CARTESIAN_POINT ( 'NONE',  ( 44.55648932407425633, 70.88445800887258486, 29.45539723777780239 ) ) ;
#99=CARTESIAN_POINT ( 'NONE',  ( 38.01140435219952707, 132.7104996726487514, 34.21067981925357060 ) ) ;
#100=CARTESIAN_POINT ( 'NONE',  ( 45.74753988029933538, 89.06518717409399244, 30.44471234641811819 ) ) ;
#104=DIRECTION ( 'NONE',  ( 0.000000000000000000, 1.000000000000000000, 0.000000000000000000 ) ) ;
#105=CARTESIAN_POINT ( 'NONE',  ( 43.01140435219951286, 126.5344580088725621, 39.21067981925356349 ) ) ;
#106=LINE ( 'NONE', #6386, #150 ) ;
#107=CARTESIAN_POINT ( 'NONE',  ( 46.59305225739526435, 152.1797705074273210, 31.60846029578754468 ) ) ;
#108=FACE_OUTER_BOUND ( 'NONE', #17831, .T. ) ;
#110=CARTESIAN_POINT ( 'NONE',  ( 47.43856463449117911, 148.7651871740940237, 32.77220824515697473 ) ) ;
#118=CARTESIAN_POINT ( 'NONE',  ( 44.37947211624943833, 127.0151871740939953, 38.42115945441014446 ) ) ;
#124=CARTESIAN_POINT ( 'NONE',  ( 38.01140435219952707, 98.78445800887259054, 34.21067981925357060 ) ) ;
#125=CARTESIAN_POINT ( 'NONE',  ( 43.01140435219951286, 154.1297705074273097, 38.86567161673127657 ) ) ;
#126=CARTESIAN_POINT ( 'NONE',  ( 38.58424406990784661, 63.52977050742730825, 35.64915139335016647 ) ) ;
#127=CARTESIAN_POINT ( 'NONE',  ( 41.64333658814960870, 114.7151871740940123, 38.42115945441014446 ) ) ;
#129=( BOUNDED_CURVE ( )  B_SPLINE_CURVE ( 2, ( #10581, #5603, #12328, #19063, #3966, #10688, #17395, #4710, #3061, #19486, #17824, #21366, #12765 ),
 .UNSPECIFIED., .F., .F. ) 
 B_SPLINE_CURVE_WITH_KNOTS ( ( 3, 2, 2, 2, 2, 2, 3 ),
 ( 0.2279411764705882304, 0.2294117647058823428, 0.2323529411764705954, 0.2352941176470588203, 0.2382352941176470451, 0.2411764705882352977, 0.2426470588235294101 ),
 .UNSPECIFIED. ) 
 CURVE ( )  GEOMETRIC_REPRESENTATION_ITEM ( )  RATIONAL_B_SPLINE_CURVE ( ( 0.9755282581475768211, 0.9755282581475768211, 1.000000000000000000, 0.9510565162951535312, 1.000000000000000000, 0.9510565162951535312, 1.000000000000000000, 0.9510565162951535312, 1.000000000000000000, 0.9510565162951535312, 1.000000000000000000, 0.9755282581475768211, 0.9755282581475768211 ) ) 
 REPRESENTATION_ITEM ( '' )  );
#130=CARTESIAN_POINT ( 'NONE',  ( 38.96631938032478359, 81.41049967264873999, 31.27175355779120025 ) ) ;
#133=CARTESIAN_POINT ( 'NONE',  ( 45.51140435220141001, 58.78519719078001060, 29.88055280033245964 ) ) ;
#134=CARTESIAN_POINT ( 'NONE',  ( 43.01140435219951286, 78.86518717409400381, 38.86567161673127657 ) ) ;
#135=CARTESIAN_POINT ( 'NONE',  ( 38.96631938032478359, 81.41049967264873999, 31.27175355779120025 ) ) ;
#137=VERTEX_POINT ( 'NONE', #11243 ) ;
#138=CARTESIAN_POINT ( 'NONE',  ( 40.27526882409969033, 65.92977050742732104, 30.44471234641811819 ) ) ;
#143=CARTESIAN_POINT ( 'NONE',  ( 47.43856463449118621, 154.6151871740940180, 34.21067981925357060 ) ) ;
#144=CARTESIAN_POINT ( 'NONE',  ( 38.58424406990785371, 158.9651871740939839, 32.77220824515697473 ) ) ;
#145=CARTESIAN_POINT ( 'NONE',  ( 39.42975644700377558, 117.0797705074273267, 31.60846029578754468 ) ) ;
#150=VECTOR ( 'NONE', #15205, 1000.000000000000000 ) ;
#152=CARTESIAN_POINT ( 'NONE',  ( 47.43856463449117200, 86.02977050742731535, 32.77220824515698183 ) ) ;
#153=CARTESIAN_POINT ( 'NONE',  ( 41.64333658814960870, 152.5151871740940237, 30.00020018409699318 ) ) ;
#162=CARTESIAN_POINT ( 'NONE',  ( 38.58424406990784661, 96.52977050742730114, 35.64915139335016647 ) ) ;
#166=CARTESIAN_POINT ( 'NONE',  ( 47.43856463449117911, 76.76518717409398107, 32.77220824515697473 ) ) ;
#168=DIRECTION ( 'NONE',  ( 0.000000000000000000, 1.000000000000000000, 0.000000000000000000 ) ) ;
#172=CARTESIAN_POINT ( 'NONE',  ( 38.58424406990785371, 141.2297705074273040, 32.77220824515697473 ) ) ;
#174=CARTESIAN_POINT ( 'NONE',  ( 41.64333658814960870, 60.97977050742731109, 38.42115945441014446 ) ) ;
#176=CARTESIAN_POINT ( 'NONE',  ( 44.37947211624943833, 149.4797705074273324, 30.00020018409699318 ) ) ;
#177=CARTESIAN_POINT ( 'NONE',  ( 41.64333658814960870, 63.71518717409399812, 38.42115945441014446 ) ) ;
#182=AXIS2_PLACEMENT_3D ( 'NONE', #12527, #5693, #7365 ) ;
#183=CARTESIAN_POINT ( 'NONE',  ( 48.01140435219951996, 145.1344580088725991, 35.83527830041810347 ) ) ;
#184=CARTESIAN_POINT ( 'NONE',  ( 47.43856463449118621, 118.8797705074273239, 34.21067981925357060 ) ) ;
#186=CARTESIAN_POINT ( 'NONE',  ( 42.21948215057683740, 140.1113394311928744, 29.21067981925357415 ) ) ;
#187=CARTESIAN_POINT ( 'NONE',  ( 46.59305225739526435, 106.3151871740939924, 36.81289934271958941 ) ) ;
#188=DIRECTION ( 'NONE',  ( 0.000000000000000000, 1.000000000000000000, 0.000000000000000000 ) ) ;
#192=EDGE_CURVE ( 'NONE', #1584, #12255, #9504, .T. ) ;
#193=CARTESIAN_POINT ( 'NONE',  ( 40.27526882409969744, 81.82977050742729830, 37.97664729208901235 ) ) ;
#195=ORIENTED_EDGE ( 'NONE', *, *, #5906, .T. ) ;
#198=CARTESIAN_POINT ( 'NONE',  ( 38.96631938032478359, 69.08445800887258770, 37.14960608071593384 ) ) ;
#199=CARTESIAN_POINT ( 'NONE',  ( 46.10157429594899270, 125.6604996726487542, 29.95742577749337343 ) ) ;
#200=CARTESIAN_POINT ( 'NONE',  ( 47.43856463449118621, 85.61518717409400381, 34.21067981925357060 ) ) ;
#204=FACE_OUTER_BOUND ( 'NONE', #7069, .T. ) ;
#207=CARTESIAN_POINT ( 'NONE',  ( 44.55648932407425633, 68.81049967264874567, 29.45539723777780239 ) ) ;
#210=CARTESIAN_POINT ( 'NONE',  ( 38.58424406990786082, 153.3797705074273097, 34.21067981925357060 ) ) ;
#213=CARTESIAN_POINT ( 'NONE',  ( 44.37947211624943833, 143.2151871740940123, 30.00020018409699318 ) ) ;
#217=CARTESIAN_POINT ( 'NONE',  ( 38.58424406990785371, 63.26518717409400239, 35.64915139335015937 ) ) ;
#221=CARTESIAN_POINT ( 'NONE',  ( 47.43856463449117200, 121.4651871740939839, 35.64915139335016647 ) ) ;
#224=CARTESIAN_POINT ( 'NONE',  ( 42.21948215057684450, 114.4575765865522925, 39.21067981925355639 ) ) ;
#226=CARTESIAN_POINT ( 'NONE',  ( 39.92123440845004723, 105.2344580088725507, 38.46393386101376421 ) ) ;
#227=CARTESIAN_POINT ( 'NONE',  ( 46.10157429594899270, 115.7604996726487201, 38.46393386101375711 ) ) ;
#228=CARTESIAN_POINT ( 'NONE',  ( 41.46631938032478359, 156.1104996726487570, 29.45539723777780239 ) ) ;
#229=CARTESIAN_POINT ( 'NONE',  ( 40.27526882409969033, 113.6651871740939868, 30.44471234641811819 ) ) ;
#232=CARTESIAN_POINT ( 'NONE',  ( 41.46631938032478359, 70.31049967264874567, 38.96596240072933170 ) ) ;
#233=CARTESIAN_POINT ( 'NONE',  ( 38.01140435219952707, 74.78445800887257633, 34.21067981925357060 ) ) ;
#236=CARTESIAN_POINT ( 'NONE',  ( 46.59305225739526435, 76.91518717409400097, 31.60846029578754468 ) ) ;
#248=CARTESIAN_POINT ( 'NONE',  ( 45.74753988029933538, 157.1651871740940010, 37.97664729208901946 ) ) ;
#250=CARTESIAN_POINT ( 'NONE',  ( 47.43856463449117911, 119.0297705074273296, 32.77220824515697473 ) ) ;
#252=EDGE_LOOP ( 'NONE', ( #9196, #12169, #13904, #16098 ) ) ;
#254=( BOUNDED_CURVE ( )  B_SPLINE_CURVE ( 2, ( #11919, #6861, #13567, #11591, #1679, #20305, #3331, #8190, #13469, #21744, #9952, #20201, #18648 ),
 .UNSPECIFIED., .F., .F. ) 
 B_SPLINE_CURVE_WITH_KNOTS ( ( 3, 2, 2, 2, 2, 2, 3 ),
 ( 0.5955882352941176405, 0.5970588235294117530, 0.5999999999999999778, 0.6029411764705882026, 0.6058823529411764275, 0.6088235294117646523, 0.6102941176470587648 ),
 .UNSPECIFIED. ) 
 CURVE ( )  GEOMETRIC_REPRESENTATION_ITEM ( )  RATIONAL_B_SPLINE_CURVE ( ( 0.9755282581475768211, 0.9755282581475768211, 1.000000000000000000, 0.9510565162951535312, 1.000000000000000000, 0.9510565162951535312, 1.000000000000000000, 0.9510565162951535312, 1.000000000000000000, 0.9510565162951535312, 1.000000000000000000, 0.9755282581475777093, 0.9755282581475768211 ) ) 
 REPRESENTATION_ITEM ( '' )  );
#256=CARTESIAN_POINT ( 'NONE',  ( 45.74753988029933538, 109.4297705074273210, 37.97664729208901946 ) ) ;
#257=FACE_BOUND ( 'NONE', #16069, .T. ) ;
#258=CARTESIAN_POINT ( 'NONE',  ( 41.46631938032478359, 128.1844580088725820, 29.45539723777780239 ) ) ;
#259=CARTESIAN_POINT ( 'NONE',  ( 43.01140435219951286, 82.12977050742730967, 38.86567161673127657 ) ) ;
#260=CARTESIAN_POINT ( 'NONE',  ( 47.43856463449118621, 145.6151871740939896, 34.21067981925357060 ) ) ;
#263=CARTESIAN_POINT ( 'NONE',  ( 43.01140435219951286, 83.03445800887257633, 29.21067981925356705 ) ) ;
#266=CARTESIAN_POINT ( 'NONE',  ( 48.01140435219951996, 101.2104996726487514, 34.21067981925357060 ) ) ;
#268=EDGE_CURVE ( 'NONE', #2815, #21594, #20508, .T. ) ;
#271=CARTESIAN_POINT ( 'NONE',  ( 44.37947211624943833, 94.27977050742731535, 38.42115945441014446 ) ) ;
#274=CARTESIAN_POINT ( 'NONE',  ( 44.37947211624943833, 82.01518717409400949, 38.42115945441014446 ) ) ;
#279=CARTESIAN_POINT ( 'NONE',  ( 41.46631938032478359, 137.1844580088725820, 29.45539723777780239 ) ) ;
#281=CARTESIAN_POINT ( 'NONE',  ( 47.43856463449118621, 142.8797705074273381, 34.21067981925357060 ) ) ;
#286=CARTESIAN_POINT ( 'NONE',  ( 38.01140435219952707, 119.9344580088725820, 35.83527830041809636 ) ) ;
#288=CARTESIAN_POINT ( 'NONE',  ( 39.42975644700377558, 135.6797705074273210, 36.81289934271958941 ) ) ;
#290=CARTESIAN_POINT ( 'NONE',  ( 39.92123440845005433, 141.2604996726487627, 29.95742577749336988 ) ) ;
#295=CARTESIAN_POINT ( 'NONE',  ( 42.21948215057684450, 108.0373810949689926, 29.21067981925356705 ) ) ;
#298=CARTESIAN_POINT ( 'NONE',  ( 43.01140435219954838, 110.0344580088725763, 29.21067981925356705 ) ) ;
#299=CARTESIAN_POINT ( 'NONE',  ( 38.01140435219951996, 143.9344580088725536, 35.83527830041810347 ) ) ;
#300=CARTESIAN_POINT ( 'NONE',  ( 47.43856463449117200, 127.7297705074272898, 35.64915139335016647 ) ) ;
#302=CARTESIAN_POINT ( 'NONE',  ( 43.01140435219951286, 99.53445800887257633, 39.21067981925356349 ) ) ;
#303=CARTESIAN_POINT ( 'NONE',  ( 40.27526882409969744, 105.5651871740939782, 37.97664729208901235 ) ) ;
#309=CARTESIAN_POINT ( 'NONE',  ( 38.58424406990785371, 90.22977050742731819, 32.77220824515697473 ) ) ;
#310=VERTEX_POINT ( 'NONE', #11904 ) ;
#311=CARTESIAN_POINT ( 'NONE',  ( 43.01140435219954838, 109.4604996726487371, 39.21067981925356349 ) ) ;
#312=CARTESIAN_POINT ( 'NONE',  ( 48.01140435219951996, 76.13445800887258486, 35.83527830041810347 ) ) ;
#313=CARTESIAN_POINT ( 'NONE',  ( 38.01140435219952707, 59.63445800887256354, 32.58608133808903773 ) ) ;
#314=CARTESIAN_POINT ( 'NONE',  ( 44.55648932407425633, 128.8104996726487457, 29.45539723777780239 ) ) ;
#316=CARTESIAN_POINT ( 'NONE',  ( 38.58424406990784661, 87.26518717409399528, 35.64915139335016647 ) ) ;
#321=CARTESIAN_POINT ( 'NONE',  ( 38.01140435219952707, 92.78445800887257633, 34.21067981925357060 ) ) ;
#322=CARTESIAN_POINT ( 'NONE',  ( 48.01140435219951996, 143.0604996726487457, 35.83527830041809636 ) ) ;
#323=CARTESIAN_POINT ( 'NONE',  ( 41.64333658814960870, 149.7797705074273154, 30.00020018409699318 ) ) ;
#324=CARTESIAN_POINT ( 'NONE',  ( 38.58424406990786082, 108.3797705074273239, 34.21067981925357060 ) ) ;
#325=EDGE_CURVE ( 'NONE', #14663, #14927, #19896, .T. ) ;
#327=CARTESIAN_POINT ( 'NONE',  ( 39.42975644700377558, 138.4151871740940010, 36.81289934271958941 ) ) ;
#330=VECTOR ( 'NONE', #1964, 1000.000000000000000 ) ;
#331=CARTESIAN_POINT ( 'NONE',  ( 46.10157429594899270, 90.83445800887255928, 38.46393386101375711 ) ) ;
#335=CARTESIAN_POINT ( 'NONE',  ( 47.43856463449117200, 115.4651871740940123, 35.64915139335016647 ) ) ;
#338=DIRECTION ( 'NONE',  ( 0.000000000000000000, 0.000000000000000000, 1.000000000000000000 ) ) ;
#339=ORIENTED_EDGE ( 'NONE', *, *, #6596, .T. ) ;
#340=CARTESIAN_POINT ( 'NONE',  ( 48.01140435219951996, 97.43445800887256780, 32.58608133808903773 ) ) ;
#341=CARTESIAN_POINT ( 'NONE',  ( 47.43856463449117911, 158.0297705074273438, 32.77220824515697473 ) ) ;
#344=CARTESIAN_POINT ( 'NONE',  ( 46.59305225739526435, 62.17977050742732104, 31.60846029578754468 ) ) ;
#345=CARTESIAN_POINT ( 'NONE',  ( 45.74753988029933538, 118.1651871740939725, 37.97664729208901946 ) ) ;
#347=CARTESIAN_POINT ( 'NONE',  ( 48.01140435219951996, 71.21049967264873715, 34.21067981925357060 ) ) ;
#350=CARTESIAN_POINT ( 'NONE',  ( 42.21948215057684450, 123.0373810949690210, 29.21067981925356705 ) ) ;
#352=CARTESIAN_POINT ( 'NONE',  ( 46.59305225739526435, 73.91518717409400097, 31.60846029578754468 ) ) ;
#356=CARTESIAN_POINT ( 'NONE',  ( 42.21948215057684450, 132.0373810949690210, 29.21067981925355994 ) ) ;
#357=ORIENTED_EDGE ( 'NONE', *, *, #9562, .T. ) ;
#361=ORIENTED_EDGE ( 'NONE', *, *, #11790, .F. ) ;
#362=CARTESIAN_POINT ( 'NONE',  ( 38.58424406990786082, 141.1151871740939896, 34.21067981925357060 ) ) ;
#365=CARTESIAN_POINT ( 'NONE',  ( 46.59305225739526435, 106.5797705074273125, 36.81289934271958941 ) ) ;
#370=CARTESIAN_POINT ( 'NONE',  ( 43.01140435219951996, 10.71049967264875491, 34.21067981925357060 ) ) ;
#372=CARTESIAN_POINT ( 'NONE',  ( 47.43856463449117200, 148.4651871740940123, 35.64915139335016647 ) ) ;
#373=CARTESIAN_POINT ( 'NONE',  ( 43.01140435219951286, 98.96049967264872294, 28.95336869806222779 ) ) ;
#381=CARTESIAN_POINT ( 'NONE',  ( 44.37947211624943833, 89.47977050742731819, 30.00020018409699318 ) ) ;
#384=CARTESIAN_POINT ( 'NONE',  ( 40.27526882409969744, 74.66518717409398675, 30.44471234641812174 ) ) ;
#388=CARTESIAN_POINT ( 'NONE',  ( 43.01140435219951286, 118.4604996726487371, 39.21067981925356349 ) ) ;
#389=CARTESIAN_POINT ( 'NONE',  ( 48.01140435219951996, 122.3604996726487428, 32.58608133808903773 ) ) ;
#390=( BOUNDED_CURVE ( )  B_SPLINE_CURVE ( 2, ( #14473, #19664, #17996, #21660, #9644, #6210, #4442, #6436, #18109, #9860, #13273, #13160, #19889 ),
 .UNSPECIFIED., .F., .F. ) 
 B_SPLINE_CURVE_WITH_KNOTS ( ( 3, 2, 2, 2, 2, 2, 3 ),
 ( 0.8455882352941176405, 0.8470588235294117530, 0.8499999999999999778, 0.8529411764705882026, 0.8558823529411764275, 0.8588235294117646523, 0.8602941176470588758 ),
 .UNSPECIFIED. ) 
 CURVE ( )  GEOMETRIC_REPRESENTATION_ITEM ( )  RATIONAL_B_SPLINE_CURVE ( ( 0.9755282581475768211, 0.9755282581475768211, 1.000000000000000000, 0.9510565162951535312, 1.000000000000000000, 0.9510565162951535312, 1.000000000000000000, 0.9510565162951535312, 1.000000000000000000, 0.9510565162951535312, 1.000000000000000000, 0.9755282581475758219, 0.9755282581475768211 ) ) 
 REPRESENTATION_ITEM ( '' )  );
#391=CARTESIAN_POINT ( 'NONE',  ( 47.43856463449118621, 133.8797705074273381, 34.21067981925357060 ) ) ;
#396=CARTESIAN_POINT ( 'NONE',  ( 41.64333658814960870, 132.9797705074273324, 38.42115945441014446 ) ) ;
#397=ADVANCED_FACE ( 'NONE', ( #5931 ), #9362, .T. ) ;
#398=CARTESIAN_POINT ( 'NONE',  ( 44.37947211624943833, 92.47977050742731819, 30.00020018409699318 ) ) ;
#399=CARTESIAN_POINT ( 'NONE',  ( 40.27526882409969033, 59.66518717409400097, 30.44471234641811819 ) ) ;
#402=CARTESIAN_POINT ( 'NONE',  ( 40.27526882409969033, 93.56518717409397823, 37.97664729208901946 ) ) ;
#403=CARTESIAN_POINT ( 'NONE',  ( 42.21948215057683740, 154.3836182503284817, 39.21067981925355639 ) ) ;
#404=CARTESIAN_POINT ( 'NONE',  ( 42.21948215057684450, 122.1113394311928460, 29.21067981925356705 ) ) ;
#407=CARTESIAN_POINT ( 'NONE',  ( 44.55648932407425633, 145.8844580088725991, 29.45539723777780239 ) ) ;
#408=CARTESIAN_POINT ( 'NONE',  ( 45.74753988029933538, 110.3297705074273125, 30.44471234641811819 ) ) ;
#411=CARTESIAN_POINT ( 'NONE',  ( 39.42975644700377558, 111.4151871740940010, 36.81289934271958941 ) ) ;
#416=CARTESIAN_POINT ( 'NONE',  ( 44.37947211624943833, 88.27977050742731535, 38.42115945441014446 ) ) ;
#419=CARTESIAN_POINT ( 'NONE',  ( 47.05648932407426344, 75.98445800887257917, 37.14960608071593384 ) ) ;
#421=CARTESIAN_POINT ( 'NONE',  ( 44.55648932407425633, 131.8104996726487457, 29.45539723777780239 ) ) ;
#422=CARTESIAN_POINT ( 'NONE',  ( 47.43856463449117200, 88.76518717409399528, 32.77220824515698183 ) ) ;
#426=FACE_OUTER_BOUND ( 'NONE', #6664, .T. ) ;
#427=CARTESIAN_POINT ( 'NONE',  ( 43.01140435219951996, 10.71049967264875491, 39.21067981925356349 ) ) ;
#432=CARTESIAN_POINT ( 'NONE',  ( 46.59305225739526435, 154.5797705074273267, 36.81289934271958941 ) ) ;
#433=CARTESIAN_POINT ( 'NONE',  ( 38.58424406990786082, 105.3797705074273239, 34.21067981925357060 ) ) ;
#435=CARTESIAN_POINT ( 'NONE',  ( 38.58424406990786082, 135.1151871740940180, 34.21067981925357060 ) ) ;
#442=CARTESIAN_POINT ( 'NONE',  ( 38.58424406990786082, 117.1151871740940038, 34.21067981925357060 ) ) ;
#446=ADVANCED_FACE ( 'NONE', ( #16065 ), #9041, .T. ) ;
#447=CARTESIAN_POINT ( 'NONE',  ( 38.96631938032478359, 102.0844580088725877, 37.14960608071593384 ) ) ;
#448=CARTESIAN_POINT ( 'NONE',  ( 39.92123440845004723, 154.1604996726487400, 38.46393386101376421 ) ) ;
#449=CARTESIAN_POINT ( 'NONE',  ( 47.43856463449117200, 115.7651871740939811, 32.77220824515698183 ) ) ;
#451=CARTESIAN_POINT ( 'NONE',  ( 43.01140435219951286, 68.96049967264870872, 28.95336869806222779 ) ) ;
#453=CARTESIAN_POINT ( 'NONE',  ( 47.05648932407426344, 148.5844580088725877, 31.27175355779120025 ) ) ;
#456=CARTESIAN_POINT ( 'NONE',  ( 45.74753988029933538, 80.06518717409397823, 30.44471234641811819 ) ) ;
#463=ORIENTED_EDGE ( 'NONE', *, *, #5564, .F. ) ;
#464=CARTESIAN_POINT ( 'NONE',  ( 43.01140435219951286, 143.3651871740939896, 29.55568802177586463 ) ) ;
#466=CARTESIAN_POINT ( 'NONE',  ( 41.64333658814960870, 102.9797705074273182, 38.42115945441014446 ) ) ;
#470=VERTEX_POINT ( 'NONE', #5719 ) ;
#471=ADVANCED_FACE ( 'NONE', ( #19170 ), #4070, .T. ) ;
#472=CARTESIAN_POINT ( 'NONE',  ( 43.01140435219951996, 10.71049967264875491, 34.21067981925357060 ) ) ;
#473=CARTESIAN_POINT ( 'NONE',  ( 42.21948215057684450, 76.38361825032846752, 39.21067981925355639 ) ) ;
#475=CARTESIAN_POINT ( 'NONE',  ( 41.64333658814960870, 146.5151871740939953, 30.00020018409699318 ) ) ;
#476=CARTESIAN_POINT ( 'NONE',  ( 43.01140435219951286, 97.46049967264873715, 39.46799094044489209 ) ) ;
#483=CARTESIAN_POINT ( 'NONE',  ( 44.37947211624943833, 80.47977050742731819, 30.00020018409699318 ) ) ;
#485=CARTESIAN_POINT ( 'NONE',  ( 43.01140435219951286, 77.36518717409400381, 29.55568802177586107 ) ) ;
#486=DIRECTION ( 'NONE',  ( 0.000000000000000000, 1.000000000000000000, 0.000000000000000000 ) ) ;
#489=ADVANCED_FACE ( 'NONE', ( #5496 ), #2517, .T. ) ;
#492=PLANE ( 'NONE',  #20835 ) ;
#493=CARTESIAN_POINT ( 'NONE',  ( 39.42975644700377558, 135.6797705074273210, 36.81289934271958941 ) ) ;
#495=VERTEX_POINT ( 'NONE', #2413 ) ;
#498=CARTESIAN_POINT ( 'NONE',  ( 46.59305225739526435, 136.5797705074272983, 36.81289934271958941 ) ) ;
#499=CARTESIAN_POINT ( 'NONE',  ( 47.43856463449117200, 92.02977050742730114, 32.77220824515698183 ) ) ;
#501=CARTESIAN_POINT ( 'NONE',  ( 39.92123440845005433, 100.1604996726487258, 38.46393386101375711 ) ) ;
#502=CARTESIAN_POINT ( 'NONE',  ( 43.80332655382220253, 121.9575765865522925, 29.21067981925356705 ) ) ;
#503=CARTESIAN_POINT ( 'NONE',  ( 39.42975644700377558, 98.81518717409400665, 31.60846029578754468 ) ) ;
#505=CARTESIAN_POINT ( 'NONE',  ( 42.21948215057684450, 123.4575765865523067, 39.21067981925355639 ) ) ;
#508=CARTESIAN_POINT ( 'NONE',  ( 41.46631938032478359, 146.1844580088725820, 29.45539723777780239 ) ) ;
#510=CARTESIAN_POINT ( 'NONE',  ( 47.43856463449118621, 115.8797705074273097, 34.21067981925357060 ) ) ;
#511=( BOUNDED_CURVE ( )  B_SPLINE_CURVE ( 2, ( #19906, #21339, #7897, #18468, #16576, #6226, #16693, #1600, #6570, #18355, #3146, #3259, #5025 ),
 .UNSPECIFIED., .F., .F. ) 
 B_SPLINE_CURVE_WITH_KNOTS ( ( 3, 2, 2, 2, 2, 2, 3 ),
 ( 0.7279411764705882026, 0.7294117647058823151, 0.7323529411764705399, 0.7352941176470588758, 0.7382352941176471006, 0.7411764705882353255, 0.7426470588235294379 ),
 .UNSPECIFIED. ) 
 CURVE ( )  GEOMETRIC_REPRESENTATION_ITEM ( )  RATIONAL_B_SPLINE_CURVE ( ( 0.9755282581475768211, 0.9755282581475768211, 1.000000000000000000, 0.9510565162951535312, 1.000000000000000000, 0.9510565162951535312, 1.000000000000000000, 0.9510565162951535312, 1.000000000000000000, 0.9510565162951535312, 1.000000000000000000, 0.9755282581475768211, 0.9755282581475768211 ) ) 
 REPRESENTATION_ITEM ( '' )  );
#513=CARTESIAN_POINT ( 'NONE',  ( 42.21948215057683740, 141.4575765865523351, 39.21067981925357060 ) ) ;
#514=CARTESIAN_POINT ( 'NONE',  ( 44.37947211624943833, 109.0151871740940095, 38.42115945441014446 ) ) ;
#521=CARTESIAN_POINT ( 'NONE',  ( 45.74753988029934249, 80.32977050742731251, 30.44471234641812174 ) ) ;
#523=CARTESIAN_POINT ( 'NONE',  ( 48.01140435219951996, 61.43445800887257491, 32.58608133808903773 ) ) ;
#525=CARTESIAN_POINT ( 'NONE',  ( 41.46631938032478359, 129.1104996726487570, 29.45539723777780239 ) ) ;
#526=CARTESIAN_POINT ( 'NONE',  ( 40.27526882409969033, 84.56518717409397823, 37.97664729208901946 ) ) ;
#531=CARTESIAN_POINT ( 'NONE',  ( 43.01140435219950575, 140.0344580088726332, 29.21067981925357060 ) ) ;
#532=CARTESIAN_POINT ( 'NONE',  ( 47.43856463449118621, 139.8797705074273381, 34.21067981925357060 ) ) ;
#533=CARTESIAN_POINT ( 'NONE',  ( 47.43856463449118621, 100.8797705074273239, 34.21067981925357060 ) ) ;
#535=CARTESIAN_POINT ( 'NONE',  ( 46.59305225739526435, 133.3151871740940067, 36.81289934271958941 ) ) ;
#542=CARTESIAN_POINT ( 'NONE',  ( 39.92123440845005433, 121.1604996726487400, 38.46393386101375711 ) ) ;
#543=CARTESIAN_POINT ( 'NONE',  ( 39.42975644700377558, 116.8151871740940067, 31.60846029578754468 ) ) ;
#547=CARTESIAN_POINT ( 'NONE',  ( 39.92123440845004723, 99.23445800887257917, 38.46393386101376421 ) ) ;
#548=CARTESIAN_POINT ( 'NONE',  ( 40.27526882409969744, 146.9297705074273495, 30.44471234641812174 ) ) ;
#549=CARTESIAN_POINT ( 'NONE',  ( 44.55648932407425633, 158.8104996726487457, 29.45539723777780239 ) ) ;
#550=CARTESIAN_POINT ( 'NONE',  ( 40.27526882409969033, 117.5651871740940067, 37.97664729208901946 ) ) ;
#552=CARTESIAN_POINT ( 'NONE',  ( 46.10157429594899270, 76.76049967264872009, 38.46393386101376421 ) ) ;
#554=CARTESIAN_POINT ( 'NONE',  ( 43.80332655382220253, 135.6113394311928460, 39.21067981925355639 ) ) ;
#555=CARTESIAN_POINT ( 'NONE',  ( 39.92123440845005433, 124.1604996726487400, 38.46393386101375711 ) ) ;
#557=LINE ( 'NONE', #7302, #21391 ) ;
#560=AXIS2_PLACEMENT_3D ( 'NONE', #8557, #13714, #11956 ) ;
#565=CARTESIAN_POINT ( 'NONE',  ( 45.74753988029933538, 142.1651871740940010, 37.97664729208901946 ) ) ;
#568=CARTESIAN_POINT ( 'NONE',  ( 38.58424406990786082, 108.3797705074273239, 34.21067981925357060 ) ) ;
#572=AXIS2_PLACEMENT_3D ( 'NONE', #18716, #10458, #2366 ) ;
#574=CARTESIAN_POINT ( 'NONE',  ( 39.42975644700377558, 111.6797705074273210, 36.81289934271958941 ) ) ;
#575=CARTESIAN_POINT ( 'NONE',  ( 39.92123440845005433, 131.3344580088725593, 29.95742577749336988 ) ) ;
#576=CARTESIAN_POINT ( 'NONE',  ( 46.10157429594899270, 88.76049967264872009, 38.46393386101375711 ) ) ;
#577=CARTESIAN_POINT ( 'NONE',  ( 40.27526882409969033, 81.82977050742729830, 37.97664729208901946 ) ) ;
#578=CARTESIAN_POINT ( 'NONE',  ( 44.37947211624943833, 146.2151871740940123, 30.00020018409699318 ) ) ;
#579=CARTESIAN_POINT ( 'NONE',  ( 48.01140435219951996, 101.2104996726487514, 34.21067981925357060 ) ) ;
#581=CARTESIAN_POINT ( 'NONE',  ( 41.46631938032478359, 60.11049967264874283, 29.45539723777780239 ) ) ;
#585=CARTESIAN_POINT ( 'NONE',  ( 38.96631938032478359, 143.4844580088725650, 31.27175355779120025 ) ) ;
#587=CARTESIAN_POINT ( 'NONE',  ( 48.01140435219951996, 106.1344580088725849, 35.83527830041809636 ) ) ;
#588=EDGE_CURVE ( 'NONE', #6094, #10912, #2565, .T. ) ;
#591=CARTESIAN_POINT ( 'NONE',  ( 38.58424406990784661, 81.22977050742731819, 32.77220824515698183 ) ) ;
#594=CARTESIAN_POINT ( 'NONE',  ( 46.59305225739526435, 82.91518717409400097, 31.60846029578754468 ) ) ;
#596=ORIENTED_EDGE ( 'NONE', *, *, #1004, .F. ) ;
#597=CARTESIAN_POINT ( 'NONE',  ( 38.96631938032478359, 117.4104996726487400, 31.27175355779120025 ) ) ;
#599=CARTESIAN_POINT ( 'NONE',  ( 45.74753988029934249, 133.4297705074273210, 37.97664729208901235 ) ) ;
#605=VECTOR ( 'NONE', #15968, 1000.000000000000000 ) ;
#606=CARTESIAN_POINT ( 'NONE',  ( 38.58424406990784661, 138.2297705074273324, 32.77220824515698183 ) ) ;
#607=CARTESIAN_POINT ( 'NONE',  ( 47.43856463449118621, 91.87977050742732388, 34.21067981925357060 ) ) ;
#610=CARTESIAN_POINT ( 'NONE',  ( 39.92123440845005433, 130.1604996726487684, 38.46393386101375711 ) ) ;
#613=CARTESIAN_POINT ( 'NONE',  ( 46.59305225739526435, 94.31518717409399244, 36.81289934271958941 ) ) ;
#614=CARTESIAN_POINT ( 'NONE',  ( 43.01140435219951286, 124.4604996726487371, 39.21067981925356349 ) ) ;
#617=CARTESIAN_POINT ( 'NONE',  ( 47.05648932407426344, 108.9844580088725792, 37.14960608071593384 ) ) ;
#618=EDGE_CURVE ( 'NONE', #16530, #3067, #6233, .T. ) ;
#619=CARTESIAN_POINT ( 'NONE',  ( 44.55648932407425633, 129.6844580088725820, 38.96596240072933170 ) ) ;
#620=CARTESIAN_POINT ( 'NONE',  ( 39.42975644700377558, 114.6797705074273210, 36.81289934271958941 ) ) ;
#623=CARTESIAN_POINT ( 'NONE',  ( 40.27526882409969744, 104.6651871740940010, 30.44471234641812174 ) ) ;
#626=CARTESIAN_POINT ( 'NONE',  ( 42.21948215057684450, 87.03738109496902098, 29.21067981925356705 ) ) ;
#629=CYLINDRICAL_SURFACE ( 'NONE', #11092, 4.999999999999997335 ) ;
#630=CARTESIAN_POINT ( 'NONE',  ( 43.01140435219951286, 73.12977050742730967, 38.86567161673127657 ) ) ;
#634=CARTESIAN_POINT ( 'NONE',  ( 48.01140435219951996, 61.13445800887257775, 35.83527830041810347 ) ) ;
#637=CARTESIAN_POINT ( 'NONE',  ( 44.55648932407425633, 116.8104996726487599, 29.45539723777780239 ) ) ;
#638=CARTESIAN_POINT ( 'NONE',  ( 44.37947211624943833, 74.21518717409399812, 30.00020018409699318 ) ) ;
#640=( BOUNDED_CURVE ( )  B_SPLINE_CURVE ( 2, ( #17679, #2582, #18348, #21774, #1486, #18236, #11620, #1154, #16245, #3251, #11392, #16459, #13390 ),
 .UNSPECIFIED., .F., .F. ) 
 B_SPLINE_CURVE_WITH_KNOTS ( ( 3, 2, 2, 2, 2, 2, 3 ),
 ( 0.6691176470588234837, 0.6705882352941175961, 0.6735294117647059320, 0.6764705882352941568, 0.6794117647058823817, 0.6823529411764706065, 0.6838235294117647189 ),
 .UNSPECIFIED. ) 
 CURVE ( )  GEOMETRIC_REPRESENTATION_ITEM ( )  RATIONAL_B_SPLINE_CURVE ( ( 0.9755282581475768211, 0.9755282581475768211, 1.000000000000000000, 0.9510565162951535312, 1.000000000000000000, 0.9510565162951535312, 1.000000000000000000, 0.9510565162951535312, 1.000000000000000000, 0.9510565162951535312, 1.000000000000000000, 0.9755282581475768211, 0.9755282581475768211 ) ) 
 REPRESENTATION_ITEM ( '' )  );
#642=CARTESIAN_POINT ( 'NONE',  ( 47.05648932407426344, 113.5104996726487485, 31.27175355779120025 ) ) ;
#644=FACE_OUTER_BOUND ( 'NONE', #12393, .T. ) ;
#645=CARTESIAN_POINT ( 'NONE',  ( 39.92123440845004723, 158.3344580088725877, 29.95742577749337343 ) ) ;
#646=CARTESIAN_POINT ( 'NONE',  ( 44.37947211624943833, 142.2797705074273154, 38.42115945441014446 ) ) ;
#647=CARTESIAN_POINT ( 'NONE',  ( 43.01140435219951286, 107.6297705074272955, 29.55568802177586463 ) ) ;
#649=CARTESIAN_POINT ( 'NONE',  ( 40.27526882409969744, 132.5651871740939782, 37.97664729208901235 ) ) ;
#655=CARTESIAN_POINT ( 'NONE',  ( 47.43856463449117200, 118.7651871740940237, 32.77220824515698183 ) ) ;
#659=CARTESIAN_POINT ( 'NONE',  ( 38.96631938032478359, 95.48445800887257917, 31.27175355779120025 ) ) ;
#662=CARTESIAN_POINT ( 'NONE',  ( 38.96631938032478359, 157.0104996726487343, 37.14960608071593384 ) ) ;
#663=CARTESIAN_POINT ( 'NONE',  ( 47.43856463449117200, 103.4651871740939839, 35.64915139335016647 ) ) ;
#665=CARTESIAN_POINT ( 'NONE',  ( 43.01140435219951286, 76.46049967264872294, 39.46799094044489209 ) ) ;
#671=CARTESIAN_POINT ( 'NONE',  ( 39.42975644700377558, 68.81518717409400665, 31.60846029578754468 ) ) ;
#679=CARTESIAN_POINT ( 'NONE',  ( 47.43856463449117200, 148.4651871740940123, 35.64915139335016647 ) ) ;
#680=CARTESIAN_POINT ( 'NONE',  ( 38.58424406990786082, 156.1151871740940180, 34.21067981925357060 ) ) ;
#681=CARTESIAN_POINT ( 'NONE',  ( 47.43856463449118621, 109.8797705074273239, 34.21067981925357060 ) ) ;
#687=CARTESIAN_POINT ( 'NONE',  ( 48.01140435219951996, 118.2844580088725763, 34.21067981925357060 ) ) ;
#688=CARTESIAN_POINT ( 'NONE',  ( 47.05648932407426344, 88.91049967264873999, 37.14960608071593384 ) ) ;
#689=CARTESIAN_POINT ( 'NONE',  ( 38.58424406990786082, 147.1151871740939896, 34.21067981925357060 ) ) ;
#690=CARTESIAN_POINT ( 'NONE',  ( 46.10157429594899270, 97.76049967264872009, 38.46393386101376421 ) ) ;
#693=EDGE_CURVE ( 'NONE', #7475, #16674, #7926, .T. ) ;
#695=CARTESIAN_POINT ( 'NONE',  ( 43.01140435219951996, 158.9604996726487514, 29.21067981925357060 ) ) ;
#698=CARTESIAN_POINT ( 'NONE',  ( 47.43856463449118621, 148.6151871740939896, 34.21067981925357060 ) ) ;
#699=ORIENTED_EDGE ( 'NONE', *, *, #16016, .T. ) ;
#700=CARTESIAN_POINT ( 'NONE',  ( 47.43856463449118621, 82.87977050742730967, 34.21067981925357060 ) ) ;
#702=CARTESIAN_POINT ( 'NONE',  ( 45.74753988029934249, 67.16518717409400097, 37.97664729208901235 ) ) ;
#708=CARTESIAN_POINT ( 'NONE',  ( 41.46631938032478359, 105.3844580088725849, 38.96596240072933170 ) ) ;
#709=CARTESIAN_POINT ( 'NONE',  ( 46.59305225739526435, 137.1797705074273210, 31.60846029578754468 ) ) ;
#711=VERTEX_POINT ( 'NONE', #6143 ) ;
#712=EDGE_CURVE ( 'NONE', #6431, #3596, #14744, .T. ) ;
#713=CARTESIAN_POINT ( 'NONE',  ( 43.01140435219953417, 140.9604996726487514, 29.21067981925357060 ) ) ;
#715=CARTESIAN_POINT ( 'NONE',  ( 43.01140435219951286, 139.1297705074272812, 38.86567161673127657 ) ) ;
#716=CARTESIAN_POINT ( 'NONE',  ( 47.05648932407426344, 133.9104996726487400, 37.14960608071593384 ) ) ;
#717=CARTESIAN_POINT ( 'NONE',  ( 38.58424406990786082, 93.37977050742732388, 34.21067981925357060 ) ) ;
#718=CARTESIAN_POINT ( 'NONE',  ( 48.01140435219951996, 155.2104996726487514, 34.21067981925357060 ) ) ;
#719=EDGE_CURVE ( 'NONE', #19361, #7226, #16390, .T. ) ;
#721=CARTESIAN_POINT ( 'NONE',  ( 43.01140435219951286, 120.5344580088725763, 39.21067981925356349 ) ) ;
#723=CARTESIAN_POINT ( 'NONE',  ( 47.43856463449117200, 100.7651871740939953, 32.77220824515698183 ) ) ;
#725=CARTESIAN_POINT ( 'NONE',  ( 43.01140435219951286, 125.9604996726487514, 29.21067981925356705 ) ) ;
#728=CARTESIAN_POINT ( 'NONE',  ( 48.01140435219951996, 71.36049967264874283, 32.58608133808903773 ) ) ;
#729=CARTESIAN_POINT ( 'NONE',  ( 46.10157429594899270, 136.7344580088725365, 29.95742577749337343 ) ) ;
#730=CARTESIAN_POINT ( 'NONE',  ( 40.27526882409969033, 116.9297705074273210, 30.44471234641811819 ) ) ;
#733=CARTESIAN_POINT ( 'NONE',  ( 39.42975644700377558, 95.81518717409399244, 31.60846029578754468 ) ) ;
#734=CARTESIAN_POINT ( 'NONE',  ( 43.01140435219951286, 91.46049967264873715, 39.21067981925356349 ) ) ;
#737=CARTESIAN_POINT ( 'NONE',  ( 39.92123440845005433, 87.26049967264874851, 29.95742577749336988 ) ) ;
#740=CARTESIAN_POINT ( 'NONE',  ( 46.59305225739526435, 80.17977050742732104, 31.60846029578754468 ) ) ;
#741=ORIENTED_EDGE ( 'NONE', *, *, #12992, .T. ) ;
#742=EDGE_LOOP ( 'NONE', ( #2278, #4882, #741, #4097, #12117, #6348, #5852, #596 ) ) ;
#744=CARTESIAN_POINT ( 'NONE',  ( 46.10157429594899270, 115.7604996726487343, 38.46393386101376421 ) ) ;
#745=CARTESIAN_POINT ( 'NONE',  ( 45.74753988029933538, 76.16518717409400097, 37.97664729208901946 ) ) ;
#748=CARTESIAN_POINT ( 'NONE',  ( 43.01140435219951286, 112.4604996726487514, 39.21067981925356349 ) ) ;
#750=CARTESIAN_POINT ( 'NONE',  ( 38.01140435219952707, 80.78445800887257633, 34.21067981925357060 ) ) ;
#752=CARTESIAN_POINT ( 'NONE',  ( 41.46631938032478359, 150.3844580088725991, 38.96596240072933170 ) ) ;
#753=CARTESIAN_POINT ( 'NONE',  ( 47.43856463449117200, 143.0297705074273154, 32.77220824515698183 ) ) ;
#755=CARTESIAN_POINT ( 'NONE',  ( 40.27526882409969744, 140.6651871740939725, 30.44471234641812174 ) ) ;
#756=CARTESIAN_POINT ( 'NONE',  ( 38.96631938032478359, 70.01049967264874851, 37.14960608071593384 ) ) ;
#762=CARTESIAN_POINT ( 'NONE',  ( 45.74753988029933538, 103.1651871740940010, 37.97664729208901946 ) ) ;
#768=CARTESIAN_POINT ( 'NONE',  ( 44.55648932407425633, 90.68445800887258201, 38.96596240072933170 ) ) ;
#769=CARTESIAN_POINT ( 'NONE',  ( 47.43856463449118621, 148.8797705074273097, 34.21067981925357060 ) ) ;
#772=CARTESIAN_POINT ( 'NONE',  ( 38.96631938032478359, 145.0104996726487627, 37.14960608071593384 ) ) ;
#773=CARTESIAN_POINT ( 'NONE',  ( 40.27526882409969033, 102.5651871740939782, 37.97664729208901946 ) ) ;
#775=CARTESIAN_POINT ( 'NONE',  ( 44.55648932407425633, 59.81049967264874567, 29.45539723777780239 ) ) ;
#780=CARTESIAN_POINT ( 'NONE',  ( 39.42975644700377558, 66.41518717409400097, 36.81289934271958941 ) ) ;
#787=AXIS2_PLACEMENT_3D ( 'NONE', #2416, #20942, #338 ) ;
#788=CARTESIAN_POINT ( 'NONE',  ( 38.58424406990784661, 146.9651871740940123, 32.77220824515698183 ) ) ;
#789=CARTESIAN_POINT ( 'NONE',  ( 43.01140435219951286, 155.3651871740940180, 29.55568802177586107 ) ) ;
#790=CARTESIAN_POINT ( 'NONE',  ( 38.58424406990785371, 105.5297705074273011, 35.64915139335015937 ) ) ;
#791=ORIENTED_EDGE ( 'NONE', *, *, #18308, .F. ) ;
#795=CARTESIAN_POINT ( 'NONE',  ( 44.55648932407425633, 114.6844580088725820, 38.96596240072933170 ) ) ;
#796=CARTESIAN_POINT ( 'NONE',  ( 47.05648932407426344, 89.51049967264873430, 31.27175355779120025 ) ) ;
#797=CARTESIAN_POINT ( 'NONE',  ( 39.42975644700377558, 78.67977050742732104, 36.81289934271958941 ) ) ;
#798=CARTESIAN_POINT ( 'NONE',  ( 47.43856463449117200, 133.4651871740940123, 35.64915139335016647 ) ) ;
#799=CARTESIAN_POINT ( 'NONE',  ( 38.96631938032478359, 102.4104996726487400, 31.27175355779120025 ) ) ;
#801=CARTESIAN_POINT ( 'NONE',  ( 47.05648932407426344, 119.5104996726487343, 31.27175355779120025 ) ) ;
#806=ORIENTED_EDGE ( 'NONE', *, *, #5935, .F. ) ;
#807=CARTESIAN_POINT ( 'NONE',  ( 45.74753988029933538, 88.42977050742729261, 37.97664729208901946 ) ) ;
#813=CYLINDRICAL_SURFACE ( 'NONE', #17657, 4.999999999999997335 ) ;
#814=CARTESIAN_POINT ( 'NONE',  ( 38.58424406990785371, 135.2297705074273324, 32.77220824515697473 ) ) ;
#817=CARTESIAN_POINT ( 'NONE',  ( 43.80332655382220253, 72.61133943119284595, 39.21067981925355639 ) ) ;
#819=CARTESIAN_POINT ( 'NONE',  ( 39.42975644700377558, 126.0797705074273267, 31.60846029578754468 ) ) ;
#820=CARTESIAN_POINT ( 'NONE',  ( 46.10157429594899270, 144.8344580088725877, 38.46393386101375711 ) ) ;
#821=CARTESIAN_POINT ( 'NONE',  ( 40.27526882409969033, 93.82977050742731251, 37.97664729208901946 ) ) ;
#822=CARTESIAN_POINT ( 'NONE',  ( 43.01140435219951996, 154.4604996726487798, 39.21067981925357060 ) ) ;
#823=CARTESIAN_POINT ( 'NONE',  ( 43.01140435219951286, 100.4604996726487371, 39.21067981925356349 ) ) ;
#824=CARTESIAN_POINT ( 'NONE',  ( 39.92123440845005433, 129.2604996726487343, 29.95742577749336988 ) ) ;
#829=CARTESIAN_POINT ( 'NONE',  ( 47.43856463449117200, 97.76518717409398107, 32.77220824515698183 ) ) ;
#830=CARTESIAN_POINT ( 'NONE',  ( 48.01140435219951996, 74.21049967264873715, 34.21067981925357060 ) ) ;
#833=CARTESIAN_POINT ( 'NONE',  ( 39.92123440845005433, 132.2344580088725650, 38.46393386101375711 ) ) ;
#834=CARTESIAN_POINT ( 'NONE',  ( 48.01140435219951996, 130.1344580088725422, 35.83527830041810347 ) ) ;
#835=CARTESIAN_POINT ( 'NONE',  ( 44.37947211624943833, 115.2797705074273296, 38.42115945441014446 ) ) ;
#838=CARTESIAN_POINT ( 'NONE',  ( 41.64333658814960870, 93.71518717409401233, 38.42115945441014446 ) ) ;
#839=CARTESIAN_POINT ( 'NONE',  ( 38.96631938032478359, 91.01049967264873430, 37.14960608071593384 ) ) ;
#840=ORIENTED_EDGE ( 'NONE', *, *, #12750, .F. ) ;
#841=DIRECTION ( 'NONE',  ( 0.000000000000000000, 1.000000000000000000, 0.000000000000000000 ) ) ;
#845=CARTESIAN_POINT ( 'NONE',  ( 46.59305225739526435, 76.57977050742731251, 36.81289934271958941 ) ) ;
#848=CARTESIAN_POINT ( 'NONE',  ( 38.58424406990786082, 159.3797705074273381, 34.21067981925357060 ) ) ;
#851=CARTESIAN_POINT ( 'NONE',  ( 38.96631938032478359, 120.4104996726487400, 31.27175355779120025 ) ) ;
#852=CARTESIAN_POINT ( 'NONE',  ( 39.42975644700377558, 80.81518717409400665, 31.60846029578754468 ) ) ;
#859=CARTESIAN_POINT ( 'NONE',  ( 47.05648932407426344, 156.9844580088725934, 37.14960608071593384 ) ) ;
#860=CARTESIAN_POINT ( 'NONE',  ( 44.37947211624943833, 140.4797705074273324, 30.00020018409699318 ) ) ;
#862=CARTESIAN_POINT ( 'NONE',  ( 41.64333658814960870, 123.7151871740940123, 38.42115945441014446 ) ) ;
#865=EDGE_CURVE ( 'NONE', #890, #8983, #9337, .T. ) ;
#870=CARTESIAN_POINT ( 'NONE',  ( 42.21948215057684450, 121.3836182503284533, 39.21067981925355639 ) ) ;
#871=CARTESIAN_POINT ( 'NONE',  ( 39.42975644700377558, 104.8151871740939924, 31.60846029578754468 ) ) ;
#872=VERTEX_POINT ( 'NONE', #20055 ) ;
#873=CARTESIAN_POINT ( 'NONE',  ( 44.55648932407425633, 85.61049967264872862, 38.96596240072933170 ) ) ;
#875=CARTESIAN_POINT ( 'NONE',  ( 39.92123440845004723, 96.23445800887257917, 38.46393386101376421 ) ) ;
#876=CARTESIAN_POINT ( 'NONE',  ( 43.01140435219951286, 146.9604996726486945, 28.95336869806222779 ) ) ;
#877=CARTESIAN_POINT ( 'NONE',  ( 47.43856463449117200, 106.7651871740939811, 32.77220824515698183 ) ) ;
#885=CARTESIAN_POINT ( 'NONE',  ( 38.58424406990784661, 71.96518717409399812, 32.77220824515698183 ) ) ;
#887=CARTESIAN_POINT ( 'NONE',  ( 38.01140435219952707, 114.7104996726487371, 34.21067981925357060 ) ) ;
#890=VERTEX_POINT ( 'NONE', #11652 ) ;
#893=CARTESIAN_POINT ( 'NONE',  ( 38.58424406990784661, 132.2651871740939953, 35.64915139335016647 ) ) ;
#894=( BOUNDED_CURVE ( )  B_SPLINE_CURVE ( 2, ( #2570, #4122, #20991, #5548, #8879, #5768, #10532, #13928, #13824, #12275, #5447, #12497, #15586 ),
 .UNSPECIFIED., .F., .F. ) 
 B_SPLINE_CURVE_WITH_KNOTS ( ( 3, 2, 2, 2, 2, 2, 3 ),
 ( 0.7132352941176470784, 0.7147058823529411908, 0.7176470588235294157, 0.7205882352941176405, 0.7235294117647058654, 0.7264705882352940902, 0.7279411764705882026 ),
 .UNSPECIFIED. ) 
 CURVE ( )  GEOMETRIC_REPRESENTATION_ITEM ( )  RATIONAL_B_SPLINE_CURVE ( ( 0.9755282581475768211, 0.9755282581475768211, 1.000000000000000000, 0.9510565162951535312, 1.000000000000000000, 0.9510565162951535312, 1.000000000000000000, 0.9510565162951535312, 1.000000000000000000, 0.9510565162951535312, 1.000000000000000000, 0.9755282581475768211, 0.9755282581475768211 ) ) 
 REPRESENTATION_ITEM ( '' )  );
#895=CARTESIAN_POINT ( 'NONE',  ( 41.64333658814960870, 95.77977050742732956, 30.00020018409699318 ) ) ;
#901=CARTESIAN_POINT ( 'NONE',  ( 44.37947211624943833, 79.27977050742731535, 38.42115945441014446 ) ) ;
#902=CARTESIAN_POINT ( 'NONE',  ( 39.42975644700377558, 131.8151871740940067, 31.60846029578754468 ) ) ;
#903=CARTESIAN_POINT ( 'NONE',  ( 48.01140435219951996, 92.06049967264871725, 35.83527830041810347 ) ) ;
#910=CARTESIAN_POINT ( 'NONE',  ( 44.55648932407425633, 106.8844580088725849, 29.45539723777780239 ) ) ;
#913=CARTESIAN_POINT ( 'NONE',  ( 47.43856463449117200, 71.02977050742730114, 32.77220824515698183 ) ) ;
#921=CARTESIAN_POINT ( 'NONE',  ( 38.01140435219952707, 104.9344580088725820, 35.83527830041809636 ) ) ;
#922=CARTESIAN_POINT ( 'NONE',  ( 41.64333658814960870, 120.9797705074273182, 38.42115945441014446 ) ) ;
#923=ORIENTED_EDGE ( 'NONE', *, *, #17652, .T. ) ;
#924=CARTESIAN_POINT ( 'NONE',  ( 43.80332655382220253, 73.95757658655232092, 29.21067981925356705 ) ) ;
#926=CARTESIAN_POINT ( 'NONE',  ( 46.59305225739526435, 131.1797705074273210, 31.60846029578754468 ) ) ;
#927=CARTESIAN_POINT ( 'NONE',  ( 43.01140435219951286, 134.9604996726487514, 29.21067981925356705 ) ) ;
#930=CARTESIAN_POINT ( 'NONE',  ( 39.92123440845005433, 99.26049967264873430, 29.95742577749336988 ) ) ;
#931=CARTESIAN_POINT ( 'NONE',  ( 43.01140435219951286, 112.4604996726487514, 39.21067981925356349 ) ) ;
#934=CARTESIAN_POINT ( 'NONE',  ( 47.05648932407426344, 73.91049967264873999, 37.14960608071593384 ) ) ;
#938=CARTESIAN_POINT ( 'NONE',  ( 43.01140435219951286, 132.5344580088725479, 39.46799094044489209 ) ) ;
#939=CARTESIAN_POINT ( 'NONE',  ( 43.01140435219951286, 103.1297705074272955, 38.86567161673127657 ) ) ;
#942=CARTESIAN_POINT ( 'NONE',  ( 39.42975644700377558, 99.41518717409400097, 36.81289934271958941 ) ) ;
#944=ORIENTED_EDGE ( 'NONE', *, *, #13725, .T. ) ;
#945=CARTESIAN_POINT ( 'NONE',  ( 38.01140435219952707, 87.86049967264872862, 35.83527830041809636 ) ) ;
#950=CARTESIAN_POINT ( 'NONE',  ( 39.42975644700377558, 81.07977050742731251, 31.60846029578754468 ) ) ;
#953=CARTESIAN_POINT ( 'NONE',  ( 47.43856463449117200, 155.0297705074273154, 32.77220824515698183 ) ) ;
#957=CARTESIAN_POINT ( 'NONE',  ( 48.01140435219951996, 119.0604996726487315, 35.83527830041810347 ) ) ;
#958=CARTESIAN_POINT ( 'NONE',  ( 41.64333658814960870, 80.51518717409400949, 30.00020018409699318 ) ) ;
#967=CARTESIAN_POINT ( 'NONE',  ( 45.74753988029933538, 146.3297705074273267, 30.44471234641811819 ) ) ;
#969=CARTESIAN_POINT ( 'NONE',  ( 39.42975644700377558, 128.8151871740940067, 31.60846029578754468 ) ) ;
#972=CARTESIAN_POINT ( 'NONE',  ( 39.42975644700377558, 60.07977050742731251, 31.60846029578754468 ) ) ;
#976=DIRECTION ( 'NONE',  ( 0.000000000000000000, 1.000000000000000000, 0.000000000000000000 ) ) ;
#977=CARTESIAN_POINT ( 'NONE',  ( 38.58424406990784661, 105.2651871740939953, 35.64915139335016647 ) ) ;
#983=CARTESIAN_POINT ( 'NONE',  ( 48.01140435219951996, 94.43445800887256780, 32.58608133808903773 ) ) ;
#985=CARTESIAN_POINT ( 'NONE',  ( 48.01140435219951996, 146.3604996726487570, 32.58608133808903773 ) ) ;
#986=CARTESIAN_POINT ( 'NONE',  ( 43.01140435219951286, 107.3651871740940038, 29.55568802177586463 ) ) ;
#989=CARTESIAN_POINT ( 'NONE',  ( 38.96631938032478359, 66.41049967264873999, 31.27175355779120025 ) ) ;
#991=FACE_OUTER_BOUND ( 'NONE', #14368, .T. ) ;
#993=CARTESIAN_POINT ( 'NONE',  ( 44.55648932407425633, 78.68445800887258201, 38.96596240072933170 ) ) ;
#994=CARTESIAN_POINT ( 'NONE',  ( 43.01140435219951286, 146.9604996726487229, 29.21067981925356705 ) ) ;
#995=CARTESIAN_POINT ( 'NONE',  ( 38.58424406990784661, 72.26518717409398107, 35.64915139335016647 ) ) ;
#997=ADVANCED_FACE ( 'NONE', ( #1851 ), #5796, .T. ) ;
#998=CARTESIAN_POINT ( 'NONE',  ( 44.55648932407425633, 95.81049967264873146, 29.45539723777780239 ) ) ;
#1004=EDGE_CURVE ( 'NONE', #1468, #11797, #19255, .T. ) ;
#1006=CARTESIAN_POINT ( 'NONE',  ( 46.59305225739526435, 133.3151871740940067, 36.81289934271958941 ) ) ;
#1007=CARTESIAN_POINT ( 'NONE',  ( 46.59305225739526435, 157.3151871740940067, 36.81289934271958941 ) ) ;
#1008=CARTESIAN_POINT ( 'NONE',  ( 43.01140435219951286, 98.62977050742730967, 29.55568802177586107 ) ) ;
#1009=ORIENTED_EDGE ( 'NONE', *, *, #12907, .T. ) ;
#1013=VERTEX_POINT ( 'NONE', #10774 ) ;
#1014=CARTESIAN_POINT ( 'NONE',  ( 43.01140435219951286, 87.53445800887257633, 39.21067981925356349 ) ) ;
#1016=CARTESIAN_POINT ( 'NONE',  ( 39.42975644700377558, 75.07977050742731251, 31.60846029578754468 ) ) ;
#1017=CARTESIAN_POINT ( 'NONE',  ( 47.43856463449118621, 133.6151871740940180, 34.21067981925357060 ) ) ;
#1018=CARTESIAN_POINT ( 'NONE',  ( 46.10157429594899270, 88.76049967264870588, 38.46393386101376421 ) ) ;
#1024=CARTESIAN_POINT ( 'NONE',  ( 44.55648932407425633, 62.81049967264873146, 29.45539723777780239 ) ) ;
#1026=CARTESIAN_POINT ( 'NONE',  ( 46.59305225739526435, 73.57977050742732672, 36.81289934271958941 ) ) ;
#1030=VERTEX_POINT ( 'NONE', #5472 ) ;
#1033=CARTESIAN_POINT ( 'NONE',  ( 48.01140435219951996, 124.1344580088725706, 35.83527830041809636 ) ) ;
#1034=CARTESIAN_POINT ( 'NONE',  ( 46.59305225739526435, 121.5797705074273267, 36.81289934271958941 ) ) ;
#1035=ORIENTED_EDGE ( 'NONE', *, *, #7465, .F. ) ;
#1037=CARTESIAN_POINT ( 'NONE',  ( 43.80332655382220253, 129.6113394311928460, 39.21067981925355639 ) ) ;
#1038=ORIENTED_EDGE ( 'NONE', *, *, #10703, .F. ) ;
#1039=CARTESIAN_POINT ( 'NONE',  ( 44.37947211624943833, 128.4797705074273040, 30.00020018409699318 ) ) ;
#1041=CARTESIAN_POINT ( 'NONE',  ( 48.01140435219951996, 64.13445800887257064, 35.83527830041810347 ) ) ;
#1047=CARTESIAN_POINT ( 'NONE',  ( 43.80332655382220253, 73.53738109496899256, 39.21067981925355639 ) ) ;
#1048=CARTESIAN_POINT ( 'NONE',  ( 44.55648932407425633, 94.88445800887257064, 29.45539723777780239 ) ) ;
#1050=CARTESIAN_POINT ( 'NONE',  ( 43.01140435219951286, 135.5344580088726048, 39.46799094044489209 ) ) ;
#1051=CARTESIAN_POINT ( 'NONE',  ( 45.74753988029933538, 104.3297705074272983, 30.44471234641811819 ) ) ;
#1053=DIRECTION ( 'NONE',  ( 0.000000000000000000, 1.000000000000000000, 0.000000000000000000 ) ) ;
#1054=CARTESIAN_POINT ( 'NONE',  ( 47.43856463449118621, 97.61518717409400381, 34.21067981925357060 ) ) ;
#1056=VERTEX_POINT ( 'NONE', #12418 ) ;
#1059=CARTESIAN_POINT ( 'NONE',  ( 47.43856463449117911, 146.0297705074272869, 32.77220824515697473 ) ) ;
#1064=CARTESIAN_POINT ( 'NONE',  ( 46.59305225739526435, 64.57977050742731251, 36.81289934271958941 ) ) ;
#1065=EDGE_LOOP ( 'NONE', ( #5086, #8694, #5474, #2167 ) ) ;
#1066=ORIENTED_EDGE ( 'NONE', *, *, #4103, .F. ) ;
#1067=CARTESIAN_POINT ( 'NONE',  ( 40.27526882409969033, 152.9297705074273210, 30.44471234641811819 ) ) ;
#1070=CARTESIAN_POINT ( 'NONE',  ( 46.10157429594899270, 124.7604996726487485, 38.46393386101376421 ) ) ;
#1071=CARTESIAN_POINT ( 'NONE',  ( 43.01140435219951286, 74.36518717409400381, 29.55568802177586463 ) ) ;
#1078=DIRECTION ( 'NONE',  ( 0.000000000000000000, 1.000000000000000000, 0.000000000000000000 ) ) ;
#1079=CARTESIAN_POINT ( 'NONE',  ( 38.58424406990784661, 129.2297705074273324, 32.77220824515698183 ) ) ;
#1081=CARTESIAN_POINT ( 'NONE',  ( 47.43856463449117911, 124.7651871740940095, 32.77220824515697473 ) ) ;
#1082=CARTESIAN_POINT ( 'NONE',  ( 38.96631938032478359, 69.41049967264873999, 31.27175355779120025 ) ) ;
#1083=CARTESIAN_POINT ( 'NONE',  ( 43.01140435219951996, 149.9604996726487798, 29.21067981925357060 ) ) ;
#1084=CARTESIAN_POINT ( 'NONE',  ( 44.55648932407425633, 139.6104996726487286, 38.96596240072933170 ) ) ;
#1087=CARTESIAN_POINT ( 'NONE',  ( 43.01140435219951286, 83.96049967264873715, 29.21067981925356705 ) ) ;
#1088=CARTESIAN_POINT ( 'NONE',  ( 40.27526882409969033, 105.5651871740939782, 37.97664729208901946 ) ) ;
#1089=( BOUNDED_CURVE ( )  B_SPLINE_CURVE ( 2, ( #9097, #10319, #12063, #10425, #15488, #389, #7118, #15798, #13610, #17021, #1929, #12166, #10533 ),
 .UNSPECIFIED., .F., .F. ) 
 B_SPLINE_CURVE_WITH_KNOTS ( ( 3, 2, 2, 2, 2, 2, 3 ),
 ( 0.3602941176470588203, 0.3617647058823529327, 0.3647058823529411575, 0.3676470588235294379, 0.3705882352941176627, 0.3735294117647058876, 0.3750000000000000000 ),
 .UNSPECIFIED. ) 
 CURVE ( )  GEOMETRIC_REPRESENTATION_ITEM ( )  RATIONAL_B_SPLINE_CURVE ( ( 0.9755282581475768211, 0.9755282581475768211, 1.000000000000000000, 0.9510565162951535312, 1.000000000000000000, 0.9510565162951535312, 1.000000000000000000, 0.9510565162951535312, 1.000000000000000000, 0.9510565162951535312, 1.000000000000000000, 0.9755282581475768211, 0.9755282581475768211 ) ) 
 REPRESENTATION_ITEM ( '' )  );
#1094=CARTESIAN_POINT ( 'NONE',  ( 48.01140435219951996, 94.13445800887258486, 35.83527830041810347 ) ) ;
#1095=CARTESIAN_POINT ( 'NONE',  ( 38.96631938032478359, 151.0104996726487343, 37.14960608071593384 ) ) ;
#1096=CARTESIAN_POINT ( 'NONE',  ( 44.37947211624943833, 110.2151871740940123, 30.00020018409699318 ) ) ;
#1100=DIRECTION ( 'NONE',  ( 0.000000000000000000, 0.000000000000000000, 1.000000000000000000 ) ) ;
#1103=CARTESIAN_POINT ( 'NONE',  ( 38.58424406990784661, 59.96518717409398391, 32.77220824515698183 ) ) ;
#1105=CARTESIAN_POINT ( 'NONE',  ( 40.27526882409969744, 152.6651871740940010, 30.44471234641812174 ) ) ;
#1106=CARTESIAN_POINT ( 'NONE',  ( 43.01140435219951286, 113.9604996726487371, 29.21067981925356705 ) ) ;
#1110=CARTESIAN_POINT ( 'NONE',  ( 38.58424406990786082, 72.11518717409400381, 34.21067981925357060 ) ) ;
#1113=SURFACE_STYLE_USAGE ( .BOTH. , #16419 ) ;
#1114=CARTESIAN_POINT ( 'NONE',  ( 43.01140435219951286, 131.3651871740940180, 29.55568802177586463 ) ) ;
#1117=EDGE_LOOP ( 'NONE', ( #9478, #7959, #7011, #10296 ) ) ;
#1120=ORIENTED_EDGE ( 'NONE', *, *, #3662, .F. ) ;
#1121=CARTESIAN_POINT ( 'NONE',  ( 38.01140435219952707, 116.7844580088725763, 34.21067981925357060 ) ) ;
#1124=CARTESIAN_POINT ( 'NONE',  ( 47.43856463449117200, 79.72977050742728977, 35.64915139335016647 ) ) ;
#1125=CARTESIAN_POINT ( 'NONE',  ( 43.01140435219951286, 137.3651871740940180, 29.55568802177586463 ) ) ;
#1126=CARTESIAN_POINT ( 'NONE',  ( 39.92123440845004723, 94.16049967264871157, 38.46393386101376421 ) ) ;
#1130=CARTESIAN_POINT ( 'NONE',  ( 46.10157429594899270, 151.7344580088725934, 29.95742577749336988 ) ) ;
#1133=ORIENTED_EDGE ( 'NONE', *, *, #15104, .F. ) ;
#1134=CARTESIAN_POINT ( 'NONE',  ( 47.43856463449118621, 70.87977050742732388, 34.21067981925357060 ) ) ;
#1140=CARTESIAN_POINT ( 'NONE',  ( 48.01140435219951996, 124.4344580088725678, 32.58608133808903773 ) ) ;
#1141=ADVANCED_FACE ( 'NONE', ( #15726 ), #629, .T. ) ;
#1142=CARTESIAN_POINT ( 'NONE',  ( 39.42975644700377558, 123.6797705074273210, 36.81289934271958941 ) ) ;
#1144=FACE_OUTER_BOUND ( 'NONE', #21457, .T. ) ;
#1146=CARTESIAN_POINT ( 'NONE',  ( 43.01140435219951286, 127.1297705074273381, 38.86567161673127657 ) ) ;
#1147=CARTESIAN_POINT ( 'NONE',  ( 45.51140435220141001, 58.78519719078001060, 29.88055280033245964 ) ) ;
#1148=CARTESIAN_POINT ( 'NONE',  ( 41.46631938032478359, 60.38445800887257064, 38.96596240072933170 ) ) ;
#1150=CARTESIAN_POINT ( 'NONE',  ( 38.96631938032478359, 101.4844580088725792, 31.27175355779120025 ) ) ;
#1154=CARTESIAN_POINT ( 'NONE',  ( 38.01140435219952707, 89.63445800887258486, 32.58608133808903773 ) ) ;
#1155=CARTESIAN_POINT ( 'NONE',  ( 47.05648932407426344, 130.9104996726487684, 37.14960608071593384 ) ) ;
#1158=EDGE_CURVE ( 'NONE', #8610, #10777, #21440, .T. ) ;
#1159=CARTESIAN_POINT ( 'NONE',  ( 44.55648932407425633, 126.6844580088725678, 38.96596240072933170 ) ) ;
#1160=CARTESIAN_POINT ( 'NONE',  ( 43.01140435219951286, 101.6297705074273239, 29.55568802177586463 ) ) ;
#1163=CARTESIAN_POINT ( 'NONE',  ( 41.64333658814960870, 99.71518717409399812, 38.42115945441014446 ) ) ;
#1164=DIRECTION ( 'NONE',  ( 0.000000000000000000, 1.000000000000000000, 0.000000000000000000 ) ) ;
#1166=CARTESIAN_POINT ( 'NONE',  ( 43.80332655382220253, 127.5373810949690068, 39.21067981925355639 ) ) ;
#1169=CARTESIAN_POINT ( 'NONE',  ( 43.01140435219951286, 64.12977050742730967, 38.86567161673127657 ) ) ;
#1170=ORIENTED_EDGE ( 'NONE', *, *, #12310, .T. ) ;
#1172=CARTESIAN_POINT ( 'NONE',  ( 47.43856463449118621, 157.8797705074273381, 34.21067981925357060 ) ) ;
#1174=CARTESIAN_POINT ( 'NONE',  ( 41.46631938032478359, 109.3104996726487457, 38.96596240072933170 ) ) ;
#1175=CARTESIAN_POINT ( 'NONE',  ( 45.74753988029933538, 70.16518717409397254, 37.97664729208901946 ) ) ;
#1182=FACE_OUTER_BOUND ( 'NONE', #1117, .T. ) ;
#1183=CARTESIAN_POINT ( 'NONE',  ( 47.05648932407426344, 148.5844580088725877, 31.27175355779120025 ) ) ;
#1184=CARTESIAN_POINT ( 'NONE',  ( 43.01140435219951286, 133.1297705074273381, 38.86567161673127657 ) ) ;
#1186=CARTESIAN_POINT ( 'NONE',  ( 40.27526882409969744, 122.6651871740939725, 30.44471234641812174 ) ) ;
#1189=CARTESIAN_POINT ( 'NONE',  ( 48.01140435219951996, 65.06049967264873146, 35.83527830041809636 ) ) ;
#1193=VERTEX_POINT ( 'NONE', #2609 ) ;
#1195=VERTEX_POINT ( 'NONE', #9025 ) ;
#1196=CARTESIAN_POINT ( 'NONE',  ( 43.01140435219951286, 84.53445800887256212, 39.46799094044489209 ) ) ;
#1198=CARTESIAN_POINT ( 'NONE',  ( 43.01140435219951286, 151.4604996726486945, 39.46799094044489209 ) ) ;
#1199=CARTESIAN_POINT ( 'NONE',  ( 38.58424406990784661, 95.96518717409396970, 32.77220824515698183 ) ) ;
#1202=EDGE_CURVE ( 'NONE', #15353, #21725, #13833, .T. ) ;
#1203=CARTESIAN_POINT ( 'NONE',  ( 46.10157429594899270, 64.76049967264873430, 38.46393386101376421 ) ) ;
#1206=CARTESIAN_POINT ( 'NONE',  ( 43.01140435219951286, 104.9604996726487371, 29.21067981925356705 ) ) ;
#1207=CARTESIAN_POINT ( 'NONE',  ( 43.01140435219951286, 78.53445800887259054, 39.21067981925356349 ) ) ;
#1209=CARTESIAN_POINT ( 'NONE',  ( 40.27526882409969033, 59.66518717409400097, 30.44471234641811819 ) ) ;
#1212=CARTESIAN_POINT ( 'NONE',  ( 47.43856463449117911, 151.4651871740939839, 35.64915139335015937 ) ) ;
#1213=CARTESIAN_POINT ( 'NONE',  ( 38.96631938032478359, 114.4104996726487400, 31.27175355779120025 ) ) ;
#1217=CARTESIAN_POINT ( 'NONE',  ( 46.59305225739526435, 64.91518717409400097, 31.60846029578754468 ) ) ;
#1218=( BOUNDED_CURVE ( )  B_SPLINE_CURVE ( 2, ( #11812, #15004, #3449, #13140, #2997, #1458, #19987, #9736, #16657, #9842, #14785, #16768, #6653 ),
 .UNSPECIFIED., .F., .F. ) 
 B_SPLINE_CURVE_WITH_KNOTS ( ( 3, 2, 2, 2, 2, 2, 3 ),
 ( 0.1985294117647058987, 0.2000000000000000111, 0.2029411764705882359, 0.2058823529411764608, 0.2088235294117647134, 0.2117647058823529382, 0.2132352941176470507 ),
 .UNSPECIFIED. ) 
 CURVE ( )  GEOMETRIC_REPRESENTATION_ITEM ( )  RATIONAL_B_SPLINE_CURVE ( ( 0.9755282581475768211, 0.9755282581475770431, 1.000000000000000000, 0.9510565162951535312, 1.000000000000000000, 0.9510565162951535312, 1.000000000000000000, 0.9510565162951535312, 1.000000000000000000, 0.9510565162951535312, 1.000000000000000000, 0.9755282581475768211, 0.9755282581475768211 ) ) 
 REPRESENTATION_ITEM ( '' )  );
#1221=CARTESIAN_POINT ( 'NONE',  ( 47.05648932407426344, 111.9844580088725792, 37.14960608071593384 ) ) ;
#1222=CARTESIAN_POINT ( 'NONE',  ( 43.01140435219951286, 137.3651871740940180, 29.55568802177586463 ) ) ;
#1228=CYLINDRICAL_SURFACE ( 'NONE', #10090, 4.999999999999997335 ) ;
#1229=CARTESIAN_POINT ( 'NONE',  ( 47.43856463449118621, 136.6151871740940180, 34.21067981925357060 ) ) ;
#1231=CARTESIAN_POINT ( 'NONE',  ( 43.01140435219951286, 86.96049967264873715, 28.95336869806222779 ) ) ;
#1235=CARTESIAN_POINT ( 'NONE',  ( 45.74753988029933538, 89.06518717409399244, 30.44471234641811819 ) ) ;
#1236=CARTESIAN_POINT ( 'NONE',  ( 48.01140435219951996, 107.2104996726487371, 34.21067981925357060 ) ) ;
#1238=CARTESIAN_POINT ( 'NONE',  ( 43.80332655382220253, 142.9575765865523351, 29.21067981925356705 ) ) ;
#1241=CARTESIAN_POINT ( 'NONE',  ( 38.58424406990784661, 78.22977050742731819, 32.77220824515698183 ) ) ;
#1248=CARTESIAN_POINT ( 'NONE',  ( 45.74753988029934249, 121.4297705074273210, 37.97664729208901235 ) ) ;
#1251=ORIENTED_EDGE ( 'NONE', *, *, #15611, .F. ) ;
#1252=CARTESIAN_POINT ( 'NONE',  ( 45.74753988029933538, 115.4297705074272926, 37.97664729208901946 ) ) ;
#1254=EDGE_CURVE ( 'NONE', #5159, #8610, #16077, .T. ) ;
#1255=CARTESIAN_POINT ( 'NONE',  ( 41.46631938032478359, 62.18445800887258201, 29.45539723777780239 ) ) ;
#1259=CARTESIAN_POINT ( 'NONE',  ( 38.01140435219952707, 96.71049967264875136, 34.21067981925357060 ) ) ;
#1261=EDGE_CURVE ( 'NONE', #872, #17856, #18371, .T. ) ;
#1263=CARTESIAN_POINT ( 'NONE',  ( 38.01140435219952707, 102.7104996726487514, 34.21067981925357060 ) ) ;
#1267=CARTESIAN_POINT ( 'NONE',  ( 38.01140435219951996, 119.9344580088725678, 35.83527830041810347 ) ) ;
#1268=CARTESIAN_POINT ( 'NONE',  ( 38.58424406990784661, 102.2297705074273182, 32.77220824515698183 ) ) ;
#1271=CARTESIAN_POINT ( 'NONE',  ( 47.43856463449118621, 85.61518717409400381, 34.21067981925357060 ) ) ;
#1273=CARTESIAN_POINT ( 'NONE',  ( 43.01140435219951996, 10.71049967264875491, 34.21067981925357060 ) ) ;
#1274=ORIENTED_EDGE ( 'NONE', *, *, #9783, .F. ) ;
#1275=CARTESIAN_POINT ( 'NONE',  ( 48.01140435219951996, 128.2104996726487514, 34.21067981925357060 ) ) ;
#1278=CARTESIAN_POINT ( 'NONE',  ( 44.37947211624943833, 67.27977050742731535, 38.42115945441014446 ) ) ;
#1281=CARTESIAN_POINT ( 'NONE',  ( 41.64333658814960870, 152.7797705074273438, 30.00020018409699318 ) ) ;
#1283=AXIS2_PLACEMENT_3D ( 'NONE', #5031, #8562, #5245 ) ;
#1284=DIRECTION ( 'NONE',  ( 0.000000000000000000, 1.000000000000000000, 0.000000000000000000 ) ) ;
#1285=EDGE_CURVE ( 'NONE', #17073, #9338, #6245, .T. ) ;
#1286=CARTESIAN_POINT ( 'NONE',  ( 48.01140435219951996, 107.3604996726487428, 32.58608133808903773 ) ) ;
#1287=CARTESIAN_POINT ( 'NONE',  ( 47.43856463449117200, 67.46518717409399812, 35.64915139335016647 ) ) ;
#1288=CARTESIAN_POINT ( 'NONE',  ( 38.96631938032478359, 66.08445800887258770, 37.14960608071593384 ) ) ;
#1290=CARTESIAN_POINT ( 'NONE',  ( 42.21948215057684450, 156.4575765865523351, 39.21067981925356349 ) ) ;
#1292=CARTESIAN_POINT ( 'NONE',  ( 47.05648932407426344, 150.9844580088725934, 37.14960608071593384 ) ) ;
#1293=CARTESIAN_POINT ( 'NONE',  ( 41.64333658814960870, 128.7797705074273438, 30.00020018409699318 ) ) ;
#1295=AXIS2_PLACEMENT_3D ( 'NONE', #8946, #12021, #2108 ) ;
#1296=CARTESIAN_POINT ( 'NONE',  ( 43.01140435219951286, 125.3651871740939896, 29.55568802177586107 ) ) ;
#1298=CARTESIAN_POINT ( 'NONE',  ( 38.01140435219952707, 150.8604996726487570, 35.83527830041809636 ) ) ;
#1299=DIRECTION ( 'NONE',  ( 0.000000000000000000, 1.000000000000000000, 0.000000000000000000 ) ) ;
#1306=CARTESIAN_POINT ( 'NONE',  ( 41.46631938032478359, 86.18445800887256780, 29.45539723777780239 ) ) ;
#1309=CARTESIAN_POINT ( 'NONE',  ( 48.01140435219951996, 137.0604996726487457, 35.83527830041810347 ) ) ;
#1310=CARTESIAN_POINT ( 'NONE',  ( 40.27526882409969033, 96.56518717409399244, 37.97664729208901946 ) ) ;
#1319=CARTESIAN_POINT ( 'NONE',  ( 48.01140435219951996, 80.21049967264875136, 34.21067981925357060 ) ) ;
#1320=CARTESIAN_POINT ( 'NONE',  ( 38.58424406990784661, 62.96518717409399812, 32.77220824515698183 ) ) ;
#1326=CARTESIAN_POINT ( 'NONE',  ( 43.01140435219951286, 72.86518717409400381, 38.86567161673127657 ) ) ;
#1330=CARTESIAN_POINT ( 'NONE',  ( 43.80332655382220253, 112.9575765865522925, 29.21067981925356705 ) ) ;
#1331=CARTESIAN_POINT ( 'NONE',  ( 45.74753988029933538, 133.1651871740940010, 37.97664729208901946 ) ) ;
#1333=ORIENTED_EDGE ( 'NONE', *, *, #2207, .T. ) ;
#1337=VERTEX_POINT ( 'NONE', #14617 ) ;
#1338=FACE_OUTER_BOUND ( 'NONE', #2820, .T. ) ;
#1339=CARTESIAN_POINT ( 'NONE',  ( 47.43856463449117200, 67.72977050742731819, 35.64915139335016647 ) ) ;
#1340=CARTESIAN_POINT ( 'NONE',  ( 39.42975644700377558, 128.8151871740940067, 31.60846029578754468 ) ) ;
#1343=CARTESIAN_POINT ( 'NONE',  ( 48.01140435219951996, 92.36049967264871441, 32.58608133808903773 ) ) ;
#1347=( BOUNDED_CURVE ( )  B_SPLINE_CURVE ( 2, ( #695, #14130, #5757, #4111, #5868, #12598, #19319, #4217, #10947, #16956, #16516, #8496, #1868 ),
 .UNSPECIFIED., .F., .F. ) 
 B_SPLINE_CURVE_WITH_KNOTS ( ( 3, 2, 2, 2, 2, 2, 3 ),
 ( 0.007352941176470590735, 0.008823529411764705760, 0.01176470588235294101, 0.01470588235294117627, 0.01764705882352941152, 0.02058823529411764677, 0.02205882352941176267 ),
 .UNSPECIFIED. ) 
 CURVE ( )  GEOMETRIC_REPRESENTATION_ITEM ( )  RATIONAL_B_SPLINE_CURVE ( ( 0.9755282581475768211, 0.9755282581475768211, 1.000000000000000000, 0.9510565162951535312, 1.000000000000000000, 0.9510565162951535312, 1.000000000000000000, 0.9510565162951535312, 1.000000000000000000, 0.9510565162951535312, 1.000000000000000000, 0.9755282581475768211, 0.9755282581475768211 ) ) 
 REPRESENTATION_ITEM ( '' )  );
#1348=CARTESIAN_POINT ( 'NONE',  ( 43.01140435219951286, 90.86518717409400381, 38.86567161673127657 ) ) ;
#1350=LINE ( 'NONE', #11046, #6604 ) ;
#1353=CARTESIAN_POINT ( 'NONE',  ( 38.58424406990784661, 78.52977050742730114, 35.64915139335016647 ) ) ;
#1359=LINE ( 'NONE', #8090, #5000 ) ;
#1360=CARTESIAN_POINT ( 'NONE',  ( 38.58424406990786082, 123.3797705074273239, 34.21067981925357060 ) ) ;
#1362=CARTESIAN_POINT ( 'NONE',  ( 46.10157429594899270, 129.8344580088725877, 38.46393386101375711 ) ) ;
#1364=CARTESIAN_POINT ( 'NONE',  ( 44.37947211624943833, 121.2797705074273296, 38.42115945441014446 ) ) ;
#1365=CARTESIAN_POINT ( 'NONE',  ( 44.37947211624943833, 154.0151871740940237, 38.42115945441014446 ) ) ;
#1368=CARTESIAN_POINT ( 'NONE',  ( 38.01140435219952707, 83.63445800887258486, 32.58608133808903773 ) ) ;
#1371=LINE ( 'NONE', #8103, #10134 ) ;
#1377=CARTESIAN_POINT ( 'NONE',  ( 41.46631938032478359, 128.1844580088725820, 29.45539723777780239 ) ) ;
#1378=CARTESIAN_POINT ( 'NONE',  ( 40.27526882409969033, 102.8297705074272983, 37.97664729208901946 ) ) ;
#1381=CARTESIAN_POINT ( 'NONE',  ( 45.74753988029934249, 85.16518717409400097, 37.97664729208901235 ) ) ;
#1384=CARTESIAN_POINT ( 'NONE',  ( 48.01140435219951996, 128.3604996726487286, 32.58608133808903773 ) ) ;
#1387=CARTESIAN_POINT ( 'NONE',  ( 46.59305225739526435, 146.1797705074273495, 31.60846029578754468 ) ) ;
#1389=CARTESIAN_POINT ( 'NONE',  ( 43.01140435219951286, 62.62977050742732388, 29.55568802177586107 ) ) ;
#1391=EDGE_CURVE ( 'NONE', #3863, #16834, #3608, .T. ) ;
#1392=ORIENTED_EDGE ( 'NONE', *, *, #20409, .F. ) ;
#1393=CARTESIAN_POINT ( 'NONE',  ( 38.58424406990784661, 150.5297705074272869, 35.64915139335016647 ) ) ;
#1394=VECTOR ( 'NONE', #2475, 1000.000000000000000 ) ;
#1396=CARTESIAN_POINT ( 'NONE',  ( 47.05648932407426344, 109.9104996726487400, 37.14960608071593384 ) ) ;
#1397=CARTESIAN_POINT ( 'NONE',  ( 40.27526882409969033, 66.56518717409400665, 37.97664729208901946 ) ) ;
#1398=CARTESIAN_POINT ( 'NONE',  ( 41.46631938032478359, 95.18445800887258201, 29.45539723777780239 ) ) ;
#1402=DIRECTION ( 'NONE',  ( 0.000000000000000000, 1.000000000000000000, 0.000000000000000000 ) ) ;
#1403=CARTESIAN_POINT ( 'NONE',  ( 48.01140435219951996, 151.4344580088725820, 32.58608133808903773 ) ) ;
#1404=CARTESIAN_POINT ( 'NONE',  ( 44.37947211624943833, 130.2797705074273154, 38.42115945441014446 ) ) ;
#1406=CARTESIAN_POINT ( 'NONE',  ( 45.74753988029934249, 115.1651871740940010, 37.97664729208901235 ) ) ;
#1411=CARTESIAN_POINT ( 'NONE',  ( 43.01140435219950575, 139.4604996726487514, 39.21067981925356349 ) ) ;
#1414=CARTESIAN_POINT ( 'NONE',  ( 47.05648932407426344, 82.91049967264873999, 37.14960608071593384 ) ) ;
#1415=CARTESIAN_POINT ( 'NONE',  ( 43.01140435219951286, 91.12977050742732388, 38.86567161673127657 ) ) ;
#1416=EDGE_LOOP ( 'NONE', ( #13580, #12610, #16747, #17987 ) ) ;
#1419=CARTESIAN_POINT ( 'NONE',  ( 46.10157429594899270, 84.83445800887258770, 38.46393386101376421 ) ) ;
#1421=CARTESIAN_POINT ( 'NONE',  ( 38.01140435219951996, 138.8604996726487286, 35.83527830041810347 ) ) ;
#1422=CARTESIAN_POINT ( 'NONE',  ( 47.43856463449118621, 97.61518717409400381, 34.21067981925357060 ) ) ;
#1430=DIRECTION ( 'NONE',  ( 0.000000000000000000, 1.000000000000000000, 0.000000000000000000 ) ) ;
#1432=CARTESIAN_POINT ( 'NONE',  ( 47.43856463449117200, 158.0297705074273438, 32.77220824515698183 ) ) ;
#1434=CARTESIAN_POINT ( 'NONE',  ( 38.58424406990786082, 144.1151871740939896, 34.21067981925357060 ) ) ;
#1437=EDGE_CURVE ( 'NONE', #15249, #13513, #20359, .T. ) ;
#1438=EDGE_CURVE ( 'NONE', #310, #16002, #8512, .T. ) ;
#1439=ORIENTED_EDGE ( 'NONE', *, *, #1940, .T. ) ;
#1440=CARTESIAN_POINT ( 'NONE',  ( 45.74753988029934249, 73.16518717409400097, 37.97664729208901235 ) ) ;
#1444=CARTESIAN_POINT ( 'NONE',  ( 46.59305225739526435, 124.3151871740940067, 36.81289934271958941 ) ) ;
#1448=ORIENTED_EDGE ( 'NONE', *, *, #20139, .F. ) ;
#1450=CARTESIAN_POINT ( 'NONE',  ( 38.01140435219951996, 107.9344580088725536, 35.83527830041810347 ) ) ;
#1452=CARTESIAN_POINT ( 'NONE',  ( 44.37947211624943833, 68.47977050742731819, 30.00020018409699318 ) ) ;
#1453=CARTESIAN_POINT ( 'NONE',  ( 40.27526882409969033, 125.6651871740939868, 30.44471234641811819 ) ) ;
#1455=CARTESIAN_POINT ( 'NONE',  ( 38.96631938032478359, 85.01049967264874851, 37.14960608071593384 ) ) ;
#1458=CARTESIAN_POINT ( 'NONE',  ( 38.01140435219952707, 138.8604996726487286, 35.83527830041809636 ) ) ;
#1459=CARTESIAN_POINT ( 'NONE',  ( 39.42975644700377558, 89.81518717409400665, 31.60846029578754468 ) ) ;
#1460=CARTESIAN_POINT ( 'NONE',  ( 43.01140435219951286, 156.5344580088725479, 39.21067981925355639 ) ) ;
#1464=CARTESIAN_POINT ( 'NONE',  ( 45.74753988029933538, 65.32977050742732672, 30.44471234641811819 ) ) ;
#1468=VERTEX_POINT ( 'NONE', #3500 ) ;
#1469=CARTESIAN_POINT ( 'NONE',  ( 40.27526882409969033, 156.5651871740939498, 37.97664729208901946 ) ) ;
#1470=CARTESIAN_POINT ( 'NONE',  ( 43.01140435219951996, 10.71049967264875491, 29.21067981925357060 ) ) ;
#1471=CARTESIAN_POINT ( 'NONE',  ( 40.27526882409969744, 116.9297705074273210, 30.44471234641812174 ) ) ;
#1474=CARTESIAN_POINT ( 'NONE',  ( 46.10157429594899270, 130.7344580088725934, 29.95742577749336988 ) ) ;
#1475=ORIENTED_EDGE ( 'NONE', *, *, #325, .F. ) ;
#1476=CARTESIAN_POINT ( 'NONE',  ( 41.64333658814960870, 114.9797705074273324, 38.42115945441014446 ) ) ;
#1478=CARTESIAN_POINT ( 'NONE',  ( 38.58424406990784661, 158.9651871740940123, 32.77220824515698183 ) ) ;
#1479=( BOUNDED_CURVE ( )  B_SPLINE_CURVE ( 2, ( #2640, #9383, #998, #6712, #9497, #14436, #1624, #6163, #7626, #15976, #16194, #17956, #7841 ),
 .UNSPECIFIED., .F., .F. ) 
 B_SPLINE_CURVE_WITH_KNOTS ( ( 3, 2, 2, 2, 2, 2, 3 ),
 ( 0.6250000000000000000, 0.6264705882352941124, 0.6294117647058823373, 0.6323529411764705621, 0.6352941176470587870, 0.6382352941176470118, 0.6397058823529411242 ),
 .UNSPECIFIED. ) 
 CURVE ( )  GEOMETRIC_REPRESENTATION_ITEM ( )  RATIONAL_B_SPLINE_CURVE ( ( 0.9755282581475768211, 0.9755282581475768211, 1.000000000000000000, 0.9510565162951535312, 1.000000000000000000, 0.9510565162951535312, 1.000000000000000000, 0.9510565162951535312, 1.000000000000000000, 0.9510565162951535312, 1.000000000000000000, 0.9755282581475777093, 0.9755282581475768211 ) ) 
 REPRESENTATION_ITEM ( '' )  );
#1480=AXIS2_PLACEMENT_3D ( 'NONE', #7219, #13919, #14029 ) ;
#1482=DIRECTION ( 'NONE',  ( 0.000000000000000000, 0.000000000000000000, -1.000000000000000000 ) ) ;
#1483=CARTESIAN_POINT ( 'NONE',  ( 42.21948215057684450, 84.45757658655229250, 39.21067981925355639 ) ) ;
#1486=CARTESIAN_POINT ( 'NONE',  ( 38.96631938032478359, 90.08445800887257349, 37.14960608071593384 ) ) ;
#1487=CARTESIAN_POINT ( 'NONE',  ( 43.80332655382222384, 93.61133943119286016, 39.21067981925354928 ) ) ;
#1490=CARTESIAN_POINT ( 'NONE',  ( 48.01140435219951996, 127.4344580088725962, 32.58608133808903773 ) ) ;
#1491=CARTESIAN_POINT ( 'NONE',  ( 46.59305225739526435, 95.17977050742732104, 31.60846029578754468 ) ) ;
#1494=CARTESIAN_POINT ( 'NONE',  ( 47.43856463449117911, 88.46518717409399812, 35.64915139335015937 ) ) ;
#1495=FACE_OUTER_BOUND ( 'NONE', #11432, .T. ) ;
#1500=CARTESIAN_POINT ( 'NONE',  ( 46.59305225739526435, 103.3151871740940067, 36.81289934271958941 ) ) ;
#1502=CARTESIAN_POINT ( 'NONE',  ( 45.74753988029934249, 68.32977050742732672, 30.44471234641812174 ) ) ;
#1504=CARTESIAN_POINT ( 'NONE',  ( 45.74753988029933538, 146.3297705074273267, 30.44471234641811819 ) ) ;
#1505=CARTESIAN_POINT ( 'NONE',  ( 39.42975644700377558, 99.67977050742732104, 36.81289934271958941 ) ) ;
#1508=CARTESIAN_POINT ( 'NONE',  ( 39.92123440845004723, 106.1604996726487400, 38.46393386101376421 ) ) ;
#1509=CARTESIAN_POINT ( 'NONE',  ( 41.64333658814960870, 71.51518717409399528, 30.00020018409699318 ) ) ;
#1515=CARTESIAN_POINT ( 'NONE',  ( 43.01140435219951286, 147.5344580088725763, 39.46799094044489209 ) ) ;
#1516=CARTESIAN_POINT ( 'NONE',  ( 39.42975644700377558, 135.6797705074273210, 36.81289934271958941 ) ) ;
#1518=CARTESIAN_POINT ( 'NONE',  ( 45.74753988029934249, 121.1651871740939868, 37.97664729208901235 ) ) ;
#1521=CARTESIAN_POINT ( 'NONE',  ( 44.55648932407425633, 64.61049967264874283, 38.96596240072933170 ) ) ;
#1524=CARTESIAN_POINT ( 'NONE',  ( 41.64333658814960870, 99.97977050742731819, 38.42115945441014446 ) ) ;
#1526=CARTESIAN_POINT ( 'NONE',  ( 43.01140435219951286, 146.0344580088725479, 29.21067981925356705 ) ) ;
#1528=CARTESIAN_POINT ( 'NONE',  ( 44.55648932407425633, 82.88445800887257064, 29.45539723777780239 ) ) ;
#1529=CARTESIAN_POINT ( 'NONE',  ( 41.46631938032478359, 86.18445800887256780, 29.45539723777780239 ) ) ;
#1530=CARTESIAN_POINT ( 'NONE',  ( 44.55648932407425633, 137.8104996726487457, 29.45539723777780239 ) ) ;
#1531=CARTESIAN_POINT ( 'NONE',  ( 44.37947211624943833, 97.01518717409400949, 38.42115945441014446 ) ) ;
#1539=CARTESIAN_POINT ( 'NONE',  ( 41.46631938032478359, 147.1104996726487570, 29.45539723777780239 ) ) ;
#1540=CARTESIAN_POINT ( 'NONE',  ( 48.01140435219951996, 115.1344580088725991, 35.83527830041809636 ) ) ;
#1541=CARTESIAN_POINT ( 'NONE',  ( 45.74753988029933538, 64.16518717409400097, 37.97664729208901946 ) ) ;
#1545=CARTESIAN_POINT ( 'NONE',  ( 45.74753988029934249, 148.1651871740940010, 37.97664729208901235 ) ) ;
#1548=ORIENTED_EDGE ( 'NONE', *, *, #12026, .F. ) ;
#1549=CARTESIAN_POINT ( 'NONE',  ( 43.01140435219951286, 78.53445800887259054, 39.21067981925356349 ) ) ;
#1553=CARTESIAN_POINT ( 'NONE',  ( 45.74753988029933538, 128.0651871740940067, 30.44471234641811819 ) ) ;
#1555=VERTEX_POINT ( 'NONE', #12182 ) ;
#1556=ORIENTED_EDGE ( 'NONE', *, *, #9958, .F. ) ;
#1558=ORIENTED_EDGE ( 'NONE', *, *, #4729, .F. ) ;
#1559=CARTESIAN_POINT ( 'NONE',  ( 38.96631938032478359, 108.0844580088725877, 37.14960608071593384 ) ) ;
#1560=CARTESIAN_POINT ( 'NONE',  ( 44.37947211624943833, 155.4797705074273324, 30.00020018409699318 ) ) ;
#1562=CARTESIAN_POINT ( 'NONE',  ( 41.64333658814960870, 68.77977050742731535, 30.00020018409699318 ) ) ;
#1563=CARTESIAN_POINT ( 'NONE',  ( 40.27526882409969033, 123.5651871740939924, 37.97664729208901946 ) ) ;
#1566=CARTESIAN_POINT ( 'NONE',  ( 39.92123440845004723, 78.26049967264873430, 29.95742577749337343 ) ) ;
#1568=CARTESIAN_POINT ( 'NONE',  ( 42.21948215057684450, 144.0373810949689641, 29.21067981925356705 ) ) ;
#1570=CARTESIAN_POINT ( 'NONE',  ( 44.37947211624943833, 88.01518717409399528, 38.42115945441014446 ) ) ;
#1571=CARTESIAN_POINT ( 'NONE',  ( 39.92123440845005433, 81.26049967264872009, 29.95742577749336988 ) ) ;
#1574=CARTESIAN_POINT ( 'NONE',  ( 46.59305225739526435, 64.57977050742731251, 36.81289934271958941 ) ) ;
#1579=CARTESIAN_POINT ( 'NONE',  ( 44.37947211624943833, 149.2151871740940123, 30.00020018409699318 ) ) ;
#1582=CARTESIAN_POINT ( 'NONE',  ( 47.43856463449118621, 112.8797705074273097, 34.21067981925357060 ) ) ;
#1584=VERTEX_POINT ( 'NONE', #10112 ) ;
#1588=CARTESIAN_POINT ( 'NONE',  ( 41.64333658814960870, 150.7151871740940123, 38.42115945441014446 ) ) ;
#1592=CARTESIAN_POINT ( 'NONE',  ( 43.01140435219951996, 10.71049967264875491, 34.21067981925357060 ) ) ;
#1594=CARTESIAN_POINT ( 'NONE',  ( 43.01140435219951996, 10.71049967264875491, 39.21067981925356349 ) ) ;
#1596=CARTESIAN_POINT ( 'NONE',  ( 38.58424406990784661, 96.22977050742728977, 32.77220824515698183 ) ) ;
#1599=CARTESIAN_POINT ( 'NONE',  ( 39.42975644700377558, 90.41518717409400097, 36.81289934271958941 ) ) ;
#1600=CARTESIAN_POINT ( 'NONE',  ( 38.01140435219952707, 84.56049967264873146, 32.58608133808903773 ) ) ;
#1603=CYLINDRICAL_SURFACE ( 'NONE', #18577, 4.999999999999997335 ) ;
#1606=CARTESIAN_POINT ( 'NONE',  ( 47.43856463449117911, 61.72977050742730398, 35.64915139335015937 ) ) ;
#1607=( BOUNDED_CURVE ( )  B_SPLINE_CURVE ( 2, ( #12617, #17569, #17677, #610, #9317, #19023, #16019, #7676, #12285, #824, #9216, #7560, #14258 ),
 .UNSPECIFIED., .F., .F. ) 
 B_SPLINE_CURVE_WITH_KNOTS ( ( 3, 2, 2, 2, 2, 2, 3 ),
 ( 0.2867647058823529216, 0.2882352941176470340, 0.2911764705882353144, 0.2941176470588235392, 0.2970588235294117641, 0.2999999999999999889, 0.3014705882352941013 ),
 .UNSPECIFIED. ) 
 CURVE ( )  GEOMETRIC_REPRESENTATION_ITEM ( )  RATIONAL_B_SPLINE_CURVE ( ( 0.9755282581475768211, 0.9755282581475768211, 1.000000000000000000, 0.9510565162951535312, 1.000000000000000000, 0.9510565162951535312, 1.000000000000000000, 0.9510565162951535312, 1.000000000000000000, 0.9510565162951535312, 1.000000000000000000, 0.9755282581475768211, 0.9755282581475768211 ) ) 
 REPRESENTATION_ITEM ( '' )  );
#1609=CARTESIAN_POINT ( 'NONE',  ( 38.58424406990784661, 144.5297705074273154, 35.64915139335016647 ) ) ;
#1610=EDGE_CURVE ( 'NONE', #1195, #15871, #4962, .T. ) ;
#1611=CARTESIAN_POINT ( 'NONE',  ( 44.37947211624943833, 97.27977050742732956, 38.42115945441014446 ) ) ;
#1614=CARTESIAN_POINT ( 'NONE',  ( 44.55648932407425633, 110.8104996726487457, 29.45539723777780239 ) ) ;
#1615=CARTESIAN_POINT ( 'NONE',  ( 38.58424406990784661, 71.96518717409399812, 32.77220824515698183 ) ) ;
#1618=DIRECTION ( 'NONE',  ( -0.000000000000000000, 1.000000000000000000, -0.000000000000000000 ) ) ;
#1620=CARTESIAN_POINT ( 'NONE',  ( 39.92123440845005433, 112.1604996726487258, 38.46393386101375711 ) ) ;
#1621=CARTESIAN_POINT ( 'NONE',  ( 43.01140435219951286, 150.5344580088725479, 39.46799094044489209 ) ) ;
#1622=CARTESIAN_POINT ( 'NONE',  ( 39.42975644700377558, 126.6797705074273210, 36.81289934271958941 ) ) ;
#1624=CARTESIAN_POINT ( 'NONE',  ( 48.01140435219951996, 95.21049967264875136, 34.21067981925357060 ) ) ;
#1625=CARTESIAN_POINT ( 'NONE',  ( 47.43856463449117911, 112.4651871740939981, 35.64915139335015937 ) ) ;
#1627=CYLINDRICAL_SURFACE ( 'NONE', #21761, 4.999999999999997335 ) ;
#1630=VECTOR ( 'NONE', #21496, 1000.000000000000000 ) ;
#1632=CARTESIAN_POINT ( 'NONE',  ( 44.37947211624943833, 97.27977050742732956, 38.42115945441014446 ) ) ;
#1637=CARTESIAN_POINT ( 'NONE',  ( 43.01140435219951286, 71.03445800887256212, 28.95336869806222779 ) ) ;
#1639=CARTESIAN_POINT ( 'NONE',  ( 44.55648932407425633, 140.8104996726487457, 29.45539723777780239 ) ) ;
#1640=CARTESIAN_POINT ( 'NONE',  ( 46.59305225739526435, 94.91518717409400097, 31.60846029578754468 ) ) ;
#1647=CARTESIAN_POINT ( 'NONE',  ( 47.05648932407426344, 69.98445800887257917, 37.14960608071593384 ) ) ;
#1651=CARTESIAN_POINT ( 'NONE',  ( 42.21948215057684450, 78.03738109496902098, 29.21067981925356705 ) ) ;
#1652=CARTESIAN_POINT ( 'NONE',  ( 44.37947211624943833, 148.2797705074273154, 38.42115945441014446 ) ) ;
#1654=CARTESIAN_POINT ( 'NONE',  ( 39.42975644700377558, 140.8151871740940067, 31.60846029578754468 ) ) ;
#1661=CARTESIAN_POINT ( 'NONE',  ( 40.27526882409969033, 120.5651871740940209, 37.97664729208901946 ) ) ;
#1666=CARTESIAN_POINT ( 'NONE',  ( 38.96631938032478359, 146.4844580088725934, 31.27175355779120025 ) ) ;
#1669=CARTESIAN_POINT ( 'NONE',  ( 38.01140435219952707, 107.7844580088725763, 34.21067981925357060 ) ) ;
#1670=CARTESIAN_POINT ( 'NONE',  ( 45.74753988029934249, 154.4297705074272926, 37.97664729208901235 ) ) ;
#1671=CARTESIAN_POINT ( 'NONE',  ( 46.59305225739526435, 64.57977050742731251, 36.81289934271958941 ) ) ;
#1672=CARTESIAN_POINT ( 'NONE',  ( 43.01140435219951286, 125.3651871740940180, 29.55568802177586463 ) ) ;
#1674=( BOUNDED_CURVE ( )  B_SPLINE_CURVE ( 2, ( #298, #17145, #8790, #12624, #20789, #14165, #17980, #19346, #617, #5894, #7972, #3001, #5681 ),
 .UNSPECIFIED., .F., .F. ) 
 B_SPLINE_CURVE_WITH_KNOTS ( ( 3, 2, 2, 2, 2, 2, 3 ),
 ( 0.4779411764705882582, 0.4794117647058823706, 0.4823529411764705954, 0.4852941176470588203, 0.4882352941176470451, 0.4911764705882352700, 0.4926470588235293824 ),
 .UNSPECIFIED. ) 
 CURVE ( )  GEOMETRIC_REPRESENTATION_ITEM ( )  RATIONAL_B_SPLINE_CURVE ( ( 0.9755282581475768211, 0.9755282581475772652, 1.000000000000000000, 0.9510565162951535312, 1.000000000000000000, 0.9510565162951535312, 1.000000000000000000, 0.9510565162951535312, 1.000000000000000000, 0.9510565162951535312, 1.000000000000000000, 0.9755282581475772652, 0.9755282581475768211 ) ) 
 REPRESENTATION_ITEM ( '' )  );
#1677=CARTESIAN_POINT ( 'NONE',  ( 44.55648932407425633, 86.81049967264874567, 29.45539723777780239 ) ) ;
#1679=CARTESIAN_POINT ( 'NONE',  ( 47.05648932407426344, 98.51049967264874851, 31.27175355779120025 ) ) ;
#1681=CARTESIAN_POINT ( 'NONE',  ( 47.43856463449118621, 85.61518717409400381, 34.21067981925357060 ) ) ;
#1682=AXIS2_PLACEMENT_3D ( 'NONE', #6827, #13534, #14958 ) ;
#1683=CARTESIAN_POINT ( 'NONE',  ( 43.01140435219951286, 72.53445800887256212, 39.21067981925356349 ) ) ;
#1684=VERTEX_POINT ( 'NONE', #20895 ) ;
#1685=CARTESIAN_POINT ( 'NONE',  ( 47.43856463449117200, 61.72977050742730398, 35.64915139335016647 ) ) ;
#1691=CARTESIAN_POINT ( 'NONE',  ( 41.64333658814960870, 150.7151871740940123, 38.42115945441014446 ) ) ;
#1693=CARTESIAN_POINT ( 'NONE',  ( 39.42975644700377558, 111.0797705074273125, 31.60846029578754468 ) ) ;
#1695=VECTOR ( 'NONE', #20159, 1000.000000000000000 ) ;
#1700=CARTESIAN_POINT ( 'NONE',  ( 47.43856463449118621, 121.8797705074273239, 34.21067981925357060 ) ) ;
#1703=CARTESIAN_POINT ( 'NONE',  ( 43.01140435219951286, 153.8651871740939612, 38.86567161673127657 ) ) ;
#1705=CARTESIAN_POINT ( 'NONE',  ( 47.05648932407426344, 81.98445800887257917, 37.14960608071593384 ) ) ;
#1708=DIRECTION ( 'NONE',  ( 0.000000000000000000, 1.000000000000000000, 0.000000000000000000 ) ) ;
#1710=CARTESIAN_POINT ( 'NONE',  ( 39.92123440845005433, 98.33445800887258770, 29.95742577749336988 ) ) ;
#1711=CARTESIAN_POINT ( 'NONE',  ( 40.27526882409969033, 90.82977050742731251, 37.97664729208901946 ) ) ;
#1714=CARTESIAN_POINT ( 'NONE',  ( 40.27526882409969744, 87.56518717409400665, 37.97664729208901235 ) ) ;
#1718=EDGE_CURVE ( 'NONE', #7475, #15486, #20604, .T. ) ;
#1719=CARTESIAN_POINT ( 'NONE',  ( 38.96631938032478359, 137.4844580088725650, 31.27175355779120025 ) ) ;
#1722=CARTESIAN_POINT ( 'NONE',  ( 43.01140435219951286, 142.1297705074273097, 38.86567161673127657 ) ) ;
#1726=CARTESIAN_POINT ( 'NONE',  ( 47.43856463449118621, 145.8797705074273097, 34.21067981925357060 ) ) ;
#1727=CARTESIAN_POINT ( 'NONE',  ( 41.64333658814960870, 95.77977050742732956, 30.00020018409699318 ) ) ;
#1733=CARTESIAN_POINT ( 'NONE',  ( 38.01140435219952707, 111.7104996726487514, 34.21067981925357060 ) ) ;
#1734=CARTESIAN_POINT ( 'NONE',  ( 43.01140435219951286, 146.0344580088725195, 28.95336869806222779 ) ) ;
#1735=CARTESIAN_POINT ( 'NONE',  ( 41.64333658814960870, 122.7797705074273296, 30.00020018409699318 ) ) ;
#1737=CARTESIAN_POINT ( 'NONE',  ( 38.01140435219952707, 140.7844580088725763, 34.21067981925357060 ) ) ;
#1738=CARTESIAN_POINT ( 'NONE',  ( 46.59305225739526435, 121.3151871740940067, 36.81289934271958941 ) ) ;
#1746=CARTESIAN_POINT ( 'NONE',  ( 47.43856463449117911, 82.72977050742731819, 35.64915139335015937 ) ) ;
#1750=CARTESIAN_POINT ( 'NONE',  ( 38.01140435219951996, 71.93445800887258201, 35.83527830041810347 ) ) ;
#1752=CARTESIAN_POINT ( 'NONE',  ( 46.10157429594899270, 139.7604996726487627, 38.46393386101376421 ) ) ;
#1753=CARTESIAN_POINT ( 'NONE',  ( 43.01140435219951286, 90.86518717409400381, 38.86567161673127657 ) ) ;
#1757=CARTESIAN_POINT ( 'NONE',  ( 38.96631938032478359, 93.41049967264873999, 31.27175355779120025 ) ) ;
#1758=CARTESIAN_POINT ( 'NONE',  ( 43.01140435219951286, 128.0344580088725479, 29.21067981925356705 ) ) ;
#1759=CARTESIAN_POINT ( 'NONE',  ( 38.96631938032478359, 148.0104996726487627, 37.14960608071593384 ) ) ;
#1761=CARTESIAN_POINT ( 'NONE',  ( 38.58424406990784661, 156.5297705074272869, 35.64915139335016647 ) ) ;
#1764=CARTESIAN_POINT ( 'NONE',  ( 46.59305225739526435, 145.3151871740940067, 36.81289934271958941 ) ) ;
#1771=CARTESIAN_POINT ( 'NONE',  ( 39.92123440845005433, 134.3344580088725877, 29.95742577749336988 ) ) ;
#1772=CARTESIAN_POINT ( 'NONE',  ( 38.58424406990784661, 128.9651871740939839, 32.77220824515698183 ) ) ;
#1775=ORIENTED_EDGE ( 'NONE', *, *, #1391, .T. ) ;
#1777=CARTESIAN_POINT ( 'NONE',  ( 41.46631938032478359, 114.3844580088725849, 38.96596240072933170 ) ) ;
#1779=CARTESIAN_POINT ( 'NONE',  ( 41.46631938032478359, 98.18445800887256780, 29.45539723777780239 ) ) ;
#1780=CARTESIAN_POINT ( 'NONE',  ( 39.42975644700377558, 156.0797705074273267, 31.60846029578754468 ) ) ;
#1781=CARTESIAN_POINT ( 'NONE',  ( 43.01140435219951286, 67.12977050742732388, 38.86567161673127657 ) ) ;
#1782=CARTESIAN_POINT ( 'NONE',  ( 44.37947211624943833, 127.0151871740939953, 38.42115945441014446 ) ) ;
#1785=CARTESIAN_POINT ( 'NONE',  ( 46.10157429594899270, 85.76049967264873430, 38.46393386101376421 ) ) ;
#1790=CARTESIAN_POINT ( 'NONE',  ( 44.37947211624943833, 80.21518717409399812, 30.00020018409699318 ) ) ;
#1796=CARTESIAN_POINT ( 'NONE',  ( 39.42975644700377558, 66.67977050742732104, 36.81289934271958941 ) ) ;
#1801=CARTESIAN_POINT ( 'NONE',  ( 44.37947211624943833, 157.0151871740940237, 38.42115945441014446 ) ) ;
#1802=CARTESIAN_POINT ( 'NONE',  ( 43.01140435219951286, 116.6297705074273097, 29.55568802177586107 ) ) ;
#1806=( BOUNDED_CURVE ( )  B_SPLINE_CURVE ( 2, ( #21685, #11860, #20037, #13516, #20249, #19916, #8567, #4924, #11635, #17029, #6701, #18365, #10326 ),
 .UNSPECIFIED., .F., .F. ) 
 B_SPLINE_CURVE_WITH_KNOTS ( ( 3, 2, 2, 2, 2, 2, 3 ),
 ( 0.06617647058823528106, 0.06764705882352940736, 0.07058823529411764608, 0.07352941176470588480, 0.07647058823529412352, 0.07941176470588234837, 0.08088235294117646079 ),
 .UNSPECIFIED. ) 
 CURVE ( )  GEOMETRIC_REPRESENTATION_ITEM ( )  RATIONAL_B_SPLINE_CURVE ( ( 0.9755282581475765991, 0.9755282581475764880, 1.000000000000000000, 0.9510565162951535312, 1.000000000000000000, 0.9510565162951535312, 1.000000000000000000, 0.9510565162951535312, 1.000000000000000000, 0.9510565162951535312, 1.000000000000000000, 0.9755282581475768211, 0.9755282581475767101 ) ) 
 REPRESENTATION_ITEM ( '' )  );
#1808=CARTESIAN_POINT ( 'NONE',  ( 43.01140435219951286, 110.6297705074273097, 29.55568802177586463 ) ) ;
#1810=CARTESIAN_POINT ( 'NONE',  ( 39.42975644700377558, 153.4151871740940010, 36.81289934271958941 ) ) ;
#1815=CARTESIAN_POINT ( 'NONE',  ( 44.55648932407425633, 101.8104996726487457, 29.45539723777780239 ) ) ;
#1818=CARTESIAN_POINT ( 'NONE',  ( 46.10157429594899270, 77.66049967264872578, 29.95742577749336988 ) ) ;
#1819=CARTESIAN_POINT ( 'NONE',  ( 40.27526882409969033, 95.92977050742732104, 30.44471234641811819 ) ) ;
#1823=CARTESIAN_POINT ( 'NONE',  ( 46.59305225739526435, 79.91518717409400097, 31.60846029578754468 ) ) ;
#1828=CARTESIAN_POINT ( 'NONE',  ( 41.64333658814960870, 141.9797705074273324, 38.42115945441014446 ) ) ;
#1830=CARTESIAN_POINT ( 'NONE',  ( 38.01140435219952707, 119.6344580088725706, 32.58608133808903773 ) ) ;
#1832=CARTESIAN_POINT ( 'NONE',  ( 38.58424406990784661, 147.2297705074273324, 32.77220824515698183 ) ) ;
#1837=EDGE_CURVE ( 'NONE', #5662, #890, #11711, .T. ) ;
#1841=CARTESIAN_POINT ( 'NONE',  ( 38.96631938032478359, 109.0104996726487485, 37.14960608071593384 ) ) ;
#1844=CARTESIAN_POINT ( 'NONE',  ( 43.01140435219951286, 140.0344580088726048, 28.95336869806222779 ) ) ;
#1845=CARTESIAN_POINT ( 'NONE',  ( 43.01140435219951286, 125.6297705074273381, 29.55568802177586463 ) ) ;
#1847=DIRECTION ( 'NONE',  ( -0.8660537913735167903, 0.0001295314220487989892, -0.4999508112496346413 ) ) ;
#1848=CARTESIAN_POINT ( 'NONE',  ( 39.42975644700377558, 117.4151871740940010, 36.81289934271958941 ) ) ;
#1851=FACE_OUTER_BOUND ( 'NONE', #14691, .T. ) ;
#1852=CARTESIAN_POINT ( 'NONE',  ( 47.43856463449117911, 83.02977050742731535, 32.77220824515697473 ) ) ;
#1855=CARTESIAN_POINT ( 'NONE',  ( 43.01140435219951286, 69.53445800887257633, 39.46799094044489209 ) ) ;
#1858=CARTESIAN_POINT ( 'NONE',  ( 38.01140435219951996, 132.5604996726487457, 32.58608133808903773 ) ) ;
#1859=CARTESIAN_POINT ( 'NONE',  ( 46.59305225739526435, 91.91518717409400097, 31.60846029578754468 ) ) ;
#1863=CARTESIAN_POINT ( 'NONE',  ( 41.46631938032478359, 116.1844580088725820, 29.45539723777780239 ) ) ;
#1865=DIRECTION ( 'NONE',  ( 0.000000000000000000, 1.000000000000000000, 0.000000000000000000 ) ) ;
#1867=CARTESIAN_POINT ( 'NONE',  ( 43.01140435219951286, 155.6297705074273381, 29.55568802177586463 ) ) ;
#1868=CARTESIAN_POINT ( 'NONE',  ( 43.01140435219951996, 157.4604996726487514, 39.21067981925355639 ) ) ;
#1870=CARTESIAN_POINT ( 'NONE',  ( 40.27526882409969744, 141.5651871740940067, 37.97664729208901235 ) ) ;
#1871=CARTESIAN_POINT ( 'NONE',  ( 43.01140435219957681, 68.03445800887257633, 29.21067981925356705 ) ) ;
#1873=CARTESIAN_POINT ( 'NONE',  ( 39.42975644700377558, 59.81518717409399244, 31.60846029578754468 ) ) ;
#1877=CARTESIAN_POINT ( 'NONE',  ( 43.01140435219951286, 123.8651871740939896, 38.86567161673127657 ) ) ;
#1880=CARTESIAN_POINT ( 'NONE',  ( 38.96631938032478359, 114.0844580088725877, 37.14960608071593384 ) ) ;
#1882=CARTESIAN_POINT ( 'NONE',  ( 41.46631938032478359, 105.3844580088725849, 38.96596240072933170 ) ) ;
#1883=CARTESIAN_POINT ( 'NONE',  ( 44.55648932407425633, 157.6104996726487570, 38.96596240072933170 ) ) ;
#1884=CARTESIAN_POINT ( 'NONE',  ( 38.58424406990784661, 119.9651871740939839, 32.77220824515698183 ) ) ;
#1886=CARTESIAN_POINT ( 'NONE',  ( 38.01140435219952707, 81.71049967264873715, 34.21067981925357060 ) ) ;
#1887=CARTESIAN_POINT ( 'NONE',  ( 46.10157429594899270, 147.8344580088725309, 38.46393386101375711 ) ) ;
#1888=CARTESIAN_POINT ( 'NONE',  ( 43.01140435219951996, 10.71049967264875491, 34.21067981925357060 ) ) ;
#1890=CARTESIAN_POINT ( 'NONE',  ( 44.37947211624943833, 82.01518717409400949, 38.42115945441014446 ) ) ;
#1892=CARTESIAN_POINT ( 'NONE',  ( 41.46631938032478359, 123.3844580088725849, 38.96596240072933170 ) ) ;
#1893=CARTESIAN_POINT ( 'NONE',  ( 43.01140435219954838, 131.9604996726487229, 29.21067981925356705 ) ) ;
#1900=CARTESIAN_POINT ( 'NONE',  ( 40.27526882409969033, 155.6651871740940010, 30.44471234641811819 ) ) ;
#1902=CARTESIAN_POINT ( 'NONE',  ( 39.42975644700377558, 117.6797705074273210, 36.81289934271958941 ) ) ;
#1906=CARTESIAN_POINT ( 'NONE',  ( 47.43856463449118621, 109.8797705074273239, 34.21067981925357060 ) ) ;
#1910=CARTESIAN_POINT ( 'NONE',  ( 40.27526882409969033, 146.6651871740940294, 30.44471234641811819 ) ) ;
#1918=CARTESIAN_POINT ( 'NONE',  ( 43.01140435219951286, 91.46049967264873715, 39.21067981925356349 ) ) ;
#1919=FACE_OUTER_BOUND ( 'NONE', #6043, .T. ) ;
#1920=CARTESIAN_POINT ( 'NONE',  ( 38.58424406990786082, 96.37977050742732388, 34.21067981925357060 ) ) ;
#1924=CARTESIAN_POINT ( 'NONE',  ( 47.43856463449118621, 82.61518717409398960, 34.21067981925357060 ) ) ;
#1929=CARTESIAN_POINT ( 'NONE',  ( 44.55648932407425633, 121.6104996726487570, 38.96596240072933170 ) ) ;
#1931=CARTESIAN_POINT ( 'NONE',  ( 44.37947211624943833, 142.2797705074273154, 38.42115945441014446 ) ) ;
#1935=CARTESIAN_POINT ( 'NONE',  ( 43.01140435219951286, 59.62977050742730967, 29.55568802177586107 ) ) ;
#1937=CARTESIAN_POINT ( 'NONE',  ( 44.37947211624943833, 137.4797705074273324, 30.00020018409699318 ) ) ;
#1938=CARTESIAN_POINT ( 'NONE',  ( 38.58424406990786082, 96.37977050742732388, 34.21067981925357060 ) ) ;
#1939=CARTESIAN_POINT ( 'NONE',  ( 38.96631938032478359, 142.0104996726487627, 37.14960608071593384 ) ) ;
#1940=EDGE_CURVE ( 'NONE', #1193, #13207, #16209, .T. ) ;
#1942=CARTESIAN_POINT ( 'NONE',  ( 43.01140435219951996, 10.71049967264875491, 34.21067981925357060 ) ) ;
#1943=EDGE_CURVE ( 'NONE', #2795, #13772, #5523, .T. ) ;
#1945=CARTESIAN_POINT ( 'NONE',  ( 42.21948215057684450, 109.3836182503284533, 39.21067981925356349 ) ) ;
#1949=CARTESIAN_POINT ( 'NONE',  ( 38.96631938032478359, 143.4844580088725650, 31.27175355779120025 ) ) ;
#1950=CARTESIAN_POINT ( 'NONE',  ( 39.42975644700377558, 126.0797705074273267, 31.60846029578754468 ) ) ;
#1952=CARTESIAN_POINT ( 'NONE',  ( 48.01140435219951996, 100.1344580088725706, 35.83527830041809636 ) ) ;
#1953=CARTESIAN_POINT ( 'NONE',  ( 41.64333658814960870, 111.7151871740940123, 38.42115945441014446 ) ) ;
#1957=CARTESIAN_POINT ( 'NONE',  ( 45.51140435220141001, 58.78519719078001060, 29.88055280033245964 ) ) ;
#1958=CARTESIAN_POINT ( 'NONE',  ( 38.58424406990785371, 81.52977050742732956, 35.64915139335015937 ) ) ;
#1959=ORIENTED_EDGE ( 'NONE', *, *, #10473, .T. ) ;
#1961=EDGE_CURVE ( 'NONE', #19429, #495, #10053, .T. ) ;
#1962=CARTESIAN_POINT ( 'NONE',  ( 46.10157429594899270, 110.6604996726487400, 29.95742577749336988 ) ) ;
#1963=CARTESIAN_POINT ( 'NONE',  ( 46.10157429594899270, 73.73445800887257917, 29.95742577749337343 ) ) ;
#1964=DIRECTION ( 'NONE',  ( 0.000000000000000000, 1.000000000000000000, 0.000000000000000000 ) ) ;
#1965=CARTESIAN_POINT ( 'NONE',  ( 48.01140435219951996, 134.2104996726487514, 34.21067981925357060 ) ) ;
#1966=CARTESIAN_POINT ( 'NONE',  ( 47.43856463449117200, 88.46518717409399812, 35.64915139335016647 ) ) ;
#1972=CARTESIAN_POINT ( 'NONE',  ( 48.01140435219951996, 68.36049967264872862, 32.58608133808903773 ) ) ;
#1974=CARTESIAN_POINT ( 'NONE',  ( 43.01140435219951286, 148.1297705074272812, 38.86567161673127657 ) ) ;
#1975=CARTESIAN_POINT ( 'NONE',  ( 41.64333658814960870, 104.7797705074273154, 30.00020018409699318 ) ) ;
#1978=CARTESIAN_POINT ( 'NONE',  ( 43.01140435219951286, 131.3651871740940180, 29.55568802177586107 ) ) ;
#1982=CARTESIAN_POINT ( 'NONE',  ( 43.01140435219951286, 63.86518717409398960, 38.86567161673127657 ) ) ;
#1985=CARTESIAN_POINT ( 'NONE',  ( 41.64333658814960870, 111.7151871740940123, 38.42115945441014446 ) ) ;
#1986=ORIENTED_EDGE ( 'NONE', *, *, #14599, .F. ) ;
#1987=ORIENTED_EDGE ( 'NONE', *, *, #2982, .T. ) ;
#1988=FACE_OUTER_BOUND ( 'NONE', #16011, .T. ) ;
#1990=CARTESIAN_POINT ( 'NONE',  ( 44.55648932407425633, 105.6844580088725820, 38.96596240072933170 ) ) ;
#1992=CARTESIAN_POINT ( 'NONE',  ( 44.37947211624943833, 154.2797705074273438, 38.42115945441014446 ) ) ;
#1994=CARTESIAN_POINT ( 'NONE',  ( 47.05648932407426344, 155.5104996726487343, 31.27175355779120025 ) ) ;
#1995=CARTESIAN_POINT ( 'NONE',  ( 44.37947211624943833, 116.2151871740940123, 30.00020018409699318 ) ) ;
#1998=CARTESIAN_POINT ( 'NONE',  ( 43.01140435219951286, 73.46049967264872294, 39.46799094044489209 ) ) ;
#2000=CARTESIAN_POINT ( 'NONE',  ( 38.01140435219952707, 74.63445800887258486, 32.58608133808903773 ) ) ;
#2001=CARTESIAN_POINT ( 'NONE',  ( 38.01140435219952707, 123.7104996726487371, 34.21067981925357060 ) ) ;
#2003=CARTESIAN_POINT ( 'NONE',  ( 44.37947211624943833, 74.21518717409399812, 30.00020018409699318 ) ) ;
#2009=VECTOR ( 'NONE', #8730, 1000.000000000000000 ) ;
#2014=CARTESIAN_POINT ( 'NONE',  ( 44.37947211624943833, 146.2151871740940123, 30.00020018409699318 ) ) ;
#2015=DIRECTION ( 'NONE',  ( -0.000000000000000000, 1.000000000000000000, -0.000000000000000000 ) ) ;
#2016=CARTESIAN_POINT ( 'NONE',  ( 39.42975644700377558, 102.0797705074273267, 31.60846029578754468 ) ) ;
#2021=CARTESIAN_POINT ( 'NONE',  ( 41.64333658814960870, 113.7797705074273296, 30.00020018409699318 ) ) ;
#2022=CARTESIAN_POINT ( 'NONE',  ( 39.92123440845005433, 127.1604996726487542, 38.46393386101375711 ) ) ;
#2023=CARTESIAN_POINT ( 'NONE',  ( 41.64333658814960870, 149.5151871740940237, 30.00020018409699318 ) ) ;
#2024=VECTOR ( 'NONE', #19238, 1000.000000000000000 ) ;
#2025=EDGE_CURVE ( 'NONE', #1195, #13896, #18678, .T. ) ;
#2026=CARTESIAN_POINT ( 'NONE',  ( 39.92123440845004723, 103.1604996726487258, 38.46393386101376421 ) ) ;
#2028=CARTESIAN_POINT ( 'NONE',  ( 43.80332655382220253, 118.5373810949690068, 39.21067981925355639 ) ) ;
#2033=CARTESIAN_POINT ( 'NONE',  ( 46.59305225739526435, 83.17977050742732104, 31.60846029578754468 ) ) ;
#2036=CARTESIAN_POINT ( 'NONE',  ( 38.58424406990786082, 75.11518717409400381, 34.21067981925357060 ) ) ;
#2037=DIRECTION ( 'NONE',  ( 0.000000000000000000, 1.000000000000000000, 0.000000000000000000 ) ) ;
#2038=AXIS2_PLACEMENT_3D ( 'NONE', #18017, #7791, #4796 ) ;
#2043=CARTESIAN_POINT ( 'NONE',  ( 40.27526882409969744, 140.9297705074273210, 30.44471234641812174 ) ) ;
#2050=CARTESIAN_POINT ( 'NONE',  ( 44.37947211624943833, 133.2797705074273154, 38.42115945441014446 ) ) ;
#2051=CARTESIAN_POINT ( 'NONE',  ( 40.27526882409969033, 60.56518717409398533, 37.97664729208901946 ) ) ;
#2052=CARTESIAN_POINT ( 'NONE',  ( 38.58424406990786082, 159.3797705074273381, 34.21067981925357060 ) ) ;
#2054=CARTESIAN_POINT ( 'NONE',  ( 47.43856463449117200, 94.46518717409398391, 35.64915139335016647 ) ) ;
#2055=CARTESIAN_POINT ( 'NONE',  ( 39.92123440845005433, 154.1604996726487400, 38.46393386101375711 ) ) ;
#2060=CARTESIAN_POINT ( 'NONE',  ( 38.01140435219952707, 146.7844580088725763, 34.21067981925357060 ) ) ;
#2061=B_SPLINE_CURVE_WITH_KNOTS ( 'NONE', 1,
 ( #10082, #20332 ),
 .UNSPECIFIED., .F., .F.,
 ( 2, 2 ),
 ( 0.000000000000000000, 1.000000000000000000 ),
 .UNSPECIFIED. ) ;
#2062=CARTESIAN_POINT ( 'NONE',  ( 40.27526882409969033, 123.8297705074273125, 37.97664729208901946 ) ) ;
#2063=( BOUNDED_CURVE ( )  B_SPLINE_CURVE ( 2, ( #15208, #11673, #4731, #19961, #5071, #9927, #3529, #18178, #13445, #14974, #15093, #3308, #3525 ),
 .UNSPECIFIED., .F., .F. ) 
 B_SPLINE_CURVE_WITH_KNOTS ( ( 3, 2, 2, 2, 2, 2, 3 ),
 ( 0.9338235294117647189, 0.9352941176470588314, 0.9382352941176470562, 0.9411764705882352811, 0.9441176470588235059, 0.9470588235294117307, 0.9485294117647058432 ),
 .UNSPECIFIED. ) 
 CURVE ( )  GEOMETRIC_REPRESENTATION_ITEM ( )  RATIONAL_B_SPLINE_CURVE ( ( 0.9755282581475768211, 0.9755282581475768211, 1.000000000000000000, 0.9510565162951535312, 1.000000000000000000, 0.9510565162951535312, 1.000000000000000000, 0.9510565162951535312, 1.000000000000000000, 0.9510565162951535312, 1.000000000000000000, 0.9755282581475768211, 0.9755282581475768211 ) ) 
 REPRESENTATION_ITEM ( '' )  );
#2066=CARTESIAN_POINT ( 'NONE',  ( 41.64333658814960870, 105.7151871740940123, 38.42115945441014446 ) ) ;
#2067=CARTESIAN_POINT ( 'NONE',  ( 38.01140435219952707, 125.6344580088725706, 32.58608133808903773 ) ) ;
#2072=CARTESIAN_POINT ( 'NONE',  ( 38.58424406990786082, 87.37977050742732388, 34.21067981925357060 ) ) ;
#2074=CARTESIAN_POINT ( 'NONE',  ( 48.01140435219951996, 76.43445800887258201, 32.58608133808903773 ) ) ;
#2076=CARTESIAN_POINT ( 'NONE',  ( 47.05648932407426344, 133.9104996726487400, 37.14960608071593384 ) ) ;
#2077=CARTESIAN_POINT ( 'NONE',  ( 41.64333658814960870, 89.51518717409399528, 30.00020018409699318 ) ) ;
#2085=CARTESIAN_POINT ( 'NONE',  ( 38.58424406990786082, 156.3797705074273097, 34.21067981925357060 ) ) ;
#2086=CARTESIAN_POINT ( 'NONE',  ( 45.74753988029933538, 101.3297705074273267, 30.44471234641811819 ) ) ;
#2088=CARTESIAN_POINT ( 'NONE',  ( 47.43856463449118621, 139.6151871740939896, 34.21067981925357060 ) ) ;
#2091=CIRCLE ( 'NONE', #15467, 24.99999999999998934 ) ;
#2094=CARTESIAN_POINT ( 'NONE',  ( 40.27526882409969033, 117.5651871740940067, 37.97664729208901946 ) ) ;
#2098=CARTESIAN_POINT ( 'NONE',  ( 48.01140435219951996, 100.1344580088725564, 35.83527830041810347 ) ) ;
#2099=CARTESIAN_POINT ( 'NONE',  ( 38.58424406990784661, 60.52977050742731535, 35.64915139335016647 ) ) ;
#2100=CARTESIAN_POINT ( 'NONE',  ( 41.64333658814960870, 119.5151871740940095, 30.00020018409699318 ) ) ;
#2102=CARTESIAN_POINT ( 'NONE',  ( 38.96631938032478359, 69.41049967264873999, 31.27175355779120025 ) ) ;
#2108=DIRECTION ( 'NONE',  ( 0.000000000000000000, 0.000000000000000000, 1.000000000000000000 ) ) ;
#2109=CARTESIAN_POINT ( 'NONE',  ( 41.64333658814960870, 78.71518717409399812, 38.42115945441014446 ) ) ;
#2110=CARTESIAN_POINT ( 'NONE',  ( 43.01140435219951286, 64.46049967264873715, 39.21067981925356349 ) ) ;
#2113=EDGE_LOOP ( 'NONE', ( #4351, #6041, #11601, #2152 ) ) ;
#2117=CARTESIAN_POINT ( 'NONE',  ( 40.27526882409969033, 146.6651871740940294, 30.44471234641811819 ) ) ;
#2119=CARTESIAN_POINT ( 'NONE',  ( 43.01140435219951996, 2.710499672648754466, 9.210679819253577705 ) ) ;
#2120=CARTESIAN_POINT ( 'NONE',  ( 47.43856463449117911, 107.0297705074273154, 32.77220824515697473 ) ) ;
#2122=ORIENTED_EDGE ( 'NONE', *, *, #1202, .F. ) ;
#2125=CARTESIAN_POINT ( 'NONE',  ( 40.27526882409969033, 113.9297705074273068, 30.44471234641811819 ) ) ;
#2126=CARTESIAN_POINT ( 'NONE',  ( 42.21948215057683740, 158.1113394311928744, 29.21067981925356705 ) ) ;
#2127=CARTESIAN_POINT ( 'NONE',  ( 38.58424406990786082, 81.37977050742730967, 34.21067981925357060 ) ) ;
#2128=CARTESIAN_POINT ( 'NONE',  ( 45.74753988029933538, 142.1651871740940010, 37.97664729208901946 ) ) ;
#2129=CARTESIAN_POINT ( 'NONE',  ( 48.01140435219951996, 104.3604996726487144, 32.58608133808903773 ) ) ;
#2134=CARTESIAN_POINT ( 'NONE',  ( 39.92123440845005433, 61.16049967264873288, 38.46393386101375711 ) ) ;
#2139=CARTESIAN_POINT ( 'NONE',  ( 43.01140435219951286, 99.53445800887257633, 39.21067981925356349 ) ) ;
#2140=CARTESIAN_POINT ( 'NONE',  ( 38.58424406990786082, 84.37977050742730967, 34.21067981925357060 ) ) ;
#2142=CARTESIAN_POINT ( 'NONE',  ( 41.64333658814960870, 81.71518717409399812, 38.42115945441014446 ) ) ;
#2146=CARTESIAN_POINT ( 'NONE',  ( 38.01140435219952707, 158.7844580088725763, 34.21067981925357060 ) ) ;
#2148=CARTESIAN_POINT ( 'NONE',  ( 47.43856463449117911, 137.0297705074272869, 32.77220824515697473 ) ) ;
#2152=ORIENTED_EDGE ( 'NONE', *, *, #1254, .T. ) ;
#2153=CARTESIAN_POINT ( 'NONE',  ( 44.37947211624943833, 140.4797705074273324, 30.00020018409699318 ) ) ;
#2154=CARTESIAN_POINT ( 'NONE',  ( 44.37947211624943833, 91.27977050742731535, 38.42115945441014446 ) ) ;
#2156=CARTESIAN_POINT ( 'NONE',  ( 41.64333658814960870, 59.51518717409400239, 30.00020018409699318 ) ) ;
#2158=CARTESIAN_POINT ( 'NONE',  ( 41.46631938032478359, 159.1104996726487570, 29.45539723777780239 ) ) ;
#2159=CARTESIAN_POINT ( 'NONE',  ( 38.58424406990784661, 98.96518717409398391, 32.77220824515698183 ) ) ;
#2163=CARTESIAN_POINT ( 'NONE',  ( 48.01140435219951996, 145.2844580088725763, 34.21067981925357060 ) ) ;
#2164=CARTESIAN_POINT ( 'NONE',  ( 41.64333658814960870, 116.7797705074273296, 30.00020018409699318 ) ) ;
#2166=CARTESIAN_POINT ( 'NONE',  ( 38.58424406990785371, 110.9651871740940123, 32.77220824515697473 ) ) ;
#2167=ORIENTED_EDGE ( 'NONE', *, *, #19885, .T. ) ;
#2174=CARTESIAN_POINT ( 'NONE',  ( 38.58424406990785371, 84.52977050742731535, 35.64915139335015937 ) ) ;
#2176=CARTESIAN_POINT ( 'NONE',  ( 44.55648932407425633, 61.88445800887257064, 29.45539723777780239 ) ) ;
#2178=CARTESIAN_POINT ( 'NONE',  ( 38.01140435219951996, 129.5604996726487457, 32.58608133808903773 ) ) ;
#2179=CARTESIAN_POINT ( 'NONE',  ( 40.27526882409969033, 86.66518717409400097, 30.44471234641811819 ) ) ;
#2181=( BOUNDED_CURVE ( )  B_SPLINE_CURVE ( 2, ( #5019, #15037, #6682, #3477, #15148, #20443, #7003, #15375, #16904, #21776, #13814, #10201, #1918 ),
 .UNSPECIFIED., .F., .T. ) 
 B_SPLINE_CURVE_WITH_KNOTS ( ( 3, 2, 2, 2, 2, 2, 3 ),
 ( 0.6544117647058823595, 0.6558823529411764719, 0.6588235294117646967, 0.6617647058823529216, 0.6647058823529411464, 0.6676470588235293713, 0.6691176470588234837 ),
 .UNSPECIFIED. ) 
 CURVE ( )  GEOMETRIC_REPRESENTATION_ITEM ( )  RATIONAL_B_SPLINE_CURVE ( ( 0.9755282581475768211, 0.9755282581475768211, 1.000000000000000000, 0.9510565162951535312, 1.000000000000000000, 0.9510565162951535312, 1.000000000000000000, 0.9510565162951535312, 1.000000000000000000, 0.9510565162951535312, 1.000000000000000000, 0.9755282581475768211, 0.9755282581475768211 ) ) 
 REPRESENTATION_ITEM ( '' )  );
#2184=CARTESIAN_POINT ( 'NONE',  ( 41.46631938032478359, 94.31049967264874567, 38.96596240072933170 ) ) ;
#2185=CARTESIAN_POINT ( 'NONE',  ( 44.55648932407425633, 126.6844580088725678, 38.96596240072933170 ) ) ;
#2189=CARTESIAN_POINT ( 'NONE',  ( 48.01140435219951996, 68.06049967264874567, 35.83527830041809636 ) ) ;
#2190=CARTESIAN_POINT ( 'NONE',  ( 44.55648932407425633, 143.8104996726487457, 29.45539723777780239 ) ) ;
#2191=CARTESIAN_POINT ( 'NONE',  ( 47.43856463449117200, 142.7297705074273324, 35.64915139335016647 ) ) ;
#2192=CARTESIAN_POINT ( 'NONE',  ( 46.59305225739526435, 103.5797705074273267, 36.81289934271958941 ) ) ;
#2194=CARTESIAN_POINT ( 'NONE',  ( 44.37947211624943833, 136.0151871740939953, 38.42115945441014446 ) ) ;
#2196=DIRECTION ( 'NONE',  ( 0.000000000000000000, 1.000000000000000000, 0.000000000000000000 ) ) ;
#2198=CARTESIAN_POINT ( 'NONE',  ( 43.01140435219951286, 67.12977050742732388, 38.86567161673127657 ) ) ;
#2202=CARTESIAN_POINT ( 'NONE',  ( 43.01140435219951286, 114.8651871740939754, 38.86567161673127657 ) ) ;
#2205=CARTESIAN_POINT ( 'NONE',  ( 48.01140435219951996, 106.2844580088725763, 34.21067981925357060 ) ) ;
#2206=CARTESIAN_POINT ( 'NONE',  ( 38.58424406990786082, 147.3797705074273097, 34.21067981925357060 ) ) ;
#2207=EDGE_CURVE ( 'NONE', #14908, #1684, #11948, .T. ) ;
#2208=CARTESIAN_POINT ( 'NONE',  ( 47.43856463449118621, 61.87977050742732388, 34.21067981925357060 ) ) ;
#2209=CARTESIAN_POINT ( 'NONE',  ( 43.01140435219951286, 119.3651871740939896, 29.55568802177586463 ) ) ;
#2212=CARTESIAN_POINT ( 'NONE',  ( 48.01140435219951996, 68.06049967264874567, 35.83527830041810347 ) ) ;
#2215=CARTESIAN_POINT ( 'NONE',  ( 38.01140435219952707, 71.63445800887258486, 32.58608133808903773 ) ) ;
#2217=CARTESIAN_POINT ( 'NONE',  ( 41.64333658814960870, 68.51518717409399528, 30.00020018409699318 ) ) ;
#2218=CARTESIAN_POINT ( 'NONE',  ( 43.01140435219951286, 103.4604996726487371, 39.21067981925356349 ) ) ;
#2225=CARTESIAN_POINT ( 'NONE',  ( 46.59305225739526435, 142.9151871740940294, 31.60846029578754468 ) ) ;
#2226=DIRECTION ( 'NONE',  ( 0.000000000000000000, 1.000000000000000000, 0.000000000000000000 ) ) ;
#2227=CARTESIAN_POINT ( 'NONE',  ( 38.58424406990786082, 102.3797705074273381, 34.21067981925357060 ) ) ;
#2232=ORIENTED_EDGE ( 'NONE', *, *, #18992, .F. ) ;
#2234=CARTESIAN_POINT ( 'NONE',  ( 46.10157429594899270, 89.66049967264873999, 29.95742577749336988 ) ) ;
#2235=CARTESIAN_POINT ( 'NONE',  ( 40.27526882409969033, 147.5651871740939498, 37.97664729208901946 ) ) ;
#2236=CARTESIAN_POINT ( 'NONE',  ( 39.92123440845004723, 105.2604996726487627, 29.95742577749337343 ) ) ;
#2238=CARTESIAN_POINT ( 'NONE',  ( 43.01140435219951286, 119.9604996726487229, 29.21067981925356705 ) ) ;
#2241=CARTESIAN_POINT ( 'NONE',  ( 48.01140435219951996, 64.43445800887258201, 32.58608133808903773 ) ) ;
#2242=CARTESIAN_POINT ( 'NONE',  ( 43.80332655382220253, 105.6113394311928460, 39.21067981925355639 ) ) ;
#2243=ORIENTED_EDGE ( 'NONE', *, *, #12450, .T. ) ;
#2244=CARTESIAN_POINT ( 'NONE',  ( 44.37947211624943833, 86.47977050742731819, 30.00020018409699318 ) ) ;
#2246=CARTESIAN_POINT ( 'NONE',  ( 41.64333658814960870, 75.71518717409401233, 38.42115945441014446 ) ) ;
#2249=ORIENTED_EDGE ( 'NONE', *, *, #16232, .F. ) ;
#2250=CARTESIAN_POINT ( 'NONE',  ( 38.96631938032478359, 118.0104996726487485, 37.14960608071593384 ) ) ;
#2252=CARTESIAN_POINT ( 'NONE',  ( 47.43856463449117911, 131.0297705074272869, 32.77220824515697473 ) ) ;
#2255=PLANE ( 'NONE',  #17823 ) ;
#2257=CARTESIAN_POINT ( 'NONE',  ( 40.27526882409969033, 132.8297705074273267, 37.97664729208901946 ) ) ;
#2261=CARTESIAN_POINT ( 'NONE',  ( 38.58424406990784661, 99.26518717409396686, 35.64915139335016647 ) ) ;
#2267=CARTESIAN_POINT ( 'NONE',  ( 48.01140435219951996, 130.4344580088725820, 32.58608133808903773 ) ) ;
#2268=CARTESIAN_POINT ( 'NONE',  ( 38.58424406990786082, 114.3797705074273097, 34.21067981925357060 ) ) ;
#2271=CARTESIAN_POINT ( 'NONE',  ( 39.42975644700377558, 107.8151871740939924, 31.60846029578754468 ) ) ;
#2277=CARTESIAN_POINT ( 'NONE',  ( 44.37947211624943833, 79.27977050742731535, 38.42115945441014446 ) ) ;
#2278=ORIENTED_EDGE ( 'NONE', *, *, #19182, .T. ) ;
#2279=CARTESIAN_POINT ( 'NONE',  ( 47.05648932407426344, 63.98445800887257917, 37.14960608071593384 ) ) ;
#2281=CARTESIAN_POINT ( 'NONE',  ( 48.01140435219951996, 125.2104996726487514, 34.21067981925357060 ) ) ;
#2282=CARTESIAN_POINT ( 'NONE',  ( 38.58424406990786082, 78.11518717409400381, 34.21067981925357060 ) ) ;
#2288=CYLINDRICAL_SURFACE ( 'NONE', #7550, 4.999999999999997335 ) ;
#2289=CARTESIAN_POINT ( 'NONE',  ( 38.01140435219952707, 158.7844580088725763, 34.21067981925357060 ) ) ;
#2290=CARTESIAN_POINT ( 'NONE',  ( 41.64333658814960870, 146.7797705074273154, 30.00020018409699318 ) ) ;
#2291=CARTESIAN_POINT ( 'NONE',  ( 44.37947211624943833, 106.2797705074273154, 38.42115945441014446 ) ) ;
#2293=CARTESIAN_POINT ( 'NONE',  ( 41.64333658814960870, 132.7151871740940123, 38.42115945441014446 ) ) ;
#2296=CARTESIAN_POINT ( 'NONE',  ( 39.42975644700377558, 60.67977050742731393, 36.81289934271958941 ) ) ;
#2300=CARTESIAN_POINT ( 'NONE',  ( 43.01140435219951996, 2.710499672648754466, 34.21067981925357060 ) ) ;
#2301=CARTESIAN_POINT ( 'NONE',  ( 44.37947211624943833, 115.0151871740940095, 38.42115945441014446 ) ) ;
#2307=CARTESIAN_POINT ( 'NONE',  ( 38.96631938032478359, 93.08445800887257349, 37.14960608071593384 ) ) ;
#2308=CARTESIAN_POINT ( 'NONE',  ( 45.74753988029934249, 151.4297705074273210, 37.97664729208901235 ) ) ;
#2309=CARTESIAN_POINT ( 'NONE',  ( 44.37947211624943833, 59.47977050742732530, 30.00020018409699318 ) ) ;
#2310=CARTESIAN_POINT ( 'NONE',  ( 47.43856463449118621, 103.6151871740940038, 34.21067981925357060 ) ) ;
#2312=CARTESIAN_POINT ( 'NONE',  ( 38.96631938032478359, 76.01049967264873430, 37.14960608071593384 ) ) ;
#2314=CARTESIAN_POINT ( 'NONE',  ( 48.01140435219951996, 136.2844580088726048, 34.21067981925357060 ) ) ;
#2316=CIRCLE ( 'NONE', #9711, 4.999999999999997335 ) ;
#2327=CARTESIAN_POINT ( 'NONE',  ( 44.37947211624943833, 143.2151871740940123, 30.00020018409699318 ) ) ;
#2329=CARTESIAN_POINT ( 'NONE',  ( 40.27526882409969744, 105.8297705074273125, 37.97664729208901235 ) ) ;
#2335=ORIENTED_EDGE ( 'NONE', *, *, #7205, .T. ) ;
#2336=CARTESIAN_POINT ( 'NONE',  ( 46.10157429594899270, 114.8344580088725877, 38.46393386101376421 ) ) ;
#2337=CARTESIAN_POINT ( 'NONE',  ( 39.92123440845005433, 75.26049967264873430, 29.95742577749336988 ) ) ;
#2338=CARTESIAN_POINT ( 'NONE',  ( 40.27526882409969033, 83.92977050742732104, 30.44471234641811819 ) ) ;
#2339=CARTESIAN_POINT ( 'NONE',  ( 44.37947211624943833, 143.2151871740940123, 30.00020018409699318 ) ) ;
#2340=CARTESIAN_POINT ( 'NONE',  ( 39.92123440845004723, 99.26049967264876273, 29.95742577749337343 ) ) ;
#2345=CARTESIAN_POINT ( 'NONE',  ( 38.96631938032478359, 152.4844580088725934, 31.27175355779120025 ) ) ;
#2347=CARTESIAN_POINT ( 'NONE',  ( 44.55648932407425633, 105.6844580088725820, 38.96596240072933170 ) ) ;
#2351=CARTESIAN_POINT ( 'NONE',  ( 47.43856463449117200, 88.72977050742730398, 35.64915139335016647 ) ) ;
#2353=CARTESIAN_POINT ( 'NONE',  ( 39.42975644700377558, 71.81518717409400665, 31.60846029578754468 ) ) ;
#2357=CARTESIAN_POINT ( 'NONE',  ( 41.46631938032478359, 117.1104996726487428, 29.45539723777780239 ) ) ;
#2358=DIRECTION ( 'NONE',  ( 0.000000000000000000, 0.000000000000000000, 1.000000000000000000 ) ) ;
#2359=CARTESIAN_POINT ( 'NONE',  ( 47.43856463449117911, 136.7297705074273040, 35.64915139335015937 ) ) ;
#2363=ORIENTED_EDGE ( 'NONE', *, *, #1940, .F. ) ;
#2364=VECTOR ( 'NONE', #12399, 1000.000000000000000 ) ;
#2365=CARTESIAN_POINT ( 'NONE',  ( 44.37947211624943833, 136.2797705074273154, 38.42115945441014446 ) ) ;
#2366=DIRECTION ( 'NONE',  ( 0.000000000000000000, 0.000000000000000000, 1.000000000000000000 ) ) ;
#2367=CARTESIAN_POINT ( 'NONE',  ( 46.59305225739526435, 92.17977050742732104, 31.60846029578754468 ) ) ;
#2370=CARTESIAN_POINT ( 'NONE',  ( 38.01140435219952707, 159.7104996726487514, 34.21067981925357060 ) ) ;
#2373=CARTESIAN_POINT ( 'NONE',  ( 47.43856463449118621, 94.61518717409400381, 34.21067981925357060 ) ) ;
#2374=CARTESIAN_POINT ( 'NONE',  ( 48.01140435219951996, 133.1344580088725706, 35.83527830041809636 ) ) ;
#2378=CARTESIAN_POINT ( 'NONE',  ( 46.10157429594899270, 70.76049967264873430, 38.46393386101375711 ) ) ;
#2379=CARTESIAN_POINT ( 'NONE',  ( 39.92123440845004723, 129.2344580088725934, 38.46393386101376421 ) ) ;
#2380=CARTESIAN_POINT ( 'NONE',  ( 45.74753988029933538, 109.4297705074273210, 37.97664729208901946 ) ) ;
#2383=CARTESIAN_POINT ( 'NONE',  ( 45.74753988029934249, 109.1651871740940010, 37.97664729208901235 ) ) ;
#2387=CARTESIAN_POINT ( 'NONE',  ( 44.55648932407425633, 156.6844580088725820, 38.96596240072933170 ) ) ;
#2391=CARTESIAN_POINT ( 'NONE',  ( 44.37947211624943833, 73.27977050742731535, 38.42115945441014446 ) ) ;
#2392=ORIENTED_EDGE ( 'NONE', *, *, #15713, .T. ) ;
#2396=CARTESIAN_POINT ( 'NONE',  ( 47.05648932407426344, 121.9104996726487542, 37.14960608071593384 ) ) ;
#2397=CARTESIAN_POINT ( 'NONE',  ( 40.27526882409969033, 80.66518717409400097, 30.44471234641811819 ) ) ;
#2403=CARTESIAN_POINT ( 'NONE',  ( 0.000000000000000000, 0.000000000000000000, 0.000000000000000000 ) ) ;
#2406=CARTESIAN_POINT ( 'NONE',  ( 38.58424406990786082, 138.3797705074273381, 34.21067981925357060 ) ) ;
#2408=CARTESIAN_POINT ( 'NONE',  ( 40.27526882409969744, 134.6651871740940010, 30.44471234641812174 ) ) ;
#2411=CARTESIAN_POINT ( 'NONE',  ( 48.01140435219951996, 91.28445800887257633, 34.21067981925357060 ) ) ;
#2413=CARTESIAN_POINT ( 'NONE',  ( 43.01140435219951286, 101.9604996726487371, 29.21067981925356705 ) ) ;
#2414=CARTESIAN_POINT ( 'NONE',  ( 43.01140435219951286, 117.8651871740939754, 38.86567161673127657 ) ) ;
#2415=ORIENTED_EDGE ( 'NONE', *, *, #12477, .T. ) ;
#2416=CARTESIAN_POINT ( 'NONE',  ( 43.01140435219951996, 10.71049967264875491, 34.21067981925357060 ) ) ;
#2418=CARTESIAN_POINT ( 'NONE',  ( 41.46631938032478359, 87.38445800887258486, 38.96596240072933170 ) ) ;
#2419=CARTESIAN_POINT ( 'NONE',  ( 38.58424406990785371, 150.2297705074273040, 32.77220824515697473 ) ) ;
#2420=CARTESIAN_POINT ( 'NONE',  ( 43.01140435219951286, 145.4604996726487229, 39.46799094044489209 ) ) ;
#2421=CARTESIAN_POINT ( 'NONE',  ( 44.37947211624943833, 103.0151871740939953, 38.42115945441014446 ) ) ;
#2423=CARTESIAN_POINT ( 'NONE',  ( 47.05648932407426344, 76.91049967264873999, 37.14960608071593384 ) ) ;
#2425=CARTESIAN_POINT ( 'NONE',  ( 48.01140435219951996, 61.28445800887258343, 34.21067981925357060 ) ) ;
#2426=CARTESIAN_POINT ( 'NONE',  ( 43.01140435219951996, 10.71049967264875491, 39.21067981925356349 ) ) ;
#2427=VECTOR ( 'NONE', #15194, 1000.000000000000000 ) ;
#2428=CARTESIAN_POINT ( 'NONE',  ( 43.01140435219951996, 10.71049967264875491, 34.21067981925357060 ) ) ;
#2430=CARTESIAN_POINT ( 'NONE',  ( 40.27526882409969033, 66.56518717409400665, 37.97664729208901946 ) ) ;
#2431=DIRECTION ( 'NONE',  ( 0.000000000000000000, 1.000000000000000000, 0.000000000000000000 ) ) ;
#2434=ORIENTED_EDGE ( 'NONE', *, *, #13221, .T. ) ;
#2437=CARTESIAN_POINT ( 'NONE',  ( 38.58424406990784661, 144.2651871740940237, 35.64915139335016647 ) ) ;
#2438=CARTESIAN_POINT ( 'NONE',  ( 41.64333658814960870, 104.7797705074273154, 30.00020018409699318 ) ) ;
#2444=CARTESIAN_POINT ( 'NONE',  ( 47.05648932407426344, 114.9844580088725792, 37.14960608071593384 ) ) ;
#2446=CARTESIAN_POINT ( 'NONE',  ( 38.58424406990784661, 75.22977050742730398, 32.77220824515698183 ) ) ;
#2447=CARTESIAN_POINT ( 'NONE',  ( 46.59305225739526435, 136.9151871740940010, 31.60846029578754468 ) ) ;
#2448=CARTESIAN_POINT ( 'NONE',  ( 38.01140435219951996, 105.5604996726487173, 32.58608133808903773 ) ) ;
#2453=LINE ( 'NONE', #16000, #13982 ) ;
#2454=CARTESIAN_POINT ( 'NONE',  ( 43.01140435219951996, 10.71049967264875491, 34.21067981925357060 ) ) ;
#2455=( GEOMETRIC_REPRESENTATION_CONTEXT ( 3 ) GLOBAL_UNCERTAINTY_ASSIGNED_CONTEXT ( ( #3580 ) ) GLOBAL_UNIT_ASSIGNED_CONTEXT ( ( #3502, #19924, #18484 ) ) REPRESENTATION_CONTEXT ( 'NONE', 'WORKASPACE' ) );
#2457=CARTESIAN_POINT ( 'NONE',  ( 41.64333658814960870, 87.97977050742731819, 38.42115945441014446 ) ) ;
#2464=CARTESIAN_POINT ( 'NONE',  ( 40.27526882409969744, 137.9297705074273210, 30.44471234641812174 ) ) ;
#2468=EDGE_LOOP ( 'NONE', ( #13014, #8962, #5399, #8911 ) ) ;
#2469=CARTESIAN_POINT ( 'NONE',  ( 39.42975644700377558, 123.6797705074273210, 36.81289934271958941 ) ) ;
#2470=CARTESIAN_POINT ( 'NONE',  ( 46.10157429594899270, 138.8344580088725877, 38.46393386101375711 ) ) ;
#2472=CARTESIAN_POINT ( 'NONE',  ( 46.10157429594899270, 155.6604996726487116, 29.95742577749336988 ) ) ;
#2474=DIRECTION ( 'NONE',  ( 0.000000000000000000, 1.000000000000000000, 0.000000000000000000 ) ) ;
#2475=DIRECTION ( 'NONE',  ( 0.000000000000000000, 1.000000000000000000, 0.000000000000000000 ) ) ;
#2477=CARTESIAN_POINT ( 'NONE',  ( 44.37947211624943833, 100.0151871740939953, 38.42115945441014446 ) ) ;
#2481=CARTESIAN_POINT ( 'NONE',  ( 43.01140435219957681, 71.96049967264872294, 29.21067981925356705 ) ) ;
#2482=CARTESIAN_POINT ( 'NONE',  ( 39.92123440845004723, 137.3344580088725593, 29.95742577749337343 ) ) ;
#2483=CARTESIAN_POINT ( 'NONE',  ( 39.42975644700377558, 114.0797705074273125, 31.60846029578754468 ) ) ;
#2486=CARTESIAN_POINT ( 'NONE',  ( 45.74753988029934249, 95.06518717409399244, 30.44471234641812174 ) ) ;
#2490=CARTESIAN_POINT ( 'NONE',  ( 43.80332655382220253, 76.95757658655229250, 29.21067981925356705 ) ) ;
#2493=CARTESIAN_POINT ( 'NONE',  ( 43.80332655382220253, 154.9575765865523067, 29.21067981925356705 ) ) ;
#2494=CARTESIAN_POINT ( 'NONE',  ( 43.01140435219951286, 80.62977050742732388, 29.55568802177586107 ) ) ;
#2500=CARTESIAN_POINT ( 'NONE',  ( 38.01140435219951996, 120.8604996726487428, 35.83527830041810347 ) ) ;
#2501=CARTESIAN_POINT ( 'NONE',  ( 46.59305225739526435, 73.91518717409400097, 31.60846029578754468 ) ) ;
#2509=CARTESIAN_POINT ( 'NONE',  ( 40.27526882409969033, 141.8297705074273267, 37.97664729208901946 ) ) ;
#2511=CARTESIAN_POINT ( 'NONE',  ( 39.42975644700377558, 126.4151871740940010, 36.81289934271958941 ) ) ;
#2514=CARTESIAN_POINT ( 'NONE',  ( 43.01140435219951286, 59.62977050742730967, 29.55568802177586463 ) ) ;
#2517=CYLINDRICAL_SURFACE ( 'NONE', #19740, 4.999999999999997335 ) ;
#2518=CARTESIAN_POINT ( 'NONE',  ( 38.58424406990786082, 108.1151871740940038, 34.21067981925357060 ) ) ;
#2519=ORIENTED_EDGE ( 'NONE', *, *, #2728, .T. ) ;
#2522=ORIENTED_EDGE ( 'NONE', *, *, #3156, .F. ) ;
#2523=CARTESIAN_POINT ( 'NONE',  ( 41.46631938032478359, 92.18445800887258201, 29.45539723777780239 ) ) ;
#2524=CARTESIAN_POINT ( 'NONE',  ( 46.59305225739526435, 149.1797705074273210, 31.60846029578754468 ) ) ;
#2528=CARTESIAN_POINT ( 'NONE',  ( 41.46631938032478359, 145.3104996726487457, 38.96596240072933170 ) ) ;
#2529=CARTESIAN_POINT ( 'NONE',  ( 38.58424406990784661, 104.9651871740940123, 32.77220824515698183 ) ) ;
#2531=CARTESIAN_POINT ( 'NONE',  ( 43.01140435219951996, 10.71049967264875491, 29.21067981925357060 ) ) ;
#2533=DIRECTION ( 'NONE',  ( 0.000000000000000000, 0.000000000000000000, 1.000000000000000000 ) ) ;
#2544=FACE_OUTER_BOUND ( 'NONE', #1416, .T. ) ;
#2545=CARTESIAN_POINT ( 'NONE',  ( 39.42975644700377558, 138.4151871740940010, 36.81289934271958941 ) ) ;
#2546=CARTESIAN_POINT ( 'NONE',  ( 40.27526882409969744, 98.92977050742732104, 30.44471234641812174 ) ) ;
#2552=CARTESIAN_POINT ( 'NONE',  ( 48.01140435219951996, 112.4344580088725678, 32.58608133808903773 ) ) ;
#2553=CARTESIAN_POINT ( 'NONE',  ( 38.01140435219952707, 75.56049967264873146, 32.58608133808903773 ) ) ;
#2554=CARTESIAN_POINT ( 'NONE',  ( 45.74753988029933538, 76.42977050742729261, 37.97664729208901946 ) ) ;
#2555=CARTESIAN_POINT ( 'NONE',  ( 38.58424406990784661, 132.2651871740939953, 35.64915139335016647 ) ) ;
#2556=CARTESIAN_POINT ( 'NONE',  ( 38.96631938032478359, 93.41049967264873999, 31.27175355779120025 ) ) ;
#2560=CARTESIAN_POINT ( 'NONE',  ( 38.01140435219952707, 152.9344580088725536, 35.83527830041809636 ) ) ;
#2561=CARTESIAN_POINT ( 'NONE',  ( 42.21948215057684450, 144.4575765865522783, 39.21067981925355639 ) ) ;
#2564=CARTESIAN_POINT ( 'NONE',  ( 41.64333658814960870, 71.77977050742731535, 30.00020018409699318 ) ) ;
#2565=( BOUNDED_CURVE ( )  B_SPLINE_CURVE ( 2, ( #15957, #870, #10908, #542, #17611, #7605, #14307, #21050, #18156, #13096, #14524, #6258, #16495 ),
 .UNSPECIFIED., .F., .T. ) 
 B_SPLINE_CURVE_WITH_KNOTS ( ( 3, 2, 2, 2, 2, 2, 3 ),
 ( 0.3750000000000000000, 0.3764705882352941124, 0.3794117647058823373, 0.3823529411764705621, 0.3852941176470588425, 0.3882352941176470673, 0.3897058823529411797 ),
 .UNSPECIFIED. ) 
 CURVE ( )  GEOMETRIC_REPRESENTATION_ITEM ( )  RATIONAL_B_SPLINE_CURVE ( ( 0.9755282581475768211, 0.9755282581475768211, 1.000000000000000000, 0.9510565162951535312, 1.000000000000000000, 0.9510565162951535312, 1.000000000000000000, 0.9510565162951535312, 1.000000000000000000, 0.9510565162951535312, 1.000000000000000000, 0.9755282581475768211, 0.9755282581475768211 ) ) 
 REPRESENTATION_ITEM ( '' )  );
#2570=CARTESIAN_POINT ( 'NONE',  ( 43.01140435219951286, 86.03445800887256212, 29.21067981925356705 ) ) ;
#2571=CARTESIAN_POINT ( 'NONE',  ( 41.64333658814960870, 122.7797705074273296, 30.00020018409699318 ) ) ;
#2575=CARTESIAN_POINT ( 'NONE',  ( 41.64333658814960870, 129.9797705074273040, 38.42115945441014446 ) ) ;
#2576=CARTESIAN_POINT ( 'NONE',  ( 47.05648932407426344, 144.9844580088725934, 37.14960608071593384 ) ) ;
#2577=ADVANCED_FACE ( 'NONE', ( #20626 ), #13998, .T. ) ;
#2578=CARTESIAN_POINT ( 'NONE',  ( 39.92123440845005433, 110.3344580088725735, 29.95742577749336988 ) ) ;
#2582=CARTESIAN_POINT ( 'NONE',  ( 42.21948215057684450, 90.45757658655230671, 39.21067981925355639 ) ) ;
#2586=CARTESIAN_POINT ( 'NONE',  ( 38.01140435219951996, 137.6344580088725991, 32.58608133808903773 ) ) ;
#2587=CARTESIAN_POINT ( 'NONE',  ( 46.59305225739526435, 104.1797705074273210, 31.60846029578754468 ) ) ;
#2590=CARTESIAN_POINT ( 'NONE',  ( 38.58424406990785371, 93.26518717409400949, 35.64915139335015937 ) ) ;
#2591=CARTESIAN_POINT ( 'NONE',  ( 43.01140435219951996, 10.71049967264875491, 29.21067981925357060 ) ) ;
#2593=CARTESIAN_POINT ( 'NONE',  ( 38.01140435219952707, 87.56049967264873146, 32.58608133808903773 ) ) ;
#2597=CARTESIAN_POINT ( 'NONE',  ( 40.27526882409969744, 80.92977050742730682, 30.44471234641812174 ) ) ;
#2598=EDGE_LOOP ( 'NONE', ( #791, #15937, #339, #11454 ) ) ;
#2601=CARTESIAN_POINT ( 'NONE',  ( 46.59305225739526435, 157.5797705074273267, 36.81289934271958941 ) ) ;
#2602=LINE ( 'NONE', #8124, #17554 ) ;
#2603=AXIS2_PLACEMENT_3D ( 'NONE', #20097, #8623, #20628 ) ;
#2604=EDGE_CURVE ( 'NONE', #711, #10505, #8246, .T. ) ;
#2605=CARTESIAN_POINT ( 'NONE',  ( 38.01140435219952707, 117.7104996726487371, 34.21067981925357060 ) ) ;
#2606=CARTESIAN_POINT ( 'NONE',  ( 44.37947211624943833, 80.21518717409399812, 30.00020018409699318 ) ) ;
#2609=CARTESIAN_POINT ( 'NONE',  ( 43.01140435219954838, 131.9604996726487229, 29.21067981925356705 ) ) ;
#2612=CARTESIAN_POINT ( 'NONE',  ( 42.21948215057684450, 150.4575765865522783, 39.21067981925356349 ) ) ;
#2613=CARTESIAN_POINT ( 'NONE',  ( 43.01140435219951286, 146.6297705074273381, 29.55568802177586463 ) ) ;
#2615=CARTESIAN_POINT ( 'NONE',  ( 43.01140435219951286, 123.8651871740939896, 38.86567161673127657 ) ) ;
#2618=CARTESIAN_POINT ( 'NONE',  ( 40.27526882409969033, 59.92977050742730682, 30.44471234641811819 ) ) ;
#2622=CARTESIAN_POINT ( 'NONE',  ( 47.43856463449117200, 106.4651871740939981, 35.64915139335016647 ) ) ;
#2623=( BOUNDED_CURVE ( )  B_SPLINE_CURVE ( 2, ( #13699, #6673, #5008, #15366, #5427, #10406, #12046, #13804, #20434, #18453, #258, #16788, #18775 ),
 .UNSPECIFIED., .F., .F. ) 
 B_SPLINE_CURVE_WITH_KNOTS ( ( 3, 2, 2, 2, 2, 2, 3 ),
 ( 0.2867647058823529216, 0.2882352941176470340, 0.2911764705882353144, 0.2941176470588235392, 0.2970588235294117641, 0.2999999999999999889, 0.3014705882352941013 ),
 .UNSPECIFIED. ) 
 CURVE ( )  GEOMETRIC_REPRESENTATION_ITEM ( )  RATIONAL_B_SPLINE_CURVE ( ( 0.9755282581475768211, 0.9755282581475768211, 1.000000000000000000, 0.9510565162951535312, 1.000000000000000000, 0.9510565162951535312, 1.000000000000000000, 0.9510565162951535312, 1.000000000000000000, 0.9510565162951535312, 1.000000000000000000, 0.9755282581475768211, 0.9755282581475768211 ) ) 
 REPRESENTATION_ITEM ( '' )  );
#2627=CARTESIAN_POINT ( 'NONE',  ( 48.01140435219951996, 88.28445800887257633, 34.21067981925357060 ) ) ;
#2629=CARTESIAN_POINT ( 'NONE',  ( 47.05648932407426344, 152.5104996726487343, 31.27175355779120025 ) ) ;
#2630=CARTESIAN_POINT ( 'NONE',  ( 38.58424406990786082, 102.1151871740940180, 34.21067981925357060 ) ) ;
#2632=CARTESIAN_POINT ( 'NONE',  ( 43.01140435219951286, 65.96049967264873715, 28.95336869806222779 ) ) ;
#2634=CARTESIAN_POINT ( 'NONE',  ( 43.80332655382220253, 60.61133943119284595, 39.21067981925355639 ) ) ;
#2638=CARTESIAN_POINT ( 'NONE',  ( 44.37947211624943833, 73.01518717409399528, 38.42115945441014446 ) ) ;
#2640=CARTESIAN_POINT ( 'NONE',  ( 43.01140435219951286, 95.96049967264873715, 29.21067981925356705 ) ) ;
#2648=CARTESIAN_POINT ( 'NONE',  ( 44.37947211624943833, 139.0151871740939953, 38.42115945441014446 ) ) ;
#2649=CARTESIAN_POINT ( 'NONE',  ( 39.42975644700377558, 93.07977050742731251, 31.60846029578754468 ) ) ;
#2651=EDGE_LOOP ( 'NONE', ( #10950, #13324, #7415, #10977 ) ) ;
#2654=CARTESIAN_POINT ( 'NONE',  ( 46.10157429594899270, 112.7344580088725792, 29.95742577749337343 ) ) ;
#2655=CARTESIAN_POINT ( 'NONE',  ( 43.01140435219951996, 10.71049967264875491, 34.21067981925357060 ) ) ;
#2656=CARTESIAN_POINT ( 'NONE',  ( 39.42975644700377558, 81.07977050742731251, 31.60846029578754468 ) ) ;
#2657=CARTESIAN_POINT ( 'NONE',  ( 41.64333658814960870, 138.7151871740940123, 38.42115945441014446 ) ) ;
#2658=CARTESIAN_POINT ( 'NONE',  ( 48.01140435219951996, 89.06049967264871725, 35.83527830041810347 ) ) ;
#2665=CARTESIAN_POINT ( 'NONE',  ( 47.05648932407426344, 106.9104996726487400, 37.14960608071593384 ) ) ;
#2666=DIRECTION ( 'NONE',  ( 0.000000000000000000, 1.000000000000000000, 0.000000000000000000 ) ) ;
#2668=CARTESIAN_POINT ( 'NONE',  ( 40.27526882409969033, 72.82977050742732672, 37.97664729208901946 ) ) ;
#2676=CARTESIAN_POINT ( 'NONE',  ( 43.01140435219951286, 123.5344580088725621, 39.21067981925356349 ) ) ;
#2677=CARTESIAN_POINT ( 'NONE',  ( 46.59305225739526435, 125.1797705074273210, 31.60846029578754468 ) ) ;
#2679=CARTESIAN_POINT ( 'NONE',  ( 43.01140435219951996, 10.71049967264875491, 34.21067981925357060 ) ) ;
#2681=CARTESIAN_POINT ( 'NONE',  ( 47.43856463449117200, 122.0297705074273011, 32.77220824515698183 ) ) ;
#2683=CARTESIAN_POINT ( 'NONE',  ( 43.80332655382220253, 144.6113394311928744, 39.21067981925355639 ) ) ;
#2684=CARTESIAN_POINT ( 'NONE',  ( 38.01140435219951996, 59.63445800887255643, 32.58608133808903773 ) ) ;
#2692=CARTESIAN_POINT ( 'NONE',  ( 39.92123440845005433, 66.26049967264874851, 29.95742577749336988 ) ) ;
#2696=CARTESIAN_POINT ( 'NONE',  ( 43.01140435219951286, 134.0344580088726048, 28.95336869806222779 ) ) ;
#2697=CARTESIAN_POINT ( 'NONE',  ( 38.58424406990784661, 108.5297705074273011, 35.64915139335016647 ) ) ;
#2700=CARTESIAN_POINT ( 'NONE',  ( 38.58424406990785371, 102.2651871740939811, 35.64915139335015937 ) ) ;
#2704=ADVANCED_FACE ( 'NONE', ( #6860 ), #10706, .T. ) ;
#2706=CARTESIAN_POINT ( 'NONE',  ( 45.74753988029934249, 146.3297705074273267, 30.44471234641812174 ) ) ;
#2710=CARTESIAN_POINT ( 'NONE',  ( 47.43856463449117911, 76.72977050742731819, 35.64915139335015937 ) ) ;
#2711=ORIENTED_EDGE ( 'NONE', *, *, #8181, .F. ) ;
#2713=CARTESIAN_POINT ( 'NONE',  ( 40.27526882409969033, 153.8297705074273267, 37.97664729208901946 ) ) ;
#2716=CARTESIAN_POINT ( 'NONE',  ( 43.01140435219951286, 119.9604996726487229, 28.95336869806222779 ) ) ;
#2717=CARTESIAN_POINT ( 'NONE',  ( 41.64333658814960870, 77.51518717409399528, 30.00020018409699318 ) ) ;
#2726=CARTESIAN_POINT ( 'NONE',  ( 42.21948215057684450, 149.1113394311928744, 29.21067981925357060 ) ) ;
#2727=CARTESIAN_POINT ( 'NONE',  ( 47.43856463449118621, 133.8797705074273381, 34.21067981925357060 ) ) ;
#2728=EDGE_CURVE ( 'NONE', #14631, #14663, #15698, .T. ) ;
#2730=CARTESIAN_POINT ( 'NONE',  ( 44.37947211624943833, 128.2151871740939839, 30.00020018409699318 ) ) ;
#2732=CARTESIAN_POINT ( 'NONE',  ( 38.01140435219952707, 150.5604996726487457, 32.58608133808903773 ) ) ;
#2736=AXIS2_PLACEMENT_3D ( 'NONE', #20692, #841, #10665 ) ;
#2738=CARTESIAN_POINT ( 'NONE',  ( 43.01140435219951286, 110.3651871740939754, 29.55568802177586463 ) ) ;
#2739=ORIENTED_EDGE ( 'NONE', *, *, #19264, .T. ) ;
#2741=CARTESIAN_POINT ( 'NONE',  ( 48.01140435219951996, 86.21049967264873715, 34.21067981925357060 ) ) ;
#2743=CARTESIAN_POINT ( 'NONE',  ( 43.01140435219951286, 92.03445800887256212, 28.95336869806222779 ) ) ;
#2744=DIRECTION ( 'NONE',  ( 0.000000000000000000, 0.000000000000000000, 1.000000000000000000 ) ) ;
#2745=CARTESIAN_POINT ( 'NONE',  ( 46.10157429594899270, 146.6604996726487400, 29.95742577749337343 ) ) ;
#2746=CARTESIAN_POINT ( 'NONE',  ( 39.42975644700377558, 107.8151871740939924, 31.60846029578754468 ) ) ;
#2749=DIRECTION ( 'NONE',  ( 0.000000000000000000, 1.000000000000000000, 0.000000000000000000 ) ) ;
#2750=FACE_OUTER_BOUND ( 'NONE', #21346, .T. ) ;
#2751=CARTESIAN_POINT ( 'NONE',  ( 44.55648932407425633, 79.88445800887257064, 29.45539723777780239 ) ) ;
#2753=CARTESIAN_POINT ( 'NONE',  ( 43.01140435219951286, 65.36518717409400381, 29.55568802177586463 ) ) ;
#2754=EDGE_CURVE ( 'NONE', #17127, #13513, #13456, .T. ) ;
#2756=CARTESIAN_POINT ( 'NONE',  ( 38.01140435219952707, 114.8604996726487428, 35.83527830041809636 ) ) ;
#2759=ORIENTED_EDGE ( 'NONE', *, *, #9496, .T. ) ;
#2760=CARTESIAN_POINT ( 'NONE',  ( 44.37947211624943833, 70.01518717409399528, 38.42115945441014446 ) ) ;
#2761=( BOUNDED_CURVE ( )  B_SPLINE_CURVE ( 2, ( #7654, #9193, #15679, #6389, #15890, #2560, #14027, #14240, #2345, #5975, #19213, #3902, #20760 ),
 .UNSPECIFIED., .F., .F. ) 
 B_SPLINE_CURVE_WITH_KNOTS ( ( 3, 2, 2, 2, 2, 2, 3 ),
 ( 0.05147058823529412214, 0.05294117647058823456, 0.05588235294117647328, 0.05882352941176470507, 0.06176470588235294379, 0.06470588235294118251, 0.06617647058823529493 ),
 .UNSPECIFIED. ) 
 CURVE ( )  GEOMETRIC_REPRESENTATION_ITEM ( )  RATIONAL_B_SPLINE_CURVE ( ( 0.9755282581475768211, 0.9755282581475768211, 1.000000000000000000, 0.9510565162951535312, 1.000000000000000000, 0.9510565162951535312, 1.000000000000000000, 0.9510565162951535312, 1.000000000000000000, 0.9510565162951535312, 1.000000000000000000, 0.9755282581475768211, 0.9755282581475768211 ) ) 
 REPRESENTATION_ITEM ( '' )  );
#2764=CARTESIAN_POINT ( 'NONE',  ( 48.01140435219951996, 112.1344580088725706, 35.83527830041809636 ) ) ;
#2765=CARTESIAN_POINT ( 'NONE',  ( 40.27526882409969033, 132.5651871740940067, 37.97664729208901946 ) ) ;
#2766=CARTESIAN_POINT ( 'NONE',  ( 44.37947211624943833, 154.0151871740940237, 38.42115945441014446 ) ) ;
#2769=ORIENTED_EDGE ( 'NONE', *, *, #21718, .F. ) ;
#2771=ORIENTED_EDGE ( 'NONE', *, *, #19995, .T. ) ;
#2772=CARTESIAN_POINT ( 'NONE',  ( 43.01140435219951286, 59.96049967264874425, 29.21067981925356705 ) ) ;
#2773=EDGE_CURVE ( 'NONE', #12910, #3828, #2316, .T. ) ;
#2775=CARTESIAN_POINT ( 'NONE',  ( 39.42975644700377558, 72.07977050742732672, 31.60846029578754468 ) ) ;
#2776=CARTESIAN_POINT ( 'NONE',  ( 41.64333658814960870, 137.5151871740939953, 30.00020018409699318 ) ) ;
#2777=CARTESIAN_POINT ( 'NONE',  ( 43.01140435219951286, 88.46049967264873715, 39.46799094044489209 ) ) ;
#2781=CARTESIAN_POINT ( 'NONE',  ( 43.80332655382220253, 107.8836182503284675, 29.21067981925356705 ) ) ;
#2783=CARTESIAN_POINT ( 'NONE',  ( 39.42975644700377558, 72.07977050742732672, 31.60846029578754468 ) ) ;
#2790=VECTOR ( 'NONE', #8913, 1000.000000000000000 ) ;
#2792=CARTESIAN_POINT ( 'NONE',  ( 43.01140435219951286, 124.1297705074273097, 38.86567161673127657 ) ) ;
#2795=VERTEX_POINT ( 'NONE', #10919 ) ;
#2796=CARTESIAN_POINT ( 'NONE',  ( 40.27526882409969033, 128.9297705074272926, 30.44471234641811819 ) ) ;
#2799=CARTESIAN_POINT ( 'NONE',  ( 38.96631938032478359, 62.48445800887257917, 31.27175355779120025 ) ) ;
#2801=CARTESIAN_POINT ( 'NONE',  ( 43.01140435219950575, 139.4604996726487514, 39.21067981925356349 ) ) ;
#2802=CARTESIAN_POINT ( 'NONE',  ( 38.01140435219952707, 101.7844580088725905, 34.21067981925357060 ) ) ;
#2805=CARTESIAN_POINT ( 'NONE',  ( 41.46631938032478359, 66.11049967264874283, 29.45539723777780239 ) ) ;
#2809=CARTESIAN_POINT ( 'NONE',  ( 46.10157429594899270, 126.8344580088725451, 38.46393386101376421 ) ) ;
#2810=CARTESIAN_POINT ( 'NONE',  ( 45.74753988029933538, 100.4297705074273210, 37.97664729208901946 ) ) ;
#2813=CARTESIAN_POINT ( 'NONE',  ( 41.64333658814960870, 101.5151871740939953, 30.00020018409699318 ) ) ;
#2815=VERTEX_POINT ( 'NONE', #15864 ) ;
#2816=CARTESIAN_POINT ( 'NONE',  ( 44.55648932407425633, 127.6104996726487570, 38.96596240072933170 ) ) ;
#2819=CARTESIAN_POINT ( 'NONE',  ( 47.43856463449117911, 68.02977050742731535, 32.77220824515697473 ) ) ;
#2820=EDGE_LOOP ( 'NONE', ( #17336, #13853, #8094, #3101 ) ) ;
#2821=EDGE_LOOP ( 'NONE', ( #1120, #8396, #2909, #14667 ) ) ;
#2822=CARTESIAN_POINT ( 'NONE',  ( 46.59305225739526435, 155.1797705074273210, 31.60846029578754468 ) ) ;
#2824=CARTESIAN_POINT ( 'NONE',  ( 44.55648932407425633, 112.6104996726487428, 38.96596240072933170 ) ) ;
#2826=CARTESIAN_POINT ( 'NONE',  ( 38.01140435219952707, 95.78445800887259054, 34.21067981925357060 ) ) ;
#2832=CARTESIAN_POINT ( 'NONE',  ( 38.01140435219952707, 149.7844580088725763, 34.21067981925357060 ) ) ;
#2833=CARTESIAN_POINT ( 'NONE',  ( 40.27526882409969033, 128.9297705074272926, 30.44471234641811819 ) ) ;
#2835=CARTESIAN_POINT ( 'NONE',  ( 41.64333658814960870, 129.7151871740940123, 38.42115945441014446 ) ) ;
#2844=ORIENTED_EDGE ( 'NONE', *, *, #8212, .T. ) ;
#2845=CARTESIAN_POINT ( 'NONE',  ( 44.55648932407425633, 81.68445800887258201, 38.96596240072933170 ) ) ;
#2847=CARTESIAN_POINT ( 'NONE',  ( 47.05648932407426344, 145.9104996726487400, 37.14960608071593384 ) ) ;
#2848=CARTESIAN_POINT ( 'NONE',  ( 46.59305225739526435, 100.9151871740940010, 31.60846029578754468 ) ) ;
#2850=EDGE_CURVE ( 'NONE', #11358, #11797, #16663, .T. ) ;
#2852=CARTESIAN_POINT ( 'NONE',  ( 44.55648932407425633, 64.61049967264874283, 38.96596240072933170 ) ) ;
#2858=CARTESIAN_POINT ( 'NONE',  ( 41.64333658814960870, 63.71518717409399812, 38.42115945441014446 ) ) ;
#2860=CARTESIAN_POINT ( 'NONE',  ( 43.01140435219951286, 150.8651871740939896, 38.86567161673127657 ) ) ;
#2865=CARTESIAN_POINT ( 'NONE',  ( 43.01140435219951286, 71.36518717409398960, 29.55568802177586107 ) ) ;
#2869=CARTESIAN_POINT ( 'NONE',  ( 47.43856463449117200, 130.7651871740939953, 32.77220824515698183 ) ) ;
#2870=ADVANCED_FACE ( 'NONE', ( #991 ), #14430, .T. ) ;
#2874=VECTOR ( 'NONE', #16221, 1000.000000000000000 ) ;
#2877=ORIENTED_EDGE ( 'NONE', *, *, #6972, .T. ) ;
#2881=CARTESIAN_POINT ( 'NONE',  ( 47.43856463449117200, 77.02977050742731535, 32.77220824515698183 ) ) ;
#2882=CARTESIAN_POINT ( 'NONE',  ( 38.58424406990786082, 138.1151871740940180, 34.21067981925357060 ) ) ;
#2884=EDGE_CURVE ( 'NONE', #5761, #1030, #19493, .T. ) ;
#2885=CARTESIAN_POINT ( 'NONE',  ( 43.01140435219951286, 92.96049967264873715, 28.95336869806222779 ) ) ;
#2889=( BOUNDED_CURVE ( )  B_SPLINE_CURVE ( 2, ( #14252, #924, #3811, #20996, #15591, #20885, #20672, #5556, #12280, #4233, #15906, #817, #13933 ),
 .UNSPECIFIED., .F., .F. ) 
 B_SPLINE_CURVE_WITH_KNOTS ( ( 3, 2, 2, 2, 2, 2, 3 ),
 ( 0.8308823529411765163, 0.8323529411764706287, 0.8352941176470588536, 0.8382352941176470784, 0.8411764705882353033, 0.8441176470588235281, 0.8455882352941176405 ),
 .UNSPECIFIED. ) 
 CURVE ( )  GEOMETRIC_REPRESENTATION_ITEM ( )  RATIONAL_B_SPLINE_CURVE ( ( 0.9755282581475768211, 0.9755282581475768211, 1.000000000000000000, 0.9510565162951535312, 1.000000000000000000, 0.9510565162951535312, 1.000000000000000000, 0.9510565162951535312, 1.000000000000000000, 0.9510565162951535312, 1.000000000000000000, 0.9755282581475768211, 0.9755282581475768211 ) ) 
 REPRESENTATION_ITEM ( '' )  );
#2890=CARTESIAN_POINT ( 'NONE',  ( 41.64333658814960870, 83.51518717409400949, 30.00020018409699318 ) ) ;
#2894=CARTESIAN_POINT ( 'NONE',  ( 43.01140435219951286, 61.46049967264873715, 39.21067981925356349 ) ) ;
#2897=CARTESIAN_POINT ( 'NONE',  ( 45.74753988029933538, 79.42977050742732104, 37.97664729208901946 ) ) ;
#2905=CARTESIAN_POINT ( 'NONE',  ( 39.42975644700377558, 126.6797705074273210, 36.81289934271958941 ) ) ;
#2909=ORIENTED_EDGE ( 'NONE', *, *, #7540, .T. ) ;
#2910=CARTESIAN_POINT ( 'NONE',  ( 47.43856463449118621, 124.8797705074273239, 34.21067981925357060 ) ) ;
#2911=CARTESIAN_POINT ( 'NONE',  ( 43.01140435219953417, 138.5344580088726048, 39.21067981925356349 ) ) ;
#2912=CARTESIAN_POINT ( 'NONE',  ( 43.01140435219951286, 88.12977050742732388, 38.86567161673127657 ) ) ;
#2913=CARTESIAN_POINT ( 'NONE',  ( 44.55648932407425633, 64.88445800887257064, 29.45539723777780239 ) ) ;
#2915=CYLINDRICAL_SURFACE ( 'NONE', #19100, 4.999999999999997335 ) ;
#2917=CARTESIAN_POINT ( 'NONE',  ( 41.46631938032478359, 156.1104996726487570, 29.45539723777780239 ) ) ;
#2921=CARTESIAN_POINT ( 'NONE',  ( 41.46631938032478359, 120.3844580088725849, 38.96596240072933170 ) ) ;
#2922=CARTESIAN_POINT ( 'NONE',  ( 46.59305225739526435, 106.5797705074273125, 36.81289934271958941 ) ) ;
#2925=CARTESIAN_POINT ( 'NONE',  ( 46.59305225739526435, 91.31518717409399244, 36.81289934271958941 ) ) ;
#2931=CARTESIAN_POINT ( 'NONE',  ( 38.58424406990785371, 69.22977050742731819, 32.77220824515697473 ) ) ;
#2933=EDGE_LOOP ( 'NONE', ( #12689, #2522, #10282, #17668 ) ) ;
#2934=CARTESIAN_POINT ( 'NONE',  ( 45.74753988029933538, 154.4297705074272926, 37.97664729208901946 ) ) ;
#2936=CARTESIAN_POINT ( 'NONE',  ( 46.10157429594899270, 113.6604996726487542, 29.95742577749337343 ) ) ;
#2937=CARTESIAN_POINT ( 'NONE',  ( 38.58424406990784661, 66.26518717409400949, 35.64915139335016647 ) ) ;
#2941=CARTESIAN_POINT ( 'NONE',  ( 48.01140435219951996, 151.2844580088725763, 34.21067981925357060 ) ) ;
#2942=CARTESIAN_POINT ( 'NONE',  ( 41.64333658814960870, 132.9797705074273324, 38.42115945441014446 ) ) ;
#2944=CARTESIAN_POINT ( 'NONE',  ( 46.59305225739526435, 130.3151871740940067, 36.81289934271958941 ) ) ;
#2947=FACE_OUTER_BOUND ( 'NONE', #18981, .T. ) ;
#2948=CARTESIAN_POINT ( 'NONE',  ( 46.10157429594899270, 139.7604996726487627, 38.46393386101375711 ) ) ;
#2955=VERTEX_POINT ( 'NONE', #3419 ) ;
#2956=CARTESIAN_POINT ( 'NONE',  ( 43.01140435219951286, 86.03445800887257633, 28.95336869806222779 ) ) ;
#2959=CARTESIAN_POINT ( 'NONE',  ( 41.46631938032478359, 144.1104996726487570, 29.45539723777780239 ) ) ;
#2960=CARTESIAN_POINT ( 'NONE',  ( 41.64333658814960870, 93.71518717409401233, 38.42115945441014446 ) ) ;
#2965=CARTESIAN_POINT ( 'NONE',  ( 43.01140435219957681, 71.03445800887256212, 29.21067981925356705 ) ) ;
#2966=CARTESIAN_POINT ( 'NONE',  ( 38.01140435219952707, 105.8604996726487428, 35.83527830041809636 ) ) ;
#2969=CARTESIAN_POINT ( 'NONE',  ( 44.55648932407425633, 80.81049967264873146, 29.45539723777780239 ) ) ;
#2970=CARTESIAN_POINT ( 'NONE',  ( 44.37947211624943833, 65.21518717409399812, 30.00020018409699318 ) ) ;
#2973=CARTESIAN_POINT ( 'NONE',  ( 44.37947211624943833, 151.0151871740940237, 38.42115945441014446 ) ) ;
#2977=CARTESIAN_POINT ( 'NONE',  ( 47.43856463449117911, 73.76518717409398107, 32.77220824515697473 ) ) ;
#2981=CARTESIAN_POINT ( 'NONE',  ( 38.58424406990784661, 137.9651871740939839, 32.77220824515698183 ) ) ;
#2982=EDGE_CURVE ( 'NONE', #9530, #10777, #9705, .T. ) ;
#2988=LINE ( 'NONE', #21521, #3748 ) ;
#2989=CARTESIAN_POINT ( 'NONE',  ( 40.27526882409969033, 69.82977050742729830, 37.97664729208901946 ) ) ;
#2990=CARTESIAN_POINT ( 'NONE',  ( 41.64333658814960870, 129.7151871740940123, 38.42115945441014446 ) ) ;
#2992=CARTESIAN_POINT ( 'NONE',  ( 47.05648932407426344, 92.51049967264873430, 31.27175355779120025 ) ) ;
#2997=CARTESIAN_POINT ( 'NONE',  ( 38.96631938032478359, 139.0104996726487627, 37.14960608071593384 ) ) ;
#2999=CARTESIAN_POINT ( 'NONE',  ( 43.01140435219951286, 84.86518717409398960, 38.86567161673127657 ) ) ;
#3000=CARTESIAN_POINT ( 'NONE',  ( 43.01140435219957681, 68.96049967264870872, 29.21067981925356705 ) ) ;
#3001=CARTESIAN_POINT ( 'NONE',  ( 43.80332655382221674, 108.6113394311928460, 39.21067981925355639 ) ) ;
#3002=CARTESIAN_POINT ( 'NONE',  ( 43.80332655382220253, 62.88361825032846752, 29.21067981925356705 ) ) ;
#3004=CARTESIAN_POINT ( 'NONE',  ( 44.37947211624943833, 79.27977050742731535, 38.42115945441014446 ) ) ;
#3012=CARTESIAN_POINT ( 'NONE',  ( 39.42975644700377558, 120.0797705074273267, 31.60846029578754468 ) ) ;
#3016=CARTESIAN_POINT ( 'NONE',  ( 41.64333658814960870, 119.7797705074273296, 30.00020018409699318 ) ) ;
#3017=CARTESIAN_POINT ( 'NONE',  ( 43.01140435219951286, 59.03445800887258343, 29.21067981925356705 ) ) ;
#3018=CARTESIAN_POINT ( 'NONE',  ( 39.42975644700377558, 90.67977050742732104, 36.81289934271958941 ) ) ;
#3019=CARTESIAN_POINT ( 'NONE',  ( 38.58424406990786082, 156.1151871740940180, 34.21067981925357060 ) ) ;
#3027=CARTESIAN_POINT ( 'NONE',  ( 39.92123440845005433, 103.1604996726487258, 38.46393386101375711 ) ) ;
#3029=CARTESIAN_POINT ( 'NONE',  ( 46.10157429594899270, 118.7344580088725650, 29.95742577749337343 ) ) ;
#3030=CARTESIAN_POINT ( 'NONE',  ( 45.74753988029933538, 103.4297705074273210, 37.97664729208901946 ) ) ;
#3033=CARTESIAN_POINT ( 'NONE',  ( 47.43856463449117911, 85.76518717409398107, 32.77220824515697473 ) ) ;
#3034=CARTESIAN_POINT ( 'NONE',  ( 43.01140435219954838, 133.4604996726487514, 39.21067981925356349 ) ) ;
#3036=CARTESIAN_POINT ( 'NONE',  ( 43.01140435219953417, 138.5344580088726048, 39.21067981925356349 ) ) ;
#3039=CARTESIAN_POINT ( 'NONE',  ( 38.58424406990785371, 63.22977050742731109, 32.77220824515697473 ) ) ;
#3040=EDGE_LOOP ( 'NONE', ( #14449, #15905, #15988, #16475 ) ) ;
#3042=CARTESIAN_POINT ( 'NONE',  ( 43.01140435219951286, 148.1297705074272812, 38.86567161673127657 ) ) ;
#3045=ADVANCED_FACE ( 'NONE', ( #4840 ), #4957, .T. ) ;
#3046=EDGE_CURVE ( 'NONE', #17658, #9281, #3864, .T. ) ;
#3047=CARTESIAN_POINT ( 'NONE',  ( 43.01140435219951286, 112.4604996726487514, 39.46799094044489209 ) ) ;
#3048=CARTESIAN_POINT ( 'NONE',  ( 44.37947211624943833, 73.01518717409399528, 38.42115945441014446 ) ) ;
#3053=CARTESIAN_POINT ( 'NONE',  ( 39.92123440845005433, 111.2604996726487343, 29.95742577749336988 ) ) ;
#3054=CARTESIAN_POINT ( 'NONE',  ( 39.42975644700377558, 135.0797705074272983, 31.60846029578754468 ) ) ;
#3057=CARTESIAN_POINT ( 'NONE',  ( 47.43856463449117911, 115.4651871740940123, 35.64915139335015937 ) ) ;
#3061=CARTESIAN_POINT ( 'NONE',  ( 38.96631938032478359, 135.4104996726487400, 31.27175355779120025 ) ) ;
#3064=CARTESIAN_POINT ( 'NONE',  ( 38.58424406990785371, 96.22977050742730398, 32.77220824515697473 ) ) ;
#3065=VERTEX_POINT ( 'NONE', #20599 ) ;
#3066=DIRECTION ( 'NONE',  ( 0.000000000000000000, 0.000000000000000000, 1.000000000000000000 ) ) ;
#3067=VERTEX_POINT ( 'NONE', #6836 ) ;
#3068=CARTESIAN_POINT ( 'NONE',  ( 47.05648932407426344, 79.58445800887257349, 31.27175355779120025 ) ) ;
#3070=ADVANCED_FACE ( 'NONE', ( #426 ), #15312, .T. ) ;
#3071=CARTESIAN_POINT ( 'NONE',  ( 38.01140435219952707, 135.7104996726487514, 34.21067981925357060 ) ) ;
#3072=CARTESIAN_POINT ( 'NONE',  ( 47.43856463449117200, 100.7651871740939953, 32.77220824515698183 ) ) ;
#3082=( BOUNDED_CURVE ( )  B_SPLINE_CURVE ( 2, ( #19330, #17770, #11165, #16008, #7665, #1140, #14574, #1033, #5877, #21317, #14466, #6203, #2676 ),
 .UNSPECIFIED., .F., .F. ) 
 B_SPLINE_CURVE_WITH_KNOTS ( ( 3, 2, 2, 2, 2, 2, 3 ),
 ( 0.3308823529411764608, 0.3323529411764705732, 0.3352941176470587981, 0.3382352941176470784, 0.3411764705882353033, 0.3441176470588235281, 0.3455882352941176405 ),
 .UNSPECIFIED. ) 
 CURVE ( )  GEOMETRIC_REPRESENTATION_ITEM ( )  RATIONAL_B_SPLINE_CURVE ( ( 0.9755282581475768211, 0.9755282581475768211, 1.000000000000000000, 0.9510565162951535312, 1.000000000000000000, 0.9510565162951535312, 1.000000000000000000, 0.9510565162951535312, 1.000000000000000000, 0.9510565162951535312, 1.000000000000000000, 0.9755282581475768211, 0.9755282581475768211 ) ) 
 REPRESENTATION_ITEM ( '' )  );
#3083=CARTESIAN_POINT ( 'NONE',  ( 44.37947211624943833, 61.01518717409400239, 38.42115945441014446 ) ) ;
#3086=CARTESIAN_POINT ( 'NONE',  ( 44.37947211624943833, 145.0151871740939953, 38.42115945441014446 ) ) ;
#3091=CARTESIAN_POINT ( 'NONE',  ( 38.58424406990785371, 72.26518717409398107, 35.64915139335015937 ) ) ;
#3095=SURFACE_STYLE_FILL_AREA ( #10929 ) ;
#3096=CARTESIAN_POINT ( 'NONE',  ( 47.43856463449117200, 124.4651871740939839, 35.64915139335016647 ) ) ;
#3101=ORIENTED_EDGE ( 'NONE', *, *, #3982, .T. ) ;
#3102=CARTESIAN_POINT ( 'NONE',  ( 39.92123440845004723, 108.2344580088725792, 38.46393386101376421 ) ) ;
#3103=FACE_OUTER_BOUND ( 'NONE', #3430, .T. ) ;
#3104=CARTESIAN_POINT ( 'NONE',  ( 43.01140435219951286, 62.62977050742732388, 29.55568802177586463 ) ) ;
#3105=CARTESIAN_POINT ( 'NONE',  ( 45.74753988029933538, 122.0651871740940209, 30.44471234641811819 ) ) ;
#3107=CARTESIAN_POINT ( 'NONE',  ( 39.92123440845004723, 85.16049967264873999, 38.46393386101376421 ) ) ;
#3109=CYLINDRICAL_SURFACE ( 'NONE', #17734, 4.999999999999997335 ) ;
#3111=CARTESIAN_POINT ( 'NONE',  ( 47.43856463449117200, 85.46518717409399812, 35.64915139335016647 ) ) ;
#3116=CARTESIAN_POINT ( 'NONE',  ( 39.42975644700377558, 69.07977050742732672, 31.60846029578754468 ) ) ;
#3122=ADVANCED_FACE ( 'NONE', ( #204 ), #18619, .T. ) ;
#3123=CARTESIAN_POINT ( 'NONE',  ( 43.01140435219951286, 122.9604996726487371, 29.21067981925356705 ) ) ;
#3124=CARTESIAN_POINT ( 'NONE',  ( 40.27526882409969744, 113.9297705074273068, 30.44471234641812174 ) ) ;
#3127=CARTESIAN_POINT ( 'NONE',  ( 48.01140435219951996, 88.28445800887257633, 34.21067981925357060 ) ) ;
#3129=CARTESIAN_POINT ( 'NONE',  ( 41.64333658814960870, 116.7797705074273296, 30.00020018409699318 ) ) ;
#3130=CARTESIAN_POINT ( 'NONE',  ( 43.01140435219951996, 170.7104996726487514, 34.21067981925357060 ) ) ;
#3131=CARTESIAN_POINT ( 'NONE',  ( 47.43856463449117200, 85.72977050742731819, 35.64915139335016647 ) ) ;
#3132=CARTESIAN_POINT ( 'NONE',  ( 38.58424406990784661, 149.9651871740939555, 32.77220824515698183 ) ) ;
#3138=CARTESIAN_POINT ( 'NONE',  ( 48.01140435219951996, 94.28445800887259054, 34.21067981925357060 ) ) ;
#3141=CARTESIAN_POINT ( 'NONE',  ( 38.01140435219951996, 122.9344580088725962, 35.83527830041810347 ) ) ;
#3142=CARTESIAN_POINT ( 'NONE',  ( 38.58424406990784661, 93.52977050742731535, 35.64915139335016647 ) ) ;
#3145=CARTESIAN_POINT ( 'NONE',  ( 43.01140435219951286, 90.86518717409400381, 38.86567161673127657 ) ) ;
#3146=CARTESIAN_POINT ( 'NONE',  ( 41.46631938032478359, 84.11049967264874283, 29.45539723777780239 ) ) ;
#3148=CARTESIAN_POINT ( 'NONE',  ( 43.01140435219951286, 127.4604996726487229, 39.21067981925356349 ) ) ;
#3151=CARTESIAN_POINT ( 'NONE',  ( 47.43856463449117200, 103.4651871740939839, 35.64915139335016647 ) ) ;
#3152=CARTESIAN_POINT ( 'NONE',  ( 44.37947211624943833, 70.27977050742731535, 38.42115945441014446 ) ) ;
#3155=CARTESIAN_POINT ( 'NONE',  ( 46.59305225739526435, 149.1797705074273210, 31.60846029578754468 ) ) ;
#3156=EDGE_CURVE ( 'NONE', #7690, #15802, #9916, .T. ) ;
#3157=CARTESIAN_POINT ( 'NONE',  ( 39.42975644700377558, 96.67977050742732104, 36.81289934271958941 ) ) ;
#3160=CARTESIAN_POINT ( 'NONE',  ( 39.92123440845004723, 108.2604996726487627, 29.95742577749337343 ) ) ;
#3161=CARTESIAN_POINT ( 'NONE',  ( 45.74753988029933538, 64.16518717409400097, 37.97664729208901946 ) ) ;
#3162=CARTESIAN_POINT ( 'NONE',  ( 39.92123440845005433, 66.23445800887257917, 38.46393386101375711 ) ) ;
#3168=CARTESIAN_POINT ( 'NONE',  ( 38.96631938032478359, 150.0844580088725593, 37.14960608071593384 ) ) ;
#3169=CARTESIAN_POINT ( 'NONE',  ( 38.58424406990784661, 132.2297705074272756, 32.77220824515698183 ) ) ;
#3171=CARTESIAN_POINT ( 'NONE',  ( 38.58424406990785371, 113.9651871740940123, 32.77220824515697473 ) ) ;
#3174=CARTESIAN_POINT ( 'NONE',  ( 43.01140435219952707, 140.9604996726487514, 29.21067981925357060 ) ) ;
#3178=CARTESIAN_POINT ( 'NONE',  ( 40.27526882409969744, 95.92977050742732104, 30.44471234641812174 ) ) ;
#3182=CARTESIAN_POINT ( 'NONE',  ( 39.92123440845004723, 87.23445800887259338, 38.46393386101376421 ) ) ;
#3185=CARTESIAN_POINT ( 'NONE',  ( 39.92123440845004723, 136.1604996726487116, 38.46393386101376421 ) ) ;
#3186=CARTESIAN_POINT ( 'NONE',  ( 43.01140435219951286, 92.36518717409398960, 29.55568802177586463 ) ) ;
#3192=CARTESIAN_POINT ( 'NONE',  ( 48.01140435219951996, 70.13445800887255643, 35.83527830041809636 ) ) ;
#3195=CARTESIAN_POINT ( 'NONE',  ( 48.01140435219951996, 115.4344580088725678, 32.58608133808903773 ) ) ;
#3196=CARTESIAN_POINT ( 'NONE',  ( 40.27526882409969033, 60.56518717409398533, 37.97664729208901946 ) ) ;
#3199=CARTESIAN_POINT ( 'NONE',  ( 47.43856463449117911, 142.7651871740939669, 32.77220824515697473 ) ) ;
#3203=CARTESIAN_POINT ( 'NONE',  ( 40.27526882409969744, 63.56518717409399954, 37.97664729208901235 ) ) ;
#3206=CARTESIAN_POINT ( 'NONE',  ( 44.37947211624943833, 128.2151871740939839, 30.00020018409699318 ) ) ;
#3213=CARTESIAN_POINT ( 'NONE',  ( 41.64333658814960870, 156.9797705074273040, 38.42115945441014446 ) ) ;
#3214=CARTESIAN_POINT ( 'NONE',  ( 40.27526882409969033, 65.92977050742732104, 30.44471234641811819 ) ) ;
#3215=CARTESIAN_POINT ( 'NONE',  ( 41.64333658814960870, 123.7151871740940123, 38.42115945441014446 ) ) ;
#3217=( BOUNDED_CURVE ( )  B_SPLINE_CURVE ( 2, ( #6620, #10143, #11563, #16629, #1759, #6500, #13219, #19957, #4842, #18292, #1539, #13335, #11670 ),
 .UNSPECIFIED., .F., .F. ) 
 B_SPLINE_CURVE_WITH_KNOTS ( ( 3, 2, 2, 2, 2, 2, 3 ),
 ( 0.1102941176470588203, 0.1117647058823529466, 0.1147058823529411714, 0.1176470588235294101, 0.1205882352941176489, 0.1235294117647058876, 0.1250000000000000000 ),
 .UNSPECIFIED. ) 
 CURVE ( )  GEOMETRIC_REPRESENTATION_ITEM ( )  RATIONAL_B_SPLINE_CURVE ( ( 0.9755282581475767101, 0.9755282581475765991, 1.000000000000000000, 0.9510565162951535312, 1.000000000000000000, 0.9510565162951535312, 1.000000000000000000, 0.9510565162951535312, 1.000000000000000000, 0.9510565162951535312, 1.000000000000000000, 0.9755282581475768211, 0.9755282581475768211 ) ) 
 REPRESENTATION_ITEM ( '' )  );
#3218=CARTESIAN_POINT ( 'NONE',  ( 38.01140435219952707, 78.71049967264875136, 34.21067981925357060 ) ) ;
#3220=CARTESIAN_POINT ( 'NONE',  ( 39.92123440845005433, 144.2604996726487627, 29.95742577749336988 ) ) ;
#3222=CARTESIAN_POINT ( 'NONE',  ( 38.58424406990784661, 83.96518717409399812, 32.77220824515698183 ) ) ;
#3223=CARTESIAN_POINT ( 'NONE',  ( 38.96631938032478359, 82.01049967264874851, 37.14960608071593384 ) ) ;
#3225=ORIENTED_EDGE ( 'NONE', *, *, #13221, .F. ) ;
#3226=CARTESIAN_POINT ( 'NONE',  ( 47.43856463449117200, 62.02977050742732246, 32.77220824515698183 ) ) ;
#3231=ORIENTED_EDGE ( 'NONE', *, *, #16655, .F. ) ;
#3232=CARTESIAN_POINT ( 'NONE',  ( 45.74753988029933538, 154.1651871740939441, 37.97664729208901946 ) ) ;
#3234=CARTESIAN_POINT ( 'NONE',  ( 43.01140435219951286, 106.4604996726487371, 39.21067981925356349 ) ) ;
#3235=CARTESIAN_POINT ( 'NONE',  ( 39.42975644700377558, 114.6797705074273210, 36.81289934271958941 ) ) ;
#3241=CARTESIAN_POINT ( 'NONE',  ( 39.42975644700377558, 114.6797705074273210, 36.81289934271958941 ) ) ;
#3243=CARTESIAN_POINT ( 'NONE',  ( 44.37947211624943833, 152.2151871740940123, 30.00020018409699318 ) ) ;
#3245=AXIS2_PLACEMENT_3D ( 'NONE', #14951, #21587, #3910 ) ;
#3246=AXIS2_PLACEMENT_3D ( 'NONE', #1592, #6888, #8546 ) ;
#3247=CARTESIAN_POINT ( 'NONE',  ( 42.21948215057684450, 107.1113394311928460, 29.21067981925356705 ) ) ;
#3251=CARTESIAN_POINT ( 'NONE',  ( 39.92123440845005433, 89.33445800887257349, 29.95742577749336988 ) ) ;
#3252=CARTESIAN_POINT ( 'NONE',  ( 47.05648932407426344, 131.5104996726487343, 31.27175355779120025 ) ) ;
#3253=CARTESIAN_POINT ( 'NONE',  ( 44.55648932407425633, 77.81049967264873146, 29.45539723777780239 ) ) ;
#3255=CARTESIAN_POINT ( 'NONE',  ( 44.37947211624943833, 92.47977050742731819, 30.00020018409699318 ) ) ;
#3258=CARTESIAN_POINT ( 'NONE',  ( 38.58424406990785371, 83.96518717409399812, 32.77220824515697473 ) ) ;
#3259=CARTESIAN_POINT ( 'NONE',  ( 42.21948215057684450, 84.03738109496899256, 29.21067981925356705 ) ) ;
#3265=CARTESIAN_POINT ( 'NONE',  ( 43.01140435219951286, 61.12977050742731677, 38.86567161673127657 ) ) ;
#3266=VERTEX_POINT ( 'NONE', #11164 ) ;
#3267=CARTESIAN_POINT ( 'NONE',  ( 38.58424406990784661, 141.2297705074273040, 32.77220824515698183 ) ) ;
#3268=CARTESIAN_POINT ( 'NONE',  ( 46.59305225739526435, 97.57977050742731251, 36.81289934271958941 ) ) ;
#3269=CARTESIAN_POINT ( 'NONE',  ( 47.05648932407426344, 110.5104996726487343, 31.27175355779120025 ) ) ;
#3270=CARTESIAN_POINT ( 'NONE',  ( 45.74753988029933538, 67.16518717409401518, 37.97664729208901946 ) ) ;
#3271=DIRECTION ( 'NONE',  ( 0.000000000000000000, 1.000000000000000000, 0.000000000000000000 ) ) ;
#3273=CARTESIAN_POINT ( 'NONE',  ( 43.01140435219951996, 155.0344580088726048, 29.21067981925357060 ) ) ;
#3277=CARTESIAN_POINT ( 'NONE',  ( 38.01140435219952707, 155.7844580088725763, 34.21067981925357060 ) ) ;
#3278=CARTESIAN_POINT ( 'NONE',  ( 40.27526882409969033, 120.8297705074272983, 37.97664729208901946 ) ) ;
#3281=CARTESIAN_POINT ( 'NONE',  ( 45.74753988029934249, 113.0651871740940067, 30.44471234641812174 ) ) ;
#3288=CARTESIAN_POINT ( 'NONE',  ( 38.58424406990786082, 99.37977050742732388, 34.21067981925357060 ) ) ;
#3294=CARTESIAN_POINT ( 'NONE',  ( 39.92123440845004723, 83.33445800887255928, 29.95742577749337343 ) ) ;
#3295=CARTESIAN_POINT ( 'NONE',  ( 43.01140435219951286, 87.53445800887257633, 39.21067981925356349 ) ) ;
#3296=CARTESIAN_POINT ( 'NONE',  ( 47.05648932407426344, 143.5104996726487627, 31.27175355779120025 ) ) ;
#3297=CARTESIAN_POINT ( 'NONE',  ( 44.37947211624943833, 100.0151871740939953, 38.42115945441014446 ) ) ;
#3302=CARTESIAN_POINT ( 'NONE',  ( 47.05648932407426344, 70.58445800887257349, 31.27175355779120025 ) ) ;
#3306=CARTESIAN_POINT ( 'NONE',  ( 46.10157429594899270, 114.8344580088725877, 38.46393386101375711 ) ) ;
#3307=CARTESIAN_POINT ( 'NONE',  ( 38.58424406990786082, 150.3797705074273097, 34.21067981925357060 ) ) ;
#3308=CARTESIAN_POINT ( 'NONE',  ( 42.21948215057684450, 62.11133943119284595, 29.21067981925356705 ) ) ;
#3310=CARTESIAN_POINT ( 'NONE',  ( 38.58424406990786082, 150.1151871740939896, 34.21067981925357060 ) ) ;
#3314=ORIENTED_EDGE ( 'NONE', *, *, #21402, .T. ) ;
#3315=CARTESIAN_POINT ( 'NONE',  ( 39.42975644700377558, 62.81518717409399954, 31.60846029578754468 ) ) ;
#3318=CARTESIAN_POINT ( 'NONE',  ( 42.21948215057684450, 134.1113394311928175, 29.21067981925356705 ) ) ;
#3319=CARTESIAN_POINT ( 'NONE',  ( 46.59305225739526435, 121.3151871740940067, 36.81289934271958941 ) ) ;
#3322=CARTESIAN_POINT ( 'NONE',  ( 38.96631938032478359, 113.4844580088725792, 31.27175355779120025 ) ) ;
#3324=CARTESIAN_POINT ( 'NONE',  ( 43.01140435219951286, 155.6297705074273097, 29.55568802177586107 ) ) ;
#3325=CARTESIAN_POINT ( 'NONE',  ( 40.27526882409969033, 68.92977050742733525, 30.44471234641811819 ) ) ;
#3326=CARTESIAN_POINT ( 'NONE',  ( 45.74753988029933538, 124.1651871740940152, 37.97664729208901946 ) ) ;
#3328=CARTESIAN_POINT ( 'NONE',  ( 48.01140435219951996, 77.36049967264874283, 32.58608133808903773 ) ) ;
#3331=CARTESIAN_POINT ( 'NONE',  ( 48.01140435219951996, 98.21049967264875136, 34.21067981925357060 ) ) ;
#3334=CARTESIAN_POINT ( 'NONE',  ( 44.37947211624943833, 86.21518717409399812, 30.00020018409699318 ) ) ;
#3338=CARTESIAN_POINT ( 'NONE',  ( 46.59305225739526435, 68.17977050742732104, 31.60846029578754468 ) ) ;
#3343=CARTESIAN_POINT ( 'NONE',  ( 43.01140435219951286, 153.8651871740939612, 38.86567161673127657 ) ) ;
#3344=DIRECTION ( 'NONE',  ( 0.000000000000000000, 1.000000000000000000, 0.000000000000000000 ) ) ;
#3345=CARTESIAN_POINT ( 'NONE',  ( 38.58424406990786082, 111.3797705074273239, 34.21067981925357060 ) ) ;
#3347=ORIENTED_EDGE ( 'NONE', *, *, #4494, .T. ) ;
#3352=CARTESIAN_POINT ( 'NONE',  ( 46.59305225739526435, 116.1797705074273210, 31.60846029578754468 ) ) ;
#3354=CARTESIAN_POINT ( 'NONE',  ( 39.42975644700377558, 158.8151871740940067, 31.60846029578754468 ) ) ;
#3357=CARTESIAN_POINT ( 'NONE',  ( 46.10157429594899270, 81.83445800887258770, 38.46393386101375711 ) ) ;
#3360=FACE_OUTER_BOUND ( 'NONE', #5933, .T. ) ;
#3365=CARTESIAN_POINT ( 'NONE',  ( 38.96631938032478359, 99.08445800887258770, 37.14960608071593384 ) ) ;
#3366=CARTESIAN_POINT ( 'NONE',  ( 44.37947211624943833, 91.27977050742731535, 38.42115945441014446 ) ) ;
#3370=CARTESIAN_POINT ( 'NONE',  ( 47.43856463449117911, 91.76518717409399528, 32.77220824515697473 ) ) ;
#3371=CYLINDRICAL_SURFACE ( 'NONE', #9726, 4.999999999999997335 ) ;
#3372=ORIENTED_EDGE ( 'NONE', *, *, #5121, .T. ) ;
#3377=CARTESIAN_POINT ( 'NONE',  ( 41.64333658814960870, 59.77977050742731535, 30.00020018409699318 ) ) ;
#3379=CARTESIAN_POINT ( 'NONE',  ( 47.43856463449118621, 148.8797705074273097, 34.21067981925357060 ) ) ;
#3380=CARTESIAN_POINT ( 'NONE',  ( 46.59305225739526435, 94.57977050742731251, 36.81289934271958941 ) ) ;
#3381=CARTESIAN_POINT ( 'NONE',  ( 43.80332655382220253, 155.8836182503284533, 29.21067981925356705 ) ) ;
#3382=CARTESIAN_POINT ( 'NONE',  ( 44.55648932407425633, 104.8104996726487457, 29.45539723777780239 ) ) ;
#3383=CARTESIAN_POINT ( 'NONE',  ( 39.42975644700377558, 63.41518717409400097, 36.81289934271958941 ) ) ;
#3386=CARTESIAN_POINT ( 'NONE',  ( 38.96631938032478359, 123.0844580088725735, 37.14960608071593384 ) ) ;
#3390=CARTESIAN_POINT ( 'NONE',  ( 38.01140435219952707, 140.7844580088725763, 34.21067981925357060 ) ) ;
#3392=CARTESIAN_POINT ( 'NONE',  ( 43.01140435219951286, 127.1297705074273381, 38.86567161673127657 ) ) ;
#3395=CARTESIAN_POINT ( 'NONE',  ( 38.58424406990786082, 117.1151871740940038, 34.21067981925357060 ) ) ;
#3401=AXIS2_PLACEMENT_3D ( 'NONE', #9037, #19166, #15847 ) ;
#3403=CARTESIAN_POINT ( 'NONE',  ( 40.27526882409969744, 90.82977050742731251, 37.97664729208901235 ) ) ;
#3405=ADVANCED_FACE ( 'NONE', ( #4548 ), #6833, .T. ) ;
#3410=CARTESIAN_POINT ( 'NONE',  ( 39.92123440845004723, 75.23445800887257917, 38.46393386101376421 ) ) ;
#3412=CARTESIAN_POINT ( 'NONE',  ( 41.46631938032478359, 136.3104996726487457, 38.96596240072933170 ) ) ;
#3413=CARTESIAN_POINT ( 'NONE',  ( 38.58424406990786082, 87.11518717409400381, 34.21067981925357060 ) ) ;
#3415=ADVANCED_FACE ( 'NONE', ( #4274 ), #14303, .T. ) ;
#3419=CARTESIAN_POINT ( 'NONE',  ( 43.01140435219951286, 113.0344580088725763, 29.21067981925356705 ) ) ;
#3421=CARTESIAN_POINT ( 'NONE',  ( 43.01140435219951996, 10.71049967264875491, 29.21067981925357060 ) ) ;
#3422=CARTESIAN_POINT ( 'NONE',  ( 48.01140435219951996, 146.0604996726487457, 35.83527830041809636 ) ) ;
#3424=CARTESIAN_POINT ( 'NONE',  ( 45.74753988029933538, 149.3297705074273267, 30.44471234641811819 ) ) ;
#3425=CARTESIAN_POINT ( 'NONE',  ( 43.01140435219951996, 10.71049967264875491, 34.21067981925357060 ) ) ;
#3427=CARTESIAN_POINT ( 'NONE',  ( 41.64333658814960870, 147.7151871740940123, 38.42115945441014446 ) ) ;
#3430=EDGE_LOOP ( 'NONE', ( #21340, #5954, #2243, #18078 ) ) ;
#3431=CARTESIAN_POINT ( 'NONE',  ( 47.43856463449117911, 64.46518717409399812, 35.64915139335015937 ) ) ;
#3435=CARTESIAN_POINT ( 'NONE',  ( 38.58424406990786082, 123.1151871740940038, 34.21067981925357060 ) ) ;
#3437=CARTESIAN_POINT ( 'NONE',  ( 39.92123440845005433, 114.2344580088725650, 38.46393386101375711 ) ) ;
#3439=CARTESIAN_POINT ( 'NONE',  ( 47.05648932407426344, 99.98445800887257917, 37.14960608071593384 ) ) ;
#3440=CARTESIAN_POINT ( 'NONE',  ( 38.58424406990786082, 159.3797705074273381, 34.21067981925357060 ) ) ;
#3441=CARTESIAN_POINT ( 'NONE',  ( 38.58424406990784661, 66.22977050742728977, 32.77220824515698183 ) ) ;
#3442=CARTESIAN_POINT ( 'NONE',  ( 40.27526882409969033, 128.6651871740940010, 30.44471234641811819 ) ) ;
#3446=CARTESIAN_POINT ( 'NONE',  ( 39.92123440845004723, 81.26049967264872009, 29.95742577749337343 ) ) ;
#3448=FACE_OUTER_BOUND ( 'NONE', #15721, .T. ) ;
#3449=CARTESIAN_POINT ( 'NONE',  ( 41.46631938032478359, 139.3104996726487457, 38.96596240072933170 ) ) ;
#3450=CARTESIAN_POINT ( 'NONE',  ( 46.59305225739526435, 76.31518717409399244, 36.81289934271958941 ) ) ;
#3451=CARTESIAN_POINT ( 'NONE',  ( 43.01140435219951286, 104.0344580088725763, 29.21067981925356705 ) ) ;
#3452=VECTOR ( 'NONE', #8325, 1000.000000000000000 ) ;
#3454=ORIENTED_EDGE ( 'NONE', *, *, #5441, .T. ) ;
#3455=CARTESIAN_POINT ( 'NONE',  ( 44.37947211624943833, 70.27977050742731535, 38.42115945441014446 ) ) ;
#3460=CARTESIAN_POINT ( 'NONE',  ( 38.58424406990786082, 153.1151871740939896, 34.21067981925357060 ) ) ;
#3462=CARTESIAN_POINT ( 'NONE',  ( 46.59305225739526435, 110.1797705074273210, 31.60846029578754468 ) ) ;
#3469=CARTESIAN_POINT ( 'NONE',  ( 44.37947211624943833, 86.47977050742731819, 30.00020018409699318 ) ) ;
#3470=CARTESIAN_POINT ( 'NONE',  ( 41.64333658814960870, 156.7151871740939839, 38.42115945441014446 ) ) ;
#3472=CARTESIAN_POINT ( 'NONE',  ( 44.55648932407425633, 81.68445800887258201, 38.96596240072933170 ) ) ;
#3477=CARTESIAN_POINT ( 'NONE',  ( 46.10157429594899270, 92.66049967264873999, 29.95742577749336988 ) ) ;
#3479=CARTESIAN_POINT ( 'NONE',  ( 43.01140435219951286, 98.03445800887257633, 29.21067981925356705 ) ) ;
#3480=CARTESIAN_POINT ( 'NONE',  ( 39.42975644700377558, 99.07977050742732672, 31.60846029578754468 ) ) ;
#3483=CARTESIAN_POINT ( 'NONE',  ( 41.64333658814960870, 83.51518717409400949, 30.00020018409699318 ) ) ;
#3488=( BOUNDED_CURVE ( )  B_SPLINE_CURVE ( 2, ( #8382, #16845, #2969, #9708, #5069, #15091, #1319, #13336, #6736, #21388, #18406, #13443, #4728 ),
 .UNSPECIFIED., .F., .T. ) 
 B_SPLINE_CURVE_WITH_KNOTS ( ( 3, 2, 2, 2, 2, 2, 3 ),
 ( 0.7720588235294117974, 0.7735294117647059098, 0.7764705882352941346, 0.7794117647058823595, 0.7823529411764705843, 0.7852941176470588092, 0.7867647058823529216 ),
 .UNSPECIFIED. ) 
 CURVE ( )  GEOMETRIC_REPRESENTATION_ITEM ( )  RATIONAL_B_SPLINE_CURVE ( ( 0.9755282581475768211, 0.9755282581475768211, 1.000000000000000000, 0.9510565162951535312, 1.000000000000000000, 0.9510565162951535312, 1.000000000000000000, 0.9510565162951535312, 1.000000000000000000, 0.9510565162951535312, 1.000000000000000000, 0.9755282581475768211, 0.9755282581475768211 ) ) 
 REPRESENTATION_ITEM ( '' )  );
#3489=CARTESIAN_POINT ( 'NONE',  ( 39.42975644700377558, 141.6797705074273210, 36.81289934271958941 ) ) ;
#3492=CARTESIAN_POINT ( 'NONE',  ( 41.46631938032478359, 119.1844580088725962, 29.45539723777780239 ) ) ;
#3493=ORIENTED_EDGE ( 'NONE', *, *, #5154, .F. ) ;
#3494=CARTESIAN_POINT ( 'NONE',  ( 40.27526882409969033, 141.8297705074273267, 37.97664729208901946 ) ) ;
#3500=CARTESIAN_POINT ( 'NONE',  ( 43.01140435219951996, 10.71049967264875491, 39.21067981925356349 ) ) ;
#3502=( LENGTH_UNIT ( ) NAMED_UNIT ( * ) SI_UNIT ( .MILLI., .METRE. ) );
#3503=CARTESIAN_POINT ( 'NONE',  ( 41.46631938032478359, 147.3844580088725991, 38.96596240072933170 ) ) ;
#3504=CARTESIAN_POINT ( 'NONE',  ( 41.64333658814960870, 123.9797705074273324, 38.42115945441014446 ) ) ;
#3507=CARTESIAN_POINT ( 'NONE',  ( 45.74753988029934249, 116.0651871740939924, 30.44471234641812174 ) ) ;
#3513=CARTESIAN_POINT ( 'NONE',  ( 46.59305225739526435, 83.17977050742732104, 31.60846029578754468 ) ) ;
#3516=CARTESIAN_POINT ( 'NONE',  ( 48.01140435219951996, 70.28445800887257633, 34.21067981925357060 ) ) ;
#3517=CARTESIAN_POINT ( 'NONE',  ( 38.01140435219952707, 86.63445800887257064, 32.58608133808903773 ) ) ;
#3518=CARTESIAN_POINT ( 'NONE',  ( 38.96631938032478359, 126.4104996726487542, 31.27175355779120025 ) ) ;
#3519=CARTESIAN_POINT ( 'NONE',  ( 45.74753988029933538, 83.06518717409400665, 30.44471234641811819 ) ) ;
#3523=CARTESIAN_POINT ( 'NONE',  ( 42.21948215057684450, 117.4575765865523067, 39.21067981925355639 ) ) ;
#3525=CARTESIAN_POINT ( 'NONE',  ( 43.01140435219951286, 62.03445800887256922, 29.21067981925356705 ) ) ;
#3526=CARTESIAN_POINT ( 'NONE',  ( 47.05648932407426344, 68.51049967264874851, 31.27175355779120025 ) ) ;
#3528=CARTESIAN_POINT ( 'NONE',  ( 39.42975644700377558, 156.0797705074273267, 31.60846029578754468 ) ) ;
#3529=CARTESIAN_POINT ( 'NONE',  ( 38.01140435219952707, 62.78445800887258343, 34.21067981925357060 ) ) ;
#3531=CARTESIAN_POINT ( 'NONE',  ( 39.42975644700377558, 146.8151871740940067, 31.60846029578754468 ) ) ;
#3532=CARTESIAN_POINT ( 'NONE',  ( 43.01140435219951996, 10.71049967264875491, 34.21067981925357060 ) ) ;
#3534=CARTESIAN_POINT ( 'NONE',  ( 39.42975644700377558, 60.41518717409400097, 36.81289934271958941 ) ) ;
#3537=DIRECTION ( 'NONE',  ( 0.000000000000000000, 1.000000000000000000, 0.000000000000000000 ) ) ;
#3538=CARTESIAN_POINT ( 'NONE',  ( 43.01140435219951286, 126.8651871740940180, 38.86567161673127657 ) ) ;
#3539=ORIENTED_EDGE ( 'NONE', *, *, #4151, .F. ) ;
#3543=CARTESIAN_POINT ( 'NONE',  ( 38.01140435219951996, 104.9344580088725820, 35.83527830041810347 ) ) ;
#3544=CARTESIAN_POINT ( 'NONE',  ( 43.01140435219951286, 137.9604996726487514, 29.21067981925356705 ) ) ;
#3545=CARTESIAN_POINT ( 'NONE',  ( 44.37947211624943833, 62.47977050742731109, 30.00020018409699318 ) ) ;
#3546=CARTESIAN_POINT ( 'NONE',  ( 47.43856463449118621, 112.6151871740939896, 34.21067981925357060 ) ) ;
#3548=CARTESIAN_POINT ( 'NONE',  ( 43.01140435219951286, 83.96049967264873715, 28.95336869806222779 ) ) ;
#3549=CARTESIAN_POINT ( 'NONE',  ( 48.01140435219951996, 148.2844580088725763, 34.21067981925357060 ) ) ;
#3552=CARTESIAN_POINT ( 'NONE',  ( 43.01140435219951286, 81.86518717409398960, 38.86567161673127657 ) ) ;
#3555=CARTESIAN_POINT ( 'NONE',  ( 38.01140435219951996, 125.6344580088725706, 32.58608133808903773 ) ) ;
#3562=VERTEX_POINT ( 'NONE', #5816 ) ;
#3563=CARTESIAN_POINT ( 'NONE',  ( 39.42975644700377558, 153.4151871740940010, 36.81289934271958941 ) ) ;
#3567=CARTESIAN_POINT ( 'NONE',  ( 40.27526882409969744, 114.8297705074273267, 37.97664729208901235 ) ) ;
#3571=CARTESIAN_POINT ( 'NONE',  ( 47.43856463449117200, 110.0297705074273296, 32.77220824515698183 ) ) ;
#3572=CARTESIAN_POINT ( 'NONE',  ( 38.01140435219952707, 158.6344580088725706, 32.58608133808903773 ) ) ;
#3574=CARTESIAN_POINT ( 'NONE',  ( 47.43856463449117200, 142.4651871740940123, 35.64915139335016647 ) ) ;
#3579=CARTESIAN_POINT ( 'NONE',  ( 48.01140435219951996, 101.3604996726487286, 32.58608133808903773 ) ) ;
#3580=UNCERTAINTY_MEASURE_WITH_UNIT (LENGTH_MEASURE( 1.000000000000000082E-05 ), #3502, 'distance_accuracy_value', 'NONE');
#3582=CARTESIAN_POINT ( 'NONE',  ( 44.55648932407425633, 96.68445800887258201, 38.96596240072933170 ) ) ;
#3583=CARTESIAN_POINT ( 'NONE',  ( 41.64333658814960870, 98.77977050742731535, 30.00020018409699318 ) ) ;
#3586=CARTESIAN_POINT ( 'NONE',  ( 41.64333658814960870, 80.51518717409400949, 30.00020018409699318 ) ) ;
#3589=ORIENTED_EDGE ( 'NONE', *, *, #18909, .T. ) ;
#3592=CYLINDRICAL_SURFACE ( 'NONE', #10289, 4.999999999999997335 ) ;
#3595=LINE ( 'NONE', #21789, #10796 ) ;
#3596=VERTEX_POINT ( 'NONE', #9254 ) ;
#3597=CARTESIAN_POINT ( 'NONE',  ( 40.27526882409969033, 138.8297705074272983, 37.97664729208901946 ) ) ;
#3599=VECTOR ( 'NONE', #3344, 1000.000000000000000 ) ;
#3600=CARTESIAN_POINT ( 'NONE',  ( 41.64333658814960870, 98.77977050742731535, 30.00020018409699318 ) ) ;
#3601=CARTESIAN_POINT ( 'NONE',  ( 38.01140435219952707, 141.5604996726487457, 32.58608133808903773 ) ) ;
#3602=EDGE_CURVE ( 'NONE', #14339, #10720, #6710, .T. ) ;
#3606=LINE ( 'NONE', #20464, #19004 ) ;
#3608=LINE ( 'NONE', #6915, #13566 ) ;
#3611=CARTESIAN_POINT ( 'NONE',  ( 48.01140435219951996, 145.4344580088725820, 32.58608133808903773 ) ) ;
#3612=CARTESIAN_POINT ( 'NONE',  ( 47.43856463449117200, 128.0297705074273154, 32.77220824515698183 ) ) ;
#3616=CARTESIAN_POINT ( 'NONE',  ( 44.37947211624943833, 107.2151871740940123, 30.00020018409699318 ) ) ;
#3621=CARTESIAN_POINT ( 'NONE',  ( 47.43856463449118621, 88.87977050742732388, 34.21067981925357060 ) ) ;
#3622=VERTEX_POINT ( 'NONE', #19593 ) ;
#3623=CARTESIAN_POINT ( 'NONE',  ( 43.01140435219951286, 144.5344580088726048, 39.21067981925356349 ) ) ;
#3624=CARTESIAN_POINT ( 'NONE',  ( 43.01140435219951286, 72.53445800887259054, 39.46799094044489209 ) ) ;
#3625=CARTESIAN_POINT ( 'NONE',  ( 38.96631938032478359, 87.08445800887258770, 37.14960608071593384 ) ) ;
#3626=CARTESIAN_POINT ( 'NONE',  ( 47.05648932407426344, 130.9104996726487684, 37.14960608071593384 ) ) ;
#3627=CARTESIAN_POINT ( 'NONE',  ( 40.27526882409969033, 90.56518717409400665, 37.97664729208901946 ) ) ;
#3634=CARTESIAN_POINT ( 'NONE',  ( 43.01140435219957681, 68.96049967264870872, 29.21067981925356705 ) ) ;
#3636=CARTESIAN_POINT ( 'NONE',  ( 46.59305225739526435, 151.5797705074273267, 36.81289934271958941 ) ) ;
#3637=CARTESIAN_POINT ( 'NONE',  ( 44.37947211624943833, 107.4797705074273182, 30.00020018409699318 ) ) ;
#3639=CARTESIAN_POINT ( 'NONE',  ( 38.58424406990786082, 132.1151871740940180, 34.21067981925357060 ) ) ;
#3641=CARTESIAN_POINT ( 'NONE',  ( 45.74753988029934249, 62.06518717409399244, 30.44471234641812174 ) ) ;
#3644=CARTESIAN_POINT ( 'NONE',  ( 44.37947211624943833, 118.0151871740940095, 38.42115945441014446 ) ) ;
#3645=ORIENTED_EDGE ( 'NONE', *, *, #15936, .F. ) ;
#3650=CARTESIAN_POINT ( 'NONE',  ( 38.01140435219951996, 101.6344580088725849, 32.58608133808903773 ) ) ;
#3651=CARTESIAN_POINT ( 'NONE',  ( 40.27526882409969744, 156.8297705074272983, 37.97664729208901235 ) ) ;
#3652=CARTESIAN_POINT ( 'NONE',  ( 39.92123440845004723, 157.1604996726487684, 38.46393386101376421 ) ) ;
#3653=CARTESIAN_POINT ( 'NONE',  ( 46.59305225739526435, 112.9151871740940010, 31.60846029578754468 ) ) ;
#3655=CARTESIAN_POINT ( 'NONE',  ( 39.92123440845004723, 75.26049967264873430, 29.95742577749337343 ) ) ;
#3657=DIRECTION ( 'NONE',  ( 0.000000000000000000, 0.000000000000000000, 1.000000000000000000 ) ) ;
#3658=CARTESIAN_POINT ( 'NONE',  ( 41.64333658814960870, 74.51518717409399528, 30.00020018409699318 ) ) ;
#3662=EDGE_CURVE ( 'NONE', #7305, #11189, #21769, .T. ) ;
#3663=ORIENTED_EDGE ( 'NONE', *, *, #5564, .T. ) ;
#3668=CARTESIAN_POINT ( 'NONE',  ( 45.74753988029933538, 140.0651871740940067, 30.44471234641811819 ) ) ;
#3670=CARTESIAN_POINT ( 'NONE',  ( 44.37947211624943833, 106.2797705074273154, 38.42115945441014446 ) ) ;
#3676=CARTESIAN_POINT ( 'NONE',  ( 43.01140435219951996, 10.71049967264875491, 39.21067981925356349 ) ) ;
#3679=CARTESIAN_POINT ( 'NONE',  ( 38.58424406990784661, 141.2651871740940237, 35.64915139335016647 ) ) ;
#3682=CARTESIAN_POINT ( 'NONE',  ( 44.55648932407425633, 119.8104996726487457, 29.45539723777780239 ) ) ;
#3688=CARTESIAN_POINT ( 'NONE',  ( 46.59305225739526435, 89.17977050742732104, 31.60846029578754468 ) ) ;
#3692=CARTESIAN_POINT ( 'NONE',  ( 45.74753988029934249, 83.06518717409400665, 30.44471234641812174 ) ) ;
#3695=EDGE_LOOP ( 'NONE', ( #5315, #463, #13343, #5988 ) ) ;
#3697=DIRECTION ( 'NONE',  ( 0.000000000000000000, 0.000000000000000000, 1.000000000000000000 ) ) ;
#3700=CARTESIAN_POINT ( 'NONE',  ( 39.42975644700377558, 60.07977050742731251, 31.60846029578754468 ) ) ;
#3702=CARTESIAN_POINT ( 'NONE',  ( 38.58424406990784661, 135.2297705074273324, 32.77220824515698183 ) ) ;
#3703=CARTESIAN_POINT ( 'NONE',  ( 39.42975644700377558, 93.67977050742732104, 36.81289934271958941 ) ) ;
#3706=CARTESIAN_POINT ( 'NONE',  ( 39.42975644700377558, 62.81518717409399954, 31.60846029578754468 ) ) ;
#3708=CARTESIAN_POINT ( 'NONE',  ( 39.42975644700377558, 101.8151871740940067, 31.60846029578754468 ) ) ;
#3709=DIRECTION ( 'NONE',  ( 0.000000000000000000, 1.000000000000000000, 0.000000000000000000 ) ) ;
#3710=CARTESIAN_POINT ( 'NONE',  ( 38.01140435219952707, 108.8604996726487144, 35.83527830041809636 ) ) ;
#3715=CARTESIAN_POINT ( 'NONE',  ( 38.01140435219951996, 137.9344580088726104, 35.83527830041810347 ) ) ;
#3716=CARTESIAN_POINT ( 'NONE',  ( 43.01140435219951286, 124.1297705074272955, 38.86567161673127657 ) ) ;
#3719=CARTESIAN_POINT ( 'NONE',  ( 40.27526882409969744, 110.6651871740940010, 30.44471234641812174 ) ) ;
#3720=CARTESIAN_POINT ( 'NONE',  ( 43.01140435219951996, 10.71049967264875491, 34.21067981925357060 ) ) ;
#3722=EDGE_CURVE ( 'NONE', #5192, #5761, #11213, .T. ) ;
#3725=CARTESIAN_POINT ( 'NONE',  ( 38.58424406990786082, 84.37977050742730967, 34.21067981925357060 ) ) ;
#3727=EDGE_CURVE ( 'NONE', #16987, #14880, #19708, .T. ) ;
#3729=CARTESIAN_POINT ( 'NONE',  ( 38.96631938032478359, 71.48445800887257917, 31.27175355779120025 ) ) ;
#3731=CARTESIAN_POINT ( 'NONE',  ( 38.01140435219951996, 126.5604996726487315, 32.58608133808903773 ) ) ;
#3732=CARTESIAN_POINT ( 'NONE',  ( 40.27526882409969033, 87.56518717409400665, 37.97664729208901946 ) ) ;
#3739=CARTESIAN_POINT ( 'NONE',  ( 43.01140435219951286, 92.03445800887257633, 29.21067981925356705 ) ) ;
#3742=CARTESIAN_POINT ( 'NONE',  ( 41.64333658814960870, 150.9797705074273324, 38.42115945441014446 ) ) ;
#3743=CARTESIAN_POINT ( 'NONE',  ( 40.27526882409969033, 101.9297705074273068, 30.44471234641811819 ) ) ;
#3745=CARTESIAN_POINT ( 'NONE',  ( 38.58424406990785371, 137.9651871740940123, 32.77220824515697473 ) ) ;
#3748=VECTOR ( 'NONE', #18196, 1000.000000000000000 ) ;
#3752=CARTESIAN_POINT ( 'NONE',  ( 44.37947211624943833, 112.0151871740940095, 38.42115945441014446 ) ) ;
#3753=ORIENTED_EDGE ( 'NONE', *, *, #6972, .F. ) ;
#3754=EDGE_CURVE ( 'NONE', #8983, #11479, #18131, .T. ) ;
#3757=CARTESIAN_POINT ( 'NONE',  ( 38.96631938032478359, 105.0844580088725877, 37.14960608071593384 ) ) ;
#3759=CARTESIAN_POINT ( 'NONE',  ( 38.58424406990786082, 150.3797705074273097, 34.21067981925357060 ) ) ;
#3760=CARTESIAN_POINT ( 'NONE',  ( 46.10157429594899270, 154.7604996726487343, 38.46393386101376421 ) ) ;
#3761=CARTESIAN_POINT ( 'NONE',  ( 38.58424406990784661, 113.9651871740940123, 32.77220824515698183 ) ) ;
#3763=CARTESIAN_POINT ( 'NONE',  ( 38.01140435219952707, 69.71049967264873715, 34.21067981925357060 ) ) ;
#3768=CARTESIAN_POINT ( 'NONE',  ( 44.37947211624943833, 83.21518717409399812, 30.00020018409699318 ) ) ;
#3769=CARTESIAN_POINT ( 'NONE',  ( 41.46631938032478359, 64.31049967264873146, 38.96596240072933170 ) ) ;
#3777=CARTESIAN_POINT ( 'NONE',  ( 39.42975644700377558, 147.4151871740940294, 36.81289934271958941 ) ) ;
#3779=CARTESIAN_POINT ( 'NONE',  ( 45.74753988029934249, 106.4297705074273210, 37.97664729208901235 ) ) ;
#3781=EDGE_LOOP ( 'NONE', ( #21421, #9964, #17959, #6535 ) ) ;
#3784=CARTESIAN_POINT ( 'NONE',  ( 43.01140435219951286, 113.6297705074273097, 29.55568802177586463 ) ) ;
#3787=CARTESIAN_POINT ( 'NONE',  ( 41.46631938032478359, 126.1104996726487570, 29.45539723777780239 ) ) ;
#3788=CARTESIAN_POINT ( 'NONE',  ( 39.42975644700377558, 147.4151871740940294, 36.81289934271958941 ) ) ;
#3790=CARTESIAN_POINT ( 'NONE',  ( 38.01140435219951996, 99.86049967264871441, 35.83527830041810347 ) ) ;
#3792=CARTESIAN_POINT ( 'NONE',  ( 41.46631938032478359, 61.31049967264873146, 38.96596240072933170 ) ) ;
#3798=CARTESIAN_POINT ( 'NONE',  ( 45.74753988029933538, 89.32977050742732672, 30.44471234641811819 ) ) ;
#3800=CARTESIAN_POINT ( 'NONE',  ( 41.64333658814960870, 78.71518717409399812, 38.42115945441014446 ) ) ;
#3804=ORIENTED_EDGE ( 'NONE', *, *, #1285, .F. ) ;
#3807=CARTESIAN_POINT ( 'NONE',  ( 47.43856463449117911, 130.7297705074273040, 35.64915139335015937 ) ) ;
#3811=CARTESIAN_POINT ( 'NONE',  ( 44.55648932407425633, 73.88445800887258486, 29.45539723777780239 ) ) ;
#3813=CARTESIAN_POINT ( 'NONE',  ( 39.42975644700377558, 132.6797705074273210, 36.81289934271958941 ) ) ;
#3816=CARTESIAN_POINT ( 'NONE',  ( 41.64333658814960870, 98.51518717409399528, 30.00020018409699318 ) ) ;
#3818=CARTESIAN_POINT ( 'NONE',  ( 41.46631938032478359, 108.1104996726487428, 29.45539723777780239 ) ) ;
#3821=VECTOR ( 'NONE', #14431, 1000.000000000000000 ) ;
#3823=CARTESIAN_POINT ( 'NONE',  ( 38.01140435219951996, 143.6344580088725422, 32.58608133808903773 ) ) ;
#3824=CARTESIAN_POINT ( 'NONE',  ( 41.64333658814960870, 108.9797705074273324, 38.42115945441014446 ) ) ;
#3826=CARTESIAN_POINT ( 'NONE',  ( 43.01140435219950575, 140.0344580088726332, 29.21067981925357060 ) ) ;
#3827=CARTESIAN_POINT ( 'NONE',  ( 43.01140435219951286, 110.3651871740939896, 29.55568802177586107 ) ) ;
#3828=VERTEX_POINT ( 'NONE', #19934 ) ;
#3829=CARTESIAN_POINT ( 'NONE',  ( 42.21948215057684450, 88.38361825032848174, 39.21067981925355639 ) ) ;
#3834=CARTESIAN_POINT ( 'NONE',  ( 39.42975644700377558, 87.67977050742732104, 36.81289934271958941 ) ) ;
#3836=ORIENTED_EDGE ( 'NONE', *, *, #268, .T. ) ;
#3837=CARTESIAN_POINT ( 'NONE',  ( 46.10157429594899270, 75.83445800887258770, 38.46393386101376421 ) ) ;
#3839=CARTESIAN_POINT ( 'NONE',  ( 43.01140435219951286, 127.4604996726487514, 39.46799094044489209 ) ) ;
#3840=CARTESIAN_POINT ( 'NONE',  ( 38.58424406990784661, 89.96518717409399812, 32.77220824515698183 ) ) ;
#3844=DIRECTION ( 'NONE',  ( 0.000000000000000000, 1.000000000000000000, 0.000000000000000000 ) ) ;
#3845=CARTESIAN_POINT ( 'NONE',  ( 44.55648932407425633, 127.8844580088725706, 29.45539723777780239 ) ) ;
#3846=CARTESIAN_POINT ( 'NONE',  ( 38.01140435219952707, 80.93445800887256780, 35.83527830041809636 ) ) ;
#3847=CARTESIAN_POINT ( 'NONE',  ( 43.01140435219951996, 10.71049967264875491, 34.21067981925357060 ) ) ;
#3849=CARTESIAN_POINT ( 'NONE',  ( 45.74753988029933538, 139.4297705074272926, 37.97664729208901946 ) ) ;
#3850=CARTESIAN_POINT ( 'NONE',  ( 46.59305225739526435, 101.1797705074273210, 31.60846029578754468 ) ) ;
#3852=CARTESIAN_POINT ( 'NONE',  ( 40.27526882409969744, 138.5651871740939782, 37.97664729208901235 ) ) ;
#3853=CARTESIAN_POINT ( 'NONE',  ( 44.55648932407425633, 67.88445800887258486, 29.45539723777780239 ) ) ;
#3857=CARTESIAN_POINT ( 'NONE',  ( 39.42975644700377558, 63.67977050742732104, 36.81289934271958941 ) ) ;
#3859=DIRECTION ( 'NONE',  ( 0.000000000000000000, 1.000000000000000000, 0.000000000000000000 ) ) ;
#3860=CARTESIAN_POINT ( 'NONE',  ( 44.37947211624943833, 113.2151871740940123, 30.00020018409699318 ) ) ;
#3862=CARTESIAN_POINT ( 'NONE',  ( 43.01140435219951286, 134.0344580088725763, 29.21067981925356705 ) ) ;
#3863=VERTEX_POINT ( 'NONE', #5369 ) ;
#3864=( BOUNDED_CURVE ( )  B_SPLINE_CURVE ( 2, ( #11890, #3523, #17272, #7158, #7267, #11994, #13968, #8593, #20707, #12315, #1863, #5484, #13861 ),
 .UNSPECIFIED., .F., .F. ) 
 B_SPLINE_CURVE_WITH_KNOTS ( ( 3, 2, 2, 2, 2, 2, 3 ),
 ( 0.4044117647058823595, 0.4058823529411764719, 0.4088235294117646967, 0.4117647058823529216, 0.4147058823529412019, 0.4176470588235294268, 0.4191176470588235392 ),
 .UNSPECIFIED. ) 
 CURVE ( )  GEOMETRIC_REPRESENTATION_ITEM ( )  RATIONAL_B_SPLINE_CURVE ( ( 0.9755282581475768211, 0.9755282581475768211, 1.000000000000000000, 0.9510565162951535312, 1.000000000000000000, 0.9510565162951535312, 1.000000000000000000, 0.9510565162951535312, 1.000000000000000000, 0.9510565162951535312, 1.000000000000000000, 0.9755282581475768211, 0.9755282581475768211 ) ) 
 REPRESENTATION_ITEM ( '' )  );
#3865=CARTESIAN_POINT ( 'NONE',  ( 47.05648932407426344, 105.9844580088725792, 37.14960608071593384 ) ) ;
#3866=CARTESIAN_POINT ( 'NONE',  ( 38.58424406990785371, 147.5297705074273154, 35.64915139335015937 ) ) ;
#3868=CARTESIAN_POINT ( 'NONE',  ( 39.92123440845004723, 159.2604996726487343, 29.95742577749337343 ) ) ;
#3869=CARTESIAN_POINT ( 'NONE',  ( 41.64333658814960870, 120.7151871740939981, 38.42115945441014446 ) ) ;
#3871=CARTESIAN_POINT ( 'NONE',  ( 46.10157429594899270, 68.66049967264873999, 29.95742577749337343 ) ) ;
#3876=CARTESIAN_POINT ( 'NONE',  ( 47.43856463449117200, 79.76518717409400949, 32.77220824515698183 ) ) ;
#3880=ORIENTED_EDGE ( 'NONE', *, *, #3046, .F. ) ;
#3884=CARTESIAN_POINT ( 'NONE',  ( 40.27526882409969033, 143.6651871740940294, 30.44471234641811819 ) ) ;
#3885=AXIS2_PLACEMENT_3D ( 'NONE', #14223, #20963, #12578 ) ;
#3888=CARTESIAN_POINT ( 'NONE',  ( 44.37947211624943833, 104.4797705074273182, 30.00020018409699318 ) ) ;
#3890=EDGE_LOOP ( 'NONE', ( #1251, #13688, #12799, #9181 ) ) ;
#3892=EDGE_LOOP ( 'NONE', ( #2122, #20671, #20776, #16006 ) ) ;
#3893=CARTESIAN_POINT ( 'NONE',  ( 44.37947211624943833, 112.2797705074273296, 38.42115945441014446 ) ) ;
#3896=CARTESIAN_POINT ( 'NONE',  ( 47.43856463449117200, 148.7651871740939953, 32.77220824515698183 ) ) ;
#3897=CARTESIAN_POINT ( 'NONE',  ( 39.92123440845004723, 97.16049967264873999, 38.46393386101376421 ) ) ;
#3899=CLOSED_SHELL ( 'NONE', ( #15299, #15258, #14468, #17155, #3968, #19683, #5754, #19253, #19207, #16445, #5478, #12494, #18413, #8421, #471, #2577, #5734, #4224, #95, #1141, #12963, #8690, #8430, #3122, #7394, #16637, #3070, #2870, #4361, #7557, #12193, #8612, #3415, #19344, #4485, #6002, #18639, #10349, #14764, #15015, #16830, #489, #56, #9207, #16582, #8314, #16210, #4604, #15999, #2704, #4338, #18903, #18604, #6410, #7198, #13751, #6826, #13691, #21758, #4024, #17971, #19659, #997, #20371, #15546, #8580, #3045, #12810, #446, #7597, #397, #16526, #19946, #14340, #5854, #11460, #3405, #10106 ) ) ;
#3902=CARTESIAN_POINT ( 'NONE',  ( 42.21948215057684450, 152.1113394311928175, 29.21067981925356705 ) ) ;
#3907=CARTESIAN_POINT ( 'NONE',  ( 40.27526882409969033, 83.92977050742732104, 30.44471234641811819 ) ) ;
#3909=CARTESIAN_POINT ( 'NONE',  ( 38.58424406990786082, 81.11518717409398960, 34.21067981925357060 ) ) ;
#3910=DIRECTION ( 'NONE',  ( 0.000000000000000000, 0.000000000000000000, 1.000000000000000000 ) ) ;
#3914=CARTESIAN_POINT ( 'NONE',  ( 45.74753988029934249, 134.3297705074273267, 30.44471234641812174 ) ) ;
#3918=ORIENTED_EDGE ( 'NONE', *, *, #14401, .T. ) ;
#3919=CARTESIAN_POINT ( 'NONE',  ( 40.27526882409969033, 134.9297705074272926, 30.44471234641811819 ) ) ;
#3922=( BOUNDED_CURVE ( )  B_SPLINE_CURVE ( 2, ( #2481, #21419, #10762, #6308, #13035, #728, #4654, #9003, #17467, #2378, #15714, #12517, #15814 ),
 .UNSPECIFIED., .F., .F. ) 
 B_SPLINE_CURVE_WITH_KNOTS ( ( 3, 2, 2, 2, 2, 2, 3 ),
 ( 0.8602941176470588758, 0.8617647058823529882, 0.8647058823529412130, 0.8676470588235294379, 0.8705882352941176627, 0.8735294117647058876, 0.8750000000000000000 ),
 .UNSPECIFIED. ) 
 CURVE ( )  GEOMETRIC_REPRESENTATION_ITEM ( )  RATIONAL_B_SPLINE_CURVE ( ( 0.9755282581475768211, 0.9755282581475777093, 1.000000000000000000, 0.9510565162951535312, 1.000000000000000000, 0.9510565162951535312, 1.000000000000000000, 0.9510565162951535312, 1.000000000000000000, 0.9510565162951535312, 1.000000000000000000, 0.9755282581475768211, 0.9755282581475768211 ) ) 
 REPRESENTATION_ITEM ( '' )  );
#3923=CARTESIAN_POINT ( 'NONE',  ( 44.37947211624943833, 95.21518717409399812, 30.00020018409699318 ) ) ;
#3928=CARTESIAN_POINT ( 'NONE',  ( 43.01140435219951286, 137.0344580088725479, 28.95336869806222779 ) ) ;
#3929=CARTESIAN_POINT ( 'NONE',  ( 43.01140435219951286, 116.6297705074273097, 29.55568802177586463 ) ) ;
#3932=CARTESIAN_POINT ( 'NONE',  ( 47.43856463449117911, 106.7651871740939811, 32.77220824515697473 ) ) ;
#3941=CARTESIAN_POINT ( 'NONE',  ( 41.64333658814960870, 74.77977050742731535, 30.00020018409699318 ) ) ;
#3944=CARTESIAN_POINT ( 'NONE',  ( 44.55648932407425633, 63.68445800887258201, 38.96596240072933170 ) ) ;
#3946=CARTESIAN_POINT ( 'NONE',  ( 43.01140435219951286, 125.9604996726487514, 28.95336869806222779 ) ) ;
#3948=CARTESIAN_POINT ( 'NONE',  ( 47.43856463449117200, 76.76518717409398107, 32.77220824515698183 ) ) ;
#3955=VECTOR ( 'NONE', #6141, 1000.000000000000000 ) ;
#3956=DIRECTION ( 'NONE',  ( 0.000000000000000000, 0.000000000000000000, 1.000000000000000000 ) ) ;
#3958=CARTESIAN_POINT ( 'NONE',  ( 41.64333658814960870, 137.7797705074273154, 30.00020018409699318 ) ) ;
#3959=CARTESIAN_POINT ( 'NONE',  ( 39.42975644700377558, 105.6797705074273352, 36.81289934271958941 ) ) ;
#3962=CARTESIAN_POINT ( 'NONE',  ( 39.42975644700377558, 137.8151871740940067, 31.60846029578754468 ) ) ;
#3963=CARTESIAN_POINT ( 'NONE',  ( 44.55648932407425633, 66.68445800887256780, 38.96596240072933170 ) ) ;
#3966=CARTESIAN_POINT ( 'NONE',  ( 38.96631938032478359, 136.0104996726487627, 37.14960608071593384 ) ) ;
#3968=ADVANCED_FACE ( 'NONE', ( #10013 ), #10449, .T. ) ;
#3969=CARTESIAN_POINT ( 'NONE',  ( 41.64333658814960870, 110.5151871740940095, 30.00020018409699318 ) ) ;
#3974=CARTESIAN_POINT ( 'NONE',  ( 44.55648932407425633, 94.88445800887257064, 29.45539723777780239 ) ) ;
#3975=CARTESIAN_POINT ( 'NONE',  ( 38.01140435219951996, 156.5604996726487457, 32.58608133808903773 ) ) ;
#3976=CARTESIAN_POINT ( 'NONE',  ( 39.42975644700377558, 113.8151871740940067, 31.60846029578754468 ) ) ;
#3978=CARTESIAN_POINT ( 'NONE',  ( 44.55648932407425633, 70.61049967264872862, 38.96596240072933170 ) ) ;
#3980=DIRECTION ( 'NONE',  ( 0.000000000000000000, 1.000000000000000000, 0.000000000000000000 ) ) ;
#3981=CARTESIAN_POINT ( 'NONE',  ( 43.01140435219951286, 81.53445800887257633, 39.21067981925356349 ) ) ;
#3982=EDGE_CURVE ( 'NONE', #21451, #14880, #13576, .T. ) ;
#3985=CARTESIAN_POINT ( 'NONE',  ( 45.74753988029933538, 71.06518717409400665, 30.44471234641811819 ) ) ;
#3992=ORIENTED_EDGE ( 'NONE', *, *, #4494, .F. ) ;
#3993=CARTESIAN_POINT ( 'NONE',  ( 47.43856463449117200, 148.7651871740939953, 32.77220824515698183 ) ) ;
#3994=CARTESIAN_POINT ( 'NONE',  ( 43.01140435219951286, 156.8651871740940180, 38.86567161673127657 ) ) ;
#3995=CARTESIAN_POINT ( 'NONE',  ( 38.58424406990786082, 105.3797705074273239, 34.21067981925357060 ) ) ;
#4001=CARTESIAN_POINT ( 'NONE',  ( 41.64333658814960870, 144.7151871740940123, 38.42115945441014446 ) ) ;
#4002=CARTESIAN_POINT ( 'NONE',  ( 47.05648932407426344, 104.5104996726487485, 31.27175355779120025 ) ) ;
#4007=CARTESIAN_POINT ( 'NONE',  ( 43.01140435219957681, 96.53445800887259054, 39.21067981925356349 ) ) ;
#4010=CARTESIAN_POINT ( 'NONE',  ( 39.42975644700377558, 87.07977050742732672, 31.60846029578754468 ) ) ;
#4012=CARTESIAN_POINT ( 'NONE',  ( 46.59305225739526435, 67.91518717409400097, 31.60846029578754468 ) ) ;
#4016=CARTESIAN_POINT ( 'NONE',  ( 42.21948215057687293, 68.11133943119284595, 29.21067981925355994 ) ) ;
#4018=CARTESIAN_POINT ( 'NONE',  ( 39.42975644700377558, 129.6797705074273210, 36.81289934271958941 ) ) ;
#4023=CARTESIAN_POINT ( 'NONE',  ( 45.74753988029933538, 137.3297705074273267, 30.44471234641811819 ) ) ;
#4024=ADVANCED_FACE ( 'NONE', ( #10232 ), #1627, .T. ) ;
#4025=CARTESIAN_POINT ( 'NONE',  ( 38.01140435219952707, 110.9344580088725678, 35.83527830041809636 ) ) ;
#4030=CARTESIAN_POINT ( 'NONE',  ( 40.27526882409969033, 101.6651871740940152, 30.44471234641811819 ) ) ;
#4031=CARTESIAN_POINT ( 'NONE',  ( 44.55648932407425633, 74.81049967264874567, 29.45539723777780239 ) ) ;
#4036=CARTESIAN_POINT ( 'NONE',  ( 43.01140435219951286, 129.5344580088726048, 39.46799094044489209 ) ) ;
#4037=CARTESIAN_POINT ( 'NONE',  ( 44.37947211624943833, 110.4797705074273324, 30.00020018409699318 ) ) ;
#4040=CARTESIAN_POINT ( 'NONE',  ( 39.42975644700377558, 104.8151871740939924, 31.60846029578754468 ) ) ;
#4043=CARTESIAN_POINT ( 'NONE',  ( 38.96631938032478359, 88.01049967264874851, 37.14960608071593384 ) ) ;
#4046=DIRECTION ( 'NONE',  ( 0.000000000000000000, 1.000000000000000000, 0.000000000000000000 ) ) ;
#4047=CARTESIAN_POINT ( 'NONE',  ( 44.37947211624943833, 76.27977050742731535, 38.42115945441014446 ) ) ;
#4050=( BOUNDED_CURVE ( )  B_SPLINE_CURVE ( 2, ( #5250, #3381, #17565, #2472, #12174, #15805, #718, #7449, #10752, #15912, #14154, #20889, #822 ),
 .UNSPECIFIED., .F., .F. ) 
 B_SPLINE_CURVE_WITH_KNOTS ( ( 3, 2, 2, 2, 2, 2, 3 ),
 ( 0.03676470588235294240, 0.03823529411764706176, 0.04117647058823529355, 0.04411764705882353227, 0.04705882352941176405, 0.05000000000000000278, 0.05147058823529411520 ),
 .UNSPECIFIED. ) 
 CURVE ( )  GEOMETRIC_REPRESENTATION_ITEM ( )  RATIONAL_B_SPLINE_CURVE ( ( 0.9755282581475768211, 0.9755282581475768211, 1.000000000000000000, 0.9510565162951535312, 1.000000000000000000, 0.9510565162951535312, 1.000000000000000000, 0.9510565162951535312, 1.000000000000000000, 0.9510565162951535312, 1.000000000000000000, 0.9755282581475768211, 0.9755282581475767101 ) ) 
 REPRESENTATION_ITEM ( '' )  );
#4052=CARTESIAN_POINT ( 'NONE',  ( 48.01140435219951996, 116.2104996726487371, 34.21067981925357060 ) ) ;
#4053=CARTESIAN_POINT ( 'NONE',  ( 40.27526882409969033, 75.56518717409399244, 37.97664729208901946 ) ) ;
#4058=CYLINDRICAL_SURFACE ( 'NONE', #16691, 4.999999999999997335 ) ;
#4060=CARTESIAN_POINT ( 'NONE',  ( 46.59305225739526435, 143.1797705074273210, 31.60846029578754468 ) ) ;
#4062=CARTESIAN_POINT ( 'NONE',  ( 45.74753988029934249, 136.1651871740939725, 37.97664729208901235 ) ) ;
#4063=EDGE_CURVE ( 'NONE', #20212, #10776, #15071, .T. ) ;
#4070=CYLINDRICAL_SURFACE ( 'NONE', #12334, 4.999999999999997335 ) ;
#4071=CARTESIAN_POINT ( 'NONE',  ( 38.58424406990784661, 113.9651871740940123, 32.77220824515698183 ) ) ;
#4075=CARTESIAN_POINT ( 'NONE',  ( 38.01140435219951996, 95.93445800887258201, 35.83527830041810347 ) ) ;
#4076=CARTESIAN_POINT ( 'NONE',  ( 46.59305225739526435, 148.5797705074273267, 36.81289934271958941 ) ) ;
#4078=CARTESIAN_POINT ( 'NONE',  ( 44.55648932407425633, 152.8104996726487457, 29.45539723777780239 ) ) ;
#4079=CARTESIAN_POINT ( 'NONE',  ( 45.74753988029933538, 103.1651871740940010, 37.97664729208901946 ) ) ;
#4081=CARTESIAN_POINT ( 'NONE',  ( 38.96631938032478359, 72.41049967264873999, 31.27175355779120025 ) ) ;
#4083=CARTESIAN_POINT ( 'NONE',  ( 44.55648932407425633, 147.6844580088725820, 38.96596240072933170 ) ) ;
#4087=CARTESIAN_POINT ( 'NONE',  ( 44.37947211624943833, 68.21518717409399812, 30.00020018409699318 ) ) ;
#4088=CARTESIAN_POINT ( 'NONE',  ( 38.01140435219952707, 63.71049967264874425, 34.21067981925357060 ) ) ;
#4095=CARTESIAN_POINT ( 'NONE',  ( 43.01140435219951286, 141.8651871740940180, 38.86567161673127657 ) ) ;
#4096=CARTESIAN_POINT ( 'NONE',  ( 40.27526882409969744, 108.8297705074273125, 37.97664729208901235 ) ) ;
#4097=ORIENTED_EDGE ( 'NONE', *, *, #3754, .T. ) ;
#4098=VERTEX_POINT ( 'NONE', #10882 ) ;
#4102=VERTEX_POINT ( 'NONE', #15929 ) ;
#4103=EDGE_CURVE ( 'NONE', #19572, #3065, #12867, .T. ) ;
#4105=CARTESIAN_POINT ( 'NONE',  ( 44.37947211624943833, 139.0151871740939953, 38.42115945441014446 ) ) ;
#4106=CARTESIAN_POINT ( 'NONE',  ( 43.01140435219951286, 100.4604996726487656, 39.46799094044489209 ) ) ;
#4111=CARTESIAN_POINT ( 'NONE',  ( 46.10157429594899270, 158.6604996726487116, 29.95742577749336988 ) ) ;
#4112=CARTESIAN_POINT ( 'NONE',  ( 38.01140435219952707, 143.6344580088725706, 32.58608133808903773 ) ) ;
#4114=ORIENTED_EDGE ( 'NONE', *, *, #19283, .F. ) ;
#4115=CARTESIAN_POINT ( 'NONE',  ( 39.42975644700377558, 81.67977050742732104, 36.81289934271958941 ) ) ;
#4117=CARTESIAN_POINT ( 'NONE',  ( 39.42975644700377558, 65.81518717409400665, 31.60846029578754468 ) ) ;
#4121=EDGE_CURVE ( 'NONE', #10985, #711, #11193, .T. ) ;
#4122=CARTESIAN_POINT ( 'NONE',  ( 43.80332655382220253, 85.95757658655229250, 29.21067981925356705 ) ) ;
#4124=CARTESIAN_POINT ( 'NONE',  ( 41.64333658814960870, 137.7797705074273154, 30.00020018409699318 ) ) ;
#4129=AXIS2_PLACEMENT_3D ( 'NONE', #5886, #2474, #12284 ) ;
#4130=CARTESIAN_POINT ( 'NONE',  ( 38.58424406990784661, 126.5297705074272727, 35.64915139335016647 ) ) ;
#4131=CARTESIAN_POINT ( 'NONE',  ( 47.05648932407426344, 109.9104996726487400, 37.14960608071593384 ) ) ;
#4133=LINE ( 'NONE', #19337, #2364 ) ;
#4137=CARTESIAN_POINT ( 'NONE',  ( 40.27526882409969033, 99.56518717409400665, 37.97664729208901946 ) ) ;
#4139=CARTESIAN_POINT ( 'NONE',  ( 44.55648932407425633, 124.6104996726487428, 38.96596240072933170 ) ) ;
#4142=CARTESIAN_POINT ( 'NONE',  ( 48.01140435219951996, 130.2844580088725763, 34.21067981925357060 ) ) ;
#4143=CARTESIAN_POINT ( 'NONE',  ( 47.43856463449117200, 110.0297705074273296, 32.77220824515698183 ) ) ;
#4146=CARTESIAN_POINT ( 'NONE',  ( 46.59305225739526435, 94.31518717409399244, 36.81289934271958941 ) ) ;
#4148=CARTESIAN_POINT ( 'NONE',  ( 41.46631938032478359, 91.31049967264874567, 38.96596240072933170 ) ) ;
#4151=EDGE_CURVE ( 'NONE', #14439, #5159, #6099, .T. ) ;
#4156=CARTESIAN_POINT ( 'NONE',  ( 40.27526882409969744, 77.92977050742732104, 30.44471234641812174 ) ) ;
#4159=CARTESIAN_POINT ( 'NONE',  ( 44.37947211624943833, 157.2797705074273438, 38.42115945441014446 ) ) ;
#4162=CARTESIAN_POINT ( 'NONE',  ( 46.10157429594899270, 122.6604996726487542, 29.95742577749337343 ) ) ;
#4163=CARTESIAN_POINT ( 'NONE',  ( 40.27526882409969033, 74.66518717409397254, 30.44471234641811819 ) ) ;
#4169=CARTESIAN_POINT ( 'NONE',  ( 47.05648932407426344, 157.5844580088725877, 31.27175355779120025 ) ) ;
#4170=CARTESIAN_POINT ( 'NONE',  ( 47.43856463449117200, 139.7297705074273324, 35.64915139335016647 ) ) ;
#4172=CARTESIAN_POINT ( 'NONE',  ( 45.74753988029934249, 127.1651871740939725, 37.97664729208901235 ) ) ;
#4174=CARTESIAN_POINT ( 'NONE',  ( 44.55648932407425633, 136.6104996726487286, 38.96596240072933170 ) ) ;
#4176=CARTESIAN_POINT ( 'NONE',  ( 44.82204965540741171, 59.43124467221783647, 30.14400234367970910 ) ) ;
#4179=CARTESIAN_POINT ( 'NONE',  ( 39.42975644700377558, 107.8151871740939924, 31.60846029578754468 ) ) ;
#4180=( BOUNDED_CURVE ( )  B_SPLINE_CURVE ( 2, ( #734, #19352, #4148, #15927, #839, #7573, #21018, #12630, #4250, #10976, #14385, #14926, #6452 ),
 .UNSPECIFIED., .F., .T. ) 
 B_SPLINE_CURVE_WITH_KNOTS ( ( 3, 2, 2, 2, 2, 2, 3 ),
 ( 0.6691176470588234837, 0.6705882352941175961, 0.6735294117647059320, 0.6764705882352941568, 0.6794117647058823817, 0.6823529411764706065, 0.6838235294117647189 ),
 .UNSPECIFIED. ) 
 CURVE ( )  GEOMETRIC_REPRESENTATION_ITEM ( )  RATIONAL_B_SPLINE_CURVE ( ( 0.9755282581475768211, 0.9755282581475768211, 1.000000000000000000, 0.9510565162951535312, 1.000000000000000000, 0.9510565162951535312, 1.000000000000000000, 0.9510565162951535312, 1.000000000000000000, 0.9510565162951535312, 1.000000000000000000, 0.9755282581475768211, 0.9755282581475768211 ) ) 
 REPRESENTATION_ITEM ( '' )  );
#4181=ORIENTED_EDGE ( 'NONE', *, *, #7813, .T. ) ;
#4184=CARTESIAN_POINT ( 'NONE',  ( 46.10157429594899270, 96.83445800887255928, 38.46393386101376421 ) ) ;
#4185=CARTESIAN_POINT ( 'NONE',  ( 41.64333658814960870, 149.7797705074273154, 30.00020018409699318 ) ) ;
#4186=CARTESIAN_POINT ( 'NONE',  ( 38.96631938032478359, 150.4104996726487400, 31.27175355779120025 ) ) ;
#4187=CARTESIAN_POINT ( 'NONE',  ( 38.58424406990784661, 110.9651871740940123, 32.77220824515698183 ) ) ;
#4189=CARTESIAN_POINT ( 'NONE',  ( 38.01140435219951996, 60.56049967264873146, 32.58608133808903773 ) ) ;
#4190=DIRECTION ( 'NONE',  ( 0.000000000000000000, 1.000000000000000000, 0.000000000000000000 ) ) ;
#4191=CARTESIAN_POINT ( 'NONE',  ( 43.01140435219951996, 10.71049967264875491, 34.21067981925357060 ) ) ;
#4193=CARTESIAN_POINT ( 'NONE',  ( 43.01140435219951286, 81.53445800887257633, 39.21067981925356349 ) ) ;
#4201=FILL_AREA_STYLE_COLOUR ( '', #6715 ) ;
#4202=CARTESIAN_POINT ( 'NONE',  ( 38.58424406990784661, 134.9651871740940123, 32.77220824515698183 ) ) ;
#4203=CARTESIAN_POINT ( 'NONE',  ( 38.58424406990785371, 93.22977050742731819, 32.77220824515697473 ) ) ;
#4204=VERTEX_POINT ( 'NONE', #8906 ) ;
#4208=CARTESIAN_POINT ( 'NONE',  ( 43.01140435219951286, 113.0344580088725621, 28.95336869806222779 ) ) ;
#4210=CARTESIAN_POINT ( 'NONE',  ( 38.01140435219952707, 75.86049967264874283, 35.83527830041809636 ) ) ;
#4211=CARTESIAN_POINT ( 'NONE',  ( 46.59305225739526435, 74.17977050742732104, 31.60846029578754468 ) ) ;
#4212=CARTESIAN_POINT ( 'NONE',  ( 41.64333658814960870, 132.7151871740940123, 38.42115945441014446 ) ) ;
#4213=CARTESIAN_POINT ( 'NONE',  ( 38.01140435219951996, 93.86049967264874283, 35.83527830041810347 ) ) ;
#4217=CARTESIAN_POINT ( 'NONE',  ( 48.01140435219951996, 158.0604996726487173, 35.83527830041809636 ) ) ;
#4222=CARTESIAN_POINT ( 'NONE',  ( 38.58424406990784661, 72.22977050742733240, 32.77220824515698183 ) ) ;
#4224=ADVANCED_FACE ( 'NONE', ( #13953 ), #19249, .T. ) ;
#4229=CARTESIAN_POINT ( 'NONE',  ( 39.92123440845005433, 104.3344580088725735, 29.95742577749336988 ) ) ;
#4230=CARTESIAN_POINT ( 'NONE',  ( 43.01140435219951286, 136.1297705074273381, 38.86567161673127657 ) ) ;
#4232=EDGE_LOOP ( 'NONE', ( #19120, #18194, #14335, #3347 ) ) ;
#4233=CARTESIAN_POINT ( 'NONE',  ( 46.10157429594899270, 72.83445800887257349, 38.46393386101375711 ) ) ;
#4235=CARTESIAN_POINT ( 'NONE',  ( 38.58424406990786082, 123.3797705074273239, 34.21067981925357060 ) ) ;
#4236=CARTESIAN_POINT ( 'NONE',  ( 46.10157429594899270, 139.7344580088725934, 29.95742577749336988 ) ) ;
#4239=CARTESIAN_POINT ( 'NONE',  ( 43.01140435219951996, 158.9604996726487514, 29.21067981925357060 ) ) ;
#4242=CARTESIAN_POINT ( 'NONE',  ( 43.80332655382220253, 124.5373810949689926, 39.21067981925355639 ) ) ;
#4245=CARTESIAN_POINT ( 'NONE',  ( 46.10157429594899270, 133.7344580088725650, 29.95742577749337343 ) ) ;
#4246=CARTESIAN_POINT ( 'NONE',  ( 38.58424406990784661, 111.2297705074273324, 32.77220824515698183 ) ) ;
#4249=CARTESIAN_POINT ( 'NONE',  ( 41.64333658814960870, 95.51518717409400949, 30.00020018409699318 ) ) ;
#4250=CARTESIAN_POINT ( 'NONE',  ( 38.96631938032478359, 90.41049967264875420, 31.27175355779120025 ) ) ;
#4252=CARTESIAN_POINT ( 'NONE',  ( 47.05648932407426344, 75.98445800887257917, 37.14960608071593384 ) ) ;
#4256=CARTESIAN_POINT ( 'NONE',  ( 45.74753988029934249, 74.32977050742731251, 30.44471234641812174 ) ) ;
#4257=ORIENTED_EDGE ( 'NONE', *, *, #2207, .F. ) ;
#4260=CARTESIAN_POINT ( 'NONE',  ( 44.37947211624943833, 158.4797705074273040, 30.00020018409699318 ) ) ;
#4262=CARTESIAN_POINT ( 'NONE',  ( 41.46631938032478359, 118.3104996726487457, 38.96596240072933170 ) ) ;
#4263=CARTESIAN_POINT ( 'NONE',  ( 47.43856463449117200, 79.76518717409400949, 32.77220824515698183 ) ) ;
#4269=CARTESIAN_POINT ( 'NONE',  ( 38.96631938032478359, 158.4844580088725934, 31.27175355779120025 ) ) ;
#4270=CARTESIAN_POINT ( 'NONE',  ( 47.43856463449118621, 145.8797705074273097, 34.21067981925357060 ) ) ;
#4272=CARTESIAN_POINT ( 'NONE',  ( 43.01140435219951286, 122.3651871740939896, 29.55568802177586107 ) ) ;
#4274=FACE_OUTER_BOUND ( 'NONE', #8740, .T. ) ;
#4277=CARTESIAN_POINT ( 'NONE',  ( 47.43856463449118621, 109.6151871740940038, 34.21067981925357060 ) ) ;
#4280=EDGE_LOOP ( 'NONE', ( #14464, #4432, #12496, #9 ) ) ;
#4281=CARTESIAN_POINT ( 'NONE',  ( 43.01140435219951286, 93.53445800887257633, 39.46799094044489209 ) ) ;
#4282=DIRECTION ( 'NONE',  ( 0.000000000000000000, -1.000000000000000000, 0.000000000000000000 ) ) ;
#4285=VECTOR ( 'NONE', #17335, 1000.000000000000000 ) ;
#4287=CARTESIAN_POINT ( 'NONE',  ( 39.42975644700377558, 102.4151871740940010, 36.81289934271958941 ) ) ;
#4289=CARTESIAN_POINT ( 'NONE',  ( 38.96631938032478359, 63.41049967264873999, 31.27175355779120025 ) ) ;
#4291=CARTESIAN_POINT ( 'NONE',  ( 47.05648932407426344, 60.98445800887257207, 37.14960608071593384 ) ) ;
#4293=CARTESIAN_POINT ( 'NONE',  ( 48.01140435219951996, 146.3604996726487570, 32.58608133808903773 ) ) ;
#4294=CARTESIAN_POINT ( 'NONE',  ( 43.01140435219951286, 68.36518717409400381, 29.55568802177586463 ) ) ;
#4296=DIRECTION ( 'NONE',  ( 0.000000000000000000, 1.000000000000000000, 0.000000000000000000 ) ) ;
#4303=EDGE_CURVE ( 'NONE', #20212, #11299, #8375, .T. ) ;
#4305=CARTESIAN_POINT ( 'NONE',  ( 45.74753988029933538, 136.1651871740939725, 37.97664729208901946 ) ) ;
#4306=CARTESIAN_POINT ( 'NONE',  ( 45.74753988029934249, 155.0651871740940067, 30.44471234641812174 ) ) ;
#4307=CARTESIAN_POINT ( 'NONE',  ( 44.37947211624943833, 94.27977050742731535, 38.42115945441014446 ) ) ;
#4308=ORIENTED_EDGE ( 'NONE', *, *, #21220, .T. ) ;
#4309=ORIENTED_EDGE ( 'NONE', *, *, #15936, .T. ) ;
#4311=ORIENTED_EDGE ( 'NONE', *, *, #3156, .T. ) ;
#4312=CARTESIAN_POINT ( 'NONE',  ( 43.01140435219951286, 117.5344580088725621, 39.46799094044489209 ) ) ;
#4314=CARTESIAN_POINT ( 'NONE',  ( 41.64333658814960870, 75.97977050742731819, 38.42115945441014446 ) ) ;
#4315=CARTESIAN_POINT ( 'NONE',  ( 43.01140435219951286, 135.8651871740940180, 38.86567161673127657 ) ) ;
#4316=CARTESIAN_POINT ( 'NONE',  ( 48.01140435219951996, 89.36049967264874283, 32.58608133808903773 ) ) ;
#4324=CARTESIAN_POINT ( 'NONE',  ( 40.27526882409969033, 78.82977050742731251, 37.97664729208901946 ) ) ;
#4331=CARTESIAN_POINT ( 'NONE',  ( 46.59305225739526435, 128.1797705074273210, 31.60846029578754468 ) ) ;
#4332=EDGE_LOOP ( 'NONE', ( #21563, #20807 ) ) ;
#4333=CARTESIAN_POINT ( 'NONE',  ( 44.55648932407425633, 87.68445800887258201, 38.96596240072933170 ) ) ;
#4334=ORIENTED_EDGE ( 'NONE', *, *, #1961, .T. ) ;
#4335=CARTESIAN_POINT ( 'NONE',  ( 39.42975644700377558, 129.6797705074273210, 36.81289934271958941 ) ) ;
#4336=CARTESIAN_POINT ( 'NONE',  ( 43.80332655382219542, 139.9575765865523067, 29.21067981925356705 ) ) ;
#4337=CARTESIAN_POINT ( 'NONE',  ( 38.96631938032478359, 60.08445800887257349, 37.14960608071593384 ) ) ;
#4338=ADVANCED_FACE ( 'NONE', ( #14716 ), #4459, .T. ) ;
#4340=CARTESIAN_POINT ( 'NONE',  ( 39.92123440845005433, 84.23445800887256496, 38.46393386101375711 ) ) ;
#4345=CARTESIAN_POINT ( 'NONE',  ( 43.01140435219951286, 131.0344580088725763, 28.95336869806222779 ) ) ;
#4346=CARTESIAN_POINT ( 'NONE',  ( 45.74753988029933538, 107.3297705074272983, 30.44471234641811819 ) ) ;
#4348=LINE ( 'NONE', #12628, #13097 ) ;
#4349=CARTESIAN_POINT ( 'NONE',  ( 39.42975644700377558, 92.81518717409399244, 31.60846029578754468 ) ) ;
#4351=ORIENTED_EDGE ( 'NONE', *, *, #5830, .F. ) ;
#4352=CARTESIAN_POINT ( 'NONE',  ( 43.80332655382220253, 128.8836182503284533, 29.21067981925356705 ) ) ;
#4356=CARTESIAN_POINT ( 'NONE',  ( 40.27526882409969744, 72.82977050742732672, 37.97664729208901235 ) ) ;
#4359=CARTESIAN_POINT ( 'NONE',  ( 45.74753988029933538, 151.4297705074273210, 37.97664729208901946 ) ) ;
#4361=ADVANCED_FACE ( 'NONE', ( #9878 ), #16578, .T. ) ;
#4363=CARTESIAN_POINT ( 'NONE',  ( 39.92123440845004723, 123.2604996726487201, 29.95742577749337343 ) ) ;
#4364=CARTESIAN_POINT ( 'NONE',  ( 47.43856463449118621, 82.61518717409398960, 34.21067981925357060 ) ) ;
#4370=CARTESIAN_POINT ( 'NONE',  ( 38.01140435219952707, 149.7844580088725763, 34.21067981925357060 ) ) ;
#4371=CARTESIAN_POINT ( 'NONE',  ( 46.59305225739526435, 131.1797705074273210, 31.60846029578754468 ) ) ;
#4373=CARTESIAN_POINT ( 'NONE',  ( 47.43856463449117911, 121.7651871740939953, 32.77220824515697473 ) ) ;
#4374=CARTESIAN_POINT ( 'NONE',  ( 47.05648932407426344, 136.9104996726487400, 37.14960608071593384 ) ) ;
#4375=CYLINDRICAL_SURFACE ( 'NONE', #14133, 4.999999999999997335 ) ;
#4378=AXIS2_PLACEMENT_3D ( 'NONE', #472, #13589, #10617 ) ;
#4380=CARTESIAN_POINT ( 'NONE',  ( 43.80332655382220253, 83.88361825032845331, 29.21067981925356705 ) ) ;
#4381=CARTESIAN_POINT ( 'NONE',  ( 38.58424406990784661, 104.9651871740940123, 32.77220824515698183 ) ) ;
#4386=CARTESIAN_POINT ( 'NONE',  ( 38.01140435219951996, 92.63445800887258486, 32.58608133808903773 ) ) ;
#4388=CARTESIAN_POINT ( 'NONE',  ( 43.01140435219951286, 148.4604996726487229, 39.46799094044489209 ) ) ;
#4389=CARTESIAN_POINT ( 'NONE',  ( 47.43856463449117200, 106.4651871740939981, 35.64915139335016647 ) ) ;
#4391=CARTESIAN_POINT ( 'NONE',  ( 43.01140435219951286, 61.46049967264873004, 39.46799094044489209 ) ) ;
#4394=CARTESIAN_POINT ( 'NONE',  ( 43.01140435219951286, 119.0344580088725621, 29.21067981925356705 ) ) ;
#4396=CARTESIAN_POINT ( 'NONE',  ( 43.80332655382220253, 146.8836182503284817, 29.21067981925356705 ) ) ;
#4397=CARTESIAN_POINT ( 'NONE',  ( 40.27526882409969033, 71.66518717409400097, 30.44471234641811819 ) ) ;
#4399=CARTESIAN_POINT ( 'NONE',  ( 41.46631938032478359, 115.3104996726487599, 38.96596240072933170 ) ) ;
#4407=CARTESIAN_POINT ( 'NONE',  ( 47.43856463449118621, 136.6151871740940180, 34.21067981925357060 ) ) ;
#4409=CARTESIAN_POINT ( 'NONE',  ( 46.59305225739526435, 154.3151871740940067, 36.81289934271958941 ) ) ;
#4410=CARTESIAN_POINT ( 'NONE',  ( 47.43856463449117911, 91.72977050742730398, 35.64915139335015937 ) ) ;
#4412=ORIENTED_EDGE ( 'NONE', *, *, #7246, .T. ) ;
#4415=CARTESIAN_POINT ( 'NONE',  ( 41.46631938032478359, 117.3844580088725849, 38.96596240072933170 ) ) ;
#4418=CARTESIAN_POINT ( 'NONE',  ( 40.27526882409969033, 74.92977050742732104, 30.44471234641811819 ) ) ;
#4419=CARTESIAN_POINT ( 'NONE',  ( 46.59305225739526435, 130.9151871740940010, 31.60846029578754468 ) ) ;
#4420=CARTESIAN_POINT ( 'NONE',  ( 48.01140435219951996, 95.36049967264872862, 32.58608133808903773 ) ) ;
#4424=( BOUNDED_CURVE ( )  B_SPLINE_CURVE ( 2, ( #17544, #2561, #10948, #12487, #20762, #9194, #8975, #4112, #585, #5654, #17437, #14132, #12374 ),
 .UNSPECIFIED., .F., .T. ) 
 B_SPLINE_CURVE_WITH_KNOTS ( ( 3, 2, 2, 2, 2, 2, 3 ),
 ( 0.1397058823529411797, 0.1411764705882352922, 0.1441176470588235170, 0.1470588235294117696, 0.1499999999999999944, 0.1529411764705882470, 0.1544117647058823595 ),
 .UNSPECIFIED. ) 
 CURVE ( )  GEOMETRIC_REPRESENTATION_ITEM ( )  RATIONAL_B_SPLINE_CURVE ( ( 0.9755282581475768211, 0.9755282581475768211, 1.000000000000000000, 0.9510565162951535312, 1.000000000000000000, 0.9510565162951535312, 1.000000000000000000, 0.9510565162951535312, 1.000000000000000000, 0.9510565162951535312, 1.000000000000000000, 0.9755282581475768211, 0.9755282581475768211 ) ) 
 REPRESENTATION_ITEM ( '' )  );
#4426=EDGE_LOOP ( 'NONE', ( #4992, #11145, #923, #21458 ) ) ;
#4427=CARTESIAN_POINT ( 'NONE',  ( 43.01140435219951286, 76.12977050742732388, 38.86567161673127657 ) ) ;
#4432=ORIENTED_EDGE ( 'NONE', *, *, #10310, .F. ) ;
#4436=CARTESIAN_POINT ( 'NONE',  ( 40.27526882409969744, 125.9297705074273352, 30.44471234641812174 ) ) ;
#4438=CARTESIAN_POINT ( 'NONE',  ( 48.01140435219951996, 130.4344580088725820, 32.58608133808903773 ) ) ;
#4439=VERTEX_POINT ( 'NONE', #9449 ) ;
#4440=CARTESIAN_POINT ( 'NONE',  ( 43.01140435219951286, 125.6297705074273381, 29.55568802177586463 ) ) ;
#4442=CARTESIAN_POINT ( 'NONE',  ( 38.01140435219952707, 72.71049967264873715, 34.21067981925357060 ) ) ;
#4443=CARTESIAN_POINT ( 'NONE',  ( 43.01140435219951286, 59.03445800887256922, 28.95336869806222779 ) ) ;
#4449=CARTESIAN_POINT ( 'NONE',  ( 42.21948215057684450, 67.38361825032845331, 39.21067981925355639 ) ) ;
#4450=CARTESIAN_POINT ( 'NONE',  ( 44.55648932407425633, 93.68445800887258201, 38.96596240072933170 ) ) ;
#4452=CARTESIAN_POINT ( 'NONE',  ( 43.01140435219951286, 128.0344580088725763, 28.95336869806222779 ) ) ;
#4453=CARTESIAN_POINT ( 'NONE',  ( 43.01140435219951286, 104.6297705074273239, 29.55568802177586463 ) ) ;
#4456=CARTESIAN_POINT ( 'NONE',  ( 40.27526882409969744, 96.56518717409400665, 37.97664729208901235 ) ) ;
#4458=ORIENTED_EDGE ( 'NONE', *, *, #17049, .F. ) ;
#4459=CYLINDRICAL_SURFACE ( 'NONE', #21049, 4.999999999999997335 ) ;
#4464=CARTESIAN_POINT ( 'NONE',  ( 38.58424406990785371, 63.52977050742730825, 35.64915139335015937 ) ) ;
#4465=ORIENTED_EDGE ( 'NONE', *, *, #12868, .T. ) ;
#4467=CARTESIAN_POINT ( 'NONE',  ( 43.01140435219951286, 151.1297705074273097, 38.86567161673127657 ) ) ;
#4470=CARTESIAN_POINT ( 'NONE',  ( 41.46631938032478359, 117.1104996726487428, 29.45539723777780239 ) ) ;
#4471=CARTESIAN_POINT ( 'NONE',  ( 38.58424406990786082, 69.11518717409400381, 34.21067981925357060 ) ) ;
#4473=CARTESIAN_POINT ( 'NONE',  ( 43.01140435219951286, 121.4604996726487371, 39.21067981925356349 ) ) ;
#4476=CARTESIAN_POINT ( 'NONE',  ( 38.01140435219952707, 155.7844580088725763, 34.21067981925357060 ) ) ;
#4479=CARTESIAN_POINT ( 'NONE',  ( 39.92123440845005433, 150.2344580088725650, 38.46393386101375711 ) ) ;
#4480=CARTESIAN_POINT ( 'NONE',  ( 38.58424406990786082, 132.3797705074273381, 34.21067981925357060 ) ) ;
#4482=CARTESIAN_POINT ( 'NONE',  ( 47.43856463449118621, 127.6151871740940038, 34.21067981925357060 ) ) ;
#4483=CARTESIAN_POINT ( 'NONE',  ( 43.01140435219951286, 70.46049967264873715, 39.21067981925356349 ) ) ;
#4485=ADVANCED_FACE ( 'NONE', ( #6342 ), #21341, .T. ) ;
#4490=VECTOR ( 'NONE', #1299, 1000.000000000000000 ) ;
#4492=CARTESIAN_POINT ( 'NONE',  ( 44.37947211624943833, 104.2151871740939981, 30.00020018409699318 ) ) ;
#4494=EDGE_CURVE ( 'NONE', #1056, #14631, #20223, .T. ) ;
#4496=ORIENTED_EDGE ( 'NONE', *, *, #6638, .T. ) ;
#4497=CARTESIAN_POINT ( 'NONE',  ( 47.05648932407426344, 84.98445800887257917, 37.14960608071593384 ) ) ;
#4499=CARTESIAN_POINT ( 'NONE',  ( 41.46631938032478359, 147.1104996726487570, 29.45539723777780239 ) ) ;
#4500=CARTESIAN_POINT ( 'NONE',  ( 47.43856463449117200, 103.7651871740939669, 32.77220824515698183 ) ) ;
#4503=CARTESIAN_POINT ( 'NONE',  ( 46.10157429594899270, 61.76049967264873430, 38.46393386101376421 ) ) ;
#4506=CARTESIAN_POINT ( 'NONE',  ( 43.01140435219951286, 117.5344580088725763, 39.21067981925356349 ) ) ;
#4510=CARTESIAN_POINT ( 'NONE',  ( 46.59305225739526435, 64.31518717409399244, 36.81289934271958941 ) ) ;
#4512=CARTESIAN_POINT ( 'NONE',  ( 47.43856463449118621, 151.6151871740939896, 34.21067981925357060 ) ) ;
#4518=CARTESIAN_POINT ( 'NONE',  ( 39.42975644700377558, 72.41518717409400097, 36.81289934271958941 ) ) ;
#4521=CARTESIAN_POINT ( 'NONE',  ( 43.01140435219951286, 111.5344580088725905, 39.21067981925356349 ) ) ;
#4522=CARTESIAN_POINT ( 'NONE',  ( 40.27526882409969033, 131.6651871740939725, 30.44471234641811819 ) ) ;
#4526=ADVANCED_BREP_SHAPE_REPRESENTATION ( '', ( #62, #12657 ), #2455 ) ;
#4529=CARTESIAN_POINT ( 'NONE',  ( 48.01140435219951996, 109.1344580088725849, 35.83527830041810347 ) ) ;
#4531=CARTESIAN_POINT ( 'NONE',  ( 40.27526882409969033, 77.92977050742732104, 30.44471234641811819 ) ) ;
#4532=CARTESIAN_POINT ( 'NONE',  ( 38.58424406990784661, 134.9651871740940123, 32.77220824515698183 ) ) ;
#4533=CARTESIAN_POINT ( 'NONE',  ( 39.92123440845004723, 87.26049967264874851, 29.95742577749337343 ) ) ;
#4537=CARTESIAN_POINT ( 'NONE',  ( 40.27526882409969033, 83.66518717409398675, 30.44471234641811819 ) ) ;
#4538=CARTESIAN_POINT ( 'NONE',  ( 48.01140435219951996, 107.3604996726487428, 32.58608133808903773 ) ) ;
#4540=CARTESIAN_POINT ( 'NONE',  ( 44.55648932407425633, 61.61049967264874283, 38.96596240072933170 ) ) ;
#4542=CARTESIAN_POINT ( 'NONE',  ( 47.43856463449117200, 76.72977050742733240, 35.64915139335016647 ) ) ;
#4548=FACE_OUTER_BOUND ( 'NONE', #6072, .T. ) ;
#4550=CARTESIAN_POINT ( 'NONE',  ( 38.96631938032478359, 105.0844580088725877, 37.14960608071593384 ) ) ;
#4551=CARTESIAN_POINT ( 'NONE',  ( 41.64333658814960870, 128.7797705074273438, 30.00020018409699318 ) ) ;
#4553=CYLINDRICAL_SURFACE ( 'NONE', #18890, 4.999999999999997335 ) ;
#4555=CARTESIAN_POINT ( 'NONE',  ( 45.74753988029933538, 128.3297705074273267, 30.44471234641811819 ) ) ;
#4557=CARTESIAN_POINT ( 'NONE',  ( 39.92123440845004723, 66.23445800887257917, 38.46393386101376421 ) ) ;
#4558=( BOUNDED_CURVE ( )  B_SPLINE_CURVE ( 2, ( #15595, #502, #20678, #7346, #9108, #5562, #14050, #5674, #14157, #8996, #20783, #15807, #721 ),
 .UNSPECIFIED., .F., .F. ) 
 B_SPLINE_CURVE_WITH_KNOTS ( ( 3, 2, 2, 2, 2, 2, 3 ),
 ( 0.3602941176470588203, 0.3617647058823529327, 0.3647058823529411575, 0.3676470588235294379, 0.3705882352941176627, 0.3735294117647058876, 0.3750000000000000000 ),
 .UNSPECIFIED. ) 
 CURVE ( )  GEOMETRIC_REPRESENTATION_ITEM ( )  RATIONAL_B_SPLINE_CURVE ( ( 0.9755282581475768211, 0.9755282581475768211, 1.000000000000000000, 0.9510565162951535312, 1.000000000000000000, 0.9510565162951535312, 1.000000000000000000, 0.9510565162951535312, 1.000000000000000000, 0.9510565162951535312, 1.000000000000000000, 0.9755282581475768211, 0.9755282581475768211 ) ) 
 REPRESENTATION_ITEM ( '' )  );
#4564=CARTESIAN_POINT ( 'NONE',  ( 38.96631938032478359, 156.4104996726487400, 31.27175355779120025 ) ) ;
#4565=CARTESIAN_POINT ( 'NONE',  ( 43.01140435219951286, 103.4604996726487371, 39.21067981925356349 ) ) ;
#4567=CARTESIAN_POINT ( 'NONE',  ( 48.01140435219951996, 121.4344580088725820, 32.58608133808903773 ) ) ;
#4568=CARTESIAN_POINT ( 'NONE',  ( 40.27526882409969033, 108.8297705074272983, 37.97664729208901946 ) ) ;
#4571=CARTESIAN_POINT ( 'NONE',  ( 46.59305225739526435, 100.3151871740940067, 36.81289934271958941 ) ) ;
#4572=CYLINDRICAL_SURFACE ( 'NONE', #15764, 4.999999999999997335 ) ;
#4578=CARTESIAN_POINT ( 'NONE',  ( 47.43856463449118621, 70.87977050742732388, 34.21067981925357060 ) ) ;
#4580=ORIENTED_EDGE ( 'NONE', *, *, #19729, .T. ) ;
#4581=CARTESIAN_POINT ( 'NONE',  ( 43.01140435219951286, 154.1297705074273097, 38.86567161673127657 ) ) ;
#4583=CARTESIAN_POINT ( 'NONE',  ( 38.01140435219951996, 111.5604996726487599, 32.58608133808903773 ) ) ;
#4584=CARTESIAN_POINT ( 'NONE',  ( 46.59305225739526435, 70.91518717409398675, 31.60846029578754468 ) ) ;
#4592=CARTESIAN_POINT ( 'NONE',  ( 38.96631938032478359, 156.0844580088725877, 37.14960608071593384 ) ) ;
#4594=CARTESIAN_POINT ( 'NONE',  ( 46.59305225739526435, 134.1797705074273210, 31.60846029578754468 ) ) ;
#4596=CARTESIAN_POINT ( 'NONE',  ( 38.58424406990785371, 128.9651871740940123, 32.77220824515697473 ) ) ;
#4599=CARTESIAN_POINT ( 'NONE',  ( 48.01140435219951996, 140.2104996726487514, 34.21067981925357060 ) ) ;
#4604=ADVANCED_FACE ( 'NONE', ( #9992 ), #1603, .T. ) ;
#4607=CARTESIAN_POINT ( 'NONE',  ( 48.01140435219951996, 79.43445800887258201, 32.58608133808903773 ) ) ;
#4609=CARTESIAN_POINT ( 'NONE',  ( 48.01140435219951996, 143.0604996726487173, 35.83527830041810347 ) ) ;
#4610=CARTESIAN_POINT ( 'NONE',  ( 38.58424406990786082, 99.11518717409400381, 34.21067981925357060 ) ) ;
#4614=CARTESIAN_POINT ( 'NONE',  ( 48.01140435219951996, 62.06049967264872436, 35.83527830041810347 ) ) ;
#4619=CARTESIAN_POINT ( 'NONE',  ( 42.21948215057684450, 79.38361825032846752, 39.21067981925355639 ) ) ;
#4621=CARTESIAN_POINT ( 'NONE',  ( 39.42975644700377558, 159.0797705074273267, 31.60846029578754468 ) ) ;
#4623=CARTESIAN_POINT ( 'NONE',  ( 39.42975644700377558, 153.4151871740940010, 36.81289934271958941 ) ) ;
#4628=CARTESIAN_POINT ( 'NONE',  ( 47.43856463449118621, 67.61518717409398960, 34.21067981925357060 ) ) ;
#4631=DIRECTION ( 'NONE',  ( 0.000000000000000000, 1.000000000000000000, 0.000000000000000000 ) ) ;
#4632=CARTESIAN_POINT ( 'NONE',  ( 45.74753988029933538, 130.1651871740940010, 37.97664729208901946 ) ) ;
#4634=ORIENTED_EDGE ( 'NONE', *, *, #10310, .T. ) ;
#4640=ORIENTED_EDGE ( 'NONE', *, *, #21212, .T. ) ;
#4641=CARTESIAN_POINT ( 'NONE',  ( 41.46631938032478359, 110.1844580088725820, 29.45539723777780239 ) ) ;
#4644=CARTESIAN_POINT ( 'NONE',  ( 47.43856463449118621, 76.87977050742732388, 34.21067981925357060 ) ) ;
#4645=CARTESIAN_POINT ( 'NONE',  ( 45.74753988029933538, 125.0651871740940209, 30.44471234641811819 ) ) ;
#4647=CARTESIAN_POINT ( 'NONE',  ( 41.46631938032478359, 93.11049967264874283, 29.45539723777780239 ) ) ;
#4651=CARTESIAN_POINT ( 'NONE',  ( 41.64333658814960870, 89.51518717409399528, 30.00020018409699318 ) ) ;
#4654=CARTESIAN_POINT ( 'NONE',  ( 48.01140435219951996, 71.21049967264873715, 34.21067981925357060 ) ) ;
#4659=CARTESIAN_POINT ( 'NONE',  ( 39.42975644700377558, 75.67977050742732104, 36.81289934271958941 ) ) ;
#4666=CARTESIAN_POINT ( 'NONE',  ( 43.01140435219951286, 121.1297705074273097, 38.86567161673127657 ) ) ;
#4669=ORIENTED_EDGE ( 'NONE', *, *, #7673, .F. ) ;
#4671=CARTESIAN_POINT ( 'NONE',  ( 38.01140435219951996, 62.63445800887255643, 32.58608133808903773 ) ) ;
#4672=CARTESIAN_POINT ( 'NONE',  ( 43.01140435219951286, 143.9604996726487229, 29.21067981925356705 ) ) ;
#4677=CARTESIAN_POINT ( 'NONE',  ( 43.01140435219951286, 101.9604996726487371, 29.21067981925356705 ) ) ;
#4680=CARTESIAN_POINT ( 'NONE',  ( 38.96631938032478359, 120.0844580088725735, 37.14960608071593384 ) ) ;
#4681=CARTESIAN_POINT ( 'NONE',  ( 39.42975644700377558, 108.0797705074273125, 31.60846029578754468 ) ) ;
#4684=CARTESIAN_POINT ( 'NONE',  ( 46.59305225739526435, 85.91518717409400097, 31.60846029578754468 ) ) ;
#4686=ORIENTED_EDGE ( 'NONE', *, *, #10967, .T. ) ;
#4690=CARTESIAN_POINT ( 'NONE',  ( 40.27526882409969744, 62.92977050742730682, 30.44471234641812174 ) ) ;
#4691=VERTEX_POINT ( 'NONE', #2146 ) ;
#4693=CARTESIAN_POINT ( 'NONE',  ( 44.37947211624943833, 143.4797705074273324, 30.00020018409699318 ) ) ;
#4695=CARTESIAN_POINT ( 'NONE',  ( 48.01140435219951996, 113.3604996726487286, 32.58608133808903773 ) ) ;
#4696=CARTESIAN_POINT ( 'NONE',  ( 47.43856463449118621, 64.61518717409398960, 34.21067981925357060 ) ) ;
#4702=CARTESIAN_POINT ( 'NONE',  ( 48.01140435219951996, 148.1344580088725706, 35.83527830041810347 ) ) ;
#4703=CARTESIAN_POINT ( 'NONE',  ( 44.37947211624943833, 128.4797705074273040, 30.00020018409699318 ) ) ;
#4705=CARTESIAN_POINT ( 'NONE',  ( 44.37947211624943833, 113.2151871740940123, 30.00020018409699318 ) ) ;
#4708=CARTESIAN_POINT ( 'NONE',  ( 43.01140435219951996, 151.4604996726487514, 39.21067981925356349 ) ) ;
#4709=CARTESIAN_POINT ( 'NONE',  ( 45.51140435220141001, 58.78519719078001060, 29.88055280033245964 ) ) ;
#4710=CARTESIAN_POINT ( 'NONE',  ( 38.01140435219952707, 135.5604996726487457, 32.58608133808903773 ) ) ;
#4712=CARTESIAN_POINT ( 'NONE',  ( 44.55648932407425633, 83.81049967264874567, 29.45539723777780239 ) ) ;
#4714=FACE_OUTER_BOUND ( 'NONE', #2113, .T. ) ;
#4716=CARTESIAN_POINT ( 'NONE',  ( 41.46631938032478359, 78.38445800887257064, 38.96596240072933170 ) ) ;
#4717=CARTESIAN_POINT ( 'NONE',  ( 48.01140435219951996, 103.1344580088725706, 35.83527830041809636 ) ) ;
#4718=CARTESIAN_POINT ( 'NONE',  ( 44.55648932407425633, 143.8104996726487457, 29.45539723777780239 ) ) ;
#4719=CARTESIAN_POINT ( 'NONE',  ( 40.27526882409969033, 101.6651871740940152, 30.44471234641811819 ) ) ;
#4726=CARTESIAN_POINT ( 'NONE',  ( 38.96631938032478359, 105.4104996726487400, 31.27175355779120025 ) ) ;
#4727=CARTESIAN_POINT ( 'NONE',  ( 43.01140435219951286, 115.4604996726487229, 39.21067981925356349 ) ) ;
#4728=CARTESIAN_POINT ( 'NONE',  ( 43.01140435219951286, 79.46049967264875136, 39.21067981925356349 ) ) ;
#4729=EDGE_CURVE ( 'NONE', #19857, #20247, #894, .T. ) ;
#4730=CARTESIAN_POINT ( 'NONE',  ( 45.74753988029933538, 65.06518717409400665, 30.44471234641811819 ) ) ;
#4731=CARTESIAN_POINT ( 'NONE',  ( 41.46631938032478359, 63.38445800887257064, 38.96596240072933170 ) ) ;
#4735=ORIENTED_EDGE ( 'NONE', *, *, #4151, .T. ) ;
#4736=CARTESIAN_POINT ( 'NONE',  ( 46.59305225739526435, 70.91518717409398675, 31.60846029578754468 ) ) ;
#4740=CARTESIAN_POINT ( 'NONE',  ( 40.27526882409969033, 129.5651871740940067, 37.97664729208901946 ) ) ;
#4742=ORIENTED_EDGE ( 'NONE', *, *, #12062, .T. ) ;
#4746=CARTESIAN_POINT ( 'NONE',  ( 43.01140435219951286, 108.5344580088725763, 39.46799094044489209 ) ) ;
#4747=DIRECTION ( 'NONE',  ( 0.000000000000000000, 0.000000000000000000, 1.000000000000000000 ) ) ;
#4748=CARTESIAN_POINT ( 'NONE',  ( 39.42975644700377558, 69.67977050742732104, 36.81289934271958941 ) ) ;
#4749=CARTESIAN_POINT ( 'NONE',  ( 38.58424406990784661, 129.2651871740940237, 35.64915139335016647 ) ) ;
#4752=CARTESIAN_POINT ( 'NONE',  ( 48.01140435219951996, 86.36049967264872862, 32.58608133808903773 ) ) ;
#4757=CARTESIAN_POINT ( 'NONE',  ( 39.42975644700377558, 90.41518717409400097, 36.81289934271958941 ) ) ;
#4758=CARTESIAN_POINT ( 'NONE',  ( 46.10157429594899270, 107.6604996726487116, 29.95742577749336988 ) ) ;
#4759=CARTESIAN_POINT ( 'NONE',  ( 47.05648932407426344, 142.5844580088725877, 31.27175355779120025 ) ) ;
#4761=CARTESIAN_POINT ( 'NONE',  ( 44.37947211624943833, 64.27977050742731535, 38.42115945441014446 ) ) ;
#4767=EDGE_CURVE ( 'NONE', #1030, #13261, #14987, .T. ) ;
#4770=CARTESIAN_POINT ( 'NONE',  ( 43.01140435219951286, 128.6297705074273381, 29.55568802177586107 ) ) ;
#4772=ORIENTED_EDGE ( 'NONE', *, *, #18909, .F. ) ;
#4776=CARTESIAN_POINT ( 'NONE',  ( 38.58424406990784661, 117.2297705074273040, 32.77220824515698183 ) ) ;
#4778=CARTESIAN_POINT ( 'NONE',  ( 38.58424406990784661, 155.9651871740939555, 32.77220824515698183 ) ) ;
#4779=APPLICATION_CONTEXT ( 'automotive_design' ) ;
#4785=CARTESIAN_POINT ( 'NONE',  ( 43.01140435219951996, 10.71049967264875491, 29.21067981925357060 ) ) ;
#4789=CARTESIAN_POINT ( 'NONE',  ( 43.01140435219951286, 119.0344580088725621, 28.95336869806222779 ) ) ;
#4790=CARTESIAN_POINT ( 'NONE',  ( 44.37947211624943833, 104.4797705074273182, 30.00020018409699318 ) ) ;
#4793=CARTESIAN_POINT ( 'NONE',  ( 46.59305225739526435, 91.91518717409400097, 31.60846029578754468 ) ) ;
#4794=LINE ( 'NONE', #21562, #16107 ) ;
#4796=DIRECTION ( 'NONE',  ( 0.000000000000000000, 0.000000000000000000, 1.000000000000000000 ) ) ;
#4799=CARTESIAN_POINT ( 'NONE',  ( 39.42975644700377558, 66.67977050742732104, 36.81289934271958941 ) ) ;
#4801=VECTOR ( 'NONE', #1078, 1000.000000000000000 ) ;
#4802=CARTESIAN_POINT ( 'NONE',  ( 47.43856463449117200, 146.0297705074272869, 32.77220824515698183 ) ) ;
#4804=CARTESIAN_POINT ( 'NONE',  ( 40.27526882409969033, 99.82977050742729830, 37.97664729208901946 ) ) ;
#4805=AXIS2_PLACEMENT_3D ( 'NONE', #3130, #18340, #8209 ) ;
#4807=CARTESIAN_POINT ( 'NONE',  ( 41.46631938032478359, 112.3104996726487457, 38.96596240072933170 ) ) ;
#4808=CARTESIAN_POINT ( 'NONE',  ( 38.58424406990784661, 68.96518717409398391, 32.77220824515698183 ) ) ;
#4809=CARTESIAN_POINT ( 'NONE',  ( 38.96631938032478359, 95.48445800887257917, 31.27175355779120025 ) ) ;
#4813=EDGE_CURVE ( 'NONE', #9101, #15014, #17236, .T. ) ;
#4814=CARTESIAN_POINT ( 'NONE',  ( 41.46631938032478359, 149.1844580088725820, 29.45539723777780239 ) ) ;
#4815=CARTESIAN_POINT ( 'NONE',  ( 38.58424406990786082, 135.3797705074273381, 34.21067981925357060 ) ) ;
#4818=CARTESIAN_POINT ( 'NONE',  ( 39.42975644700377558, 114.4151871740940010, 36.81289934271958941 ) ) ;
#4820=CARTESIAN_POINT ( 'NONE',  ( 45.51148226160370314, 59.71123016864974176, 29.88059778228138086 ) ) ;
#4824=CARTESIAN_POINT ( 'NONE',  ( 43.01140435219951286, 82.46049967264873715, 39.21067981925356349 ) ) ;
#4825=CARTESIAN_POINT ( 'NONE',  ( 43.01140435219951286, 97.12977050742732388, 38.86567161673127657 ) ) ;
#4830=CARTESIAN_POINT ( 'NONE',  ( 38.96631938032478359, 84.08445800887258770, 37.14960608071593384 ) ) ;
#4832=CARTESIAN_POINT ( 'NONE',  ( 38.96631938032478359, 138.4104996726487400, 31.27175355779120025 ) ) ;
#4833=CARTESIAN_POINT ( 'NONE',  ( 47.43856463449118621, 100.6151871740940180, 34.21067981925357060 ) ) ;
#4840=FACE_OUTER_BOUND ( 'NONE', #14250, .T. ) ;
#4842=CARTESIAN_POINT ( 'NONE',  ( 38.96631938032478359, 147.4104996726487400, 31.27175355779120025 ) ) ;
#4844=CARTESIAN_POINT ( 'NONE',  ( 38.58424406990784661, 63.26518717409400239, 35.64915139335016647 ) ) ;
#4847=CARTESIAN_POINT ( 'NONE',  ( 46.59305225739526435, 148.9151871740940294, 31.60846029578754468 ) ) ;
#4852=CARTESIAN_POINT ( 'NONE',  ( 45.74753988029934249, 64.16518717409400097, 37.97664729208901235 ) ) ;
#4855=VECTOR ( 'NONE', #10627, 1000.000000000000000 ) ;
#4857=CARTESIAN_POINT ( 'NONE',  ( 43.01140435219951286, 122.3651871740939754, 29.55568802177586463 ) ) ;
#4863=CARTESIAN_POINT ( 'NONE',  ( 41.46631938032478359, 111.3844580088725849, 38.96596240072933170 ) ) ;
#4864=CARTESIAN_POINT ( 'NONE',  ( 40.27526882409969744, 158.9297705074272926, 30.44471234641812174 ) ) ;
#4865=CARTESIAN_POINT ( 'NONE',  ( 45.74753988029933538, 71.32977050742732672, 30.44471234641811819 ) ) ;
#4866=CARTESIAN_POINT ( 'NONE',  ( 41.64333658814960870, 126.7151871740939981, 38.42115945441014446 ) ) ;
#4868=CARTESIAN_POINT ( 'NONE',  ( 46.10157429594899270, 79.76049967264873430, 38.46393386101376421 ) ) ;
#4871=CARTESIAN_POINT ( 'NONE',  ( 39.92123440845005433, 145.1604996726486831, 38.46393386101375711 ) ) ;
#4873=CARTESIAN_POINT ( 'NONE',  ( 38.58424406990786082, 84.11518717409400381, 34.21067981925357060 ) ) ;
#4878=CARTESIAN_POINT ( 'NONE',  ( 39.42975644700377558, 66.07977050742731251, 31.60846029578754468 ) ) ;
#4882=ORIENTED_EDGE ( 'NONE', *, *, #1285, .T. ) ;
#4883=CARTESIAN_POINT ( 'NONE',  ( 40.27526882409969033, 149.6651871740939725, 30.44471234641811819 ) ) ;
#4885=CARTESIAN_POINT ( 'NONE',  ( 47.43856463449117911, 115.7297705074273324, 35.64915139335015937 ) ) ;
#4889=( BOUNDED_CURVE ( )  B_SPLINE_CURVE ( 2, ( #9619, #14668, #21408, #13026, #19747, #18082, #9729, #16426, #6645, #227, #5088, #20297, #9945 ),
 .UNSPECIFIED., .F., .F. ) 
 B_SPLINE_CURVE_WITH_KNOTS ( ( 3, 2, 2, 2, 2, 2, 3 ),
 ( 0.4191176470588235392, 0.4205882352941176516, 0.4235294117647058765, 0.4264705882352941013, 0.4294117647058823262, 0.4323529411764706065, 0.4338235294117647189 ),
 .UNSPECIFIED. ) 
 CURVE ( )  GEOMETRIC_REPRESENTATION_ITEM ( )  RATIONAL_B_SPLINE_CURVE ( ( 0.9755282581475768211, 0.9755282581475768211, 1.000000000000000000, 0.9510565162951535312, 1.000000000000000000, 0.9510565162951535312, 1.000000000000000000, 0.9510565162951535312, 1.000000000000000000, 0.9510565162951535312, 1.000000000000000000, 0.9755282581475768211, 0.9755282581475768211 ) ) 
 REPRESENTATION_ITEM ( '' )  );
#4891=CARTESIAN_POINT ( 'NONE',  ( 44.37947211624943833, 115.2797705074273296, 38.42115945441014446 ) ) ;
#4892=CARTESIAN_POINT ( 'NONE',  ( 43.80332655382221674, 138.6113394311928744, 39.21067981925356349 ) ) ;
#4893=EDGE_CURVE ( 'NONE', #15802, #17373, #2181, .T. ) ;
#4894=CARTESIAN_POINT ( 'NONE',  ( 43.01140435219951286, 85.12977050742729546, 38.86567161673127657 ) ) ;
#4895=CARTESIAN_POINT ( 'NONE',  ( 43.01140435219951286, 158.3651871740939612, 29.55568802177586463 ) ) ;
#4907=CARTESIAN_POINT ( 'NONE',  ( 47.43856463449118621, 94.87977050742732388, 34.21067981925357060 ) ) ;
#4910=CARTESIAN_POINT ( 'NONE',  ( 38.58424406990785371, 84.26518717409399528, 35.64915139335015937 ) ) ;
#4914=CARTESIAN_POINT ( 'NONE',  ( 38.96631938032478359, 138.0844580088725877, 37.14960608071593384 ) ) ;
#4916=CARTESIAN_POINT ( 'NONE',  ( 47.43856463449117911, 140.0297705074273154, 32.77220824515697473 ) ) ;
#4918=CARTESIAN_POINT ( 'NONE',  ( 43.01140435219951286, 65.62977050742730967, 29.55568802177586107 ) ) ;
#4920=CARTESIAN_POINT ( 'NONE',  ( 39.42975644700377558, 141.6797705074273210, 36.81289934271958941 ) ) ;
#4921=EDGE_CURVE ( 'NONE', #10959, #14908, #14408, .T. ) ;
#4923=CARTESIAN_POINT ( 'NONE',  ( 38.58424406990784661, 96.22977050742728977, 32.77220824515698183 ) ) ;
#4924=CARTESIAN_POINT ( 'NONE',  ( 48.01140435219951996, 152.0604996726487457, 35.83527830041809636 ) ) ;
#4926=CARTESIAN_POINT ( 'NONE',  ( 38.96631938032478359, 111.4104996726487400, 31.27175355779120025 ) ) ;
#4927=CARTESIAN_POINT ( 'NONE',  ( 47.43856463449118621, 67.61518717409398960, 34.21067981925357060 ) ) ;
#4934=CARTESIAN_POINT ( 'NONE',  ( 43.01140435219951286, 153.5344580088726048, 39.46799094044489209 ) ) ;
#4935=CARTESIAN_POINT ( 'NONE',  ( 38.58424406990786082, 120.3797705074273239, 34.21067981925357060 ) ) ;
#4937=CARTESIAN_POINT ( 'NONE',  ( 47.43856463449118621, 115.6151871740940038, 34.21067981925357060 ) ) ;
#4939=CARTESIAN_POINT ( 'NONE',  ( 38.58424406990784661, 147.2297705074273324, 32.77220824515698183 ) ) ;
#4943=CARTESIAN_POINT ( 'NONE',  ( 43.01140435219951286, 94.12977050742730967, 38.86567161673127657 ) ) ;
#4944=ORIENTED_EDGE ( 'NONE', *, *, #17744, .T. ) ;
#4945=EDGE_CURVE ( 'NONE', #3596, #13353, #9794, .T. ) ;
#4946=CARTESIAN_POINT ( 'NONE',  ( 48.01140435219951996, 145.4344580088725820, 32.58608133808903773 ) ) ;
#4948=CARTESIAN_POINT ( 'NONE',  ( 38.01140435219952707, 86.78445800887257633, 34.21067981925357060 ) ) ;
#4951=CARTESIAN_POINT ( 'NONE',  ( 41.46631938032478359, 135.1104996726487286, 29.45539723777780239 ) ) ;
#4952=CARTESIAN_POINT ( 'NONE',  ( 43.01140435219951286, 99.86518717409400381, 38.86567161673127657 ) ) ;
#4957=CYLINDRICAL_SURFACE ( 'NONE', #10792, 4.999999999999997335 ) ;
#4958=CARTESIAN_POINT ( 'NONE',  ( 43.01140435219951286, 65.03445800887257633, 29.21067981925356705 ) ) ;
#4961=CARTESIAN_POINT ( 'NONE',  ( 41.64333658814960870, 60.71518717409399102, 38.42115945441014446 ) ) ;
#4962=( BOUNDED_CURVE ( )  B_SPLINE_CURVE ( 2, ( #10331, #1945, #11864, #8466, #1841, #3710, #13838, #8676, #15399, #5460, #3818, #295, #7026 ),
 .UNSPECIFIED., .F., .F. ) 
 B_SPLINE_CURVE_WITH_KNOTS ( ( 3, 2, 2, 2, 2, 2, 3 ),
 ( 0.4926470588235293824, 0.4941176470588235503, 0.4970588235294117752, 0.5000000000000000000, 0.5029411764705882248, 0.5058823529411764497, 0.5073529411764705621 ),
 .UNSPECIFIED. ) 
 CURVE ( )  GEOMETRIC_REPRESENTATION_ITEM ( )  RATIONAL_B_SPLINE_CURVE ( ( 0.9755282581475768211, 0.9755282581475763770, 1.000000000000000000, 0.9510565162951535312, 1.000000000000000000, 0.9510565162951535312, 1.000000000000000000, 0.9510565162951535312, 1.000000000000000000, 0.9510565162951535312, 1.000000000000000000, 0.9755282581475768211, 0.9755282581475768211 ) ) 
 REPRESENTATION_ITEM ( '' )  );
#4963=DIRECTION ( 'NONE',  ( 0.000000000000000000, 1.000000000000000000, 0.000000000000000000 ) ) ;
#4965=CARTESIAN_POINT ( 'NONE',  ( 39.42975644700377558, 144.4151871740940294, 36.81289934271958941 ) ) ;
#4968=CARTESIAN_POINT ( 'NONE',  ( 42.21948215057684450, 77.11133943119284595, 29.21067981925356705 ) ) ;
#4971=CARTESIAN_POINT ( 'NONE',  ( 43.01140435219951286, 135.5344580088725763, 39.21067981925356349 ) ) ;
#4972=CARTESIAN_POINT ( 'NONE',  ( 47.43856463449117200, 121.7651871740940237, 32.77220824515698183 ) ) ;
#4978=CARTESIAN_POINT ( 'NONE',  ( 44.55648932407425633, 109.8844580088725849, 29.45539723777780239 ) ) ;
#4980=CARTESIAN_POINT ( 'NONE',  ( 47.43856463449117911, 155.0297705074273438, 32.77220824515697473 ) ) ;
#4981=CARTESIAN_POINT ( 'NONE',  ( 47.43856463449117200, 71.02977050742730114, 32.77220824515698183 ) ) ;
#4982=CARTESIAN_POINT ( 'NONE',  ( 38.58424406990784661, 128.9651871740939839, 32.77220824515698183 ) ) ;
#4984=EDGE_CURVE ( 'NONE', #7226, #4204, #18930, .T. ) ;
#4985=CARTESIAN_POINT ( 'NONE',  ( 38.96631938032478359, 78.41049967264873999, 31.27175355779120025 ) ) ;
#4989=CARTESIAN_POINT ( 'NONE',  ( 46.59305225739526435, 88.31518717409400665, 36.81289934271958941 ) ) ;
#4992=ORIENTED_EDGE ( 'NONE', *, *, #13631, .F. ) ;
#4993=CARTESIAN_POINT ( 'NONE',  ( 38.58424406990786082, 69.37977050742730967, 34.21067981925357060 ) ) ;
#4999=CARTESIAN_POINT ( 'NONE',  ( 45.74753988029933538, 158.0651871740940067, 30.44471234641811819 ) ) ;
#5000=VECTOR ( 'NONE', #16555, 1000.000000000000000 ) ;
#5002=CARTESIAN_POINT ( 'NONE',  ( 40.27526882409969744, 111.8297705074272983, 37.97664729208901235 ) ) ;
#5003=CARTESIAN_POINT ( 'NONE',  ( 44.55648932407425633, 153.6844580088725820, 38.96596240072933170 ) ) ;
#5007=CARTESIAN_POINT ( 'NONE',  ( 40.27526882409969033, 120.8297705074272983, 37.97664729208901946 ) ) ;
#5008=CARTESIAN_POINT ( 'NONE',  ( 41.46631938032478359, 129.3844580088725706, 38.96596240072933170 ) ) ;
#5009=CARTESIAN_POINT ( 'NONE',  ( 46.59305225739526435, 157.3151871740940067, 36.81289934271958941 ) ) ;
#5013=CARTESIAN_POINT ( 'NONE',  ( 38.01140435219952707, 107.9344580088725678, 35.83527830041809636 ) ) ;
#5017=CARTESIAN_POINT ( 'NONE',  ( 41.46631938032478359, 157.3104996726487457, 38.96596240072933170 ) ) ;
#5019=CARTESIAN_POINT ( 'NONE',  ( 43.01140435219951286, 92.96049967264875136, 29.21067981925356705 ) ) ;
#5021=CARTESIAN_POINT ( 'NONE',  ( 47.43856463449117200, 91.72977050742730398, 35.64915139335016647 ) ) ;
#5024=CARTESIAN_POINT ( 'NONE',  ( 45.74753988029934249, 92.06518717409399244, 30.44471234641812174 ) ) ;
#5025=CARTESIAN_POINT ( 'NONE',  ( 43.01140435219951286, 83.96049967264873715, 29.21067981925356705 ) ) ;
#5029=( BOUNDED_CURVE ( )  B_SPLINE_CURVE ( 2, ( #17564, #4336, #11062, #4236, #15909, #20485, #17456, #15804, #7448, #2470, #17673, #4892, #2911 ),
 .UNSPECIFIED., .F., .F. ) 
 B_SPLINE_CURVE_WITH_KNOTS ( ( 3, 2, 2, 2, 2, 2, 3 ),
 ( 0.1838235294117646912, 0.1852941176470588314, 0.1882352941176470562, 0.1911764705882352811, 0.1941176470588235337, 0.1970588235294117585, 0.1985294117647058709 ),
 .UNSPECIFIED. ) 
 CURVE ( )  GEOMETRIC_REPRESENTATION_ITEM ( )  RATIONAL_B_SPLINE_CURVE ( ( 0.9755282581475765991, 0.9755282581475764880, 1.000000000000000000, 0.9510565162951535312, 1.000000000000000000, 0.9510565162951535312, 1.000000000000000000, 0.9510565162951535312, 1.000000000000000000, 0.9510565162951535312, 1.000000000000000000, 0.9755282581475769321, 0.9755282581475765991 ) ) 
 REPRESENTATION_ITEM ( '' )  );
#5031=CARTESIAN_POINT ( 'NONE',  ( 43.01140435219951996, 10.71049967264875491, 34.21067981925357060 ) ) ;
#5032=ORIENTED_EDGE ( 'NONE', *, *, #1437, .T. ) ;
#5034=CARTESIAN_POINT ( 'NONE',  ( 46.59305225739526435, 143.1797705074273210, 31.60846029578754468 ) ) ;
#5035=CARTESIAN_POINT ( 'NONE',  ( 46.59305225739526435, 95.17977050742732104, 31.60846029578754468 ) ) ;
#5036=CARTESIAN_POINT ( 'NONE',  ( 43.01140435219952707, 140.9604996726487514, 29.21067981925357060 ) ) ;
#5037=CARTESIAN_POINT ( 'NONE',  ( 39.92123440845004723, 114.2604996726487343, 29.95742577749337343 ) ) ;
#5038=CARTESIAN_POINT ( 'NONE',  ( 43.01140435219951286, 62.36518717409399670, 29.55568802177586463 ) ) ;
#5041=CARTESIAN_POINT ( 'NONE',  ( 38.01140435219952707, 122.7844580088725763, 34.21067981925357060 ) ) ;
#5043=CARTESIAN_POINT ( 'NONE',  ( 41.46631938032478359, 153.3844580088725991, 38.96596240072933170 ) ) ;
#5044=CARTESIAN_POINT ( 'NONE',  ( 44.37947211624943833, 127.2797705074273438, 38.42115945441014446 ) ) ;
#5047=CARTESIAN_POINT ( 'NONE',  ( 47.43856463449118621, 118.6151871740940038, 34.21067981925357060 ) ) ;
#5053=CARTESIAN_POINT ( 'NONE',  ( 43.01140435219951286, 85.12977050742729546, 38.86567161673127657 ) ) ;
#5058=CARTESIAN_POINT ( 'NONE',  ( 46.10157429594899270, 76.73445800887255075, 29.95742577749337343 ) ) ;
#5059=CARTESIAN_POINT ( 'NONE',  ( 43.01140435219951286, 60.53445800887258343, 39.21067981925356349 ) ) ;
#5061=CARTESIAN_POINT ( 'NONE',  ( 46.10157429594899270, 140.6604996726486831, 29.95742577749337343 ) ) ;
#5062=CARTESIAN_POINT ( 'NONE',  ( 45.74753988029933538, 94.16518717409400097, 37.97664729208901946 ) ) ;
#5067=CARTESIAN_POINT ( 'NONE',  ( 41.46631938032478359, 106.3104996726487457, 38.96596240072933170 ) ) ;
#5069=CARTESIAN_POINT ( 'NONE',  ( 47.05648932407426344, 80.51049967264874851, 31.27175355779120025 ) ) ;
#5070=CARTESIAN_POINT ( 'NONE',  ( 38.58424406990784661, 150.2297705074273040, 32.77220824515698183 ) ) ;
#5071=CARTESIAN_POINT ( 'NONE',  ( 38.96631938032478359, 63.08445800887258059, 37.14960608071593384 ) ) ;
#5073=CARTESIAN_POINT ( 'NONE',  ( 40.27526882409969744, 149.6651871740939725, 30.44471234641812174 ) ) ;
#5076=EDGE_CURVE ( 'NONE', #12132, #7314, #4424, .T. ) ;
#5078=CARTESIAN_POINT ( 'NONE',  ( 38.58424406990786082, 159.3797705074273381, 34.21067981925357060 ) ) ;
#5081=CARTESIAN_POINT ( 'NONE',  ( 38.01140435219952707, 134.7844580088726048, 34.21067981925357060 ) ) ;
#5082=CARTESIAN_POINT ( 'NONE',  ( 41.64333658814960870, 126.7151871740939981, 38.42115945441014446 ) ) ;
#5086=ORIENTED_EDGE ( 'NONE', *, *, #4063, .F. ) ;
#5087=CARTESIAN_POINT ( 'NONE',  ( 38.01140435219951996, 98.93445800887255359, 35.83527830041810347 ) ) ;
#5088=CARTESIAN_POINT ( 'NONE',  ( 44.55648932407425633, 115.6104996726487428, 38.96596240072933170 ) ) ;
#5089=CARTESIAN_POINT ( 'NONE',  ( 39.42975644700377558, 66.67977050742732104, 36.81289934271958941 ) ) ;
#5090=CARTESIAN_POINT ( 'NONE',  ( 44.37947211624943833, 128.2151871740939839, 30.00020018409699318 ) ) ;
#5092=AXIS2_PLACEMENT_3D ( 'NONE', #18089, #13031, #7968 ) ;
#5093=CARTESIAN_POINT ( 'NONE',  ( 47.05648932407426344, 79.91049967264873999, 37.14960608071593384 ) ) ;
#5096=CARTESIAN_POINT ( 'NONE',  ( 47.43856463449117200, 76.46518717409401233, 35.64915139335016647 ) ) ;
#5098=CARTESIAN_POINT ( 'NONE',  ( 38.01140435219952707, 132.8604996726487286, 35.83527830041809636 ) ) ;
#5101=CARTESIAN_POINT ( 'NONE',  ( 43.01140435219951286, 64.12977050742730967, 38.86567161673127657 ) ) ;
#5106=CARTESIAN_POINT ( 'NONE',  ( 41.64333658814960870, 152.5151871740940237, 30.00020018409699318 ) ) ;
#5108=CARTESIAN_POINT ( 'NONE',  ( 38.58424406990785371, 117.2297705074273040, 32.77220824515697473 ) ) ;
#5110=ORIENTED_EDGE ( 'NONE', *, *, #14401, .F. ) ;
#5112=ORIENTED_EDGE ( 'NONE', *, *, #6212, .F. ) ;
#5113=CARTESIAN_POINT ( 'NONE',  ( 46.59305225739526435, 115.5797705074273267, 36.81289934271958941 ) ) ;
#5115=CARTESIAN_POINT ( 'NONE',  ( 39.42975644700377558, 87.67977050742732104, 36.81289934271958941 ) ) ;
#5116=CARTESIAN_POINT ( 'NONE',  ( 40.27526882409969033, 153.5651871740940067, 37.97664729208901946 ) ) ;
#5121=EDGE_CURVE ( 'NONE', #1193, #14927, #2453, .T. ) ;
#5124=CARTESIAN_POINT ( 'NONE',  ( 43.80332655382220253, 76.53738109496900677, 39.21067981925355639 ) ) ;
#5126=CARTESIAN_POINT ( 'NONE',  ( 41.64333658814960870, 89.77977050742731535, 30.00020018409699318 ) ) ;
#5129=CARTESIAN_POINT ( 'NONE',  ( 45.74753988029934249, 88.16518717409397254, 37.97664729208901235 ) ) ;
#5135=CARTESIAN_POINT ( 'NONE',  ( 39.42975644700377558, 141.0797705074273267, 31.60846029578754468 ) ) ;
#5137=CARTESIAN_POINT ( 'NONE',  ( 42.21948215057684450, 120.4575765865522925, 39.21067981925355639 ) ) ;
#5139=CARTESIAN_POINT ( 'NONE',  ( 43.01140435219951286, 145.1297705074273097, 38.86567161673127657 ) ) ;
#5140=CARTESIAN_POINT ( 'NONE',  ( 43.01140435219951286, 100.1297705074273239, 38.86567161673127657 ) ) ;
#5142=CARTESIAN_POINT ( 'NONE',  ( 38.58424406990786082, 63.11518717409400381, 34.21067981925357060 ) ) ;
#5144=CARTESIAN_POINT ( 'NONE',  ( 43.01140435219951996, 154.4604996726487798, 39.21067981925357060 ) ) ;
#5147=CARTESIAN_POINT ( 'NONE',  ( 38.96631938032478359, 141.0844580088725877, 37.14960608071593384 ) ) ;
#5148=CARTESIAN_POINT ( 'NONE',  ( 44.37947211624943833, 119.4797705074273182, 30.00020018409699318 ) ) ;
#5149=( BOUNDED_CURVE ( )  B_SPLINE_CURVE ( 2, ( #17774, #18107, #11170, #19440, #19771, #9857, #3127, #13157, #17881, #7986, #4333, #11058, #16233 ),
 .UNSPECIFIED., .F., .F. ) 
 B_SPLINE_CURVE_WITH_KNOTS ( ( 3, 2, 2, 2, 2, 2, 3 ),
 ( 0.6838235294117647189, 0.6852941176470588314, 0.6882352941176470562, 0.6911764705882352811, 0.6941176470588235059, 0.6970588235294117307, 0.6985294117647058432 ),
 .UNSPECIFIED. ) 
 CURVE ( )  GEOMETRIC_REPRESENTATION_ITEM ( )  RATIONAL_B_SPLINE_CURVE ( ( 0.9755282581475768211, 0.9755282581475768211, 1.000000000000000000, 0.9510565162951535312, 1.000000000000000000, 0.9510565162951535312, 1.000000000000000000, 0.9510565162951535312, 1.000000000000000000, 0.9510565162951535312, 1.000000000000000000, 0.9755282581475768211, 0.9755282581475768211 ) ) 
 REPRESENTATION_ITEM ( '' )  );
#5152=CARTESIAN_POINT ( 'NONE',  ( 47.43856463449117911, 118.4651871740939981, 35.64915139335015937 ) ) ;
#5153=CARTESIAN_POINT ( 'NONE',  ( 38.01140435219952707, 125.9344580088725962, 35.83527830041809636 ) ) ;
#5154=EDGE_CURVE ( 'NONE', #1337, #21594, #9213, .T. ) ;
#5158=CARTESIAN_POINT ( 'NONE',  ( 40.27526882409969744, 87.82977050742732672, 37.97664729208901235 ) ) ;
#5159=VERTEX_POINT ( 'NONE', #1460 ) ;
#5161=CARTESIAN_POINT ( 'NONE',  ( 46.10157429594899270, 70.73445800887257917, 29.95742577749337343 ) ) ;
#5163=CARTESIAN_POINT ( 'NONE',  ( 39.92123440845004723, 129.2604996726487343, 29.95742577749337343 ) ) ;
#5165=CARTESIAN_POINT ( 'NONE',  ( 38.58424406990784661, 86.96518717409398391, 32.77220824515698183 ) ) ;
#5171=CARTESIAN_POINT ( 'NONE',  ( 43.01140435219951286, 83.03445800887257633, 29.21067981925356705 ) ) ;
#5172=EDGE_CURVE ( 'NONE', #8428, #14663, #1350, .T. ) ;
#5175=CARTESIAN_POINT ( 'NONE',  ( 39.42975644700377558, 153.6797705074273210, 36.81289934271958941 ) ) ;
#5179=CARTESIAN_POINT ( 'NONE',  ( 41.64333658814960870, 146.5151871740939953, 30.00020018409699318 ) ) ;
#5182=CARTESIAN_POINT ( 'NONE',  ( 43.01140435219951286, 60.86518717409400381, 38.86567161673127657 ) ) ;
#5187=CARTESIAN_POINT ( 'NONE',  ( 43.01140435219951286, 125.3651871740940180, 29.55568802177586463 ) ) ;
#5189=ORIENTED_EDGE ( 'NONE', *, *, #8762, .F. ) ;
#5191=CARTESIAN_POINT ( 'NONE',  ( 42.21948215057683740, 146.1113394311928744, 29.21067981925357415 ) ) ;
#5192=VERTEX_POINT ( 'NONE', #3000 ) ;
#5193=CARTESIAN_POINT ( 'NONE',  ( 43.01140435219951286, 98.03445800887257633, 28.95336869806222779 ) ) ;
#5194=CARTESIAN_POINT ( 'NONE',  ( 45.74753988029934249, 157.4297705074273210, 37.97664729208901235 ) ) ;
#5195=EDGE_CURVE ( 'NONE', #15871, #17093, #10626, .T. ) ;
#5196=CARTESIAN_POINT ( 'NONE',  ( 39.42975644700377558, 60.67977050742731393, 36.81289934271958941 ) ) ;
#5197=CARTESIAN_POINT ( 'NONE',  ( 40.27526882409969033, 120.5651871740940209, 37.97664729208901946 ) ) ;
#5200=CARTESIAN_POINT ( 'NONE',  ( 47.05648932407426344, 80.51049967264874851, 31.27175355779120025 ) ) ;
#5205=CARTESIAN_POINT ( 'NONE',  ( 39.42975644700377558, 75.41518717409400097, 36.81289934271958941 ) ) ;
#5206=CARTESIAN_POINT ( 'NONE',  ( 43.01140435219951996, 10.71049967264875491, 34.21067981925357060 ) ) ;
#5208=CARTESIAN_POINT ( 'NONE',  ( 41.46631938032478359, 122.1844580088725962, 29.45539723777780239 ) ) ;
#5210=ORIENTED_EDGE ( 'NONE', *, *, #12062, .F. ) ;
#5211=CARTESIAN_POINT ( 'NONE',  ( 41.64333658814960870, 69.97977050742731819, 38.42115945441014446 ) ) ;
#5217=CARTESIAN_POINT ( 'NONE',  ( 38.58424406990784661, 149.9651871740939555, 32.77220824515698183 ) ) ;
#5219=CARTESIAN_POINT ( 'NONE',  ( 46.59305225739526435, 115.5797705074273267, 36.81289934271958941 ) ) ;
#5224=CARTESIAN_POINT ( 'NONE',  ( 45.74753988029933538, 110.3297705074273125, 30.44471234641811819 ) ) ;
#5226=DIRECTION ( 'NONE',  ( 0.000000000000000000, 1.000000000000000000, 0.000000000000000000 ) ) ;
#5227=CARTESIAN_POINT ( 'NONE',  ( 40.27526882409969033, 143.6651871740940294, 30.44471234641811819 ) ) ;
#5233=CARTESIAN_POINT ( 'NONE',  ( 47.05648932407426344, 77.51049967264873430, 31.27175355779120025 ) ) ;
#5234=CARTESIAN_POINT ( 'NONE',  ( 45.74753988029933538, 98.32977050742731251, 30.44471234641811819 ) ) ;
#5237=CARTESIAN_POINT ( 'NONE',  ( 46.59305225739526435, 76.31518717409399244, 36.81289934271958941 ) ) ;
#5239=CARTESIAN_POINT ( 'NONE',  ( 43.01140435219951996, 155.0344580088726048, 29.21067981925357060 ) ) ;
#5243=CARTESIAN_POINT ( 'NONE',  ( 44.37947211624943833, 143.4797705074273324, 30.00020018409699318 ) ) ;
#5245=DIRECTION ( 'NONE',  ( 0.000000000000000000, 0.000000000000000000, 1.000000000000000000 ) ) ;
#5247=CARTESIAN_POINT ( 'NONE',  ( 38.58424406990786082, 135.3797705074273381, 34.21067981925357060 ) ) ;
#5249=CARTESIAN_POINT ( 'NONE',  ( 38.58424406990784661, 99.22977050742731819, 32.77220824515698183 ) ) ;
#5250=CARTESIAN_POINT ( 'NONE',  ( 43.01140435219951996, 155.9604996726487514, 29.21067981925357060 ) ) ;
#5258=CARTESIAN_POINT ( 'NONE',  ( 48.01140435219951996, 139.1344580088725706, 35.83527830041810347 ) ) ;
#5259=CARTESIAN_POINT ( 'NONE',  ( 38.58424406990786082, 123.3797705074273239, 34.21067981925357060 ) ) ;
#5261=CARTESIAN_POINT ( 'NONE',  ( 41.46631938032478359, 140.1844580088725820, 29.45539723777780239 ) ) ;
#5262=CARTESIAN_POINT ( 'NONE',  ( 38.58424406990786082, 111.1151871740940038, 34.21067981925357060 ) ) ;
#5269=CARTESIAN_POINT ( 'NONE',  ( 39.42975644700377558, 81.67977050742732104, 36.81289934271958941 ) ) ;
#5270=ORIENTED_EDGE ( 'NONE', *, *, #6973, .F. ) ;
#5272=CARTESIAN_POINT ( 'NONE',  ( 38.01140435219951996, 68.63445800887258486, 32.58608133808903773 ) ) ;
#5274=CARTESIAN_POINT ( 'NONE',  ( 41.46631938032478359, 127.3104996726487315, 38.96596240072933170 ) ) ;
#5275=CARTESIAN_POINT ( 'NONE',  ( 47.43856463449118621, 88.61518717409400381, 34.21067981925357060 ) ) ;
#5277=( BOUNDED_CURVE ( )  B_SPLINE_CURVE ( 2, ( #263, #6998, #19080, #10196, #12345, #11617, #9977, #13702, #1705, #3357, #3472, #8545, #3981 ),
 .UNSPECIFIED., .F., .F. ) 
 B_SPLINE_CURVE_WITH_KNOTS ( ( 3, 2, 2, 2, 2, 2, 3 ),
 ( 0.7426470588235294379, 0.7441176470588235503, 0.7470588235294117752, 0.7500000000000000000, 0.7529411764705882248, 0.7558823529411764497, 0.7573529411764705621 ),
 .UNSPECIFIED. ) 
 CURVE ( )  GEOMETRIC_REPRESENTATION_ITEM ( )  RATIONAL_B_SPLINE_CURVE ( ( 0.9755282581475768211, 0.9755282581475768211, 1.000000000000000000, 0.9510565162951535312, 1.000000000000000000, 0.9510565162951535312, 1.000000000000000000, 0.9510565162951535312, 1.000000000000000000, 0.9510565162951535312, 1.000000000000000000, 0.9755282581475768211, 0.9755282581475768211 ) ) 
 REPRESENTATION_ITEM ( '' )  );
#5280=DIRECTION ( 'NONE',  ( 0.000000000000000000, 0.000000000000000000, 1.000000000000000000 ) ) ;
#5281=CARTESIAN_POINT ( 'NONE',  ( 43.01140435219951286, 145.4604996726487229, 39.21067981925356349 ) ) ;
#5282=CARTESIAN_POINT ( 'NONE',  ( 43.01140435219951996, 10.71049967264875491, 34.21067981925357060 ) ) ;
#5284=CARTESIAN_POINT ( 'NONE',  ( 45.74753988029933538, 154.4297705074272926, 37.97664729208901946 ) ) ;
#5285=CARTESIAN_POINT ( 'NONE',  ( 43.01140435219951286, 103.1297705074272955, 38.86567161673127657 ) ) ;
#5287=CARTESIAN_POINT ( 'NONE',  ( 43.01140435219951286, 147.8651871740939896, 38.86567161673127657 ) ) ;
#5288=DIRECTION ( 'NONE',  ( 0.000000000000000000, 1.000000000000000000, 0.000000000000000000 ) ) ;
#5290=CARTESIAN_POINT ( 'NONE',  ( 46.59305225739526435, 61.91518717409400097, 31.60846029578754468 ) ) ;
#5293=CARTESIAN_POINT ( 'NONE',  ( 46.59305225739526435, 112.3151871740940067, 36.81289934271958941 ) ) ;
#5297=MECHANICAL_DESIGN_GEOMETRIC_PRESENTATION_REPRESENTATION('',(#18325),#9523);
#5301=CARTESIAN_POINT ( 'NONE',  ( 48.01140435219951996, 106.4344580088725678, 32.58608133808903773 ) ) ;
#5302=CARTESIAN_POINT ( 'NONE',  ( 47.43856463449117911, 157.7297705074273040, 35.64915139335015937 ) ) ;
#5303=CARTESIAN_POINT ( 'NONE',  ( 41.46631938032478359, 157.3104996726487457, 38.96596240072933170 ) ) ;
#5304=CARTESIAN_POINT ( 'NONE',  ( 47.43856463449117200, 112.7651871740940095, 32.77220824515698183 ) ) ;
#5306=CARTESIAN_POINT ( 'NONE',  ( 48.01140435219951996, 77.21049967264873715, 34.21067981925357060 ) ) ;
#5307=CARTESIAN_POINT ( 'NONE',  ( 43.01140435219951286, 74.03445800887257633, 29.21067981925356705 ) ) ;
#5308=CARTESIAN_POINT ( 'NONE',  ( 41.46631938032478359, 71.18445800887258201, 29.45539723777780239 ) ) ;
#5310=CARTESIAN_POINT ( 'NONE',  ( 39.42975644700377558, 74.81518717409399244, 31.60846029578754468 ) ) ;
#5311=PRODUCT_DEFINITION_CONTEXT ( 'detailed design', #16172, 'design' ) ;
#5315=ORIENTED_EDGE ( 'NONE', *, *, #719, .F. ) ;
#5319=ORIENTED_EDGE ( 'NONE', *, *, #865, .T. ) ;
#5320=CARTESIAN_POINT ( 'NONE',  ( 39.42975644700377558, 155.8151871740940067, 31.60846029578754468 ) ) ;
#5322=CARTESIAN_POINT ( 'NONE',  ( 39.42975644700377558, 114.0797705074273125, 31.60846029578754468 ) ) ;
#5326=CARTESIAN_POINT ( 'NONE',  ( 41.64333658814960870, 108.9797705074273324, 38.42115945441014446 ) ) ;
#5327=LINE ( 'NONE', #3676, #20937 ) ;
#5328=CARTESIAN_POINT ( 'NONE',  ( 38.01140435219952707, 126.7104996726487514, 34.21067981925357060 ) ) ;
#5329=CARTESIAN_POINT ( 'NONE',  ( 41.64333658814960870, 143.5151871740939953, 30.00020018409699318 ) ) ;
#5331=CARTESIAN_POINT ( 'NONE',  ( 48.01140435219951996, 119.2104996726487371, 34.21067981925357060 ) ) ;
#5333=CARTESIAN_POINT ( 'NONE',  ( 44.55648932407425633, 100.6104996726487286, 38.96596240072933170 ) ) ;
#5337=CARTESIAN_POINT ( 'NONE',  ( 38.58424406990784661, 99.22977050742731819, 32.77220824515698183 ) ) ;
#5340=CARTESIAN_POINT ( 'NONE',  ( 43.01140435219951286, 81.86518717409398960, 38.86567161673127657 ) ) ;
#5343=EDGE_LOOP ( 'NONE', ( #2249, #2711, #19439, #8501 ) ) ;
#5347=CARTESIAN_POINT ( 'NONE',  ( 43.01140435219951996, 10.71049967264875491, 34.21067981925357060 ) ) ;
#5349=ORIENTED_EDGE ( 'NONE', *, *, #13990, .F. ) ;
#5350=CARTESIAN_POINT ( 'NONE',  ( 40.27526882409969744, 60.82977050742731251, 37.97664729208901235 ) ) ;
#5352=CARTESIAN_POINT ( 'NONE',  ( 38.58424406990784661, 135.5297705074273154, 35.64915139335016647 ) ) ;
#5358=CARTESIAN_POINT ( 'NONE',  ( 47.43856463449117200, 100.4651871740939839, 35.64915139335016647 ) ) ;
#5360=CARTESIAN_POINT ( 'NONE',  ( 39.92123440845005433, 123.2344580088725792, 38.46393386101375711 ) ) ;
#5363=CARTESIAN_POINT ( 'NONE',  ( 44.55648932407425633, 141.6844580088725820, 38.96596240072933170 ) ) ;
#5364=CARTESIAN_POINT ( 'NONE',  ( 40.27526882409969033, 125.9297705074273352, 30.44471234641811819 ) ) ;
#5367=CARTESIAN_POINT ( 'NONE',  ( 45.74753988029934249, 106.1651871740940152, 37.97664729208901235 ) ) ;
#5369=CARTESIAN_POINT ( 'NONE',  ( 43.01140435219951286, 98.96049967264873715, 29.21067981925356705 ) ) ;
#5373=CARTESIAN_POINT ( 'NONE',  ( 39.42975644700377558, 90.67977050742732104, 36.81289934271958941 ) ) ;
#5376=CARTESIAN_POINT ( 'NONE',  ( 44.55648932407425633, 75.68445800887258201, 38.96596240072933170 ) ) ;
#5377=CARTESIAN_POINT ( 'NONE',  ( 42.21948215057684450, 59.11133943119284595, 29.21067981925356705 ) ) ;
#5378=CARTESIAN_POINT ( 'NONE',  ( 41.46631938032478359, 130.3104996726487457, 38.96596240072933170 ) ) ;
#5379=CARTESIAN_POINT ( 'NONE',  ( 46.59305225739526435, 88.31518717409400665, 36.81289934271958941 ) ) ;
#5384=CARTESIAN_POINT ( 'NONE',  ( 48.01140435219951996, 127.4344580088725962, 32.58608133808903773 ) ) ;
#5386=FACE_OUTER_BOUND ( 'NONE', #21106, .T. ) ;
#5388=CARTESIAN_POINT ( 'NONE',  ( 39.42975644700377558, 150.6797705074273210, 36.81289934271958941 ) ) ;
#5389=CARTESIAN_POINT ( 'NONE',  ( 38.58424406990784661, 102.5297705074273154, 35.64915139335016647 ) ) ;
#5391=CARTESIAN_POINT ( 'NONE',  ( 38.58424406990786082, 138.1151871740940180, 34.21067981925357060 ) ) ;
#5396=CARTESIAN_POINT ( 'NONE',  ( 41.64333658814960870, 116.5151871740940095, 30.00020018409699318 ) ) ;
#5399=ORIENTED_EDGE ( 'NONE', *, *, #19804, .T. ) ;
#5400=( BOUNDED_CURVE ( )  B_SPLINE_CURVE ( 2, ( #12295, #7140, #8903, #6923, #16931, #15508, #20259, #1952, #16825, #8682, #15180, #13844, #302 ),
 .UNSPECIFIED., .F., .T. ) 
 B_SPLINE_CURVE_WITH_KNOTS ( ( 3, 2, 2, 2, 2, 2, 3 ),
 ( 0.5661764705882352811, 0.5676470588235293935, 0.5705882352941176183, 0.5735294117647058432, 0.5764705882352940680, 0.5794117647058824039, 0.5808823529411765163 ),
 .UNSPECIFIED. ) 
 CURVE ( )  GEOMETRIC_REPRESENTATION_ITEM ( )  RATIONAL_B_SPLINE_CURVE ( ( 0.9755282581475768211, 0.9755282581475768211, 1.000000000000000000, 0.9510565162951535312, 1.000000000000000000, 0.9510565162951535312, 1.000000000000000000, 0.9510565162951535312, 1.000000000000000000, 0.9510565162951535312, 1.000000000000000000, 0.9755282581475768211, 0.9755282581475768211 ) ) 
 REPRESENTATION_ITEM ( '' )  );
#5401=CARTESIAN_POINT ( 'NONE',  ( 47.05648932407426344, 96.98445800887257917, 37.14960608071593384 ) ) ;
#5402=CARTESIAN_POINT ( 'NONE',  ( 46.10157429594899270, 155.6604996726487116, 29.95742577749337343 ) ) ;
#5403=CARTESIAN_POINT ( 'NONE',  ( 46.59305225739526435, 112.3151871740940067, 36.81289934271958941 ) ) ;
#5405=CARTESIAN_POINT ( 'NONE',  ( 38.96631938032478359, 73.01049967264873430, 37.14960608071593384 ) ) ;
#5407=CARTESIAN_POINT ( 'NONE',  ( 43.80332655382220253, 136.9575765865523067, 29.21067981925356705 ) ) ;
#5410=CARTESIAN_POINT ( 'NONE',  ( 46.59305225739526435, 79.91518717409400097, 31.60846029578754468 ) ) ;
#5411=CARTESIAN_POINT ( 'NONE',  ( 39.92123440845005433, 63.26049967264874141, 29.95742577749336988 ) ) ;
#5419=CARTESIAN_POINT ( 'NONE',  ( 46.59305225739526435, 148.3151871740940067, 36.81289934271958941 ) ) ;
#5420=CARTESIAN_POINT ( 'NONE',  ( 47.43856463449118621, 157.6151871740940180, 34.21067981925357060 ) ) ;
#5421=CARTESIAN_POINT ( 'NONE',  ( 47.43856463449117911, 100.7297705074273040, 35.64915139335015937 ) ) ;
#5426=LINE ( 'NONE', #13698, #10189 ) ;
#5427=CARTESIAN_POINT ( 'NONE',  ( 38.96631938032478359, 129.0844580088725877, 37.14960608071593384 ) ) ;
#5428=CARTESIAN_POINT ( 'NONE',  ( 45.74753988029933538, 146.0651871740940067, 30.44471234641811819 ) ) ;
#5429=CARTESIAN_POINT ( 'NONE',  ( 38.96631938032478359, 100.0104996726487485, 37.14960608071593384 ) ) ;
#5431=CARTESIAN_POINT ( 'NONE',  ( 43.01140435219951286, 118.4604996726487371, 39.21067981925356349 ) ) ;
#5438=CARTESIAN_POINT ( 'NONE',  ( 43.01140435219951286, 80.62977050742732388, 29.55568802177586463 ) ) ;
#5441=EDGE_CURVE ( 'NONE', #3067, #18126, #11441, .T. ) ;
#5442=AXIS2_PLACEMENT_3D ( 'NONE', #20150, #1402, #21468 ) ;
#5443=CARTESIAN_POINT ( 'NONE',  ( 45.74753988029934249, 79.16518717409398675, 37.97664729208901235 ) ) ;
#5447=CARTESIAN_POINT ( 'NONE',  ( 44.55648932407425633, 84.68445800887256780, 38.96596240072933170 ) ) ;
#5448=CARTESIAN_POINT ( 'NONE',  ( 38.58424406990786082, 132.3797705074273381, 34.21067981925357060 ) ) ;
#5451=CARTESIAN_POINT ( 'NONE',  ( 39.92123440845005433, 120.2344580088725650, 38.46393386101375711 ) ) ;
#5452=VERTEX_POINT ( 'NONE', #3451 ) ;
#5453=CARTESIAN_POINT ( 'NONE',  ( 38.58424406990784661, 132.2297705074272756, 32.77220824515698183 ) ) ;
#5454=CARTESIAN_POINT ( 'NONE',  ( 40.27526882409969033, 92.92977050742729261, 30.44471234641811819 ) ) ;
#5455=CARTESIAN_POINT ( 'NONE',  ( 39.42975644700377558, 60.41518717409400097, 36.81289934271958941 ) ) ;
#5458=CARTESIAN_POINT ( 'NONE',  ( 39.42975644700377558, 93.41518717409400097, 36.81289934271958941 ) ) ;
#5460=CARTESIAN_POINT ( 'NONE',  ( 39.92123440845005433, 108.2604996726487485, 29.95742577749336988 ) ) ;
#5463=CARTESIAN_POINT ( 'NONE',  ( 43.01140435219951286, 144.5344580088726048, 39.46799094044489209 ) ) ;
#5464=CARTESIAN_POINT ( 'NONE',  ( 44.37947211624943833, 109.2797705074273154, 38.42115945441014446 ) ) ;
#5467=CARTESIAN_POINT ( 'NONE',  ( 47.43856463449117911, 106.4651871740940123, 35.64915139335015937 ) ) ;
#5472=CARTESIAN_POINT ( 'NONE',  ( 43.01140435219951286, 69.53445800887257633, 39.21067981925356349 ) ) ;
#5473=CARTESIAN_POINT ( 'NONE',  ( 44.37947211624943833, 89.47977050742731819, 30.00020018409699318 ) ) ;
#5474=ORIENTED_EDGE ( 'NONE', *, *, #8762, .T. ) ;
#5476=CARTESIAN_POINT ( 'NONE',  ( 41.46631938032478359, 71.18445800887258201, 29.45539723777780239 ) ) ;
#5478=ADVANCED_FACE ( 'NONE', ( #15006 ), #20308, .T. ) ;
#5479=CARTESIAN_POINT ( 'NONE',  ( 43.01140435219951286, 131.9604996726487229, 28.95336869806222779 ) ) ;
#5480=CARTESIAN_POINT ( 'NONE',  ( 47.43856463449117200, 91.76518717409400949, 32.77220824515698183 ) ) ;
#5484=CARTESIAN_POINT ( 'NONE',  ( 42.21948215057684450, 116.1113394311928602, 29.21067981925356705 ) ) ;
#5485=CARTESIAN_POINT ( 'NONE',  ( 48.01140435219951996, 127.2844580088725905, 34.21067981925357060 ) ) ;
#5487=CARTESIAN_POINT ( 'NONE',  ( 46.59305225739526435, 139.5797705074273267, 36.81289934271958941 ) ) ;
#5488=CARTESIAN_POINT ( 'NONE',  ( 46.59305225739526435, 104.1797705074273210, 31.60846029578754468 ) ) ;
#5490=CARTESIAN_POINT ( 'NONE',  ( 44.37947211624943833, 134.2151871740940123, 30.00020018409699318 ) ) ;
#5496=FACE_OUTER_BOUND ( 'NONE', #13048, .T. ) ;
#5498=CARTESIAN_POINT ( 'NONE',  ( 38.58424406990786082, 111.1151871740940038, 34.21067981925357060 ) ) ;
#5502=CARTESIAN_POINT ( 'NONE',  ( 43.01140435219951286, 104.0344580088725763, 28.95336869806222779 ) ) ;
#5504=CARTESIAN_POINT ( 'NONE',  ( 41.64333658814960870, 147.9797705074273324, 38.42115945441014446 ) ) ;
#5505=CARTESIAN_POINT ( 'NONE',  ( 40.27526882409969033, 119.6651871740939868, 30.44471234641811819 ) ) ;
#5508=CARTESIAN_POINT ( 'NONE',  ( 43.01140435219951286, 70.46049967264873715, 39.46799094044489209 ) ) ;
#5510=CARTESIAN_POINT ( 'NONE',  ( 38.01140435219952707, 74.93445800887258201, 35.83527830041809636 ) ) ;
#5512=CARTESIAN_POINT ( 'NONE',  ( 47.43856463449118621, 82.61518717409398960, 34.21067981925357060 ) ) ;
#5513=CARTESIAN_POINT ( 'NONE',  ( 38.96631938032478359, 64.01049967264873430, 37.14960608071593384 ) ) ;
#5521=CARTESIAN_POINT ( 'NONE',  ( 47.43856463449118621, 148.6151871740939896, 34.21067981925357060 ) ) ;
#5523=( BOUNDED_CURVE ( )  B_SPLINE_CURVE ( 2, ( #18349, #12950, #1048, #6107, #19671, #18237, #3138, #16568, #19899, #12836, #4450, #1487, #19554 ),
 .UNSPECIFIED., .F., .F. ) 
 B_SPLINE_CURVE_WITH_KNOTS ( ( 3, 2, 2, 2, 2, 2, 3 ),
 ( 0.6250000000000000000, 0.6264705882352941124, 0.6294117647058823373, 0.6323529411764705621, 0.6352941176470587870, 0.6382352941176470118, 0.6397058823529411242 ),
 .UNSPECIFIED. ) 
 CURVE ( )  GEOMETRIC_REPRESENTATION_ITEM ( )  RATIONAL_B_SPLINE_CURVE ( ( 0.9755282581475768211, 0.9755282581475768211, 1.000000000000000000, 0.9510565162951535312, 1.000000000000000000, 0.9510565162951535312, 1.000000000000000000, 0.9510565162951535312, 1.000000000000000000, 0.9510565162951535312, 1.000000000000000000, 0.9755282581475777093, 0.9755282581475768211 ) ) 
 REPRESENTATION_ITEM ( '' )  );
#5524=CARTESIAN_POINT ( 'NONE',  ( 47.43856463449117911, 109.7297705074273182, 35.64915139335015937 ) ) ;
#5528=ORIENTED_EDGE ( 'NONE', *, *, #20139, .T. ) ;
#5531=CARTESIAN_POINT ( 'NONE',  ( 48.01140435219951996, 89.06049967264871725, 35.83527830041809636 ) ) ;
#5532=CARTESIAN_POINT ( 'NONE',  ( 39.42975644700377558, 140.8151871740940067, 31.60846029578754468 ) ) ;
#5534=CARTESIAN_POINT ( 'NONE',  ( 43.01140435219951286, 104.9604996726487514, 28.95336869806222779 ) ) ;
#5536=CARTESIAN_POINT ( 'NONE',  ( 38.96631938032478359, 60.41049967264873288, 31.27175355779120025 ) ) ;
#5540=CARTESIAN_POINT ( 'NONE',  ( 47.05648932407426344, 63.98445800887257917, 37.14960608071593384 ) ) ;
#5542=CARTESIAN_POINT ( 'NONE',  ( 45.74753988029933538, 85.42977050742730682, 37.97664729208901946 ) ) ;
#5544=CARTESIAN_POINT ( 'NONE',  ( 43.01140435219951286, 83.36518717409398960, 29.55568802177586107 ) ) ;
#5547=ORIENTED_EDGE ( 'NONE', *, *, #1158, .T. ) ;
#5548=CARTESIAN_POINT ( 'NONE',  ( 46.10157429594899270, 85.73445800887255075, 29.95742577749336988 ) ) ;
#5549=DIRECTION ( 'NONE',  ( 0.000000000000000000, -0.000000000000000000, -1.000000000000000000 ) ) ;
#5550=CARTESIAN_POINT ( 'NONE',  ( 44.37947211624943833, 131.4797705074273040, 30.00020018409699318 ) ) ;
#5554=AXIS2_PLACEMENT_3D ( 'NONE', #4191, #20951, #1100 ) ;
#5556=CARTESIAN_POINT ( 'NONE',  ( 48.01140435219951996, 73.13445800887258486, 35.83527830041809636 ) ) ;
#5558=CARTESIAN_POINT ( 'NONE',  ( 47.43856463449118621, 136.8797705074273381, 34.21067981925357060 ) ) ;
#5560=EDGE_CURVE ( 'NONE', #10801, #6293, #557, .T. ) ;
#5561=CYLINDRICAL_SURFACE ( 'NONE', #4129, 4.999999999999997335 ) ;
#5562=CARTESIAN_POINT ( 'NONE',  ( 48.01140435219951996, 121.4344580088725820, 32.58608133808903773 ) ) ;
#5564=EDGE_CURVE ( 'NONE', #11189, #19361, #15950, .T. ) ;
#5565=CARTESIAN_POINT ( 'NONE',  ( 38.58424406990784661, 95.96518717409396970, 32.77220824515698183 ) ) ;
#5569=CARTESIAN_POINT ( 'NONE',  ( 38.01140435219951996, 131.9344580088725820, 35.83527830041810347 ) ) ;
#5570=CARTESIAN_POINT ( 'NONE',  ( 46.59305225739526435, 110.1797705074273210, 31.60846029578754468 ) ) ;
#5573=CARTESIAN_POINT ( 'NONE',  ( 45.74753988029934249, 107.0651871740939782, 30.44471234641812174 ) ) ;
#5575=CARTESIAN_POINT ( 'NONE',  ( 47.05648932407426344, 76.58445800887257349, 31.27175355779120025 ) ) ;
#5580=CARTESIAN_POINT ( 'NONE',  ( 39.42975644700377558, 78.67977050742732104, 36.81289934271958941 ) ) ;
#5581=ORIENTED_EDGE ( 'NONE', *, *, #17717, .T. ) ;
#5583=( BOUNDED_CURVE ( )  B_SPLINE_CURVE ( 2, ( #9808, #7931, #8043, #19495, #13103, #18282, #19716, #4717, #7722, #14854, #21376, #14636, #21600 ),
 .UNSPECIFIED., .F., .F. ) 
 B_SPLINE_CURVE_WITH_KNOTS ( ( 3, 2, 2, 2, 2, 2, 3 ),
 ( 0.5367647058823529216, 0.5382352941176470340, 0.5411764705882352589, 0.5441176470588234837, 0.5470588235294118196, 0.5500000000000000444, 0.5514705882352941568 ),
 .UNSPECIFIED. ) 
 CURVE ( )  GEOMETRIC_REPRESENTATION_ITEM ( )  RATIONAL_B_SPLINE_CURVE ( ( 0.9755282581475768211, 0.9755282581475768211, 1.000000000000000000, 0.9510565162951535312, 1.000000000000000000, 0.9510565162951535312, 1.000000000000000000, 0.9510565162951535312, 1.000000000000000000, 0.9510565162951535312, 1.000000000000000000, 0.9755282581475768211, 0.9755282581475768211 ) ) 
 REPRESENTATION_ITEM ( '' )  );
#5584=CARTESIAN_POINT ( 'NONE',  ( 46.10157429594899270, 64.73445800887257917, 29.95742577749337343 ) ) ;
#5586=CARTESIAN_POINT ( 'NONE',  ( 38.01140435219951996, 126.8604996726487144, 35.83527830041810347 ) ) ;
#5587=CARTESIAN_POINT ( 'NONE',  ( 38.58424406990784661, 78.26518717409400949, 35.64915139335016647 ) ) ;
#5590=DIRECTION ( 'NONE',  ( 0.000000000000000000, 0.000000000000000000, 1.000000000000000000 ) ) ;
#5594=CARTESIAN_POINT ( 'NONE',  ( 39.42975644700377558, 138.6797705074273210, 36.81289934271958941 ) ) ;
#5595=CARTESIAN_POINT ( 'NONE',  ( 45.74753988029933538, 107.3297705074272983, 30.44471234641811819 ) ) ;
#5597=CARTESIAN_POINT ( 'NONE',  ( 43.01140435219951286, 137.3651871740940180, 29.55568802177586107 ) ) ;
#5603=CARTESIAN_POINT ( 'NONE',  ( 42.21948215057684450, 136.3836182503284533, 39.21067981925355639 ) ) ;
#5606=CARTESIAN_POINT ( 'NONE',  ( 47.43856463449117200, 112.7651871740940095, 32.77220824515698183 ) ) ;
#5612=CARTESIAN_POINT ( 'NONE',  ( 39.92123440845004723, 90.23445800887257917, 38.46393386101376421 ) ) ;
#5613=CARTESIAN_POINT ( 'NONE',  ( 43.01140435219951286, 146.6297705074273097, 29.55568802177586107 ) ) ;
#5616=CARTESIAN_POINT ( 'NONE',  ( 43.01140435219951286, 61.12977050742731677, 38.86567161673127657 ) ) ;
#5617=CARTESIAN_POINT ( 'NONE',  ( 38.58424406990784661, 114.2651871740940095, 35.64915139335016647 ) ) ;
#5619=CARTESIAN_POINT ( 'NONE',  ( 38.01140435219952707, 72.71049967264873715, 34.21067981925357060 ) ) ;
#5620=EDGE_CURVE ( 'NONE', #1584, #19429, #12028, .T. ) ;
#5621=CARTESIAN_POINT ( 'NONE',  ( 43.01140435219951286, 77.03445800887257633, 29.21067981925356705 ) ) ;
#5622=CARTESIAN_POINT ( 'NONE',  ( 43.01140435219951286, 75.53445800887257633, 39.21067981925356349 ) ) ;
#5624=CARTESIAN_POINT ( 'NONE',  ( 38.96631938032478359, 72.08445800887257349, 37.14960608071593384 ) ) ;
#5625=CARTESIAN_POINT ( 'NONE',  ( 40.27526882409969033, 72.56518717409399244, 37.97664729208901946 ) ) ;
#5626=CARTESIAN_POINT ( 'NONE',  ( 42.21948215057684450, 63.03738109496900677, 29.21067981925356705 ) ) ;
#5633=CARTESIAN_POINT ( 'NONE',  ( 40.27526882409969033, 147.5651871740939498, 37.97664729208901946 ) ) ;
#5636=DIRECTION ( 'NONE',  ( 0.000000000000000000, 0.000000000000000000, 1.000000000000000000 ) ) ;
#5637=CARTESIAN_POINT ( 'NONE',  ( 41.64333658814960870, 107.7797705074273154, 30.00020018409699318 ) ) ;
#5638=ORIENTED_EDGE ( 'NONE', *, *, #5672, .T. ) ;
#5642=CARTESIAN_POINT ( 'NONE',  ( 45.74753988029933538, 112.4297705074273210, 37.97664729208901946 ) ) ;
#5644=CARTESIAN_POINT ( 'NONE',  ( 48.01140435219951996, 89.21049967264873715, 34.21067981925357060 ) ) ;
#5645=CARTESIAN_POINT ( 'NONE',  ( 47.43856463449118621, 82.87977050742730967, 34.21067981925357060 ) ) ;
#5646=CARTESIAN_POINT ( 'NONE',  ( 45.74753988029933538, 145.1651871740939725, 37.97664729208901946 ) ) ;
#5647=CARTESIAN_POINT ( 'NONE',  ( 39.92123440845004723, 102.2604996726487201, 29.95742577749337343 ) ) ;
#5654=CARTESIAN_POINT ( 'NONE',  ( 39.92123440845005433, 143.3344580088725877, 29.95742577749336988 ) ) ;
#5657=CARTESIAN_POINT ( 'NONE',  ( 44.37947211624943833, 82.27977050742732956, 38.42115945441014446 ) ) ;
#5659=CARTESIAN_POINT ( 'NONE',  ( 45.74753988029934249, 82.16518717409400097, 37.97664729208901235 ) ) ;
#5662=VERTEX_POINT ( 'NONE', #10496 ) ;
#5665=CARTESIAN_POINT ( 'NONE',  ( 39.42975644700377558, 135.0797705074272983, 31.60846029578754468 ) ) ;
#5671=CARTESIAN_POINT ( 'NONE',  ( 39.42975644700377558, 138.6797705074273210, 36.81289934271958941 ) ) ;
#5672=EDGE_CURVE ( 'NONE', #19018, #15353, #18211, .T. ) ;
#5674=CARTESIAN_POINT ( 'NONE',  ( 48.01140435219951996, 121.1344580088725706, 35.83527830041809636 ) ) ;
#5675=EDGE_CURVE ( 'NONE', #6431, #7690, #1479, .T. ) ;
#5676=CARTESIAN_POINT ( 'NONE',  ( 38.58424406990784661, 92.96518717409401233, 32.77220824515698183 ) ) ;
#5677=CARTESIAN_POINT ( 'NONE',  ( 43.80332655382220253, 74.88361825032848174, 29.21067981925356705 ) ) ;
#5681=CARTESIAN_POINT ( 'NONE',  ( 43.01140435219954838, 108.5344580088725763, 39.21067981925356349 ) ) ;
#5682=CARTESIAN_POINT ( 'NONE',  ( 38.96631938032478359, 137.4844580088725650, 31.27175355779120025 ) ) ;
#5683=CARTESIAN_POINT ( 'NONE',  ( 41.64333658814960870, 111.9797705074273324, 38.42115945441014446 ) ) ;
#5687=CARTESIAN_POINT ( 'NONE',  ( 43.01140435219951286, 104.3651871740940038, 29.55568802177586107 ) ) ;
#5690=CARTESIAN_POINT ( 'NONE',  ( 43.01140435219951286, 86.96049967264872294, 29.21067981925356705 ) ) ;
#5693=DIRECTION ( 'NONE',  ( 0.000000000000000000, 1.000000000000000000, 0.000000000000000000 ) ) ;
#5696=CARTESIAN_POINT ( 'NONE',  ( 47.43856463449117911, 79.72977050742730398, 35.64915139335015937 ) ) ;
#5699=CARTESIAN_POINT ( 'NONE',  ( 43.01140435219951286, 65.03445800887257633, 28.95336869806222779 ) ) ;
#5701=CARTESIAN_POINT ( 'NONE',  ( 47.05648932407426344, 116.5104996726487485, 31.27175355779120025 ) ) ;
#5702=CARTESIAN_POINT ( 'NONE',  ( 39.42975644700377558, 77.81518717409399244, 31.60846029578754468 ) ) ;
#5710=CARTESIAN_POINT ( 'NONE',  ( 45.74753988029933538, 140.3297705074272983, 30.44471234641811819 ) ) ;
#5712=CARTESIAN_POINT ( 'NONE',  ( 39.42975644700377558, 131.8151871740940067, 31.60846029578754468 ) ) ;
#5713=CARTESIAN_POINT ( 'NONE',  ( 48.01140435219951996, 67.43445800887256780, 32.58608133808903773 ) ) ;
#5715=CARTESIAN_POINT ( 'NONE',  ( 38.58424406990784661, 60.52977050742731535, 35.64915139335016647 ) ) ;
#5719=CARTESIAN_POINT ( 'NONE',  ( 43.01140435219953417, 142.4604996726487514, 39.21067981925356349 ) ) ;
#5720=CARTESIAN_POINT ( 'NONE',  ( 47.43856463449117200, 118.4651871740939981, 35.64915139335016647 ) ) ;
#5725=CARTESIAN_POINT ( 'NONE',  ( 47.05648932407426344, 87.98445800887257917, 37.14960608071593384 ) ) ;
#5726=CARTESIAN_POINT ( 'NONE',  ( 47.43856463449117911, 149.0297705074273154, 32.77220824515697473 ) ) ;
#5727=CARTESIAN_POINT ( 'NONE',  ( 47.05648932407426344, 149.5104996726487343, 31.27175355779120025 ) ) ;
#5728=CARTESIAN_POINT ( 'NONE',  ( 46.59305225739526435, 103.3151871740940067, 36.81289934271958941 ) ) ;
#5730=CARTESIAN_POINT ( 'NONE',  ( 41.46631938032478359, 75.11049967264874283, 29.45539723777780239 ) ) ;
#5731=CARTESIAN_POINT ( 'NONE',  ( 43.01140435219954838, 108.5344580088725763, 39.21067981925356349 ) ) ;
#5734=ADVANCED_FACE ( 'NONE', ( #16303 ), #8356, .T. ) ;
#5743=CARTESIAN_POINT ( 'NONE',  ( 41.64333658814960870, 140.5151871740939953, 30.00020018409699318 ) ) ;
#5744=CARTESIAN_POINT ( 'NONE',  ( 38.58424406990785371, 155.9651871740939555, 32.77220824515697473 ) ) ;
#5745=CARTESIAN_POINT ( 'NONE',  ( 43.01140435219951286, 107.6297705074273097, 29.55568802177586107 ) ) ;
#5746=ORIENTED_EDGE ( 'NONE', *, *, #9783, .T. ) ;
#5751=CARTESIAN_POINT ( 'NONE',  ( 47.43856463449117200, 133.7651871740939669, 32.77220824515698183 ) ) ;
#5752=CARTESIAN_POINT ( 'NONE',  ( 38.01140435219951996, 105.8604996726487570, 35.83527830041810347 ) ) ;
#5754=ADVANCED_FACE ( 'NONE', ( #7946 ), #14652, .T. ) ;
#5757=CARTESIAN_POINT ( 'NONE',  ( 44.55648932407425633, 158.8104996726487457, 29.45539723777780239 ) ) ;
#5759=DIRECTION ( 'NONE',  ( 0.000000000000000000, 1.000000000000000000, 0.000000000000000000 ) ) ;
#5761=VERTEX_POINT ( 'NONE', #21069 ) ;
#5762=CARTESIAN_POINT ( 'NONE',  ( 38.58424406990784661, 87.22977050742731819, 32.77220824515698183 ) ) ;
#5764=CARTESIAN_POINT ( 'NONE',  ( 39.42975644700377558, 66.41518717409400097, 36.81289934271958941 ) ) ;
#5768=CARTESIAN_POINT ( 'NONE',  ( 48.01140435219951996, 85.43445800887255359, 32.58608133808903773 ) ) ;
#5769=CARTESIAN_POINT ( 'NONE',  ( 42.21948215057684450, 104.1113394311928460, 29.21067981925356705 ) ) ;
#5770=CARTESIAN_POINT ( 'NONE',  ( 44.37947211624943833, 137.4797705074273324, 30.00020018409699318 ) ) ;
#5775=CARTESIAN_POINT ( 'NONE',  ( 38.58424406990784661, 123.5297705074273438, 35.64915139335016647 ) ) ;
#5776=CARTESIAN_POINT ( 'NONE',  ( 42.21948215057684450, 111.4575765865523067, 39.21067981925355639 ) ) ;
#5780=CARTESIAN_POINT ( 'NONE',  ( 47.43856463449118621, 97.61518717409400381, 34.21067981925357060 ) ) ;
#5785=CARTESIAN_POINT ( 'NONE',  ( 42.21948215057684450, 132.4575765865522783, 39.21067981925356349 ) ) ;
#5786=CARTESIAN_POINT ( 'NONE',  ( 47.05648932407426344, 133.5844580088725877, 31.27175355779120025 ) ) ;
#5787=CARTESIAN_POINT ( 'NONE',  ( 45.74753988029933538, 118.4297705074272926, 37.97664729208901946 ) ) ;
#5789=CARTESIAN_POINT ( 'NONE',  ( 43.01140435219951996, 10.71049967264875491, 34.21067981925357060 ) ) ;
#5790=CARTESIAN_POINT ( 'NONE',  ( 43.01140435219951286, 98.36518717409400381, 29.55568802177586107 ) ) ;
#5793=CARTESIAN_POINT ( 'NONE',  ( 43.80332655382220253, 75.61133943119284595, 39.21067981925355639 ) ) ;
#5796=CYLINDRICAL_SURFACE ( 'NONE', #182, 4.999999999999997335 ) ;
#5797=CARTESIAN_POINT ( 'NONE',  ( 38.58424406990786082, 81.37977050742730967, 34.21067981925357060 ) ) ;
#5802=CARTESIAN_POINT ( 'NONE',  ( 43.01140435219951286, 121.4604996726487514, 39.46799094044489209 ) ) ;
#5803=CARTESIAN_POINT ( 'NONE',  ( 43.01140435219951286, 80.36518717409398960, 29.55568802177586463 ) ) ;
#5811=CARTESIAN_POINT ( 'NONE',  ( 44.37947211624943833, 139.2797705074273154, 38.42115945441014446 ) ) ;
#5813=CARTESIAN_POINT ( 'NONE',  ( 43.01140435219951286, 129.8651871740940180, 38.86567161673127657 ) ) ;
#5814=CARTESIAN_POINT ( 'NONE',  ( 46.10157429594899270, 137.6604996726487400, 29.95742577749336988 ) ) ;
#5816=CARTESIAN_POINT ( 'NONE',  ( 43.01140435219951286, 79.46049967264875136, 39.21067981925356349 ) ) ;
#5820=DIRECTION ( 'NONE',  ( 0.000000000000000000, 0.000000000000000000, 1.000000000000000000 ) ) ;
#5821=CARTESIAN_POINT ( 'NONE',  ( 47.43856463449117200, 106.7651871740939811, 32.77220824515698183 ) ) ;
#5822=ORIENTED_EDGE ( 'NONE', *, *, #1202, .T. ) ;
#5826=CARTESIAN_POINT ( 'NONE',  ( 41.46631938032478359, 95.18445800887258201, 29.45539723777780239 ) ) ;
#5827=CARTESIAN_POINT ( 'NONE',  ( 38.01140435219952707, 144.7104996726487229, 34.21067981925357060 ) ) ;
#5828=CARTESIAN_POINT ( 'NONE',  ( 47.43856463449117200, 109.7651871740939953, 32.77220824515698183 ) ) ;
#5830=EDGE_CURVE ( 'NONE', #17591, #8610, #16715, .T. ) ;
#5831=CARTESIAN_POINT ( 'NONE',  ( 44.55648932407425633, 61.61049967264874283, 38.96596240072933170 ) ) ;
#5834=CARTESIAN_POINT ( 'NONE',  ( 44.55648932407425633, 117.6844580088725820, 38.96596240072933170 ) ) ;
#5835=AXIS2_PLACEMENT_3D ( 'NONE', #10467, #3844, #17167 ) ;
#5838=CARTESIAN_POINT ( 'NONE',  ( 38.58424406990784661, 65.96518717409399812, 32.77220824515698183 ) ) ;
#5849=CARTESIAN_POINT ( 'NONE',  ( 45.74753988029933538, 145.1651871740939725, 37.97664729208901946 ) ) ;
#5850=CARTESIAN_POINT ( 'NONE',  ( 41.64333658814960870, 93.97977050742733240, 38.42115945441014446 ) ) ;
#5852=ORIENTED_EDGE ( 'NONE', *, *, #2850, .T. ) ;
#5854=ADVANCED_FACE ( 'NONE', ( #18923 ), #15293, .T. ) ;
#5858=CARTESIAN_POINT ( 'NONE',  ( 38.01140435219951996, 113.6344580088725849, 32.58608133808903773 ) ) ;
#5861=CARTESIAN_POINT ( 'NONE',  ( 38.58424406990784661, 78.52977050742730114, 35.64915139335016647 ) ) ;
#5862=CARTESIAN_POINT ( 'NONE',  ( 41.64333658814960870, 134.5151871740939953, 30.00020018409699318 ) ) ;
#5863=CARTESIAN_POINT ( 'NONE',  ( 38.96631938032478359, 91.01049967264873430, 37.14960608071593384 ) ) ;
#5868=CARTESIAN_POINT ( 'NONE',  ( 47.05648932407426344, 158.5104996726487343, 31.27175355779120025 ) ) ;
#5869=CARTESIAN_POINT ( 'NONE',  ( 43.80332655382222384, 96.61133943119284595, 39.21067981925354928 ) ) ;
#5872=CARTESIAN_POINT ( 'NONE',  ( 43.01140435219951286, 74.62977050742732388, 29.55568802177586463 ) ) ;
#5876=CARTESIAN_POINT ( 'NONE',  ( 38.01140435219952707, 68.93445800887255359, 35.83527830041809636 ) ) ;
#5877=CARTESIAN_POINT ( 'NONE',  ( 47.05648932407426344, 123.9844580088725934, 37.14960608071593384 ) ) ;
#5878=CARTESIAN_POINT ( 'NONE',  ( 41.64333658814960870, 131.7797705074273154, 30.00020018409699318 ) ) ;
#5879=EDGE_LOOP ( 'NONE', ( #11487, #4308, #2519, #14282 ) ) ;
#5882=VECTOR ( 'NONE', #3709, 1000.000000000000000 ) ;
#5883=CARTESIAN_POINT ( 'NONE',  ( 45.74753988029933538, 125.3297705074273125, 30.44471234641811819 ) ) ;
#5884=CARTESIAN_POINT ( 'NONE',  ( 43.01140435219951996, 170.7104996726487514, 39.21067981925356349 ) ) ;
#5885=CARTESIAN_POINT ( 'NONE',  ( 40.27526882409969033, 87.82977050742732672, 37.97664729208901946 ) ) ;
#5886=CARTESIAN_POINT ( 'NONE',  ( 43.01140435219951996, 10.71049967264875491, 34.21067981925357060 ) ) ;
#5890=CARTESIAN_POINT ( 'NONE',  ( 44.55648932407425633, 133.8844580088725706, 29.45539723777780239 ) ) ;
#5894=CARTESIAN_POINT ( 'NONE',  ( 46.10157429594899270, 108.8344580088725735, 38.46393386101375711 ) ) ;
#5895=CARTESIAN_POINT ( 'NONE',  ( 44.55648932407425633, 136.8844580088725706, 29.45539723777780239 ) ) ;
#5896=CARTESIAN_POINT ( 'NONE',  ( 47.43856463449117200, 115.7297705074273324, 35.64915139335016647 ) ) ;
#5899=CARTESIAN_POINT ( 'NONE',  ( 44.37947211624943833, 97.01518717409400949, 38.42115945441014446 ) ) ;
#5903=CARTESIAN_POINT ( 'NONE',  ( 41.46631938032478359, 88.31049967264874567, 38.96596240072933170 ) ) ;
#5906=EDGE_CURVE ( 'NONE', #3622, #9753, #14277, .T. ) ;
#5909=CARTESIAN_POINT ( 'NONE',  ( 43.01140435219951286, 74.62977050742732388, 29.55568802177586107 ) ) ;
#5912=CARTESIAN_POINT ( 'NONE',  ( 39.42975644700377558, 159.0797705074273267, 31.60846029578754468 ) ) ;
#5914=CARTESIAN_POINT ( 'NONE',  ( 46.10157429594899270, 118.7604996726487201, 38.46393386101376421 ) ) ;
#5915=CARTESIAN_POINT ( 'NONE',  ( 38.58424406990786082, 75.11518717409400381, 34.21067981925357060 ) ) ;
#5922=CARTESIAN_POINT ( 'NONE',  ( 38.01140435219952707, 149.6344580088725991, 32.58608133808903773 ) ) ;
#5923=CARTESIAN_POINT ( 'NONE',  ( 41.64333658814960870, 138.9797705074273324, 38.42115945441014446 ) ) ;
#5925=CARTESIAN_POINT ( 'NONE',  ( 39.42975644700377558, 122.8151871740940067, 31.60846029578754468 ) ) ;
#5931=FACE_OUTER_BOUND ( 'NONE', #7696, .T. ) ;
#5932=CARTESIAN_POINT ( 'NONE',  ( 41.64333658814960870, 107.5151871740939953, 30.00020018409699318 ) ) ;
#5933=EDGE_LOOP ( 'NONE', ( #9070, #17560, #8614, #10670 ) ) ;
#5934=CYLINDRICAL_SURFACE ( 'NONE', #15221, 4.999999999999997335 ) ;
#5935=EDGE_CURVE ( 'NONE', #16834, #13122, #5400, .T. ) ;
#5936=ORIENTED_EDGE ( 'NONE', *, *, #19264, .F. ) ;
#5937=CARTESIAN_POINT ( 'NONE',  ( 43.01140435219951286, 90.53445800887259054, 39.46799094044489209 ) ) ;
#5939=CARTESIAN_POINT ( 'NONE',  ( 43.01140435219951286, 152.9604996726487514, 28.95336869806222779 ) ) ;
#5940=CARTESIAN_POINT ( 'NONE',  ( 45.74753988029933538, 110.0651871740939782, 30.44471234641811819 ) ) ;
#5942=CARTESIAN_POINT ( 'NONE',  ( 46.10157429594899270, 65.66049967264873999, 29.95742577749337343 ) ) ;
#5947=CARTESIAN_POINT ( 'NONE',  ( 43.01140435219951286, 116.0344580088725763, 29.21067981925356705 ) ) ;
#5948=CARTESIAN_POINT ( 'NONE',  ( 41.64333658814960870, 71.51518717409399528, 30.00020018409699318 ) ) ;
#5949=CARTESIAN_POINT ( 'NONE',  ( 38.58424406990785371, 152.9651871740940123, 32.77220824515697473 ) ) ;
#5954=ORIENTED_EDGE ( 'NONE', *, *, #4813, .F. ) ;
#5957=ORIENTED_EDGE ( 'NONE', *, *, #7246, .F. ) ;
#5958=CARTESIAN_POINT ( 'NONE',  ( 46.59305225739526435, 133.9151871740940010, 31.60846029578754468 ) ) ;
#5959=CARTESIAN_POINT ( 'NONE',  ( 47.43856463449118621, 154.6151871740940180, 34.21067981925357060 ) ) ;
#5961=CARTESIAN_POINT ( 'NONE',  ( 44.37947211624943833, 100.2797705074273154, 38.42115945441014446 ) ) ;
#5962=ORIENTED_EDGE ( 'NONE', *, *, #12310, .F. ) ;
#5965=VERTEX_POINT ( 'NONE', #20902 ) ;
#5966=CARTESIAN_POINT ( 'NONE',  ( 46.10157429594899270, 111.8344580088725735, 38.46393386101376421 ) ) ;
#5968=CARTESIAN_POINT ( 'NONE',  ( 43.01140435219951286, 73.12977050742729546, 38.86567161673127657 ) ) ;
#5969=CARTESIAN_POINT ( 'NONE',  ( 43.01140435219951286, 131.3651871740940180, 29.55568802177586463 ) ) ;
#5970=CARTESIAN_POINT ( 'NONE',  ( 48.01140435219951996, 95.06049967264874567, 35.83527830041810347 ) ) ;
#5975=CARTESIAN_POINT ( 'NONE',  ( 39.92123440845005433, 152.3344580088725593, 29.95742577749336988 ) ) ;
#5977=CARTESIAN_POINT ( 'NONE',  ( 48.01140435219951996, 106.4344580088725678, 32.58608133808903773 ) ) ;
#5980=CARTESIAN_POINT ( 'NONE',  ( 46.59305225739526435, 76.57977050742731251, 36.81289934271958941 ) ) ;
#5984=VERTEX_POINT ( 'NONE', #6006 ) ;
#5987=CARTESIAN_POINT ( 'NONE',  ( 39.42975644700377558, 120.6797705074273210, 36.81289934271958941 ) ) ;
#5988=ORIENTED_EDGE ( 'NONE', *, *, #6212, .T. ) ;
#5991=CARTESIAN_POINT ( 'NONE',  ( 44.37947211624943833, 122.4797705074273182, 30.00020018409699318 ) ) ;
#5992=CARTESIAN_POINT ( 'NONE',  ( 46.10157429594899270, 109.7604996726487343, 38.46393386101375711 ) ) ;
#5993=DIRECTION ( 'NONE',  ( 0.000000000000000000, 1.000000000000000000, 0.000000000000000000 ) ) ;
#5997=CARTESIAN_POINT ( 'NONE',  ( 43.01140435219951286, 67.46049967264873715, 39.21067981925356349 ) ) ;
#5998=CARTESIAN_POINT ( 'NONE',  ( 47.05648932407426344, 124.9104996726487542, 37.14960608071593384 ) ) ;
#6001=EDGE_CURVE ( 'NONE', #20293, #11358, #4348, .T. ) ;
#6002=ADVANCED_FACE ( 'NONE', ( #19033 ), #16145, .T. ) ;
#6003=CARTESIAN_POINT ( 'NONE',  ( 41.46631938032478359, 132.3844580088725706, 38.96596240072933170 ) ) ;
#6004=CARTESIAN_POINT ( 'NONE',  ( 44.37947211624943833, 107.4797705074273182, 30.00020018409699318 ) ) ;
#6006=CARTESIAN_POINT ( 'NONE',  ( 43.01140435219951286, 89.96049967264873715, 29.21067981925356705 ) ) ;
#6007=CARTESIAN_POINT ( 'NONE',  ( 38.58424406990785371, 101.9651871740939981, 32.77220824515697473 ) ) ;
#6010=CARTESIAN_POINT ( 'NONE',  ( 41.46631938032478359, 87.11049967264874283, 29.45539723777780239 ) ) ;
#6014=CARTESIAN_POINT ( 'NONE',  ( 45.74753988029934249, 73.42977050742730682, 37.97664729208901235 ) ) ;
#6017=CARTESIAN_POINT ( 'NONE',  ( 44.37947211624943833, 152.4797705074273324, 30.00020018409699318 ) ) ;
#6020=CARTESIAN_POINT ( 'NONE',  ( 38.01140435219952707, 120.7104996726487371, 34.21067981925357060 ) ) ;
#6021=CARTESIAN_POINT ( 'NONE',  ( 43.01140435219951286, 75.86518717409398960, 38.86567161673127657 ) ) ;
#6029=CARTESIAN_POINT ( 'NONE',  ( 46.59305225739526435, 136.5797705074272983, 36.81289934271958941 ) ) ;
#6031=CARTESIAN_POINT ( 'NONE',  ( 38.58424406990785371, 123.2651871740939953, 35.64915139335015937 ) ) ;
#6032=CARTESIAN_POINT ( 'NONE',  ( 48.01140435219951996, 137.2104996726487514, 34.21067981925357060 ) ) ;
#6033=CARTESIAN_POINT ( 'NONE',  ( 38.96631938032478359, 151.0104996726487343, 37.14960608071593384 ) ) ;
#6036=CARTESIAN_POINT ( 'NONE',  ( 48.01140435219951996, 149.0604996726487173, 35.83527830041809636 ) ) ;
#6038=CARTESIAN_POINT ( 'NONE',  ( 46.10157429594899270, 82.76049967264874851, 38.46393386101375711 ) ) ;
#6040=CARTESIAN_POINT ( 'NONE',  ( 43.01140435219951286, 108.8651871740939896, 38.86567161673127657 ) ) ;
#6041=ORIENTED_EDGE ( 'NONE', *, *, #11554, .F. ) ;
#6043=EDGE_LOOP ( 'NONE', ( #20752, #18902, #4735, #19873 ) ) ;
#6044=CARTESIAN_POINT ( 'NONE',  ( 47.05648932407426344, 93.98445800887257917, 37.14960608071593384 ) ) ;
#6049=CARTESIAN_POINT ( 'NONE',  ( 39.92123440845004723, 151.1604996726487116, 38.46393386101376421 ) ) ;
#6050=CARTESIAN_POINT ( 'NONE',  ( 41.64333658814960870, 104.5151871740939953, 30.00020018409699318 ) ) ;
#6052=CARTESIAN_POINT ( 'NONE',  ( 48.01140435219951996, 62.36049967264873573, 32.58608133808903773 ) ) ;
#6054=DIRECTION ( 'NONE',  ( 0.000000000000000000, 1.000000000000000000, 0.000000000000000000 ) ) ;
#6055=LINE ( 'NONE', #2426, #3821 ) ;
#6057=CARTESIAN_POINT ( 'NONE',  ( 43.01140435219951286, 59.03445800887258343, 29.21067981925356705 ) ) ;
#6058=CARTESIAN_POINT ( 'NONE',  ( 39.42975644700377558, 69.41518717409400097, 36.81289934271958941 ) ) ;
#6060=CARTESIAN_POINT ( 'NONE',  ( 41.64333658814960870, 153.7151871740940123, 38.42115945441014446 ) ) ;
#6068=CARTESIAN_POINT ( 'NONE',  ( 41.64333658814960870, 135.7151871740940123, 38.42115945441014446 ) ) ;
#6069=CARTESIAN_POINT ( 'NONE',  ( 40.27526882409969744, 156.5651871740939782, 37.97664729208901235 ) ) ;
#6070=CARTESIAN_POINT ( 'NONE',  ( 46.59305225739526435, 92.17977050742732104, 31.60846029578754468 ) ) ;
#6072=EDGE_LOOP ( 'NONE', ( #21296, #6121, #13350, #6205 ) ) ;
#6076=CARTESIAN_POINT ( 'NONE',  ( 46.10157429594899270, 117.8344580088725451, 38.46393386101376421 ) ) ;
#6078=CARTESIAN_POINT ( 'NONE',  ( 39.42975644700377558, 72.67977050742730682, 36.81289934271958941 ) ) ;
#6079=CARTESIAN_POINT ( 'NONE',  ( 44.37947211624943833, 133.0151871740939953, 38.42115945441014446 ) ) ;
#6080=CARTESIAN_POINT ( 'NONE',  ( 38.96631938032478359, 88.01049967264874851, 37.14960608071593384 ) ) ;
#6084=CARTESIAN_POINT ( 'NONE',  ( 48.01140435219951996, 142.1344580088725991, 35.83527830041809636 ) ) ;
#6086=CARTESIAN_POINT ( 'NONE',  ( 45.74753988029933538, 71.32977050742732672, 30.44471234641811819 ) ) ;
#6093=CARTESIAN_POINT ( 'NONE',  ( 47.43856463449117911, 124.7297705074273182, 35.64915139335015937 ) ) ;
#6094=VERTEX_POINT ( 'NONE', #4473 ) ;
#6096=CARTESIAN_POINT ( 'NONE',  ( 44.37947211624943833, 127.2797705074273438, 38.42115945441014446 ) ) ;
#6097=CARTESIAN_POINT ( 'NONE',  ( 45.05628966327351748, 58.83593637268779730, 29.61779221216752944 ) ) ;
#6098=CARTESIAN_POINT ( 'NONE',  ( 46.10157429594899270, 63.83445800887258770, 38.46393386101376421 ) ) ;
#6099=( BOUNDED_CURVE ( )  B_SPLINE_CURVE ( 2, ( #14387, #14064, #12524, #21127, #7464, #17477, #14173, #12298, #15608, #7253, #2387, #15821, #18928 ),
 .UNSPECIFIED., .F., .T. ) 
 B_SPLINE_CURVE_WITH_KNOTS ( ( 3, 2, 2, 2, 2, 2, 3 ),
 ( 0.007352941176470595940, 0.008823529411764705760, 0.01176470588235294101, 0.01470588235294117627, 0.01764705882352941152, 0.02058823529411764677, 0.02205882352941176960 ),
 .UNSPECIFIED. ) 
 CURVE ( )  GEOMETRIC_REPRESENTATION_ITEM ( )  RATIONAL_B_SPLINE_CURVE ( ( 0.9755282581475767101, 0.9755282581475768211, 1.000000000000000000, 0.9510565162951535312, 1.000000000000000000, 0.9510565162951535312, 1.000000000000000000, 0.9510565162951535312, 1.000000000000000000, 0.9510565162951535312, 1.000000000000000000, 0.9755282581475765991, 0.9755282581475767101 ) ) 
 REPRESENTATION_ITEM ( '' )  );
#6100=EDGE_CURVE ( 'NONE', #13353, #2795, #7674, .T. ) ;
#6101=LINE ( 'NONE', #12831, #11154 ) ;
#6102=CARTESIAN_POINT ( 'NONE',  ( 39.92123440845005433, 102.2344580088725650, 38.46393386101375711 ) ) ;
#6107=CARTESIAN_POINT ( 'NONE',  ( 46.10157429594899270, 94.73445800887257917, 29.95742577749336988 ) ) ;
#6109=CARTESIAN_POINT ( 'NONE',  ( 38.96631938032478359, 125.4844580088725934, 31.27175355779120025 ) ) ;
#6110=CARTESIAN_POINT ( 'NONE',  ( 41.64333658814960870, 105.9797705074273182, 38.42115945441014446 ) ) ;
#6113=CARTESIAN_POINT ( 'NONE',  ( 45.74753988029934249, 98.06518717409399244, 30.44471234641812174 ) ) ;
#6116=CARTESIAN_POINT ( 'NONE',  ( 44.55648932407425633, 128.8104996726487457, 29.45539723777780239 ) ) ;
#6120=CARTESIAN_POINT ( 'NONE',  ( 45.74753988029934249, 64.42977050742732104, 37.97664729208901235 ) ) ;
#6121=ORIENTED_EDGE ( 'NONE', *, *, #14025, .T. ) ;
#6123=CARTESIAN_POINT ( 'NONE',  ( 38.58424406990784661, 159.2297705074272756, 32.77220824515698183 ) ) ;
#6126=CARTESIAN_POINT ( 'NONE',  ( 48.01140435219951996, 122.3604996726487428, 32.58608133808903773 ) ) ;
#6127=CARTESIAN_POINT ( 'NONE',  ( 47.43856463449117200, 67.76518717409399528, 32.77220824515698183 ) ) ;
#6129=CARTESIAN_POINT ( 'NONE',  ( 43.01140435219951286, 66.53445800887257633, 39.21067981925356349 ) ) ;
#6136=CARTESIAN_POINT ( 'NONE',  ( 43.01140435219951286, 137.6297705074273381, 29.55568802177586463 ) ) ;
#6138=CARTESIAN_POINT ( 'NONE',  ( 46.59305225739526435, 130.9151871740940010, 31.60846029578754468 ) ) ;
#6141=DIRECTION ( 'NONE',  ( 0.000000000000000000, 1.000000000000000000, 0.000000000000000000 ) ) ;
#6143=CARTESIAN_POINT ( 'NONE',  ( 43.01140435219951286, 75.53445800887257633, 39.21067981925356349 ) ) ;
#6144=CARTESIAN_POINT ( 'NONE',  ( 43.01140435219951286, 104.3651871740940038, 29.55568802177586463 ) ) ;
#6148=CARTESIAN_POINT ( 'NONE',  ( 39.92123440845004723, 80.33445800887258770, 29.95742577749337343 ) ) ;
#6150=CARTESIAN_POINT ( 'NONE',  ( 41.46631938032478359, 151.3104996726487457, 38.96596240072933170 ) ) ;
#6151=CARTESIAN_POINT ( 'NONE',  ( 40.27526882409969033, 110.6651871740940010, 30.44471234641811819 ) ) ;
#6153=CARTESIAN_POINT ( 'NONE',  ( 38.01140435219952707, 66.71049967264873715, 34.21067981925357060 ) ) ;
#6158=CARTESIAN_POINT ( 'NONE',  ( 43.01140435219957681, 71.96049967264872294, 29.21067981925356705 ) ) ;
#6159=( BOUNDED_CURVE ( )  B_SPLINE_CURVE ( 2, ( #19241, #5785, #9223, #833, #7567, #14267, #21012, #8965, #8753, #575, #15365, #19388, #6882 ),
 .UNSPECIFIED., .F., .F. ) 
 B_SPLINE_CURVE_WITH_KNOTS ( ( 3, 2, 2, 2, 2, 2, 3 ),
 ( 0.2573529411764705621, 0.2588235294117647300, 0.2617647058823529549, 0.2647058823529411797, 0.2676470588235294046, 0.2705882352941176294, 0.2720588235294117974 ),
 .UNSPECIFIED. ) 
 CURVE ( )  GEOMETRIC_REPRESENTATION_ITEM ( )  RATIONAL_B_SPLINE_CURVE ( ( 0.9755282581475768211, 0.9755282581475763770, 1.000000000000000000, 0.9510565162951535312, 1.000000000000000000, 0.9510565162951535312, 1.000000000000000000, 0.9510565162951535312, 1.000000000000000000, 0.9510565162951535312, 1.000000000000000000, 0.9755282581475763770, 0.9755282581475768211 ) ) 
 REPRESENTATION_ITEM ( '' )  );
#6160=CARTESIAN_POINT ( 'NONE',  ( 45.74753988029933538, 158.3297705074273267, 30.44471234641811819 ) ) ;
#6162=CARTESIAN_POINT ( 'NONE',  ( 45.74753988029934249, 152.0651871740939782, 30.44471234641812174 ) ) ;
#6163=CARTESIAN_POINT ( 'NONE',  ( 48.01140435219951996, 95.06049967264874567, 35.83527830041809636 ) ) ;
#6168=CARTESIAN_POINT ( 'NONE',  ( 40.27526882409969744, 69.56518717409400665, 37.97664729208901235 ) ) ;
#6171=CARTESIAN_POINT ( 'NONE',  ( 43.01140435219951996, 10.71049967264875491, 34.21067981925357060 ) ) ;
#6172=CARTESIAN_POINT ( 'NONE',  ( 40.27526882409969033, 134.6651871740940294, 30.44471234641811819 ) ) ;
#6173=CARTESIAN_POINT ( 'NONE',  ( 45.74753988029934249, 157.1651871740940010, 37.97664729208901235 ) ) ;
#6177=EDGE_CURVE ( 'NONE', #17454, #15773, #7803, .T. ) ;
#6181=CARTESIAN_POINT ( 'NONE',  ( 39.92123440845004723, 117.2344580088725792, 38.46393386101376421 ) ) ;
#6182=CARTESIAN_POINT ( 'NONE',  ( 43.01140435219951286, 111.5344580088725905, 39.21067981925356349 ) ) ;
#6183=AXIS2_PLACEMENT_3D ( 'NONE', #10596, #3980, #8731 ) ;
#6184=CARTESIAN_POINT ( 'NONE',  ( 43.01140435219951286, 80.62977050742732388, 29.55568802177586463 ) ) ;
#6185=CARTESIAN_POINT ( 'NONE',  ( 39.42975644700377558, 135.4151871740940010, 36.81289934271958941 ) ) ;
#6186=CARTESIAN_POINT ( 'NONE',  ( 43.01140435219951286, 91.46049967264873715, 39.46799094044489209 ) ) ;
#6190=CARTESIAN_POINT ( 'NONE',  ( 38.58424406990784661, 87.26518717409399528, 35.64915139335016647 ) ) ;
#6193=CARTESIAN_POINT ( 'NONE',  ( 44.55648932407425633, 142.8844580088725991, 29.45539723777780239 ) ) ;
#6195=CARTESIAN_POINT ( 'NONE',  ( 44.37947211624943833, 74.47977050742731819, 30.00020018409699318 ) ) ;
#6203=CARTESIAN_POINT ( 'NONE',  ( 43.80332655382220253, 123.6113394311928317, 39.21067981925355639 ) ) ;
#6204=CARTESIAN_POINT ( 'NONE',  ( 43.01140435219951286, 119.6297705074273097, 29.55568802177586107 ) ) ;
#6205=ORIENTED_EDGE ( 'NONE', *, *, #17394, .F. ) ;
#6206=SHAPE_REPRESENTATION ( 'Material Hold-Down Screw Clamp', ( #12657 ), #2455 ) ;
#6209=CARTESIAN_POINT ( 'NONE',  ( 45.74753988029933538, 124.4297705074273068, 37.97664729208901946 ) ) ;
#6210=CARTESIAN_POINT ( 'NONE',  ( 38.01140435219952707, 72.86049967264874283, 35.83527830041809636 ) ) ;
#6211=CARTESIAN_POINT ( 'NONE',  ( 38.01140435219952707, 65.78445800887257633, 34.21067981925357060 ) ) ;
#6212=EDGE_CURVE ( 'NONE', #13667, #7226, #21179, .T. ) ;
#6215=FACE_OUTER_BOUND ( 'NONE', #2651, .T. ) ;
#6217=LINE ( 'NONE', #1594, #3452 ) ;
#6218=CARTESIAN_POINT ( 'NONE',  ( 48.01140435219951996, 131.0604996726487457, 35.83527830041809636 ) ) ;
#6221=CARTESIAN_POINT ( 'NONE',  ( 47.05648932407426344, 124.5844580088725735, 31.27175355779120025 ) ) ;
#6222=CARTESIAN_POINT ( 'NONE',  ( 41.64333658814960870, 99.97977050742731819, 38.42115945441014446 ) ) ;
#6225=CARTESIAN_POINT ( 'NONE',  ( 38.58424406990786082, 99.11518717409400381, 34.21067981925357060 ) ) ;
#6226=CARTESIAN_POINT ( 'NONE',  ( 38.01140435219952707, 84.86049967264872862, 35.83527830041809636 ) ) ;
#6232=CARTESIAN_POINT ( 'NONE',  ( 43.01140435219951286, 68.62977050742729546, 29.55568802177586107 ) ) ;
#6233=( BOUNDED_CURVE ( )  B_SPLINE_CURVE ( 2, ( #1087, #4380, #4712, #21153, #14630, #17931, #12989, #8036, #1414, #6038, #11112, #11215, #4824 ),
 .UNSPECIFIED., .F., .F. ) 
 B_SPLINE_CURVE_WITH_KNOTS ( ( 3, 2, 2, 2, 2, 2, 3 ),
 ( 0.7426470588235294379, 0.7441176470588235503, 0.7470588235294117752, 0.7500000000000000000, 0.7529411764705882248, 0.7558823529411764497, 0.7573529411764705621 ),
 .UNSPECIFIED. ) 
 CURVE ( )  GEOMETRIC_REPRESENTATION_ITEM ( )  RATIONAL_B_SPLINE_CURVE ( ( 0.9755282581475768211, 0.9755282581475768211, 1.000000000000000000, 0.9510565162951535312, 1.000000000000000000, 0.9510565162951535312, 1.000000000000000000, 0.9510565162951535312, 1.000000000000000000, 0.9510565162951535312, 1.000000000000000000, 0.9755282581475768211, 0.9755282581475768211 ) ) 
 REPRESENTATION_ITEM ( '' )  );
#6234=ORIENTED_EDGE ( 'NONE', *, *, #1158, .F. ) ;
#6237=CARTESIAN_POINT ( 'NONE',  ( 38.58424406990786082, 156.3797705074273097, 34.21067981925357060 ) ) ;
#6240=CARTESIAN_POINT ( 'NONE',  ( 39.92123440845004723, 109.1604996726487542, 38.46393386101376421 ) ) ;
#6241=CARTESIAN_POINT ( 'NONE',  ( 46.59305225739526435, 64.31518717409399244, 36.81289934271958941 ) ) ;
#6242=CARTESIAN_POINT ( 'NONE',  ( 39.92123440845005433, 65.33445800887258770, 29.95742577749336988 ) ) ;
#6244=VECTOR ( 'NONE', #11505, 1000.000000000000000 ) ;
#6245=LINE ( 'NONE', #6357, #17773 ) ;
#6248=CARTESIAN_POINT ( 'NONE',  ( 43.01140435219951286, 152.0344580088725763, 28.95336869806222779 ) ) ;
#6249=CARTESIAN_POINT ( 'NONE',  ( 45.74753988029933538, 136.4297705074273210, 37.97664729208901946 ) ) ;
#6251=CARTESIAN_POINT ( 'NONE',  ( 44.37947211624943833, 127.0151871740939953, 38.42115945441014446 ) ) ;
#6258=CARTESIAN_POINT ( 'NONE',  ( 42.21948215057684450, 120.0373810949690210, 29.21067981925356705 ) ) ;
#6262=CARTESIAN_POINT ( 'NONE',  ( 43.01140435219951286, 83.03445800887257633, 28.95336869806222779 ) ) ;
#6264=CARTESIAN_POINT ( 'NONE',  ( 38.96631938032478359, 136.0104996726487627, 37.14960608071593384 ) ) ;
#6265=CARTESIAN_POINT ( 'NONE',  ( 41.64333658814960870, 98.51518717409399528, 30.00020018409699318 ) ) ;
#6270=CARTESIAN_POINT ( 'NONE',  ( 47.05648932407426344, 64.91049967264873999, 37.14960608071593384 ) ) ;
#6271=CARTESIAN_POINT ( 'NONE',  ( 43.01140435219951286, 127.4604996726487229, 39.21067981925356349 ) ) ;
#6275=CARTESIAN_POINT ( 'NONE',  ( 43.01140435219951286, 116.0344580088725763, 29.21067981925356705 ) ) ;
#6276=CARTESIAN_POINT ( 'NONE',  ( 40.27526882409969033, 156.8297705074272983, 37.97664729208901946 ) ) ;
#6278=DIRECTION ( 'NONE',  ( 0.000000000000000000, 1.000000000000000000, 0.000000000000000000 ) ) ;
#6284=CARTESIAN_POINT ( 'NONE',  ( 47.43856463449117911, 73.46518717409398391, 35.64915139335015937 ) ) ;
#6287=CARTESIAN_POINT ( 'NONE',  ( 43.80332655382220253, 111.6113394311928317, 39.21067981925355639 ) ) ;
#6288=CARTESIAN_POINT ( 'NONE',  ( 43.01140435219951286, 132.8651871740940180, 38.86567161673127657 ) ) ;
#6291=ORIENTED_EDGE ( 'NONE', *, *, #8119, .F. ) ;
#6293=VERTEX_POINT ( 'NONE', #8348 ) ;
#6297=CARTESIAN_POINT ( 'NONE',  ( 47.43856463449117200, 74.02977050742730114, 32.77220824515698183 ) ) ;
#6298=CARTESIAN_POINT ( 'NONE',  ( 39.42975644700377558, 129.4151871740940010, 36.81289934271958941 ) ) ;
#6300=( BOUNDED_CURVE ( )  B_SPLINE_CURVE ( 2, ( #16711, #18145, #21580, #1620, #11752, #6471, #1733, #8468, #8352, #3053, #8243, #21800, #9896 ),
 .UNSPECIFIED., .F., .F. ) 
 B_SPLINE_CURVE_WITH_KNOTS ( ( 3, 2, 2, 2, 2, 2, 3 ),
 ( 0.4632352941176470784, 0.4647058823529411908, 0.4676470588235294157, 0.4705882352941176405, 0.4735294117647058654, 0.4764705882352940902, 0.4779411764705882582 ),
 .UNSPECIFIED. ) 
 CURVE ( )  GEOMETRIC_REPRESENTATION_ITEM ( )  RATIONAL_B_SPLINE_CURVE ( ( 0.9755282581475768211, 0.9755282581475768211, 1.000000000000000000, 0.9510565162951535312, 1.000000000000000000, 0.9510565162951535312, 1.000000000000000000, 0.9510565162951535312, 1.000000000000000000, 0.9510565162951535312, 1.000000000000000000, 0.9755282581475763770, 0.9755282581475768211 ) ) 
 REPRESENTATION_ITEM ( '' )  );
#6301=CARTESIAN_POINT ( 'NONE',  ( 46.10157429594899270, 95.66049967264871157, 29.95742577749337343 ) ) ;
#6303=CARTESIAN_POINT ( 'NONE',  ( 43.01140435219951286, 59.96049967264874425, 29.21067981925356705 ) ) ;
#6305=CARTESIAN_POINT ( 'NONE',  ( 45.74753988029933538, 91.16518717409397254, 37.97664729208901946 ) ) ;
#6308=CARTESIAN_POINT ( 'NONE',  ( 46.10157429594899270, 71.66049967264873999, 29.95742577749336988 ) ) ;
#6311=CARTESIAN_POINT ( 'NONE',  ( 41.64333658814960870, 75.97977050742731819, 38.42115945441014446 ) ) ;
#6316=CARTESIAN_POINT ( 'NONE',  ( 41.64333658814960870, 158.5151871740940237, 30.00020018409699318 ) ) ;
#6319=CARTESIAN_POINT ( 'NONE',  ( 45.74753988029934249, 124.4297705074273210, 37.97664729208901235 ) ) ;
#6321=EDGE_LOOP ( 'NONE', ( #2363, #3372, #15985, #5189 ) ) ;
#6322=CARTESIAN_POINT ( 'NONE',  ( 47.43856463449118621, 118.8797705074273239, 34.21067981925357060 ) ) ;
#6323=CARTESIAN_POINT ( 'NONE',  ( 43.01140435219951286, 130.4604996726487229, 39.21067981925356349 ) ) ;
#6324=CARTESIAN_POINT ( 'NONE',  ( 40.27526882409969033, 89.92977050742730682, 30.44471234641811819 ) ) ;
#6325=CARTESIAN_POINT ( 'NONE',  ( 48.01140435219951996, 67.43445800887256780, 32.58608133808903773 ) ) ;
#6326=PRODUCT_DEFINITION_FORMATION_WITH_SPECIFIED_SOURCE ( 'ANY', '', #6562, .NOT_KNOWN. ) ;
#6328=DIRECTION ( 'NONE',  ( 0.000000000000000000, 1.000000000000000000, 0.000000000000000000 ) ) ;
#6332=CARTESIAN_POINT ( 'NONE',  ( 38.96631938032478359, 102.4104996726487400, 31.27175355779120025 ) ) ;
#6335=CARTESIAN_POINT ( 'NONE',  ( 41.46631938032478359, 119.1844580088725962, 29.45539723777780239 ) ) ;
#6336=CARTESIAN_POINT ( 'NONE',  ( 46.59305225739526435, 103.5797705074273267, 36.81289934271958941 ) ) ;
#6339=CARTESIAN_POINT ( 'NONE',  ( 41.64333658814960870, 87.71518717409399812, 38.42115945441014446 ) ) ;
#6340=DIRECTION ( 'NONE',  ( 0.000000000000000000, 1.000000000000000000, 0.000000000000000000 ) ) ;
#6342=FACE_OUTER_BOUND ( 'NONE', #21079, .T. ) ;
#6345=AXIS2_PLACEMENT_3D ( 'NONE', #6171, #4631, #11458 ) ;
#6346=CARTESIAN_POINT ( 'NONE',  ( 44.37947211624943833, 71.47977050742731819, 30.00020018409699318 ) ) ;
#6348=ORIENTED_EDGE ( 'NONE', *, *, #6001, .T. ) ;
#6349=CARTESIAN_POINT ( 'NONE',  ( 43.01140435219951286, 155.6297705074273381, 29.55568802177586463 ) ) ;
#6350=EDGE_CURVE ( 'NONE', #17423, #19975, #18376, .T. ) ;
#6353=CARTESIAN_POINT ( 'NONE',  ( 46.10157429594899270, 106.7604996726487201, 38.46393386101376421 ) ) ;
#6354=CARTESIAN_POINT ( 'NONE',  ( 40.27526882409969033, 72.56518717409399244, 37.97664729208901946 ) ) ;
#6357=CARTESIAN_POINT ( 'NONE',  ( 43.01140435219951996, 10.71049967264875491, 29.21067981925357060 ) ) ;
#6361=CARTESIAN_POINT ( 'NONE',  ( 39.92123440845004723, 152.3344580088725593, 29.95742577749337343 ) ) ;
#6362=CARTESIAN_POINT ( 'NONE',  ( 47.43856463449117200, 130.7297705074273040, 35.64915139335016647 ) ) ;
#6364=CARTESIAN_POINT ( 'NONE',  ( 46.59305225739526435, 115.9151871740940010, 31.60846029578754468 ) ) ;
#6366=CARTESIAN_POINT ( 'NONE',  ( 38.01140435219952707, 150.7104996726487514, 34.21067981925357060 ) ) ;
#6370=DIRECTION ( 'NONE',  ( 0.000000000000000000, 1.000000000000000000, 0.000000000000000000 ) ) ;
#6374=CARTESIAN_POINT ( 'NONE',  ( 43.01140435219951286, 80.03445800887256212, 28.95336869806222779 ) ) ;
#6376=CARTESIAN_POINT ( 'NONE',  ( 38.01140435219952707, 138.7104996726487514, 34.21067981925357060 ) ) ;
#6377=CARTESIAN_POINT ( 'NONE',  ( 38.58424406990784661, 92.96518717409401233, 32.77220824515698183 ) ) ;
#6386=CARTESIAN_POINT ( 'NONE',  ( 43.01140435219951996, 10.71049967264875491, 39.21067981925356349 ) ) ;
#6388=CARTESIAN_POINT ( 'NONE',  ( 38.58424406990786082, 60.11518717409400381, 34.21067981925357060 ) ) ;
#6389=CARTESIAN_POINT ( 'NONE',  ( 39.92123440845005433, 153.2344580088725934, 38.46393386101375711 ) ) ;
#6395=CARTESIAN_POINT ( 'NONE',  ( 45.74753988029934249, 70.16518717409397254, 37.97664729208901235 ) ) ;
#6399=CARTESIAN_POINT ( 'NONE',  ( 46.59305225739526435, 130.3151871740940067, 36.81289934271958941 ) ) ;
#6407=CARTESIAN_POINT ( 'NONE',  ( 43.01140435219951286, 110.0344580088725621, 28.95336869806222779 ) ) ;
#6410=ADVANCED_FACE ( 'NONE', ( #18700 ), #18369, .T. ) ;
#6411=CARTESIAN_POINT ( 'NONE',  ( 39.42975644700377558, 63.07977050742731251, 31.60846029578754468 ) ) ;
#6412=CARTESIAN_POINT ( 'NONE',  ( 40.27526882409969033, 129.5651871740940067, 37.97664729208901946 ) ) ;
#6414=CARTESIAN_POINT ( 'NONE',  ( 44.55648932407425633, 83.81049967264874567, 29.45539723777780239 ) ) ;
#6418=CARTESIAN_POINT ( 'NONE',  ( 38.58424406990784661, 89.96518717409399812, 32.77220824515698183 ) ) ;
#6422=VERTEX_POINT ( 'NONE', #8674 ) ;
#6423=CARTESIAN_POINT ( 'NONE',  ( 40.27526882409969033, 68.92977050742733525, 30.44471234641811819 ) ) ;
#6430=CARTESIAN_POINT ( 'NONE',  ( 43.01140435219951286, 125.6297705074273381, 29.55568802177586107 ) ) ;
#6431=VERTEX_POINT ( 'NONE', #8569 ) ;
#6432=CARTESIAN_POINT ( 'NONE',  ( 43.01140435219951996, 158.0344580088725763, 29.21067981925357060 ) ) ;
#6433=( BOUNDED_CURVE ( )  B_SPLINE_CURVE ( 2, ( #13972, #15427, #2190, #8921, #17385, #20710, #7053, #322, #20602, #8708, #13544, #18622, #12103 ),
 .UNSPECIFIED., .F., .F. ) 
 B_SPLINE_CURVE_WITH_KNOTS ( ( 3, 2, 2, 2, 2, 2, 3 ),
 ( 0.1544117647058823595, 0.1558823529411764719, 0.1588235294117646967, 0.1617647058823529493, 0.1647058823529411742, 0.1676470588235293990, 0.1691176470588235115 ),
 .UNSPECIFIED. ) 
 CURVE ( )  GEOMETRIC_REPRESENTATION_ITEM ( )  RATIONAL_B_SPLINE_CURVE ( ( 0.9755282581475768211, 0.9755282581475768211, 1.000000000000000000, 0.9510565162951535312, 1.000000000000000000, 0.9510565162951535312, 1.000000000000000000, 0.9510565162951535312, 1.000000000000000000, 0.9510565162951535312, 1.000000000000000000, 0.9755282581475769321, 0.9755282581475765991 ) ) 
 REPRESENTATION_ITEM ( '' )  );
#6435=CARTESIAN_POINT ( 'NONE',  ( 40.27526882409969033, 119.9297705074272926, 30.44471234641811819 ) ) ;
#6436=CARTESIAN_POINT ( 'NONE',  ( 38.01140435219952707, 72.56049967264874567, 32.58608133808903773 ) ) ;
#6438=CARTESIAN_POINT ( 'NONE',  ( 38.58424406990786082, 150.1151871740939896, 34.21067981925357060 ) ) ;
#6440=CARTESIAN_POINT ( 'NONE',  ( 38.01140435219952707, 83.93445800887256780, 35.83527830041809636 ) ) ;
#6441=CARTESIAN_POINT ( 'NONE',  ( 39.92123440845005433, 96.26049967264876273, 29.95742577749336988 ) ) ;
#6443=LINE ( 'NONE', #4785, #6244 ) ;
#6444=CARTESIAN_POINT ( 'NONE',  ( 46.10157429594899270, 130.7604996726487343, 38.46393386101375711 ) ) ;
#6447=CARTESIAN_POINT ( 'NONE',  ( 46.10157429594899270, 127.7344580088725792, 29.95742577749337343 ) ) ;
#6448=CARTESIAN_POINT ( 'NONE',  ( 44.37947211624943833, 106.2797705074273154, 38.42115945441014446 ) ) ;
#6451=CARTESIAN_POINT ( 'NONE',  ( 41.64333658814960870, 84.71518717409399812, 38.42115945441014446 ) ) ;
#6452=CARTESIAN_POINT ( 'NONE',  ( 43.01140435219951286, 89.96049967264873715, 29.21067981925356705 ) ) ;
#6456=CARTESIAN_POINT ( 'NONE',  ( 39.42975644700377558, 144.0797705074273267, 31.60846029578754468 ) ) ;
#6458=CARTESIAN_POINT ( 'NONE',  ( 41.64333658814960870, 71.77977050742731535, 30.00020018409699318 ) ) ;
#6461=CARTESIAN_POINT ( 'NONE',  ( 40.27526882409969033, 147.8297705074272983, 37.97664729208901946 ) ) ;
#6464=CARTESIAN_POINT ( 'NONE',  ( 38.01140435219951996, 108.5604996726487599, 32.58608133808903773 ) ) ;
#6465=CARTESIAN_POINT ( 'NONE',  ( 40.27526882409969033, 71.66518717409400097, 30.44471234641811819 ) ) ;
#6466=CARTESIAN_POINT ( 'NONE',  ( 38.01140435219952707, 95.63445800887255643, 32.58608133808903773 ) ) ;
#6468=CARTESIAN_POINT ( 'NONE',  ( 39.92123440845005433, 156.2344580088725934, 38.46393386101375711 ) ) ;
#6471=CARTESIAN_POINT ( 'NONE',  ( 38.01140435219952707, 111.8604996726487428, 35.83527830041809636 ) ) ;
#6472=CARTESIAN_POINT ( 'NONE',  ( 48.01140435219951996, 151.1344580088726275, 35.83527830041810347 ) ) ;
#6473=CARTESIAN_POINT ( 'NONE',  ( 40.27526882409969033, 131.9297705074273210, 30.44471234641811819 ) ) ;
#6475=CARTESIAN_POINT ( 'NONE',  ( 38.58424406990785371, 116.9651871740939839, 32.77220824515697473 ) ) ;
#6478=CARTESIAN_POINT ( 'NONE',  ( 43.01140435219951996, 10.71049967264875491, 29.21067981925357060 ) ) ;
#6483=CARTESIAN_POINT ( 'NONE',  ( 41.64333658814960870, 98.77977050742731535, 30.00020018409699318 ) ) ;
#6488=CARTESIAN_POINT ( 'NONE',  ( 41.46631938032478359, 81.38445800887257064, 38.96596240072933170 ) ) ;
#6490=CARTESIAN_POINT ( 'NONE',  ( 43.01140435219951286, 143.9604996726487514, 28.95336869806222779 ) ) ;
#6491=CARTESIAN_POINT ( 'NONE',  ( 38.58424406990784661, 99.26518717409396686, 35.64915139335016647 ) ) ;
#6500=CARTESIAN_POINT ( 'NONE',  ( 38.01140435219952707, 147.8604996726487570, 35.83527830041809636 ) ) ;
#6501=CARTESIAN_POINT ( 'NONE',  ( 39.92123440845005433, 79.16049967264873999, 38.46393386101375711 ) ) ;
#6502=CARTESIAN_POINT ( 'NONE',  ( 47.43856463449118621, 61.61518717409400381, 34.21067981925357060 ) ) ;
#6506=CARTESIAN_POINT ( 'NONE',  ( 46.59305225739526435, 145.9151871740940294, 31.60846029578754468 ) ) ;
#6509=VERTEX_POINT ( 'NONE', #13939 ) ;
#6510=CARTESIAN_POINT ( 'NONE',  ( 39.92123440845005433, 78.23445800887257917, 38.46393386101375711 ) ) ;
#6513=CARTESIAN_POINT ( 'NONE',  ( 39.42975644700377558, 129.4151871740940010, 36.81289934271958941 ) ) ;
#6516=ORIENTED_EDGE ( 'NONE', *, *, #18362, .F. ) ;
#6518=CARTESIAN_POINT ( 'NONE',  ( 43.01140435219951286, 137.0344580088725763, 29.21067981925356705 ) ) ;
#6519=ORIENTED_EDGE ( 'NONE', *, *, #1610, .F. ) ;
#6520=EDGE_CURVE ( 'NONE', #13207, #20212, #1607, .T. ) ;
#6521=CARTESIAN_POINT ( 'NONE',  ( 46.10157429594899270, 106.7344580088725507, 29.95742577749337343 ) ) ;
#6523=CARTESIAN_POINT ( 'NONE',  ( 47.43856463449117200, 68.02977050742731535, 32.77220824515698183 ) ) ;
#6524=CARTESIAN_POINT ( 'NONE',  ( 47.43856463449118621, 121.6151871740940038, 34.21067981925357060 ) ) ;
#6527=CARTESIAN_POINT ( 'NONE',  ( 47.05648932407426344, 82.91049967264873999, 37.14960608071593384 ) ) ;
#6530=CARTESIAN_POINT ( 'NONE',  ( 42.21948215057684450, 145.3836182503284817, 39.21067981925355639 ) ) ;
#6532=CARTESIAN_POINT ( 'NONE',  ( 44.37947211624943833, 92.21518717409401233, 30.00020018409699318 ) ) ;
#6535=ORIENTED_EDGE ( 'NONE', *, *, #2025, .F. ) ;
#6536=CARTESIAN_POINT ( 'NONE',  ( 43.01140435219951286, 70.12977050742732388, 38.86567161673127657 ) ) ;
#6541=CARTESIAN_POINT ( 'NONE',  ( 44.37947211624943833, 152.2151871740940123, 30.00020018409699318 ) ) ;
#6542=CARTESIAN_POINT ( 'NONE',  ( 45.74753988029934249, 119.3297705074273267, 30.44471234641812174 ) ) ;
#6549=CARTESIAN_POINT ( 'NONE',  ( 39.42975644700377558, 120.6797705074273210, 36.81289934271958941 ) ) ;
#6551=CARTESIAN_POINT ( 'NONE',  ( 47.43856463449118621, 154.6151871740940180, 34.21067981925357060 ) ) ;
#6562=PRODUCT ( 'Material Hold-Down Screw Clamp', 'Material Hold-Down Screw Clamp', '', ( #14484 ) ) ;
#6564=CARTESIAN_POINT ( 'NONE',  ( 43.01140435219951286, 126.5344580088725763, 39.46799094044489209 ) ) ;
#6566=CARTESIAN_POINT ( 'NONE',  ( 43.01140435219951286, 97.12977050742732388, 38.86567161673127657 ) ) ;
#6569=CARTESIAN_POINT ( 'NONE',  ( 45.74753988029934249, 91.16518717409398675, 37.97664729208901235 ) ) ;
#6570=CARTESIAN_POINT ( 'NONE',  ( 38.96631938032478359, 84.41049967264873999, 31.27175355779120025 ) ) ;
#6571=ORIENTED_EDGE ( 'NONE', *, *, #2773, .F. ) ;
#6575=( BOUNDED_CURVE ( )  B_SPLINE_CURVE ( 2, ( #19958, #4619, #10144, #6501, #20074, #11340, #9925, #19838, #16739, #14865, #11671, #1651, #18293 ),
 .UNSPECIFIED., .F., .F. ) 
 B_SPLINE_CURVE_WITH_KNOTS ( ( 3, 2, 2, 2, 2, 2, 3 ),
 ( 0.7867647058823529216, 0.7882352941176470340, 0.7911764705882352589, 0.7941176470588234837, 0.7970588235294118196, 0.8000000000000000444, 0.8014705882352941568 ),
 .UNSPECIFIED. ) 
 CURVE ( )  GEOMETRIC_REPRESENTATION_ITEM ( )  RATIONAL_B_SPLINE_CURVE ( ( 0.9755282581475768211, 0.9755282581475768211, 1.000000000000000000, 0.9510565162951535312, 1.000000000000000000, 0.9510565162951535312, 1.000000000000000000, 0.9510565162951535312, 1.000000000000000000, 0.9510565162951535312, 1.000000000000000000, 0.9755282581475768211, 0.9755282581475768211 ) ) 
 REPRESENTATION_ITEM ( '' )  );
#6577=CARTESIAN_POINT ( 'NONE',  ( 39.42975644700377558, 69.07977050742732672, 31.60846029578754468 ) ) ;
#6580=CARTESIAN_POINT ( 'NONE',  ( 47.43856463449117200, 143.0297705074273154, 32.77220824515698183 ) ) ;
#6581=CARTESIAN_POINT ( 'NONE',  ( 47.43856463449117200, 98.02977050742731535, 32.77220824515698183 ) ) ;
#6584=CARTESIAN_POINT ( 'NONE',  ( 38.01140435219951996, 108.8604996726487144, 35.83527830041810347 ) ) ;
#6585=CARTESIAN_POINT ( 'NONE',  ( 39.42975644700377558, 71.81518717409400665, 31.60846029578754468 ) ) ;
#6592=CARTESIAN_POINT ( 'NONE',  ( 38.96631938032478359, 153.0844580088725877, 37.14960608071593384 ) ) ;
#6593=CARTESIAN_POINT ( 'NONE',  ( 45.74753988029933538, 125.3297705074273125, 30.44471234641811819 ) ) ;
#6595=CARTESIAN_POINT ( 'NONE',  ( 46.59305225739526435, 118.9151871740940010, 31.60846029578754468 ) ) ;
#6596=EDGE_CURVE ( 'NONE', #16002, #20743, #4558, .T. ) ;
#6598=CARTESIAN_POINT ( 'NONE',  ( 47.05648932407426344, 64.91049967264873999, 37.14960608071593384 ) ) ;
#6602=CARTESIAN_POINT ( 'NONE',  ( 46.59305225739526435, 95.17977050742732104, 31.60846029578754468 ) ) ;
#6604=VECTOR ( 'NONE', #12703, 1000.000000000000000 ) ;
#6605=CARTESIAN_POINT ( 'NONE',  ( 44.55648932407425633, 145.8844580088725991, 29.45539723777780239 ) ) ;
#6607=CARTESIAN_POINT ( 'NONE',  ( 47.05648932407426344, 81.98445800887257917, 37.14960608071593384 ) ) ;
#6612=CARTESIAN_POINT ( 'NONE',  ( 48.01140435219951996, 140.2104996726487514, 34.21067981925357060 ) ) ;
#6613=CARTESIAN_POINT ( 'NONE',  ( 46.59305225739526435, 97.91518717409400097, 31.60846029578754468 ) ) ;
#6618=CARTESIAN_POINT ( 'NONE',  ( 44.55648932407425633, 70.88445800887258486, 29.45539723777780239 ) ) ;
#6620=CARTESIAN_POINT ( 'NONE',  ( 43.01140435219951996, 148.4604996726487798, 39.21067981925356349 ) ) ;
#6621=CARTESIAN_POINT ( 'NONE',  ( 43.01140435219951286, 114.5344580088725621, 39.21067981925356349 ) ) ;
#6622=CARTESIAN_POINT ( 'NONE',  ( 41.64333658814960870, 158.7797705074273438, 30.00020018409699318 ) ) ;
#6623=CYLINDRICAL_SURFACE ( 'NONE', #20008, 4.999999999999997335 ) ;
#6625=CARTESIAN_POINT ( 'NONE',  ( 43.01140435219951286, 149.3651871740939612, 29.55568802177586107 ) ) ;
#6631=CARTESIAN_POINT ( 'NONE',  ( 47.43856463449118621, 64.61518717409398960, 34.21067981925357060 ) ) ;
#6637=CARTESIAN_POINT ( 'NONE',  ( 45.74753988029933538, 122.0651871740940209, 30.44471234641811819 ) ) ;
#6638=EDGE_CURVE ( 'NONE', #20247, #7422, #11313, .T. ) ;
#6644=CARTESIAN_POINT ( 'NONE',  ( 38.01140435219951996, 110.6344580088725849, 32.58608133808903773 ) ) ;
#6645=CARTESIAN_POINT ( 'NONE',  ( 47.05648932407426344, 115.9104996726487400, 37.14960608071593384 ) ) ;
#6646=CARTESIAN_POINT ( 'NONE',  ( 45.74753988029933538, 67.42977050742730682, 37.97664729208901946 ) ) ;
#6647=CARTESIAN_POINT ( 'NONE',  ( 38.58424406990786082, 126.1151871740940038, 34.21067981925357060 ) ) ;
#6649=CARTESIAN_POINT ( 'NONE',  ( 47.05648932407426344, 77.51049967264873430, 31.27175355779120025 ) ) ;
#6652=CARTESIAN_POINT ( 'NONE',  ( 41.46631938032478359, 144.1104996726487570, 29.45539723777780239 ) ) ;
#6653=CARTESIAN_POINT ( 'NONE',  ( 43.01140435219951286, 137.9604996726487514, 29.21067981925356705 ) ) ;
#6654=CARTESIAN_POINT ( 'NONE',  ( 40.27526882409969033, 90.56518717409400665, 37.97664729208901946 ) ) ;
#6659=CARTESIAN_POINT ( 'NONE',  ( 40.27526882409969033, 69.82977050742729830, 37.97664729208901946 ) ) ;
#6664=EDGE_LOOP ( 'NONE', ( #7979, #11135, #19992, #14094 ) ) ;
#6665=CARTESIAN_POINT ( 'NONE',  ( 38.58424406990784661, 156.2651871740939953, 35.64915139335016647 ) ) ;
#6667=CARTESIAN_POINT ( 'NONE',  ( 44.37947211624943833, 112.2797705074273296, 38.42115945441014446 ) ) ;
#6669=ORIENTED_EDGE ( 'NONE', *, *, #1261, .T. ) ;
#6672=CARTESIAN_POINT ( 'NONE',  ( 43.01140435219951286, 119.6297705074272955, 29.55568802177586463 ) ) ;
#6673=CARTESIAN_POINT ( 'NONE',  ( 42.21948215057684450, 129.4575765865523067, 39.21067981925355639 ) ) ;
#6674=CARTESIAN_POINT ( 'NONE',  ( 47.43856463449117200, 151.4651871740939839, 35.64915139335016647 ) ) ;
#6676=LINE ( 'NONE', #17084, #2009 ) ;
#6682=CARTESIAN_POINT ( 'NONE',  ( 44.55648932407425633, 92.81049967264874567, 29.45539723777780239 ) ) ;
#6685=CARTESIAN_POINT ( 'NONE',  ( 38.58424406990786082, 93.37977050742732388, 34.21067981925357060 ) ) ;
#6689=CARTESIAN_POINT ( 'NONE',  ( 47.43856463449118621, 88.61518717409400381, 34.21067981925357060 ) ) ;
#6694=CARTESIAN_POINT ( 'NONE',  ( 45.74753988029934249, 139.4297705074272642, 37.97664729208901235 ) ) ;
#6698=CARTESIAN_POINT ( 'NONE',  ( 47.43856463449118621, 142.8797705074273381, 34.21067981925357060 ) ) ;
#6699=VECTOR ( 'NONE', #7020, 1000.000000000000000 ) ;
#6700=CARTESIAN_POINT ( 'NONE',  ( 45.74753988029933538, 95.32977050742729830, 30.44471234641811819 ) ) ;
#6701=CARTESIAN_POINT ( 'NONE',  ( 44.55648932407425633, 151.6104996726487570, 38.96596240072933170 ) ) ;
#6703=CARTESIAN_POINT ( 'NONE',  ( 48.01140435219951996, 110.0604996726487315, 35.83527830041810347 ) ) ;
#6709=CARTESIAN_POINT ( 'NONE',  ( 47.43856463449117200, 118.7297705074272898, 35.64915139335016647 ) ) ;
#6710=( BOUNDED_CURVE ( )  B_SPLINE_CURVE ( 2, ( #3174, #11544, #11319, #16492, #20052, #14952, #4599, #21478, #18270, #2948, #1084, #16283, #1411 ),
 .UNSPECIFIED., .F., .F. ) 
 B_SPLINE_CURVE_WITH_KNOTS ( ( 3, 2, 2, 2, 2, 2, 3 ),
 ( 0.1838235294117647189, 0.1852941176470588314, 0.1882352941176470562, 0.1911764705882352811, 0.1941176470588235337, 0.1970588235294117585, 0.1985294117647058987 ),
 .UNSPECIFIED. ) 
 CURVE ( )  GEOMETRIC_REPRESENTATION_ITEM ( )  RATIONAL_B_SPLINE_CURVE ( ( 0.9755282581475768211, 0.9755282581475770431, 1.000000000000000000, 0.9510565162951535312, 1.000000000000000000, 0.9510565162951535312, 1.000000000000000000, 0.9510565162951535312, 1.000000000000000000, 0.9510565162951535312, 1.000000000000000000, 0.9755282581475765991, 0.9755282581475768211 ) ) 
 REPRESENTATION_ITEM ( '' )  );
#6712=CARTESIAN_POINT ( 'NONE',  ( 46.10157429594899270, 95.66049967264872578, 29.95742577749336988 ) ) ;
#6713=CARTESIAN_POINT ( 'NONE',  ( 45.74753988029934249, 112.1651871740939868, 37.97664729208901235 ) ) ;
#6715=COLOUR_RGB ( '', 0.66274510, 0.83137255, 0.94901961) ;
#6720=CARTESIAN_POINT ( 'NONE',  ( 47.43856463449117911, 86.02977050742731535, 32.77220824515697473 ) ) ;
#6724=CARTESIAN_POINT ( 'NONE',  ( 39.92123440845004723, 74.33445800887255928, 29.95742577749337343 ) ) ;
#6727=CARTESIAN_POINT ( 'NONE',  ( 38.01140435219951996, 138.5604996726487457, 32.58608133808903773 ) ) ;
#6728=CARTESIAN_POINT ( 'NONE',  ( 41.64333658814960870, 95.51518717409400949, 30.00020018409699318 ) ) ;
#6733=CARTESIAN_POINT ( 'NONE',  ( 48.01140435219951996, 70.43445800887256780, 32.58608133808903773 ) ) ;
#6736=CARTESIAN_POINT ( 'NONE',  ( 47.05648932407426344, 79.91049967264873999, 37.14960608071593384 ) ) ;
#6737=CARTESIAN_POINT ( 'NONE',  ( 39.42975644700377558, 147.0797705074273267, 31.60846029578754468 ) ) ;
#6740=CARTESIAN_POINT ( 'NONE',  ( 45.74753988029934249, 149.0651871740940067, 30.44471234641812174 ) ) ;
#6744=CARTESIAN_POINT ( 'NONE',  ( 40.27526882409969744, 62.66518717409400097, 30.44471234641812174 ) ) ;
#6747=CARTESIAN_POINT ( 'NONE',  ( 38.96631938032478359, 135.0844580088725877, 37.14960608071593384 ) ) ;
#6748=CARTESIAN_POINT ( 'NONE',  ( 41.64333658814960870, 120.7151871740939981, 38.42115945441014446 ) ) ;
#6749=ORIENTED_EDGE ( 'NONE', *, *, #88, .F. ) ;
#6751=CARTESIAN_POINT ( 'NONE',  ( 43.01140435219951286, 135.5344580088725763, 39.21067981925356349 ) ) ;
#6753=CARTESIAN_POINT ( 'NONE',  ( 38.96631938032478359, 111.0844580088725735, 37.14960608071593384 ) ) ;
#6755=CARTESIAN_POINT ( 'NONE',  ( 43.01140435219951286, 64.12977050742730967, 38.86567161673127657 ) ) ;
#6756=CARTESIAN_POINT ( 'NONE',  ( 46.59305225739526435, 130.3151871740940067, 36.81289934271958941 ) ) ;
#6758=CARTESIAN_POINT ( 'NONE',  ( 48.01140435219951996, 86.06049967264874567, 35.83527830041810347 ) ) ;
#6762=CARTESIAN_POINT ( 'NONE',  ( 38.58424406990786082, 78.11518717409400381, 34.21067981925357060 ) ) ;
#6766=CARTESIAN_POINT ( 'NONE',  ( 45.74753988029933538, 67.42977050742730682, 37.97664729208901946 ) ) ;
#6770=EDGE_LOOP ( 'NONE', ( #13574, #16129, #16912, #9618 ) ) ;
#6773=CARTESIAN_POINT ( 'NONE',  ( 47.43856463449117200, 157.4651871740940123, 35.64915139335016647 ) ) ;
#6776=CARTESIAN_POINT ( 'NONE',  ( 44.37947211624943833, 110.4797705074273324, 30.00020018409699318 ) ) ;
#6777=CARTESIAN_POINT ( 'NONE',  ( 43.80332655382220253, 153.6113394311928744, 39.21067981925355639 ) ) ;
#6781=CARTESIAN_POINT ( 'NONE',  ( 47.43856463449118621, 115.8797705074273097, 34.21067981925357060 ) ) ;
#6783=CARTESIAN_POINT ( 'NONE',  ( 41.64333658814960870, 155.5151871740940237, 30.00020018409699318 ) ) ;
#6792=CARTESIAN_POINT ( 'NONE',  ( 48.01140435219951996, 77.21049967264873715, 34.21067981925357060 ) ) ;
#6794=CARTESIAN_POINT ( 'NONE',  ( 38.58424406990784661, 90.22977050742731819, 32.77220824515698183 ) ) ;
#6797=CARTESIAN_POINT ( 'NONE',  ( 38.58424406990785371, 86.96518717409398391, 32.77220824515697473 ) ) ;
#6803=CARTESIAN_POINT ( 'NONE',  ( 39.92123440845005433, 119.3344580088725735, 29.95742577749336988 ) ) ;
#6805=CARTESIAN_POINT ( 'NONE',  ( 41.64333658814960870, 149.7797705074273154, 30.00020018409699318 ) ) ;
#6807=CARTESIAN_POINT ( 'NONE',  ( 43.01140435219951286, 98.62977050742730967, 29.55568802177586463 ) ) ;
#6808=CARTESIAN_POINT ( 'NONE',  ( 38.96631938032478359, 141.4104996726487400, 31.27175355779120025 ) ) ;
#6816=CARTESIAN_POINT ( 'NONE',  ( 48.01140435219951996, 142.4344580088725820, 32.58608133808903773 ) ) ;
#6817=CARTESIAN_POINT ( 'NONE',  ( 38.58424406990784661, 120.5297705074273154, 35.64915139335016647 ) ) ;
#6819=CARTESIAN_POINT ( 'NONE',  ( 38.58424406990785371, 119.9651871740939839, 32.77220824515697473 ) ) ;
#6823=EDGE_CURVE ( 'NONE', #6422, #16834, #15124, .T. ) ;
#6824=CARTESIAN_POINT ( 'NONE',  ( 47.43856463449118621, 82.87977050742730967, 34.21067981925357060 ) ) ;
#6826=ADVANCED_FACE ( 'NONE', ( #6215 ), #2915, .T. ) ;
#6827=CARTESIAN_POINT ( 'NONE',  ( 43.01140435219951996, 2.710499672648754466, 34.21067981925357060 ) ) ;
#6828=CARTESIAN_POINT ( 'NONE',  ( 41.46631938032478359, 75.38445800887258486, 38.96596240072933170 ) ) ;
#6830=CARTESIAN_POINT ( 'NONE',  ( 38.96631938032478359, 129.4104996726487684, 31.27175355779120025 ) ) ;
#6831=CARTESIAN_POINT ( 'NONE',  ( 40.27526882409969033, 83.66518717409398675, 30.44471234641811819 ) ) ;
#6833=( BOUNDED_SURFACE ( )  B_SPLINE_SURFACE ( 1, 2, ( 
 ( #9637, #16337, #7980, #14687, #6316, #20109, #8635, #4999, #18332, #14902, #15245, #6773, #18660, #248, #1801, #18554, #11930, #1469, #16554, #6665, #6986, #13689, #5320, #1900, #15356, #20423, #13481, #18767, #13372, #11709, #143, #15016, #8533, #3232, #21755, #3343, #12034, #16992, #3563, #18445, #3460, #10288, #20213, #8420, #5106, #9965, #6541, #19999, #16780, #10071, #9852, #20318, #6874, #15130, #21650, #8201, #1691, #13581, #13262, #11822, #33, #5217, #10184, #4883, #11602, #16668, #1579, #8308, #16884, #3993, #5521, #679, #5419, #17421, #18869, #20639, #10609, #5633, #3777, #10506, #17202, #788, #12251, #2117, #17527, #15662, #2014, #10398, #17314, #12357, #18982, #15560, #19198, #5849, #12136, #9177, #8854, #7416, #15874, #2437, #7310, #12579, #7196, #3884, #9066, #464, #2327, #13900, #2225, #8956, #7523, #10828, #12467, #565, #19094, #4095, #14011, #20744, #10718, #15774, #362, #13794, #14116, #20854, #5743, #14224, #20964, #3668, #15462, #17098, #8745, #7090, #20532, #14552, #2648, #14659, #19515, #16311, #2545, #7632, #17964, #2981, #18074, #19629, #21177, #1222, #21076, #11244, #12684, #14443, #4407, #21294, #19407, #4305, #11030, #16420, #6068, #17743, #11351, #9505, #17638, #4202, #11139, #6172, #12795, #9390, #13019, #21514, #5958, #9719, #16096, #7955, #1006, #1331, #17854, #6288, #19739, #2765, #8064, #893, #10930, #15983, #14771, #4522, #16202, #1114, #21401, #7849, #12906, #2869, #9613, #7742, #6399, #4632, #19304, #9282, #14336, #4740, #6513, #11576, #13556, #1772, #16752, #20291, #14878, #13127, #3206, #1553, #11905, #8284, #21623, #18188, #18527, #10048, #118, #3538, #5082, #7, #15218, #11459, #19849, #9937, #10263, #16965, #8608, #5187, #8395, #18304, #8506, #13348, #10157, #3096, #1444, #11796, #18634, #1877, #13455, #14984, #16858, #13234, #3435, #19972, #21730, #20085, #15103, #4857, #16643, #6637, #15329, #4972, #11684, #221, #3319, #9827, #16525, #18421, #6748, #1661, #20189, #6849, #8173, #15436, #12444, #7063, #10692, #13767, #19171, #13875, #15752, #655, #12226, #5720, #10371, #13665, #3644, #2414, #7284, #2094, #10585, #17398, #442, #20614, #543, #13984, #5396, #9153, #14092, #20721, #9042, #17288, #20398, #335, #12114, #7392, #2301, #2202, #20828, #8718, #6957, #18845, #17181, #4071, #8828, #20509, #12006, #12331, #3860, #10800, #17504, #5606, #15638, #15851, #5293, #18741, #3752, #17072, #1985, #10480, #15536, #7172, #5498, #8932, #18958, #19067, #3969, #2738, #7606, #11113, #17612, #14308, #4277, #18251, #12878, #14525, #21051, #6040, #21265, #14418, #9363, #21154, #2518, #12553, #4179, #17716, #5932, #7821, #16177, #9477, #16066, #5821, #9883, #2622, #17828, #19279, #19489, #12662, #7717, #1088, #11006, #977, #12768, #4381, #871, #16581, #19598, #6144, #4492, #11216, #14201, #9258, #19383, #3151, #1500, #762, #7499, #15958, #20939, #10909, #8896, #19237, #15597, #7132, #3708, #4030, #17356, #7453, #10868, #12400, #7349, #723, #12074, #5358, #17245, #17570, #2477, #15916, #12511, #4137, #9218, #2261, #7563, #2159, #503, #10756, #3816, #19132, #13836, #10545, #13942, #829, #5780, #14160, #7240, #14053, #20893, #8998, #19025, #15707, #20572, #17140, #8786, #5565, #20680, #20465, #9110, #17462, #3923, #10440, #18805, #12287, #2373, #2054, #613, #10654, #15810, #20785, #15500, #402, #5458, #12180, #18915, #5676, #14893, #16434, #11593, #16326, #6532, #7970, #9737, #21528, #16543, #14676, #21417, #6305, #11699, #1348, #13033, #6654, #4757, #12921, #21007, #6418, #1459, #8080, #4651, #8298, #16769, #1235, #20100, #19757, #18321, #11370, #4989, #13141, #1570, #15005, #19870, #13362, #17978, #6190, #11257, #10062, #21746, #16658, #14786, #21641, #3334, #18434, #11476, #18204, #1681, #3111, #19646, #18091, #13251, #2999, #14261, #9843, #8192, #19988, #4873, #3222, #9954, #4537, #2890, #9627, #3768, #10495, #18973, #10388, #5512, #11813, #10174, #15553, #1890, #3552, #18758, #8734, #17196, #12243, #15119, #11921, #17305, #20630, #18650, #16874, #1790, #456, #5410, #3876, #10278, #10601, #6864, #8410, #22, #134, #2109, #12128, #8846, #20523, #6762, #18544, #7187, #13471, #20203, #18861, #13784, #8522, #236, #13893, #6976, #5096, #3450, #15235, #13569, #13680, #20414, #20307, #5205, #16981, #8626, #15344, #5310, #12022, #3658, #17089, #2003, #15453, #352, #9380, #16084, #21067, #17732, #17629, #2638, #19504, #20736, #5625, #14434, #995, #14002, #885, #7733, #4397, #5948, #21168, #7407, #3985, #7624, #12349, #15767, #15654, #14107, #19085, #14325, #10710, #12784, #9273, #6058, #11130, #19398, #19189, #671, #15974, #2217, #4294, #4087, #8947, #17413, #14215, #9057, #20845, #12459, #10818, #9169, #10922, #17519, #2430, #780, #7515, #20954, #5838, #12569, #19296, #16192, #2753, #2970, #4730, #13008, #7942, #11565, #20075, #4510, #1541, #17952, #21612, #2858, #8273, #9709, #4844, #18294, #1320, #16631, #21281, #9494, #14540, #13337, #18177, #19728, #21501, #6502, #11341, #16411, #11449, #3083, #16301, #4961, #3196, #9817, #19960, #6388, #1103, #11232, #1209, #9926, #13222, #13116, #14973, #19615 ),
 ( #21719, #16515, #4621, #17845, #6622, #8053, #7838, #6160, #18064, #1432, #12895, #9601, #14759, #19839, #14649, #8161, #21389, #6276, #14866, #1761, #2085, #10145, #3528, #13653, #18513, #1867, #20387, #16740, #11784, #18731, #7054, #13759, #432, #5284, #8817, #15092, #13444, #18836, #5175, #6839, #210, #11998, #20499, #15527, #18407, #15207, #20603, #7163, #107, #20179, #11894, #18623, #3636, #10361, #16846, #13866, #3742, #17062, #5388, #15316, #3307, #5070, #8495, #12104, #323, #6947, #10471, #3424, #11672, #13545, #20281, #17172, #10253, #16955, #1652, #1974, #8597, #10035, #8383, #8709, #15428, #4939, #6737, #12214, #2290, #2613, #9351, #967, #19375, #10998, #4270, #9142, #14407, #9030, #7381, #10899, #10681, #19270, #13973, #17386, #20819, #16055, #12651, #14296, #15741, #14190, #21040, #15842, #4060, #753, #20711, #2191, #15627, #12434, #646, #7596, #15949, #2509, #10789, #17276, #7708, #19161, #17603, #8922, #7488, #14082, #860, #5710, #9250, #10575, #532, #4170, #5487, #3849, #5811, #17495, #5923, #7271, #5594, #12321, #2406, #20929, #12542, #19056, #3958, #6136, #18265, #7918, #14516, #13194, #11312, #19480, #6029, #6249, #8028, #16278, #11207, #14836, #1516, #7810, #4815, #21256, #3054, #12866, #11538, #12979, #8133, #21583, #4594, #19927, #2727, #12759, #17815, #16600, #21471, #1184, #2942, #9793, #19587, #16487, #4480, #3169, #19703, #6473, #9898, #18037, #8245, #9468, #4371, #16167, #21144, #6362, #14621, #9684, #1404, #21358, #16381, #14735, #13086, #17924, #11102, #1079, #19814, #2833, #1293, #9572, #4703, #11421, #18147, #3612, #18600, #300, #16713, #14947, #5044, #3392, #13734, #10116, #1622, #20048, #20364, #11868, #1950, #5364, #6921, #1845, #17038, #6593, #21694, #11755, #12081, #18811, #10445, #7029, #20472, #3716, #3504, #2062, #18486, #16823, #5259, #20152, #13625, #8354, #1735, #8470, #17147, #13312, #8680, #15178, #8575, #15402, #10227, #13523, #16929, #15065, #11645, #3278, #80, #6817, #4935, #10335, #11976, #20257, #18377, #10008, #5148, #18706, #21802, #15291, #184, #6709, #13417, #5787, #13842, #18921, #7458, #14269, #7569, #9118, #10660, #12519, #10550, #730, #2164, #3929, #15716, #10764, #8901, #15603, #510, #5896, #17362, #7248, #835, #20791, #7138, #15506, #620, #17470, #2268, #20686, #2483, #10972, #17251, #21014, #12626, #19243, #9005, #13948, #15816, #9225, #14167, #7355, #17684, #19348, #5683, #15923, #10876, #14058, #20900, #4246, #8792, #12407, #19138, #17577, #4037, #408, #5570, #4143, #12293, #20578, #19031, #2380, #5464, #12186, #3824, #4568, #7684, #2697, #9657, #19789, #4681, #13170, #11290, #21558, #6004, #4346, #9767, #17897, #19558, #12953, #2922, #11396, #6448, #9327, #6110, #11510, #14813, #12840, #11074, #17789, #16464, #21446, #19902, #4453, #4790, #1051, #2587, #16026, #16142, #18120, #6336, #3030, #14710, #939, #12733, #1378, #14381, #21120, #13061, #1268, #9442, #16251, #8107, #1160, #19456, #7785, #14489, #21231, #7893, #14594, #11184, #2810, #9548, #21335, #6222, #19676, #18011, #16357, #8003, #5337, #3480, #8221, #3583, #10311, #15265, #5234, #11844, #11951, #13709, #14922, #21671, #8656, #18681, #6566, #16907, #17013, #20445, #162, #1920, #1596, #20021, #1819, #13286, #9984, #9872, #8329, #1491, #8553, #4907, #7005, #18573, #15378, #271, #13602, #15038, #18240, #21779, #3142, #6685, #6894, #16572, #11623, #10204, #18351, #3255, #16688, #20339, #13393, #20127, #5021, #11730, #18463, #3366, #10091, #16798, #1711, #8445, #15151, #52, #6794, #13501, #20233, #5126, #17440, #381, #3798, #3688, #17224, #17121, #2351, #13815, #807, #12380, #9197, #2457, #9088, #7220, #10526, #19115, #5762, #4010, #13921, #20986, #15895, #2244, #12490, #14137, #20661, #10738, #7544, #17547, #5542, #8978, #20874, #12269, #10416, #18891, #15791, #2140, #14243, #8873, #3907, #14031, #15580, #15684, #20766, #2033, #12159, #700, #7434, #19217, #12054, #5657, #18785, #15480, #20555, #4115, #19005, #10634, #591, #10851, #8765, #7110, #5438, #483, #17337, #7331, #9412, #7659, #21097, #13038, #2897, #3004, #7763, #9742, #4324, #16439, #1353, #19430, #1241, #9632, #7975, #17983, #8084, #9302, #14682, #14791, #17659, #16331, #4542, #5980, #19533, #21422, #4427, #6311, #19762, #4659, #11374, #11159, #17872, #16003, #11264, #18095, #5872, #6195, #14460, #12601, #14356, #19651, #12706, #1026, #12814, #7868, #11049, #17764, #2668, #19323, #21202, #16120, #4222, #2783, #10951, #2564, #9525, #14568, #6086, #16223, #913, #1134, #21310, #12926, #21645, #3455, #6536, #5211, #6659, #8527, #15240, #4993, #20312, #3116, #6423, #18210, #17283, #28, #16662, #3338, #10178, #15009, #13367, #15123, #6766, #19993, #2198, #6868, #13475, #1796, #10066, #13145, #14897, #4878, #138, #16879, #16773, #13575, #1464, #21533, #11597, #9960, #12220, #1574, #8196, #4761, #5101, #18439, #18954, #3857, #20207, #8415, #10580, #19874, #11480, #18327, #8928, #9847, #16548, #13256, #3226, #8302, #1685, #21750, #20104, #11703, #11817, #18548, #7601, #2296, #5715, #9148, #12764, #972, #2618, #12440, #2514, #9357, #4176, #14196 ) ),
 .UNSPECIFIED., .F., .F., .T. ) 
 B_SPLINE_SURFACE_WITH_KNOTS ( ( 2, 2 ),
 ( 3, 2, 2, 2, 2, 2, 2, 2, 2, 2, 2, 2, 2, 2, 2, 2, 2, 2, 2, 2, 2, 2, 2, 2, 2, 2, 2, 2, 2, 2, 2, 2, 2, 2, 2, 2, 2, 2, 2, 2, 2, 2, 2, 2, 2, 2, 2, 2, 2, 2, 2, 2, 2, 2, 2, 2, 2, 2, 2, 2, 2, 2, 2, 2, 2, 2, 2, 2, 2, 2, 2, 2, 2, 2, 2, 2, 2, 2, 2, 2, 2, 2, 2, 2, 2, 2, 2, 2, 2, 2, 2, 2, 2, 2, 2, 2, 2, 2, 2, 2, 2, 2, 2, 2, 2, 2, 2, 2, 2, 2, 2, 2, 2, 2, 2, 2, 2, 2, 2, 2, 2, 2, 2, 2, 2, 2, 2, 2, 2, 2, 2, 2, 2, 2, 2, 2, 2, 2, 2, 2, 2, 2, 2, 2, 2, 2, 2, 2, 2, 2, 2, 2, 2, 2, 2, 2, 2, 2, 2, 2, 2, 2, 2, 2, 2, 2, 2, 2, 2, 2, 2, 2, 2, 2, 2, 2, 2, 2, 2, 2, 2, 2, 2, 2, 2, 2, 2, 2, 2, 2, 2, 2, 2, 2, 2, 2, 2, 2, 2, 2, 2, 2, 2, 2, 2, 2, 2, 2, 2, 2, 2, 2, 2, 2, 2, 2, 2, 2, 2, 2, 2, 2, 2, 2, 2, 2, 2, 2, 2, 2, 2, 2, 2, 2, 2, 2, 2, 2, 2, 2, 2, 2, 2, 2, 2, 2, 2, 2, 2, 2, 2, 2, 2, 2, 2, 2, 2, 2, 2, 2, 2, 2, 2, 2, 2, 2, 2, 2, 2, 2, 2, 2, 2, 2, 2, 2, 2, 2, 2, 2, 2, 2, 2, 2, 2, 2, 2, 2, 2, 2, 2, 2, 2, 2, 2, 2, 2, 2, 2, 2, 2, 2, 2, 2, 2, 2, 2, 2, 2, 2, 2, 2, 2, 2, 2, 2, 2, 2, 2, 2, 2, 2, 2, 2, 2, 2, 2, 2, 2, 2, 2, 2, 2, 2, 3 ),
 ( 0.000000000000000000, 1.000000000000000000 ),
 ( 0.000000000000000000, 0.002941176470588235253, 0.005882352941176470507, 0.008823529411764705760, 0.01176470588235294101, 0.01470588235294117627, 0.01764705882352941152, 0.02058823529411764677, 0.02352941176470588203, 0.02647058823529411728, 0.02941176470588235253, 0.03235294117647059126, 0.03529411764705882304, 0.03823529411764706176, 0.04117647058823529355, 0.04411764705882353227, 0.04705882352941176405, 0.05000000000000000278, 0.05294117647058823456, 0.05588235294117647328, 0.05882352941176470507, 0.06176470588235294379, 0.06470588235294118251, 0.06764705882352940736, 0.07058823529411764608, 0.07352941176470588480, 0.07647058823529412352, 0.07941176470588234837, 0.08235294117647058709, 0.08529411764705882582, 0.08823529411764706454, 0.09117647058823528938, 0.09411764705882352811, 0.09705882352941176683, 0.1000000000000000056, 0.1029411764705882304, 0.1058823529411764691, 0.1088235294117647078, 0.1117647058823529466, 0.1147058823529411714, 0.1176470588235294101, 0.1205882352941176489, 0.1235294117647058876, 0.1264705882352941124, 0.1294117647058823650, 0.1323529411764705899, 0.1352941176470588147, 0.1382352941176470673, 0.1411764705882352922, 0.1441176470588235170, 0.1470588235294117696, 0.1499999999999999944, 0.1529411764705882470, 0.1558823529411764719, 0.1588235294117646967, 0.1617647058823529493, 0.1647058823529411742, 0.1676470588235293990, 0.1705882352941176516, 0.1735294117647058765, 0.1764705882352941291, 0.1794117647058823539, 0.1823529411764705788, 0.1852941176470588314, 0.1882352941176470562, 0.1911764705882352811, 0.1941176470588235337, 0.1970588235294117585, 0.2000000000000000111, 0.2029411764705882359, 0.2058823529411764608, 0.2088235294117647134, 0.2117647058823529382, 0.2147058823529411631, 0.2176470588235294157, 0.2205882352941176405, 0.2235294117647058931, 0.2264705882352941180, 0.2294117647058823428, 0.2323529411764705954, 0.2352941176470588203, 0.2382352941176470451, 0.2411764705882352977, 0.2441176470588235226, 0.2470588235294117752, 0.2500000000000000000, 0.2529411764705882248, 0.2558823529411764497, 0.2588235294117647300, 0.2617647058823529549, 0.2647058823529411797, 0.2676470588235294046, 0.2705882352941176294, 0.2735294117647059098, 0.2764705882352941346, 0.2794117647058823595, 0.2823529411764705843, 0.2852941176470588092, 0.2882352941176470340, 0.2911764705882353144, 0.2941176470588235392, 0.2970588235294117641, 0.2999999999999999889, 0.3029411764705882137, 0.3058823529411764941, 0.3088235294117647189, 0.3117647058823529438, 0.3147058823529411686, 0.3176470588235293935, 0.3205882352941176738, 0.3235294117647058987, 0.3264705882352941235, 0.3294117647058823484, 0.3323529411764705732, 0.3352941176470587981, 0.3382352941176470784, 0.3411764705882353033, 0.3441176470588235281, 0.3470588235294117530, 0.3499999999999999778, 0.3529411764705882582, 0.3558823529411764830, 0.3588235294117647078, 0.3617647058823529327, 0.3647058823529411575, 0.3676470588235294379, 0.3705882352941176627, 0.3735294117647058876, 0.3764705882352941124, 0.3794117647058823373, 0.3823529411764705621, 0.3852941176470588425, 0.3882352941176470673, 0.3911764705882352922, 0.3941176470588235170, 0.3970588235294117418, 0.4000000000000000222, 0.4029411764705882470, 0.4058823529411764719, 0.4088235294117646967, 0.4117647058823529216, 0.4147058823529412019, 0.4176470588235294268, 0.4205882352941176516, 0.4235294117647058765, 0.4264705882352941013, 0.4294117647058823262, 0.4323529411764706065, 0.4352941176470588314, 0.4382352941176470562, 0.4411764705882352811, 0.4441176470588235059, 0.4470588235294117863, 0.4500000000000000111, 0.4529411764705882359, 0.4558823529411764608, 0.4588235294117646856, 0.4617647058823529660, 0.4647058823529411908, 0.4676470588235294157, 0.4705882352941176405, 0.4735294117647058654, 0.4764705882352940902, 0.4794117647058823706, 0.4823529411764705954, 0.4852941176470588203, 0.4882352941176470451, 0.4911764705882352700, 0.4941176470588235503, 0.4970588235294117752, 0.5000000000000000000, 0.5029411764705882248, 0.5058823529411764497, 0.5088235294117646745, 0.5117647058823528994, 0.5147058823529411242, 0.5176470588235294601, 0.5205882352941176849, 0.5235294117647059098, 0.5264705882352941346, 0.5294117647058823595, 0.5323529411764705843, 0.5352941176470588092, 0.5382352941176470340, 0.5411764705882352589, 0.5441176470588234837, 0.5470588235294118196, 0.5500000000000000444, 0.5529411764705882693, 0.5558823529411764941, 0.5588235294117647189, 0.5617647058823529438, 0.5647058823529411686, 0.5676470588235293935, 0.5705882352941176183, 0.5735294117647058432, 0.5764705882352940680, 0.5794117647058824039, 0.5823529411764706287, 0.5852941176470588536, 0.5882352941176470784, 0.5911764705882353033, 0.5941176470588235281, 0.5970588235294117530, 0.5999999999999999778, 0.6029411764705882026, 0.6058823529411764275, 0.6088235294117646523, 0.6117647058823529882, 0.6147058823529412130, 0.6176470588235294379, 0.6205882352941176627, 0.6235294117647058876, 0.6264705882352941124, 0.6294117647058823373, 0.6323529411764705621, 0.6352941176470587870, 0.6382352941176470118, 0.6411764705882353477, 0.6441176470588235725, 0.6470588235294117974, 0.6500000000000000222, 0.6529411764705882470, 0.6558823529411764719, 0.6588235294117646967, 0.6617647058823529216, 0.6647058823529411464, 0.6676470588235293713, 0.6705882352941175961, 0.6735294117647059320, 0.6764705882352941568, 0.6794117647058823817, 0.6823529411764706065, 0.6852941176470588314, 0.6882352941176470562, 0.6911764705882352811, 0.6941176470588235059, 0.6970588235294117307, 0.6999999999999999556, 0.7029411764705881804, 0.7058823529411765163, 0.7088235294117647411, 0.7117647058823529660, 0.7147058823529411908, 0.7176470588235294157, 0.7205882352941176405, 0.7235294117647058654, 0.7264705882352940902, 0.7294117647058823151, 0.7323529411764705399, 0.7352941176470588758, 0.7382352941176471006, 0.7411764705882353255, 0.7441176470588235503, 0.7470588235294117752, 0.7500000000000000000, 0.7529411764705882248, 0.7558823529411764497, 0.7588235294117646745, 0.7617647058823528994, 0.7647058823529411242, 0.7676470588235294601, 0.7705882352941176849, 0.7735294117647059098, 0.7764705882352941346, 0.7794117647058823595, 0.7823529411764705843, 0.7852941176470588092, 0.7882352941176470340, 0.7911764705882352589, 0.7941176470588234837, 0.7970588235294118196, 0.8000000000000000444, 0.8029411764705882693, 0.8058823529411764941, 0.8088235294117647189, 0.8117647058823529438, 0.8147058823529411686, 0.8176470588235293935, 0.8205882352941176183, 0.8235294117647058432, 0.8264705882352940680, 0.8294117647058824039, 0.8323529411764706287, 0.8352941176470588536, 0.8382352941176470784, 0.8411764705882353033, 0.8441176470588235281, 0.8470588235294117530, 0.8499999999999999778, 0.8529411764705882026, 0.8558823529411764275, 0.8588235294117646523, 0.8617647058823529882, 0.8647058823529412130, 0.8676470588235294379, 0.8705882352941176627, 0.8735294117647058876, 0.8764705882352941124, 0.8794117647058823373, 0.8823529411764705621, 0.8852941176470587870, 0.8882352941176470118, 0.8911764705882353477, 0.8941176470588235725, 0.8970588235294117974, 0.9000000000000000222, 0.9029411764705882470, 0.9058823529411764719, 0.9088235294117646967, 0.9117647058823529216, 0.9147058823529411464, 0.9176470588235293713, 0.9205882352941175961, 0.9235294117647059320, 0.9264705882352941568, 0.9294117647058823817, 0.9323529411764706065, 0.9352941176470588314, 0.9382352941176470562, 0.9411764705882352811, 0.9441176470588235059, 0.9470588235294117307, 0.9499999999999999556, 0.9529411764705881804, 0.9558823529411765163, 0.9588235294117647411, 0.9617647058823529660, 0.9647058823529411908, 0.9676470588235294157, 0.9705882352941176405, 0.9735294117647058654, 0.9764705882352940902, 0.9794117647058823151, 0.9803958342062288889 ),
 .UNSPECIFIED. ) 
 GEOMETRIC_REPRESENTATION_ITEM ( )  RATIONAL_B_SPLINE_SURFACE ( (
 ( 1.000000000000000000, 0.9510565162951535312, 1.000000000000000000, 0.9510565162951535312, 1.000000000000000000, 0.9510565162951535312, 1.000000000000000000, 0.9510565162951535312, 1.000000000000000000, 0.9510565162951535312, 1.000000000000000000, 0.9510565162951535312, 1.000000000000000000, 0.9510565162951535312, 1.000000000000000000, 0.9510565162951535312, 1.000000000000000000, 0.9510565162951535312, 1.000000000000000000, 0.9510565162951535312, 1.000000000000000000, 0.9510565162951535312, 1.000000000000000000, 0.9510565162951535312, 1.000000000000000000, 0.9510565162951535312, 1.000000000000000000, 0.9510565162951535312, 1.000000000000000000, 0.9510565162951535312, 1.000000000000000000, 0.9510565162951535312, 1.000000000000000000, 0.9510565162951535312, 1.000000000000000000, 0.9510565162951535312, 1.000000000000000000, 0.9510565162951535312, 1.000000000000000000, 0.9510565162951535312, 1.000000000000000000, 0.9510565162951535312, 1.000000000000000000, 0.9510565162951535312, 1.000000000000000000, 0.9510565162951535312, 1.000000000000000000, 0.9510565162951535312, 1.000000000000000000, 0.9510565162951535312, 1.000000000000000000, 0.9510565162951535312, 1.000000000000000000, 0.9510565162951535312, 1.000000000000000000, 0.9510565162951535312, 1.000000000000000000, 0.9510565162951535312, 1.000000000000000000, 0.9510565162951535312, 1.000000000000000000, 0.9510565162951535312, 1.000000000000000000, 0.9510565162951535312, 1.000000000000000000, 0.9510565162951535312, 1.000000000000000000, 0.9510565162951535312, 1.000000000000000000, 0.9510565162951535312, 1.000000000000000000, 0.9510565162951535312, 1.000000000000000000, 0.9510565162951535312, 1.000000000000000000, 0.9510565162951535312, 1.000000000000000000, 0.9510565162951535312, 1.000000000000000000, 0.9510565162951535312, 1.000000000000000000, 0.9510565162951535312, 1.000000000000000000, 0.9510565162951535312, 1.000000000000000000, 0.9510565162951535312, 1.000000000000000000, 0.9510565162951535312, 1.000000000000000000, 0.9510565162951535312, 1.000000000000000000, 0.9510565162951535312, 1.000000000000000000, 0.9510565162951535312, 1.000000000000000000, 0.9510565162951535312, 1.000000000000000000, 0.9510565162951535312, 1.000000000000000000, 0.9510565162951535312, 1.000000000000000000, 0.9510565162951535312, 1.000000000000000000, 0.9510565162951535312, 1.000000000000000000, 0.9510565162951535312, 1.000000000000000000, 0.9510565162951535312, 1.000000000000000000, 0.9510565162951535312, 1.000000000000000000, 0.9510565162951535312, 1.000000000000000000, 0.9510565162951535312, 1.000000000000000000, 0.9510565162951535312, 1.000000000000000000, 0.9510565162951535312, 1.000000000000000000, 0.9510565162951535312, 1.000000000000000000, 0.9510565162951535312, 1.000000000000000000, 0.9510565162951535312, 1.000000000000000000, 0.9510565162951535312, 1.000000000000000000, 0.9510565162951535312, 1.000000000000000000, 0.9510565162951535312, 1.000000000000000000, 0.9510565162951535312, 1.000000000000000000, 0.9510565162951535312, 1.000000000000000000, 0.9510565162951535312, 1.000000000000000000, 0.9510565162951535312, 1.000000000000000000, 0.9510565162951535312, 1.000000000000000000, 0.9510565162951535312, 1.000000000000000000, 0.9510565162951535312, 1.000000000000000000, 0.9510565162951535312, 1.000000000000000000, 0.9510565162951535312, 1.000000000000000000, 0.9510565162951535312, 1.000000000000000000, 0.9510565162951535312, 1.000000000000000000, 0.9510565162951535312, 1.000000000000000000, 0.9510565162951535312, 1.000000000000000000, 0.9510565162951535312, 1.000000000000000000, 0.9510565162951535312, 1.000000000000000000, 0.9510565162951535312, 1.000000000000000000, 0.9510565162951535312, 1.000000000000000000, 0.9510565162951535312, 1.000000000000000000, 0.9510565162951535312, 1.000000000000000000, 0.9510565162951535312, 1.000000000000000000, 0.9510565162951535312, 1.000000000000000000, 0.9510565162951535312, 1.000000000000000000, 0.9510565162951535312, 1.000000000000000000, 0.9510565162951535312, 1.000000000000000000, 0.9510565162951535312, 1.000000000000000000, 0.9510565162951535312, 1.000000000000000000, 0.9510565162951535312, 1.000000000000000000, 0.9510565162951535312, 1.000000000000000000, 0.9510565162951535312, 1.000000000000000000, 0.9510565162951535312, 1.000000000000000000, 0.9510565162951535312, 1.000000000000000000, 0.9510565162951535312, 1.000000000000000000, 0.9510565162951535312, 1.000000000000000000, 0.9510565162951535312, 1.000000000000000000, 0.9510565162951535312, 1.000000000000000000, 0.9510565162951535312, 1.000000000000000000, 0.9510565162951535312, 1.000000000000000000, 0.9510565162951535312, 1.000000000000000000, 0.9510565162951535312, 1.000000000000000000, 0.9510565162951535312, 1.000000000000000000, 0.9510565162951535312, 1.000000000000000000, 0.9510565162951535312, 1.000000000000000000, 0.9510565162951535312, 1.000000000000000000, 0.9510565162951535312, 1.000000000000000000, 0.9510565162951535312, 1.000000000000000000, 0.9510565162951535312, 1.000000000000000000, 0.9510565162951535312, 1.000000000000000000, 0.9510565162951535312, 1.000000000000000000, 0.9510565162951535312, 1.000000000000000000, 0.9510565162951535312, 1.000000000000000000, 0.9510565162951535312, 1.000000000000000000, 0.9510565162951535312, 1.000000000000000000, 0.9510565162951535312, 1.000000000000000000, 0.9510565162951535312, 1.000000000000000000, 0.9510565162951535312, 1.000000000000000000, 0.9510565162951535312, 1.000000000000000000, 0.9510565162951535312, 1.000000000000000000, 0.9510565162951535312, 1.000000000000000000, 0.9510565162951535312, 1.000000000000000000, 0.9510565162951535312, 1.000000000000000000, 0.9510565162951535312, 1.000000000000000000, 0.9510565162951535312, 1.000000000000000000, 0.9510565162951535312, 1.000000000000000000, 0.9510565162951535312, 1.000000000000000000, 0.9510565162951535312, 1.000000000000000000, 0.9510565162951535312, 1.000000000000000000, 0.9510565162951535312, 1.000000000000000000, 0.9510565162951535312, 1.000000000000000000, 0.9510565162951535312, 1.000000000000000000, 0.9510565162951535312, 1.000000000000000000, 0.9510565162951535312, 1.000000000000000000, 0.9510565162951535312, 1.000000000000000000, 0.9510565162951535312, 1.000000000000000000, 0.9510565162951535312, 1.000000000000000000, 0.9510565162951535312, 1.000000000000000000, 0.9510565162951535312, 1.000000000000000000, 0.9510565162951535312, 1.000000000000000000, 0.9510565162951535312, 1.000000000000000000, 0.9510565162951535312, 1.000000000000000000, 0.9510565162951535312, 1.000000000000000000, 0.9510565162951535312, 1.000000000000000000, 0.9510565162951535312, 1.000000000000000000, 0.9510565162951535312, 1.000000000000000000, 0.9510565162951535312, 1.000000000000000000, 0.9510565162951535312, 1.000000000000000000, 0.9510565162951535312, 1.000000000000000000, 0.9510565162951535312, 1.000000000000000000, 0.9510565162951535312, 1.000000000000000000, 0.9510565162951535312, 1.000000000000000000, 0.9510565162951535312, 1.000000000000000000, 0.9510565162951535312, 1.000000000000000000, 0.9510565162951535312, 1.000000000000000000, 0.9510565162951535312, 1.000000000000000000, 0.9510565162951535312, 1.000000000000000000, 0.9510565162951535312, 1.000000000000000000, 0.9510565162951535312, 1.000000000000000000, 0.9510565162951535312, 1.000000000000000000, 0.9510565162951535312, 1.000000000000000000, 0.9510565162951535312, 1.000000000000000000, 0.9510565162951535312, 1.000000000000000000, 0.9510565162951535312, 1.000000000000000000, 0.9510565162951535312, 1.000000000000000000, 0.9510565162951535312, 1.000000000000000000, 0.9510565162951535312, 1.000000000000000000, 0.9510565162951535312, 1.000000000000000000, 0.9510565162951535312, 1.000000000000000000, 0.9510565162951535312, 1.000000000000000000, 0.9510565162951535312, 1.000000000000000000, 0.9510565162951535312, 1.000000000000000000, 0.9510565162951535312, 1.000000000000000000, 0.9510565162951535312, 1.000000000000000000, 0.9510565162951535312, 1.000000000000000000, 0.9510565162951535312, 1.000000000000000000, 0.9510565162951535312, 1.000000000000000000, 0.9510565162951535312, 1.000000000000000000, 0.9510565162951535312, 1.000000000000000000, 0.9510565162951535312, 1.000000000000000000, 0.9510565162951535312, 1.000000000000000000, 0.9510565162951535312, 1.000000000000000000, 0.9510565162951535312, 1.000000000000000000, 0.9510565162951535312, 1.000000000000000000, 0.9510565162951535312, 1.000000000000000000, 0.9510565162951535312, 1.000000000000000000, 0.9510565162951535312, 1.000000000000000000, 0.9510565162951535312, 1.000000000000000000, 0.9510565162951535312, 1.000000000000000000, 0.9510565162951535312, 1.000000000000000000, 0.9510565162951535312, 1.000000000000000000, 0.9510565162951535312, 1.000000000000000000, 0.9510565162951535312, 1.000000000000000000, 0.9510565162951535312, 1.000000000000000000, 0.9510565162951535312, 1.000000000000000000, 0.9510565162951535312, 1.000000000000000000, 0.9510565162951535312, 1.000000000000000000, 0.9510565162951535312, 1.000000000000000000, 0.9510565162951535312, 1.000000000000000000, 0.9510565162951535312, 1.000000000000000000, 0.9510565162951535312, 1.000000000000000000, 0.9510565162951535312, 1.000000000000000000, 0.9510565162951535312, 1.000000000000000000, 0.9510565162951535312, 1.000000000000000000, 0.9510565162951535312, 1.000000000000000000, 0.9510565162951535312, 1.000000000000000000, 0.9510565162951535312, 1.000000000000000000, 0.9510565162951535312, 1.000000000000000000, 0.9510565162951535312, 1.000000000000000000, 0.9510565162951535312, 1.000000000000000000, 0.9510565162951535312, 1.000000000000000000, 0.9510565162951535312, 1.000000000000000000, 0.9510565162951535312, 1.000000000000000000, 0.9510565162951535312, 1.000000000000000000, 0.9510565162951535312, 1.000000000000000000, 0.9510565162951535312, 1.000000000000000000, 0.9510565162951535312, 1.000000000000000000, 0.9510565162951535312, 1.000000000000000000, 0.9510565162951535312, 1.000000000000000000, 0.9510565162951535312, 1.000000000000000000, 0.9510565162951535312, 1.000000000000000000, 0.9510565162951535312, 1.000000000000000000, 0.9510565162951535312, 1.000000000000000000, 0.9510565162951535312, 1.000000000000000000, 0.9510565162951535312, 1.000000000000000000, 0.9510565162951535312, 1.000000000000000000, 0.9510565162951535312, 1.000000000000000000, 0.9510565162951535312, 1.000000000000000000, 0.9510565162951535312, 1.000000000000000000, 0.9510565162951535312, 1.000000000000000000, 0.9510565162951535312, 1.000000000000000000, 0.9510565162951535312, 1.000000000000000000, 0.9510565162951535312, 1.000000000000000000, 0.9510565162951535312, 1.000000000000000000, 0.9510565162951535312, 1.000000000000000000, 0.9510565162951535312, 1.000000000000000000, 0.9510565162951535312, 1.000000000000000000, 0.9510565162951535312, 1.000000000000000000, 0.9510565162951535312, 1.000000000000000000, 0.9510565162951535312, 1.000000000000000000, 0.9510565162951535312, 1.000000000000000000, 0.9510565162951535312, 1.000000000000000000, 0.9510565162951535312, 1.000000000000000000, 0.9510565162951535312, 1.000000000000000000, 0.9510565162951535312, 1.000000000000000000, 0.9510565162951535312, 1.000000000000000000, 0.9510565162951535312, 1.000000000000000000, 0.9510565162951535312, 1.000000000000000000, 0.9510565162951535312, 1.000000000000000000, 0.9510565162951535312, 1.000000000000000000, 0.9510565162951535312, 1.000000000000000000, 0.9510565162951535312, 1.000000000000000000, 0.9510565162951535312, 1.000000000000000000, 0.9510565162951535312, 1.000000000000000000, 0.9510565162951535312, 1.000000000000000000, 0.9510565162951535312, 1.000000000000000000, 0.9510565162951535312, 1.000000000000000000, 0.9510565162951535312, 1.000000000000000000, 0.9510565162951535312, 1.000000000000000000, 0.9510565162951535312, 1.000000000000000000, 0.9510565162951535312, 1.000000000000000000, 0.9510565162951535312, 1.000000000000000000, 0.9510565162951535312, 1.000000000000000000, 0.9510565162951535312, 1.000000000000000000, 0.9510565162951535312, 1.000000000000000000, 0.9510565162951535312, 1.000000000000000000, 0.9510565162951535312, 1.000000000000000000, 0.9510565162951535312, 1.000000000000000000, 0.9510565162951535312, 1.000000000000000000, 0.9510565162951535312, 1.000000000000000000, 0.9510565162951535312, 1.000000000000000000, 0.9510565162951535312, 1.000000000000000000, 0.9510565162951535312, 1.000000000000000000, 0.9510565162951535312, 1.000000000000000000, 0.9510565162951535312, 1.000000000000000000, 0.9510565162951535312, 1.000000000000000000, 0.9510565162951535312, 1.000000000000000000, 0.9510565162951535312, 1.000000000000000000, 0.9510565162951535312, 1.000000000000000000, 0.9510565162951535312, 1.000000000000000000, 0.9510565162951535312, 1.000000000000000000, 0.9510565162951535312, 1.000000000000000000, 0.9510565162951535312, 1.000000000000000000, 0.9510565162951535312, 1.000000000000000000, 0.9510565162951535312, 1.000000000000000000, 0.9510565162951535312, 1.000000000000000000, 0.9510565162951535312, 1.000000000000000000, 0.9510565162951535312, 1.000000000000000000, 0.9510565162951535312, 1.000000000000000000, 0.9510565162951535312, 1.000000000000000000, 0.9510565162951535312, 1.000000000000000000, 0.9510565162951535312, 1.000000000000000000, 0.9510565162951535312, 1.000000000000000000, 0.9510565162951535312, 1.000000000000000000, 0.9510565162951535312, 1.000000000000000000, 0.9510565162951535312, 1.000000000000000000, 0.9510565162951535312, 1.000000000000000000, 0.9510565162951535312, 1.000000000000000000, 0.9510565162951535312, 1.000000000000000000, 0.9510565162951535312, 1.000000000000000000, 0.9510565162951535312, 1.000000000000000000, 0.9510565162951535312, 1.000000000000000000, 0.9510565162951535312, 1.000000000000000000, 0.9510565162951535312, 1.000000000000000000, 0.9510565162951535312, 1.000000000000000000, 0.9510565162951535312, 1.000000000000000000, 0.9510565162951535312, 1.000000000000000000, 0.9510565162951535312, 1.000000000000000000, 0.9510565162951535312, 1.000000000000000000, 0.9510565162951535312, 1.000000000000000000, 0.9510565162951535312, 1.000000000000000000, 0.9510565162951535312, 1.000000000000000000, 0.9510565162951535312, 1.000000000000000000, 0.9510565162951535312, 1.000000000000000000, 0.9510565162951535312, 1.000000000000000000, 0.9510565162951535312, 1.000000000000000000, 0.9510565162951535312, 1.000000000000000000, 0.9510565162951535312, 1.000000000000000000, 0.9510565162951535312, 1.000000000000000000, 0.9510565162951535312, 1.000000000000000000, 0.9510565162951535312, 1.000000000000000000, 0.9510565162951535312, 1.000000000000000000, 0.9510565162951535312, 1.000000000000000000, 0.9510565162951535312, 1.000000000000000000, 0.9510565162951535312, 1.000000000000000000, 0.9510565162951535312, 1.000000000000000000, 0.9510565162951535312, 1.000000000000000000, 0.9510565162951535312, 1.000000000000000000, 0.9510565162951535312, 1.000000000000000000, 0.9510565162951535312, 1.000000000000000000, 0.9510565162951535312, 1.000000000000000000, 0.9836243115514193835, 0.9782066976764483002),
 ( 1.000000000000000000, 0.9510565162951535312, 1.000000000000000000, 0.9510565162951535312, 1.000000000000000000, 0.9510565162951535312, 1.000000000000000000, 0.9510565162951535312, 1.000000000000000000, 0.9510565162951535312, 1.000000000000000000, 0.9510565162951535312, 1.000000000000000000, 0.9510565162951535312, 1.000000000000000000, 0.9510565162951535312, 1.000000000000000000, 0.9510565162951535312, 1.000000000000000000, 0.9510565162951535312, 1.000000000000000000, 0.9510565162951535312, 1.000000000000000000, 0.9510565162951535312, 1.000000000000000000, 0.9510565162951535312, 1.000000000000000000, 0.9510565162951535312, 1.000000000000000000, 0.9510565162951535312, 1.000000000000000000, 0.9510565162951535312, 1.000000000000000000, 0.9510565162951535312, 1.000000000000000000, 0.9510565162951535312, 1.000000000000000000, 0.9510565162951535312, 1.000000000000000000, 0.9510565162951535312, 1.000000000000000000, 0.9510565162951535312, 1.000000000000000000, 0.9510565162951535312, 1.000000000000000000, 0.9510565162951535312, 1.000000000000000000, 0.9510565162951535312, 1.000000000000000000, 0.9510565162951535312, 1.000000000000000000, 0.9510565162951535312, 1.000000000000000000, 0.9510565162951535312, 1.000000000000000000, 0.9510565162951535312, 1.000000000000000000, 0.9510565162951535312, 1.000000000000000000, 0.9510565162951535312, 1.000000000000000000, 0.9510565162951535312, 1.000000000000000000, 0.9510565162951535312, 1.000000000000000000, 0.9510565162951535312, 1.000000000000000000, 0.9510565162951535312, 1.000000000000000000, 0.9510565162951535312, 1.000000000000000000, 0.9510565162951535312, 1.000000000000000000, 0.9510565162951535312, 1.000000000000000000, 0.9510565162951535312, 1.000000000000000000, 0.9510565162951535312, 1.000000000000000000, 0.9510565162951535312, 1.000000000000000000, 0.9510565162951535312, 1.000000000000000000, 0.9510565162951535312, 1.000000000000000000, 0.9510565162951535312, 1.000000000000000000, 0.9510565162951535312, 1.000000000000000000, 0.9510565162951535312, 1.000000000000000000, 0.9510565162951535312, 1.000000000000000000, 0.9510565162951535312, 1.000000000000000000, 0.9510565162951535312, 1.000000000000000000, 0.9510565162951535312, 1.000000000000000000, 0.9510565162951535312, 1.000000000000000000, 0.9510565162951535312, 1.000000000000000000, 0.9510565162951535312, 1.000000000000000000, 0.9510565162951535312, 1.000000000000000000, 0.9510565162951535312, 1.000000000000000000, 0.9510565162951535312, 1.000000000000000000, 0.9510565162951535312, 1.000000000000000000, 0.9510565162951535312, 1.000000000000000000, 0.9510565162951535312, 1.000000000000000000, 0.9510565162951535312, 1.000000000000000000, 0.9510565162951535312, 1.000000000000000000, 0.9510565162951535312, 1.000000000000000000, 0.9510565162951535312, 1.000000000000000000, 0.9510565162951535312, 1.000000000000000000, 0.9510565162951535312, 1.000000000000000000, 0.9510565162951535312, 1.000000000000000000, 0.9510565162951535312, 1.000000000000000000, 0.9510565162951535312, 1.000000000000000000, 0.9510565162951535312, 1.000000000000000000, 0.9510565162951535312, 1.000000000000000000, 0.9510565162951535312, 1.000000000000000000, 0.9510565162951535312, 1.000000000000000000, 0.9510565162951535312, 1.000000000000000000, 0.9510565162951535312, 1.000000000000000000, 0.9510565162951535312, 1.000000000000000000, 0.9510565162951535312, 1.000000000000000000, 0.9510565162951535312, 1.000000000000000000, 0.9510565162951535312, 1.000000000000000000, 0.9510565162951535312, 1.000000000000000000, 0.9510565162951535312, 1.000000000000000000, 0.9510565162951535312, 1.000000000000000000, 0.9510565162951535312, 1.000000000000000000, 0.9510565162951535312, 1.000000000000000000, 0.9510565162951535312, 1.000000000000000000, 0.9510565162951535312, 1.000000000000000000, 0.9510565162951535312, 1.000000000000000000, 0.9510565162951535312, 1.000000000000000000, 0.9510565162951535312, 1.000000000000000000, 0.9510565162951535312, 1.000000000000000000, 0.9510565162951535312, 1.000000000000000000, 0.9510565162951535312, 1.000000000000000000, 0.9510565162951535312, 1.000000000000000000, 0.9510565162951535312, 1.000000000000000000, 0.9510565162951535312, 1.000000000000000000, 0.9510565162951535312, 1.000000000000000000, 0.9510565162951535312, 1.000000000000000000, 0.9510565162951535312, 1.000000000000000000, 0.9510565162951535312, 1.000000000000000000, 0.9510565162951535312, 1.000000000000000000, 0.9510565162951535312, 1.000000000000000000, 0.9510565162951535312, 1.000000000000000000, 0.9510565162951535312, 1.000000000000000000, 0.9510565162951535312, 1.000000000000000000, 0.9510565162951535312, 1.000000000000000000, 0.9510565162951535312, 1.000000000000000000, 0.9510565162951535312, 1.000000000000000000, 0.9510565162951535312, 1.000000000000000000, 0.9510565162951535312, 1.000000000000000000, 0.9510565162951535312, 1.000000000000000000, 0.9510565162951535312, 1.000000000000000000, 0.9510565162951535312, 1.000000000000000000, 0.9510565162951535312, 1.000000000000000000, 0.9510565162951535312, 1.000000000000000000, 0.9510565162951535312, 1.000000000000000000, 0.9510565162951535312, 1.000000000000000000, 0.9510565162951535312, 1.000000000000000000, 0.9510565162951535312, 1.000000000000000000, 0.9510565162951535312, 1.000000000000000000, 0.9510565162951535312, 1.000000000000000000, 0.9510565162951535312, 1.000000000000000000, 0.9510565162951535312, 1.000000000000000000, 0.9510565162951535312, 1.000000000000000000, 0.9510565162951535312, 1.000000000000000000, 0.9510565162951535312, 1.000000000000000000, 0.9510565162951535312, 1.000000000000000000, 0.9510565162951535312, 1.000000000000000000, 0.9510565162951535312, 1.000000000000000000, 0.9510565162951535312, 1.000000000000000000, 0.9510565162951535312, 1.000000000000000000, 0.9510565162951535312, 1.000000000000000000, 0.9510565162951535312, 1.000000000000000000, 0.9510565162951535312, 1.000000000000000000, 0.9510565162951535312, 1.000000000000000000, 0.9510565162951535312, 1.000000000000000000, 0.9510565162951535312, 1.000000000000000000, 0.9510565162951535312, 1.000000000000000000, 0.9510565162951535312, 1.000000000000000000, 0.9510565162951535312, 1.000000000000000000, 0.9510565162951535312, 1.000000000000000000, 0.9510565162951535312, 1.000000000000000000, 0.9510565162951535312, 1.000000000000000000, 0.9510565162951535312, 1.000000000000000000, 0.9510565162951535312, 1.000000000000000000, 0.9510565162951535312, 1.000000000000000000, 0.9510565162951535312, 1.000000000000000000, 0.9510565162951535312, 1.000000000000000000, 0.9510565162951535312, 1.000000000000000000, 0.9510565162951535312, 1.000000000000000000, 0.9510565162951535312, 1.000000000000000000, 0.9510565162951535312, 1.000000000000000000, 0.9510565162951535312, 1.000000000000000000, 0.9510565162951535312, 1.000000000000000000, 0.9510565162951535312, 1.000000000000000000, 0.9510565162951535312, 1.000000000000000000, 0.9510565162951535312, 1.000000000000000000, 0.9510565162951535312, 1.000000000000000000, 0.9510565162951535312, 1.000000000000000000, 0.9510565162951535312, 1.000000000000000000, 0.9510565162951535312, 1.000000000000000000, 0.9510565162951535312, 1.000000000000000000, 0.9510565162951535312, 1.000000000000000000, 0.9510565162951535312, 1.000000000000000000, 0.9510565162951535312, 1.000000000000000000, 0.9510565162951535312, 1.000000000000000000, 0.9510565162951535312, 1.000000000000000000, 0.9510565162951535312, 1.000000000000000000, 0.9510565162951535312, 1.000000000000000000, 0.9510565162951535312, 1.000000000000000000, 0.9510565162951535312, 1.000000000000000000, 0.9510565162951535312, 1.000000000000000000, 0.9510565162951535312, 1.000000000000000000, 0.9510565162951535312, 1.000000000000000000, 0.9510565162951535312, 1.000000000000000000, 0.9510565162951535312, 1.000000000000000000, 0.9510565162951535312, 1.000000000000000000, 0.9510565162951535312, 1.000000000000000000, 0.9510565162951535312, 1.000000000000000000, 0.9510565162951535312, 1.000000000000000000, 0.9510565162951535312, 1.000000000000000000, 0.9510565162951535312, 1.000000000000000000, 0.9510565162951535312, 1.000000000000000000, 0.9510565162951535312, 1.000000000000000000, 0.9510565162951535312, 1.000000000000000000, 0.9510565162951535312, 1.000000000000000000, 0.9510565162951535312, 1.000000000000000000, 0.9510565162951535312, 1.000000000000000000, 0.9510565162951535312, 1.000000000000000000, 0.9510565162951535312, 1.000000000000000000, 0.9510565162951535312, 1.000000000000000000, 0.9510565162951535312, 1.000000000000000000, 0.9510565162951535312, 1.000000000000000000, 0.9510565162951535312, 1.000000000000000000, 0.9510565162951535312, 1.000000000000000000, 0.9510565162951535312, 1.000000000000000000, 0.9510565162951535312, 1.000000000000000000, 0.9510565162951535312, 1.000000000000000000, 0.9510565162951535312, 1.000000000000000000, 0.9510565162951535312, 1.000000000000000000, 0.9510565162951535312, 1.000000000000000000, 0.9510565162951535312, 1.000000000000000000, 0.9510565162951535312, 1.000000000000000000, 0.9510565162951535312, 1.000000000000000000, 0.9510565162951535312, 1.000000000000000000, 0.9510565162951535312, 1.000000000000000000, 0.9510565162951535312, 1.000000000000000000, 0.9510565162951535312, 1.000000000000000000, 0.9510565162951535312, 1.000000000000000000, 0.9510565162951535312, 1.000000000000000000, 0.9510565162951535312, 1.000000000000000000, 0.9510565162951535312, 1.000000000000000000, 0.9510565162951535312, 1.000000000000000000, 0.9510565162951535312, 1.000000000000000000, 0.9510565162951535312, 1.000000000000000000, 0.9510565162951535312, 1.000000000000000000, 0.9510565162951535312, 1.000000000000000000, 0.9510565162951535312, 1.000000000000000000, 0.9510565162951535312, 1.000000000000000000, 0.9510565162951535312, 1.000000000000000000, 0.9510565162951535312, 1.000000000000000000, 0.9510565162951535312, 1.000000000000000000, 0.9510565162951535312, 1.000000000000000000, 0.9510565162951535312, 1.000000000000000000, 0.9510565162951535312, 1.000000000000000000, 0.9510565162951535312, 1.000000000000000000, 0.9510565162951535312, 1.000000000000000000, 0.9510565162951535312, 1.000000000000000000, 0.9510565162951535312, 1.000000000000000000, 0.9510565162951535312, 1.000000000000000000, 0.9510565162951535312, 1.000000000000000000, 0.9510565162951535312, 1.000000000000000000, 0.9510565162951535312, 1.000000000000000000, 0.9510565162951535312, 1.000000000000000000, 0.9510565162951535312, 1.000000000000000000, 0.9510565162951535312, 1.000000000000000000, 0.9510565162951535312, 1.000000000000000000, 0.9510565162951535312, 1.000000000000000000, 0.9510565162951535312, 1.000000000000000000, 0.9510565162951535312, 1.000000000000000000, 0.9510565162951535312, 1.000000000000000000, 0.9510565162951535312, 1.000000000000000000, 0.9510565162951535312, 1.000000000000000000, 0.9510565162951535312, 1.000000000000000000, 0.9510565162951535312, 1.000000000000000000, 0.9510565162951535312, 1.000000000000000000, 0.9510565162951535312, 1.000000000000000000, 0.9510565162951535312, 1.000000000000000000, 0.9510565162951535312, 1.000000000000000000, 0.9510565162951535312, 1.000000000000000000, 0.9510565162951535312, 1.000000000000000000, 0.9510565162951535312, 1.000000000000000000, 0.9510565162951535312, 1.000000000000000000, 0.9510565162951535312, 1.000000000000000000, 0.9510565162951535312, 1.000000000000000000, 0.9510565162951535312, 1.000000000000000000, 0.9510565162951535312, 1.000000000000000000, 0.9510565162951535312, 1.000000000000000000, 0.9510565162951535312, 1.000000000000000000, 0.9510565162951535312, 1.000000000000000000, 0.9510565162951535312, 1.000000000000000000, 0.9510565162951535312, 1.000000000000000000, 0.9510565162951535312, 1.000000000000000000, 0.9510565162951535312, 1.000000000000000000, 0.9510565162951535312, 1.000000000000000000, 0.9510565162951535312, 1.000000000000000000, 0.9510565162951535312, 1.000000000000000000, 0.9510565162951535312, 1.000000000000000000, 0.9510565162951535312, 1.000000000000000000, 0.9510565162951535312, 1.000000000000000000, 0.9510565162951535312, 1.000000000000000000, 0.9510565162951535312, 1.000000000000000000, 0.9510565162951535312, 1.000000000000000000, 0.9510565162951535312, 1.000000000000000000, 0.9510565162951535312, 1.000000000000000000, 0.9510565162951535312, 1.000000000000000000, 0.9510565162951535312, 1.000000000000000000, 0.9510565162951535312, 1.000000000000000000, 0.9510565162951535312, 1.000000000000000000, 0.9510565162951535312, 1.000000000000000000, 0.9510565162951535312, 1.000000000000000000, 0.9510565162951535312, 1.000000000000000000, 0.9510565162951535312, 1.000000000000000000, 0.9510565162951535312, 1.000000000000000000, 0.9510565162951535312, 1.000000000000000000, 0.9510565162951535312, 1.000000000000000000, 0.9510565162951535312, 1.000000000000000000, 0.9510565162951535312, 1.000000000000000000, 0.9510565162951535312, 1.000000000000000000, 0.9510565162951535312, 1.000000000000000000, 0.9510565162951535312, 1.000000000000000000, 0.9510565162951535312, 1.000000000000000000, 0.9510565162951535312, 1.000000000000000000, 0.9510565162951535312, 1.000000000000000000, 0.9510565162951535312, 1.000000000000000000, 0.9510565162951535312, 1.000000000000000000, 0.9510565162951535312, 1.000000000000000000, 0.9510565162951535312, 1.000000000000000000, 0.9510565162951535312, 1.000000000000000000, 0.9510565162951535312, 1.000000000000000000, 0.9510565162951535312, 1.000000000000000000, 0.9510565162951535312, 1.000000000000000000, 0.9510565162951535312, 1.000000000000000000, 0.9510565162951535312, 1.000000000000000000, 0.9510565162951535312, 1.000000000000000000, 0.9510565162951535312, 1.000000000000000000, 0.9510565162951535312, 1.000000000000000000, 0.9510565162951535312, 1.000000000000000000, 0.9510565162951535312, 1.000000000000000000, 0.9510565162951535312, 1.000000000000000000, 0.9510565162951535312, 1.000000000000000000, 0.9510565162951535312, 1.000000000000000000, 0.9510565162951535312, 1.000000000000000000, 0.9510565162951535312, 1.000000000000000000, 0.9510565162951535312, 1.000000000000000000, 0.9510565162951535312, 1.000000000000000000, 0.9510565162951535312, 1.000000000000000000, 0.9510565162951535312, 1.000000000000000000, 0.9510565162951535312, 1.000000000000000000, 0.9510565162951535312, 1.000000000000000000, 0.9510565162951535312, 1.000000000000000000, 0.9510565162951535312, 1.000000000000000000, 0.9510565162951535312, 1.000000000000000000, 0.9510565162951535312, 1.000000000000000000, 0.9510565162951535312, 1.000000000000000000, 0.9510565162951535312, 1.000000000000000000, 0.9510565162951535312, 1.000000000000000000, 0.9510565162951535312, 1.000000000000000000, 0.9510565162951535312, 1.000000000000000000, 0.9510565162951535312, 1.000000000000000000, 0.9510565162951535312, 1.000000000000000000, 0.9510565162951535312, 1.000000000000000000, 0.9510565162951535312, 1.000000000000000000, 0.9510565162951535312, 1.000000000000000000, 0.9510565162951535312, 1.000000000000000000, 0.9510565162951535312, 1.000000000000000000, 0.9836243115514193835, 0.9782066976764483002) ) ) 
 REPRESENTATION_ITEM ( '' )  SURFACE ( )  );
#6836=CARTESIAN_POINT ( 'NONE',  ( 43.01140435219951286, 82.46049967264873715, 39.21067981925356349 ) ) ;
#6839=CARTESIAN_POINT ( 'NONE',  ( 38.58424406990784661, 153.5297705074273154, 35.64915139335016647 ) ) ;
#6842=CARTESIAN_POINT ( 'NONE',  ( 47.43856463449117911, 145.4651871740939555, 35.64915139335015937 ) ) ;
#6845=CARTESIAN_POINT ( 'NONE',  ( 43.01140435219951286, 70.46049967264873715, 39.21067981925356349 ) ) ;
#6849=CARTESIAN_POINT ( 'NONE',  ( 38.58424406990784661, 120.2651871740939953, 35.64915139335016647 ) ) ;
#6853=CARTESIAN_POINT ( 'NONE',  ( 38.01140435219951996, 104.6344580088725564, 32.58608133808903773 ) ) ;
#6854=CARTESIAN_POINT ( 'NONE',  ( 43.01140435219951286, 158.6297705074273381, 29.55568802177586107 ) ) ;
#6855=CARTESIAN_POINT ( 'NONE',  ( 38.58424406990786082, 63.37977050742732388, 34.21067981925357060 ) ) ;
#6856=CARTESIAN_POINT ( 'NONE',  ( 41.64333658814960870, 113.5151871740940095, 30.00020018409699318 ) ) ;
#6859=CARTESIAN_POINT ( 'NONE',  ( 38.01140435219951996, 84.86049967264872862, 35.83527830041810347 ) ) ;
#6860=FACE_OUTER_BOUND ( 'NONE', #4280, .T. ) ;
#6861=CARTESIAN_POINT ( 'NONE',  ( 43.80332655382220253, 98.88361825032845331, 29.21067981925356705 ) ) ;
#6863=AXIS2_PLACEMENT_3D ( 'NONE', #20277, #10572, #5280 ) ;
#6864=CARTESIAN_POINT ( 'NONE',  ( 46.59305225739526435, 79.31518717409399244, 36.81289934271958941 ) ) ;
#6866=CARTESIAN_POINT ( 'NONE',  ( 43.01140435219954838, 133.4604996726487514, 39.21067981925356349 ) ) ;
#6868=CARTESIAN_POINT ( 'NONE',  ( 41.64333658814960870, 66.97977050742731819, 38.42115945441014446 ) ) ;
#6874=CARTESIAN_POINT ( 'NONE',  ( 46.59305225739526435, 151.3151871740940067, 36.81289934271958941 ) ) ;
#6875=CARTESIAN_POINT ( 'NONE',  ( 39.42975644700377558, 158.8151871740940067, 31.60846029578754468 ) ) ;
#6876=CARTESIAN_POINT ( 'NONE',  ( 47.43856463449118621, 115.8797705074273097, 34.21067981925357060 ) ) ;
#6881=CARTESIAN_POINT ( 'NONE',  ( 39.42975644700377558, 114.0797705074273125, 31.60846029578754468 ) ) ;
#6882=CARTESIAN_POINT ( 'NONE',  ( 43.01140435219954838, 131.0344580088725479, 29.21067981925356705 ) ) ;
#6885=CARTESIAN_POINT ( 'NONE',  ( 45.74753988029933538, 152.0651871740939782, 30.44471234641811819 ) ) ;
#6888=DIRECTION ( 'NONE',  ( 0.000000000000000000, 1.000000000000000000, 0.000000000000000000 ) ) ;
#6892=CARTESIAN_POINT ( 'NONE',  ( 48.01140435219951996, 97.43445800887256780, 32.58608133808903773 ) ) ;
#6893=CARTESIAN_POINT ( 'NONE',  ( 38.96631938032478359, 98.48445800887257917, 31.27175355779120025 ) ) ;
#6894=CARTESIAN_POINT ( 'NONE',  ( 38.58424406990784661, 93.22977050742730398, 32.77220824515698183 ) ) ;
#6895=( BOUNDED_CURVE ( )  B_SPLINE_CURVE ( 2, ( #3634, #17274, #207, #10359, #3526, #1972, #16953, #2189, #8707, #14080, #18947, #20817, #11892 ),
 .UNSPECIFIED., .F., .F. ) 
 B_SPLINE_CURVE_WITH_KNOTS ( ( 3, 2, 2, 2, 2, 2, 3 ),
 ( 0.8897058823529412352, 0.8911764705882353477, 0.8941176470588235725, 0.8970588235294117974, 0.9000000000000000222, 0.9029411764705882470, 0.9044117647058823595 ),
 .UNSPECIFIED. ) 
 CURVE ( )  GEOMETRIC_REPRESENTATION_ITEM ( )  RATIONAL_B_SPLINE_CURVE ( ( 0.9755282581475768211, 0.9755282581475777093, 1.000000000000000000, 0.9510565162951535312, 1.000000000000000000, 0.9510565162951535312, 1.000000000000000000, 0.9510565162951535312, 1.000000000000000000, 0.9510565162951535312, 1.000000000000000000, 0.9755282581475768211, 0.9755282581475768211 ) ) 
 REPRESENTATION_ITEM ( '' )  );
#6898=CARTESIAN_POINT ( 'NONE',  ( 46.59305225739526435, 79.31518717409399244, 36.81289934271958941 ) ) ;
#6909=CARTESIAN_POINT ( 'NONE',  ( 40.27526882409969033, 144.8297705074273267, 37.97664729208901946 ) ) ;
#6910=CARTESIAN_POINT ( 'NONE',  ( 39.42975644700377558, 96.07977050742731251, 31.60846029578754468 ) ) ;
#6911=CARTESIAN_POINT ( 'NONE',  ( 42.21948215057683740, 141.0373810949689926, 29.21067981925355994 ) ) ;
#6912=CARTESIAN_POINT ( 'NONE',  ( 38.58424406990784661, 63.26518717409400239, 35.64915139335016647 ) ) ;
#6915=CARTESIAN_POINT ( 'NONE',  ( 43.01140435219951996, 10.71049967264875491, 29.21067981925357060 ) ) ;
#6920=CARTESIAN_POINT ( 'NONE',  ( 47.05648932407426344, 139.5844580088725877, 31.27175355779120025 ) ) ;
#6921=CARTESIAN_POINT ( 'NONE',  ( 41.64333658814960870, 125.7797705074273296, 30.00020018409699318 ) ) ;
#6923=CARTESIAN_POINT ( 'NONE',  ( 46.10157429594899270, 100.7344580088725792, 29.95742577749336988 ) ) ;
#6924=CARTESIAN_POINT ( 'NONE',  ( 47.43856463449117911, 103.4651871740939839, 35.64915139335015937 ) ) ;
#6925=DIRECTION ( 'NONE',  ( 0.000000000000000000, 0.000000000000000000, 1.000000000000000000 ) ) ;
#6930=CARTESIAN_POINT ( 'NONE',  ( 45.74753988029934249, 88.42977050742729261, 37.97664729208901235 ) ) ;
#6934=CARTESIAN_POINT ( 'NONE',  ( 48.01140435219951996, 134.3604996726487286, 32.58608133808903773 ) ) ;
#6935=CARTESIAN_POINT ( 'NONE',  ( 38.01140435219951996, 68.93445800887255359, 35.83527830041810347 ) ) ;
#6936=CARTESIAN_POINT ( 'NONE',  ( 41.46631938032478359, 87.38445800887258486, 38.96596240072933170 ) ) ;
#6937=CARTESIAN_POINT ( 'NONE',  ( 44.55648932407425633, 133.6104996726487286, 38.96596240072933170 ) ) ;
#6938=CARTESIAN_POINT ( 'NONE',  ( 45.74753988029933538, 92.06518717409399244, 30.44471234641811819 ) ) ;
#6940=CIRCLE ( 'NONE', #19974, 24.99999999999998934 ) ;
#6943=CARTESIAN_POINT ( 'NONE',  ( 38.01140435219952707, 93.56049967264874567, 32.58608133808903773 ) ) ;
#6944=FACE_OUTER_BOUND ( 'NONE', #2598, .T. ) ;
#6945=CYLINDRICAL_SURFACE ( 'NONE', #12111, 4.999999999999997335 ) ;
#6947=CARTESIAN_POINT ( 'NONE',  ( 43.01140435219951286, 149.6297705074273097, 29.55568802177586463 ) ) ;
#6948=CARTESIAN_POINT ( 'NONE',  ( 47.43856463449117200, 103.7297705074273182, 35.64915139335016647 ) ) ;
#6950=CARTESIAN_POINT ( 'NONE',  ( 41.64333658814960870, 143.5151871740939953, 30.00020018409699318 ) ) ;
#6951=CARTESIAN_POINT ( 'NONE',  ( 47.05648932407426344, 66.98445800887257917, 37.14960608071593384 ) ) ;
#6953=CARTESIAN_POINT ( 'NONE',  ( 46.59305225739526435, 61.31518717409399954, 36.81289934271958941 ) ) ;
#6957=CARTESIAN_POINT ( 'NONE',  ( 39.42975644700377558, 114.4151871740940010, 36.81289934271958941 ) ) ;
#6961=CARTESIAN_POINT ( 'NONE',  ( 43.01140435219951286, 113.0344580088725763, 29.21067981925356705 ) ) ;
#6964=CARTESIAN_POINT ( 'NONE',  ( 47.05648932407426344, 100.5844580088725877, 31.27175355779120025 ) ) ;
#6966=CARTESIAN_POINT ( 'NONE',  ( 48.01140435219951996, 158.3604996726487286, 32.58608133808903773 ) ) ;
#6967=CARTESIAN_POINT ( 'NONE',  ( 47.43856463449118621, 115.6151871740940038, 34.21067981925357060 ) ) ;
#6970=CARTESIAN_POINT ( 'NONE',  ( 39.92123440845004723, 73.16049967264872578, 38.46393386101376421 ) ) ;
#6971=CARTESIAN_POINT ( 'NONE',  ( 41.46631938032478359, 74.18445800887258201, 29.45539723777780239 ) ) ;
#6972=EDGE_CURVE ( 'NONE', #4691, #137, #2061, .T. ) ;
#6973=EDGE_CURVE ( 'NONE', #7422, #18986, #5277, .T. ) ;
#6974=CARTESIAN_POINT ( 'NONE',  ( 38.01140435219952707, 71.78445800887257633, 34.21067981925357060 ) ) ;
#6976=CARTESIAN_POINT ( 'NONE',  ( 47.43856463449118621, 76.61518717409400381, 34.21067981925357060 ) ) ;
#6986=CARTESIAN_POINT ( 'NONE',  ( 38.58424406990786082, 156.1151871740940180, 34.21067981925357060 ) ) ;
#6987=CARTESIAN_POINT ( 'NONE',  ( 41.64333658814960870, 158.5151871740940237, 30.00020018409699318 ) ) ;
#6988=CARTESIAN_POINT ( 'NONE',  ( 44.37947211624943833, 116.4797705074273324, 30.00020018409699318 ) ) ;
#6992=CARTESIAN_POINT ( 'NONE',  ( 44.37947211624943833, 109.2797705074273154, 38.42115945441014446 ) ) ;
#6994=CARTESIAN_POINT ( 'NONE',  ( 43.01140435219951996, 158.0344580088725763, 29.21067981925357060 ) ) ;
#6995=CARTESIAN_POINT ( 'NONE',  ( 43.01140435219951286, 127.4604996726487229, 39.21067981925356349 ) ) ;
#6996=CARTESIAN_POINT ( 'NONE',  ( 40.27526882409969033, 144.5651871740939782, 37.97664729208901946 ) ) ;
#6998=CARTESIAN_POINT ( 'NONE',  ( 43.80332655382220253, 82.95757658655229250, 29.21067981925356705 ) ) ;
#7001=CARTESIAN_POINT ( 'NONE',  ( 48.01140435219951996, 101.0604996726487315, 35.83527830041809636 ) ) ;
#7003=CARTESIAN_POINT ( 'NONE',  ( 48.01140435219951996, 92.21049967264873715, 34.21067981925357060 ) ) ;
#7005=CARTESIAN_POINT ( 'NONE',  ( 47.43856463449117200, 94.72977050742733240, 35.64915139335016647 ) ) ;
#7008=CARTESIAN_POINT ( 'NONE',  ( 44.37947211624943833, 77.21518717409399812, 30.00020018409699318 ) ) ;
#7009=DIRECTION ( 'NONE',  ( 0.000000000000000000, 1.000000000000000000, 0.000000000000000000 ) ) ;
#7011=ORIENTED_EDGE ( 'NONE', *, *, #2754, .T. ) ;
#7012=DIRECTION ( 'NONE',  ( 0.000000000000000000, 0.000000000000000000, 1.000000000000000000 ) ) ;
#7013=CARTESIAN_POINT ( 'NONE',  ( 43.01140435219951996, 10.71049967264875491, 34.21067981925357060 ) ) ;
#7014=CARTESIAN_POINT ( 'NONE',  ( 45.74753988029934249, 142.4297705074273210, 37.97664729208901235 ) ) ;
#7019=CARTESIAN_POINT ( 'NONE',  ( 41.64333658814960870, 134.7797705074273154, 30.00020018409699318 ) ) ;
#7020=DIRECTION ( 'NONE',  ( 0.000000000000000000, 1.000000000000000000, 0.000000000000000000 ) ) ;
#7022=CARTESIAN_POINT ( 'NONE',  ( 38.58424406990784661, 59.96518717409398391, 32.77220824515698183 ) ) ;
#7024=( BOUNDED_CURVE ( )  B_SPLINE_CURVE ( 2, ( #9203, #12933, #708, #16126, #4550, #921, #14145, #14247, #21210, #4229, #11270, #5769, #12820 ),
 .UNSPECIFIED., .F., .F. ) 
 B_SPLINE_CURVE_WITH_KNOTS ( ( 3, 2, 2, 2, 2, 2, 3 ),
 ( 0.5220588235294117974, 0.5235294117647059098, 0.5264705882352941346, 0.5294117647058823595, 0.5323529411764705843, 0.5352941176470588092, 0.5367647058823529216 ),
 .UNSPECIFIED. ) 
 CURVE ( )  GEOMETRIC_REPRESENTATION_ITEM ( )  RATIONAL_B_SPLINE_CURVE ( ( 0.9755282581475768211, 0.9755282581475768211, 1.000000000000000000, 0.9510565162951535312, 1.000000000000000000, 0.9510565162951535312, 1.000000000000000000, 0.9510565162951535312, 1.000000000000000000, 0.9510565162951535312, 1.000000000000000000, 0.9755282581475768211, 0.9755282581475768211 ) ) 
 REPRESENTATION_ITEM ( '' )  );
#7026=CARTESIAN_POINT ( 'NONE',  ( 43.01140435219951286, 107.9604996726487229, 29.21067981925356705 ) ) ;
#7028=CARTESIAN_POINT ( 'NONE',  ( 41.46631938032478359, 143.1844580088725820, 29.45539723777780239 ) ) ;
#7029=CARTESIAN_POINT ( 'NONE',  ( 45.74753988029933538, 124.4297705074273068, 37.97664729208901946 ) ) ;
#7032=CARTESIAN_POINT ( 'NONE',  ( 45.74753988029934249, 104.0651871740940067, 30.44471234641812174 ) ) ;
#7038=CARTESIAN_POINT ( 'NONE',  ( 41.64333658814960870, 87.97977050742731819, 38.42115945441014446 ) ) ;
#7041=CARTESIAN_POINT ( 'NONE',  ( 38.96631938032478359, 75.08445800887257349, 37.14960608071593384 ) ) ;
#7042=LINE ( 'NONE', #18718, #330 ) ;
#7043=CARTESIAN_POINT ( 'NONE',  ( 48.01140435219951996, 128.0604996726487457, 35.83527830041810347 ) ) ;
#7044=CARTESIAN_POINT ( 'NONE',  ( 43.01140435219951286, 86.36518717409400381, 29.55568802177586463 ) ) ;
#7048=DIRECTION ( 'NONE',  ( 0.000000000000000000, 0.000000000000000000, 1.000000000000000000 ) ) ;
#7050=DIRECTION ( 'NONE',  ( 0.000000000000000000, 0.000000000000000000, 1.000000000000000000 ) ) ;
#7052=CARTESIAN_POINT ( 'NONE',  ( 38.01140435219952707, 92.63445800887258486, 32.58608133808903773 ) ) ;
#7053=CARTESIAN_POINT ( 'NONE',  ( 48.01140435219951996, 143.2104996726487514, 34.21067981925357060 ) ) ;
#7054=CARTESIAN_POINT ( 'NONE',  ( 47.43856463449118621, 154.8797705074273097, 34.21067981925357060 ) ) ;
#7055=CARTESIAN_POINT ( 'NONE',  ( 41.64333658814960870, 102.9797705074273182, 38.42115945441014446 ) ) ;
#7057=CARTESIAN_POINT ( 'NONE',  ( 38.58424406990785371, 138.2651871740939669, 35.64915139335015937 ) ) ;
#7060=CARTESIAN_POINT ( 'NONE',  ( 43.80332655382220253, 90.61133943119284595, 39.21067981925355639 ) ) ;
#7063=CARTESIAN_POINT ( 'NONE',  ( 40.27526882409969033, 119.6651871740939868, 30.44471234641811819 ) ) ;
#7064=ORIENTED_EDGE ( 'NONE', *, *, #20142, .F. ) ;
#7069=EDGE_LOOP ( 'NONE', ( #21676, #4181, #2335, #8722 ) ) ;
#7070=CARTESIAN_POINT ( 'NONE',  ( 47.05648932407426344, 103.5844580088725877, 31.27175355779120025 ) ) ;
#7071=CARTESIAN_POINT ( 'NONE',  ( 38.58424406990785371, 156.5297705074273154, 35.64915139335015937 ) ) ;
#7073=CARTESIAN_POINT ( 'NONE',  ( 44.37947211624943833, 61.27977050742732246, 38.42115945441014446 ) ) ;
#7074=CARTESIAN_POINT ( 'NONE',  ( 39.42975644700377558, 117.4151871740940010, 36.81289934271958941 ) ) ;
#7077=CARTESIAN_POINT ( 'NONE',  ( 41.46631938032478359, 73.31049967264874567, 38.96596240072933170 ) ) ;
#7079=CARTESIAN_POINT ( 'NONE',  ( 43.01140435219951286, 137.0344580088725763, 29.21067981925356705 ) ) ;
#7080=CARTESIAN_POINT ( 'NONE',  ( 43.01140435219951286, 122.9604996726487371, 29.21067981925356705 ) ) ;
#7082=CARTESIAN_POINT ( 'NONE',  ( 43.01140435219951286, 104.9604996726487371, 29.21067981925356705 ) ) ;
#7090=CARTESIAN_POINT ( 'NONE',  ( 47.43856463449117200, 139.4651871740940123, 35.64915139335016647 ) ) ;
#7092=CARTESIAN_POINT ( 'NONE',  ( 46.59305225739526435, 101.1797705074273210, 31.60846029578754468 ) ) ;
#7098=CARTESIAN_POINT ( 'NONE',  ( 44.37947211624943833, 113.4797705074273324, 30.00020018409699318 ) ) ;
#7099=CARTESIAN_POINT ( 'NONE',  ( 39.92123440845005433, 158.3344580088725877, 29.95742577749336988 ) ) ;
#7101=CARTESIAN_POINT ( 'NONE',  ( 43.01140435219951286, 141.8651871740940180, 38.86567161673127657 ) ) ;
#7103=CARTESIAN_POINT ( 'NONE',  ( 47.05648932407426344, 97.91049967264873999, 37.14960608071593384 ) ) ;
#7110=CARTESIAN_POINT ( 'NONE',  ( 41.64333658814960870, 80.77977050742732956, 30.00020018409699318 ) ) ;
#7113=CARTESIAN_POINT ( 'NONE',  ( 41.64333658814960870, 74.51518717409399528, 30.00020018409699318 ) ) ;
#7115=FACE_OUTER_BOUND ( 'NONE', #3781, .T. ) ;
#7117=CARTESIAN_POINT ( 'NONE',  ( 41.46631938032478359, 118.3104996726487457, 38.96596240072933170 ) ) ;
#7118=CARTESIAN_POINT ( 'NONE',  ( 48.01140435219951996, 122.2104996726487371, 34.21067981925357060 ) ) ;
#7119=CARTESIAN_POINT ( 'NONE',  ( 40.27526882409969744, 134.9297705074272642, 30.44471234641812174 ) ) ;
#7124=CARTESIAN_POINT ( 'NONE',  ( 41.64333658814960870, 140.7797705074273154, 30.00020018409699318 ) ) ;
#7127=CARTESIAN_POINT ( 'NONE',  ( 45.74753988029933538, 92.32977050742731251, 30.44471234641811819 ) ) ;
#7128=AXIS2_PLACEMENT_3D ( 'NONE', #11236, #18488, #19507 ) ;
#7132=CARTESIAN_POINT ( 'NONE',  ( 38.58424406990784661, 101.9651871740939981, 32.77220824515698183 ) ) ;
#7133=CARTESIAN_POINT ( 'NONE',  ( 38.96631938032478359, 153.4104996726487400, 31.27175355779120025 ) ) ;
#7137=CARTESIAN_POINT ( 'NONE',  ( 39.92123440845004723, 147.2344580088725650, 38.46393386101376421 ) ) ;
#7138=CARTESIAN_POINT ( 'NONE',  ( 41.64333658814960870, 114.9797705074273324, 38.42115945441014446 ) ) ;
#7140=CARTESIAN_POINT ( 'NONE',  ( 43.80332655382220253, 100.9575765865522925, 29.21067981925356705 ) ) ;
#7142=CARTESIAN_POINT ( 'NONE',  ( 41.64333658814960870, 102.7151871740939981, 38.42115945441014446 ) ) ;
#7148=CARTESIAN_POINT ( 'NONE',  ( 41.64333658814960870, 90.97977050742731819, 38.42115945441014446 ) ) ;
#7150=( BOUNDED_CURVE ( )  B_SPLINE_CURVE ( 2, ( #12014, #10165, #18313, #4864, #11802, #6854, #15110, #16758, #20403, #341, #20091, #5302, #16865, #5194, #16649, #18748, #3213, #3651, #11912, #7071, #10379, #8616, #1780, #8514, #15226, #3324, #1560, #19979, #18641, #4980, #11691, #17079, #20195, #1670, #1992, #125, #8289, #11584, #13561, #10269, #14, #8724, #8402, #15442, #14994, #21737, #12559, #17186, #19177, #18851, #19286, #8835, #13881, #2308, #7177, #17510, #9047, #10698, #14099, #12233, #3759, #2419, #7292, #20727, #4185, #17619, #20834, #18964, #2524, #5726, #769, #12449, #4076, #10486, #20620, #10807, #5504, #9158, #7505, #3866, #2206, #8938, #15644, #548, #13991, #5613, #12338, #2706, #1387, #1059, #9881, #19797, #18249, #8229, #8116, #21239, #18019, #17905, #12961, #16365, #8011, #21565, #6456, #19911, #10099, #16807, #5243, #11738, #8455, #18691, #281, #15160, #12064, #7014, #1931, #1722, #1828, #13718, #3489, #8336, #20454, #172, #5135, #2043, #20031, #15048, #14931, #21679, #13293, #4916, #11629, #16697, #21787, #6694, #13401, #60, #13510, #20243, #18582, #10213, #12609, #7442, #19331, #2464, #4124, #20993, #5770, #10534, #709, #2148, #10746, #2359, #8774, #12499, #20774, #4230, #10958, #17667, #493, #10859, #19226, #814, #5665, #7119, #15489, #15694, #17450, #3914, #20669, #9204, #391, #17232, #17557, #599, #9098, #20565, #15903, #13826, #7551, #15799, #5448, #7340, #14039, #14248, #5878, #12167, #5550, #12389, #18900, #2252, #19124, #3807, #8881, #14146, #13930, #15588, #20882, #7230, #4018, #12277, #19013, #10641, #17344, #8987, #4551, #4770, #16447, #7771, #4331, #7984, #12714, #16127, #16010, #14469, #7666, #14689, #11056, #13152, #2905, #21539, #14798, #9310, #11382, #4436, #9533, #6430, #11166, #21429, #2677, #16230, #11491, #6093, #17879, #6319, #21211, #2792, #13045, #9750, #1142, #19882, #1360, #9419, #16340, #12822, #2571, #14363, #9640, #19540, #11271, #14576, #17990, #21105, #1034, #1248, #19769, #4666, #922, #18105, #5987, #19438, #17771, #7876, #3012, #21318, #8091, #6204, #19658, #6542, #16888, #250, #11932, #13583, #8637, #15247, #20001, #10186, #11606, #20215, #1902, #15359, #21759, #5108, #145, #1471, #13267, #1802, #6988, #18663, #20320, #13692, #6876, #4885, #5219, #18334, #11824, #18557, #18218, #3567, #3235, #9967, #20426, #10291, #5322, #3124, #9854, #21653, #16556, #8203, #14904, #16670, #1582, #8310, #10073, #15019, #6667, #13374, #20111, #5002, #11712, #18447, #3345, #16782, #1693, #8424, #15133, #35, #6776, #13483, #3462, #15665, #681, #5524, #18984, #12469, #19199, #12359, #17204, #4096, #19097, #14117, #568, #15776, #7418, #20855, #5637, #5745, #14013, #14225, #10831, #2120, #13797, #17422, #365, #3779, #3670, #8856, #17100, #2329, #20535, #790, #3995, #17529, #10400, #18769, #2438, #13902, #3888, #15876, #20641, #9068, #12138, #10611, #20965, #15563, #12253, #9179, #466, #17317, #7524, #12038, #2227, #8958, #2016, #18872, #10719, #7199, #8747, #15464, #7092, #7312, #20746, #5421, #10508, #10932, #5961, #13203, #1524, #8254, #16721, #8143, #3288, #11548, #17639, #2546, #6483, #1008, #14848, #18157, #21593, #9284, #12687, #19939, #14955, #21702, #1632, #4825, #10017, #15984, #7634, #11653, #18389, #3064, #18276, #3178, #895, #21078, #9907, #8364, #6602, #13320, #15075, #16613, #19408, #20057, #4307, #4943, #5850, #12581, #19306, #11031, #17746, #4203, #2649, #9391, #16097, #7744, #14445, #21180, #6070, #12797, #19516, #4410, #11431, #9804, #16498, #1415, #7148, #3403, #5373, #20164, #13852, #309, #8910, #20588, #20372, #13635, #5473, #18934, #8801, #11877, #3621, #10455, #15300, #6930, #416, #12197, #7038, #5158, #3834, #13744, #2072, #15412, #10562, #10127, #8691, #21812, #18819, #20483, #11984, #6720, #18608, #10236, #17261, #16937, #8481, #5053, #12089, #18714, #15514, #2174, #3725, #13426, #11765, #17156, #92, #10343, #18496, #16833, #3513, #1852, #6824, #1746, #17046, #15189, #13531, #8583, #20266, #193, #5269, #1958, #5797, #12745, #950, #2597, #12419, #2494, #9336, #521, #740, #9236, #10775, #5696, #16037, #17799, #2277, #17695, #7472, #15934, #5580, #7695, #20696, #10669, #15727, #4156, #9015, #19359, #19256, #12529, #10886, #14068, #13958, #2710, #845, #12305, #4047, #12637, #14281, #19043, #7580, #14392, #11085, #17588, #21026, #19466, #3941, #5909, #15613, #4256, #10984, #21131, #7257, #19147, #17482, #6014, #2391, #630, #17372, #4356, #7366, #20804, #9127, #15827, #14177, #20912, #6458, #9557, #6346, #20033, #7795, #12964, #4578, #16263, #13180, #21456, #3152, #11522, #11298, #9884, #17908, #21682, #9453, #2931, #6577, #16583, #18252, #6232, #18130, #1502, #19800, #2819, #8120, #16367, #18024, #19569, #1278, #21344, #8232, #19913, #4799, #8014, #21242, #13297, #12849, #11195, #14933, #4918, #19686, #7902, #9778, #11631, #18360, #16153, #1064, #6120, #11406, #1169, #14605, #9667, #14500, #4464, #14720, #3039, #13072, #4690, #16473, #1389, #14822, #21568, #18473, #17132, #15276, #1606, #18797, #11741, #15492, #3265, #174, #5350, #18585, #16700, #10102, #11963, #3700, #13612, #3377, #1935, #10215, #20246, #13405 ),
 .UNSPECIFIED., .F., .T. ) 
 B_SPLINE_CURVE_WITH_KNOTS ( ( 3, 2, 2, 2, 2, 2, 2, 2, 2, 2, 2, 2, 2, 2, 2, 2, 2, 2, 2, 2, 2, 2, 2, 2, 2, 2, 2, 2, 2, 2, 2, 2, 2, 2, 2, 2, 2, 2, 2, 2, 2, 2, 2, 2, 2, 2, 2, 2, 2, 2, 2, 2, 2, 2, 2, 2, 2, 2, 2, 2, 2, 2, 2, 2, 2, 2, 2, 2, 2, 2, 2, 2, 2, 2, 2, 2, 2, 2, 2, 2, 2, 2, 2, 2, 2, 2, 2, 2, 2, 2, 2, 2, 2, 2, 2, 2, 2, 2, 2, 2, 2, 2, 2, 2, 2, 2, 2, 2, 2, 2, 2, 2, 2, 2, 2, 2, 2, 2, 2, 2, 2, 2, 2, 2, 2, 2, 2, 2, 2, 2, 2, 2, 2, 2, 2, 2, 2, 2, 2, 2, 2, 2, 2, 2, 2, 2, 2, 2, 2, 2, 2, 2, 2, 2, 2, 2, 2, 2, 2, 2, 2, 2, 2, 2, 2, 2, 2, 2, 2, 2, 2, 2, 2, 2, 2, 2, 2, 2, 2, 2, 2, 2, 2, 2, 2, 2, 2, 2, 2, 2, 2, 2, 2, 2, 2, 2, 2, 2, 2, 2, 2, 2, 2, 2, 2, 2, 2, 2, 2, 2, 2, 2, 2, 2, 2, 2, 2, 2, 2, 2, 2, 2, 2, 2, 2, 2, 2, 2, 2, 2, 2, 2, 2, 2, 2, 2, 2, 2, 2, 2, 2, 2, 2, 2, 2, 2, 2, 2, 2, 2, 2, 2, 2, 2, 2, 2, 2, 2, 2, 2, 2, 2, 2, 2, 2, 2, 2, 2, 2, 2, 2, 2, 2, 2, 2, 2, 2, 2, 2, 2, 2, 2, 2, 2, 2, 2, 2, 2, 2, 2, 2, 2, 2, 2, 2, 2, 2, 2, 2, 2, 2, 2, 2, 2, 2, 2, 2, 2, 2, 2, 2, 2, 2, 2, 2, 2, 2, 2, 2, 2, 2, 2, 2, 2, 2, 2, 2, 2, 2, 2, 2, 2, 2, 2, 3 ),
 ( 0.000000000000000000, 0.002941176470588235253, 0.005882352941176470507, 0.008823529411764705760, 0.01176470588235294101, 0.01470588235294117627, 0.01764705882352941152, 0.02058823529411764677, 0.02352941176470588203, 0.02647058823529411728, 0.02941176470588235253, 0.03235294117647059126, 0.03529411764705882304, 0.03823529411764706176, 0.04117647058823529355, 0.04411764705882353227, 0.04705882352941176405, 0.05000000000000000278, 0.05294117647058823456, 0.05588235294117647328, 0.05882352941176470507, 0.06176470588235294379, 0.06470588235294118251, 0.06764705882352940736, 0.07058823529411764608, 0.07352941176470588480, 0.07647058823529412352, 0.07941176470588234837, 0.08235294117647058709, 0.08529411764705882582, 0.08823529411764706454, 0.09117647058823530326, 0.09411764705882352811, 0.09705882352941176683, 0.1000000000000000056, 0.1029411764705882304, 0.1058823529411764691, 0.1088235294117647078, 0.1117647058823529466, 0.1147058823529411714, 0.1176470588235294101, 0.1205882352941176489, 0.1235294117647058876, 0.1264705882352941124, 0.1294117647058823650, 0.1323529411764705899, 0.1352941176470588147, 0.1382352941176470673, 0.1411764705882352922, 0.1441176470588235170, 0.1470588235294117696, 0.1499999999999999944, 0.1529411764705882470, 0.1558823529411764719, 0.1588235294117646967, 0.1617647058823529493, 0.1647058823529411742, 0.1676470588235293990, 0.1705882352941176516, 0.1735294117647058765, 0.1764705882352941291, 0.1794117647058823539, 0.1823529411764706065, 0.1852941176470588314, 0.1882352941176470562, 0.1911764705882352811, 0.1941176470588235337, 0.1970588235294117585, 0.2000000000000000111, 0.2029411764705882359, 0.2058823529411764608, 0.2088235294117647134, 0.2117647058823529382, 0.2147058823529411631, 0.2176470588235294157, 0.2205882352941176405, 0.2235294117647058931, 0.2264705882352941180, 0.2294117647058823428, 0.2323529411764705954, 0.2352941176470588203, 0.2382352941176470451, 0.2411764705882352977, 0.2441176470588235226, 0.2470588235294117752, 0.2500000000000000000, 0.2529411764705882248, 0.2558823529411764497, 0.2588235294117647300, 0.2617647058823529549, 0.2647058823529411797, 0.2676470588235294046, 0.2705882352941176294, 0.2735294117647059098, 0.2764705882352941346, 0.2794117647058823595, 0.2823529411764705843, 0.2852941176470588092, 0.2882352941176470340, 0.2911764705882353144, 0.2941176470588235392, 0.2970588235294117641, 0.2999999999999999889, 0.3029411764705882137, 0.3058823529411764941, 0.3088235294117647189, 0.3117647058823529438, 0.3147058823529411686, 0.3176470588235293935, 0.3205882352941176738, 0.3235294117647058987, 0.3264705882352941235, 0.3294117647058823484, 0.3323529411764705732, 0.3352941176470587981, 0.3382352941176470784, 0.3411764705882353033, 0.3441176470588235281, 0.3470588235294117530, 0.3499999999999999778, 0.3529411764705882582, 0.3558823529411764830, 0.3588235294117647078, 0.3617647058823529327, 0.3647058823529412130, 0.3676470588235294379, 0.3705882352941176627, 0.3735294117647058876, 0.3764705882352941124, 0.3794117647058823373, 0.3823529411764705621, 0.3852941176470587870, 0.3882352941176470673, 0.3911764705882352922, 0.3941176470588235170, 0.3970588235294117418, 0.4000000000000000222, 0.4029411764705882470, 0.4058823529411764719, 0.4088235294117646967, 0.4117647058823529216, 0.4147058823529412019, 0.4176470588235294268, 0.4205882352941176516, 0.4235294117647058765, 0.4264705882352941013, 0.4294117647058823262, 0.4323529411764706065, 0.4352941176470588314, 0.4382352941176470562, 0.4411764705882352811, 0.4441176470588235059, 0.4470588235294117863, 0.4500000000000000111, 0.4529411764705882359, 0.4558823529411764608, 0.4588235294117646856, 0.4617647058823529660, 0.4647058823529411908, 0.4676470588235294157, 0.4705882352941176405, 0.4735294117647058654, 0.4764705882352940902, 0.4794117647058823706, 0.4823529411764705954, 0.4852941176470588203, 0.4882352941176470451, 0.4911764705882352700, 0.4941176470588235503, 0.4970588235294117752, 0.5000000000000000000, 0.5029411764705882248, 0.5058823529411764497, 0.5088235294117646745, 0.5117647058823528994, 0.5147058823529411242, 0.5176470588235294601, 0.5205882352941176849, 0.5235294117647059098, 0.5264705882352941346, 0.5294117647058823595, 0.5323529411764705843, 0.5352941176470588092, 0.5382352941176470340, 0.5411764705882352589, 0.5441176470588234837, 0.5470588235294118196, 0.5500000000000000444, 0.5529411764705882693, 0.5558823529411764941, 0.5588235294117647189, 0.5617647058823529438, 0.5647058823529411686, 0.5676470588235293935, 0.5705882352941176183, 0.5735294117647058432, 0.5764705882352940680, 0.5794117647058824039, 0.5823529411764706287, 0.5852941176470588536, 0.5882352941176470784, 0.5911764705882353033, 0.5941176470588235281, 0.5970588235294117530, 0.5999999999999999778, 0.6029411764705882026, 0.6058823529411764275, 0.6088235294117646523, 0.6117647058823529882, 0.6147058823529412130, 0.6176470588235294379, 0.6205882352941176627, 0.6235294117647058876, 0.6264705882352941124, 0.6294117647058823373, 0.6323529411764705621, 0.6352941176470587870, 0.6382352941176470118, 0.6411764705882353477, 0.6441176470588235725, 0.6470588235294117974, 0.6500000000000000222, 0.6529411764705882470, 0.6558823529411764719, 0.6588235294117646967, 0.6617647058823529216, 0.6647058823529411464, 0.6676470588235293713, 0.6705882352941175961, 0.6735294117647059320, 0.6764705882352941568, 0.6794117647058823817, 0.6823529411764706065, 0.6852941176470588314, 0.6882352941176470562, 0.6911764705882352811, 0.6941176470588235059, 0.6970588235294117307, 0.6999999999999999556, 0.7029411764705881804, 0.7058823529411765163, 0.7088235294117647411, 0.7117647058823529660, 0.7147058823529411908, 0.7176470588235294157, 0.7205882352941176405, 0.7235294117647058654, 0.7264705882352940902, 0.7294117647058824261, 0.7323529411764705399, 0.7352941176470588758, 0.7382352941176471006, 0.7411764705882353255, 0.7441176470588235503, 0.7470588235294117752, 0.7499999999999998890, 0.7529411764705882248, 0.7558823529411764497, 0.7588235294117646745, 0.7617647058823528994, 0.7647058823529411242, 0.7676470588235294601, 0.7705882352941175739, 0.7735294117647059098, 0.7764705882352941346, 0.7794117647058823595, 0.7823529411764705843, 0.7852941176470588092, 0.7882352941176470340, 0.7911764705882352589, 0.7941176470588234837, 0.7970588235294118196, 0.8000000000000000444, 0.8029411764705882693, 0.8058823529411764941, 0.8088235294117647189, 0.8117647058823529438, 0.8147058823529411686, 0.8176470588235293935, 0.8205882352941176183, 0.8235294117647058432, 0.8264705882352940680, 0.8294117647058824039, 0.8323529411764706287, 0.8352941176470588536, 0.8382352941176470784, 0.8411764705882353033, 0.8441176470588235281, 0.8470588235294117530, 0.8499999999999999778, 0.8529411764705882026, 0.8558823529411764275, 0.8588235294117646523, 0.8617647058823529882, 0.8647058823529412130, 0.8676470588235294379, 0.8705882352941176627, 0.8735294117647058876, 0.8764705882352941124, 0.8794117647058823373, 0.8823529411764705621, 0.8852941176470587870, 0.8882352941176470118, 0.8911764705882353477, 0.8941176470588235725, 0.8970588235294117974, 0.9000000000000000222, 0.9029411764705882470, 0.9058823529411764719, 0.9088235294117646967, 0.9117647058823529216, 0.9147058823529411464, 0.9176470588235293713, 0.9205882352941175961, 0.9235294117647059320, 0.9264705882352941568, 0.9294117647058823817, 0.9323529411764706065, 0.9352941176470588314, 0.9382352941176470562, 0.9411764705882352811, 0.9441176470588235059, 0.9470588235294117307, 0.9499999999999999556, 0.9529411764705881804, 0.9558823529411765163, 0.9588235294117647411, 0.9617647058823529660, 0.9647058823529411908, 0.9676470588235294157, 0.9705882352941176405, 0.9735294117647058654, 0.9764705882352940902, 0.9794117647058823151, 0.9803958342062288889 ),
 .UNSPECIFIED. ) 
 CURVE ( )  GEOMETRIC_REPRESENTATION_ITEM ( )  RATIONAL_B_SPLINE_CURVE ( ( 1.000000000000000000, 0.9510565162951535312, 1.000000000000000000, 0.9510565162951535312, 1.000000000000000000, 0.9510565162951535312, 1.000000000000000000, 0.9510565162951535312, 1.000000000000000000, 0.9510565162951535312, 1.000000000000000000, 0.9510565162951535312, 1.000000000000000000, 0.9510565162951535312, 1.000000000000000000, 0.9510565162951535312, 1.000000000000000000, 0.9510565162951535312, 1.000000000000000000, 0.9510565162951535312, 1.000000000000000000, 0.9510565162951535312, 1.000000000000000000, 0.9510565162951535312, 1.000000000000000000, 0.9510565162951535312, 1.000000000000000000, 0.9510565162951535312, 1.000000000000000000, 0.9510565162951535312, 1.000000000000000000, 0.9510565162951535312, 1.000000000000000000, 0.9510565162951535312, 1.000000000000000000, 0.9510565162951535312, 1.000000000000000000, 0.9510565162951535312, 1.000000000000000000, 0.9510565162951535312, 1.000000000000000000, 0.9510565162951535312, 1.000000000000000000, 0.9510565162951535312, 1.000000000000000000, 0.9510565162951535312, 1.000000000000000000, 0.9510565162951535312, 1.000000000000000000, 0.9510565162951535312, 1.000000000000000000, 0.9510565162951535312, 1.000000000000000000, 0.9510565162951535312, 1.000000000000000000, 0.9510565162951535312, 1.000000000000000000, 0.9510565162951535312, 1.000000000000000000, 0.9510565162951535312, 1.000000000000000000, 0.9510565162951535312, 1.000000000000000000, 0.9510565162951535312, 1.000000000000000000, 0.9510565162951535312, 1.000000000000000000, 0.9510565162951535312, 1.000000000000000000, 0.9510565162951535312, 1.000000000000000000, 0.9510565162951535312, 1.000000000000000000, 0.9510565162951535312, 1.000000000000000000, 0.9510565162951535312, 1.000000000000000000, 0.9510565162951535312, 1.000000000000000000, 0.9510565162951535312, 1.000000000000000000, 0.9510565162951535312, 1.000000000000000000, 0.9510565162951535312, 1.000000000000000000, 0.9510565162951535312, 1.000000000000000000, 0.9510565162951535312, 1.000000000000000000, 0.9510565162951535312, 1.000000000000000000, 0.9510565162951535312, 1.000000000000000000, 0.9510565162951535312, 1.000000000000000000, 0.9510565162951535312, 1.000000000000000000, 0.9510565162951535312, 1.000000000000000000, 0.9510565162951535312, 1.000000000000000000, 0.9510565162951535312, 1.000000000000000000, 0.9510565162951535312, 1.000000000000000000, 0.9510565162951535312, 1.000000000000000000, 0.9510565162951535312, 1.000000000000000000, 0.9510565162951535312, 1.000000000000000000, 0.9510565162951535312, 1.000000000000000000, 0.9510565162951535312, 1.000000000000000000, 0.9510565162951535312, 1.000000000000000000, 0.9510565162951535312, 1.000000000000000000, 0.9510565162951535312, 1.000000000000000000, 0.9510565162951535312, 1.000000000000000000, 0.9510565162951535312, 1.000000000000000000, 0.9510565162951535312, 1.000000000000000000, 0.9510565162951535312, 1.000000000000000000, 0.9510565162951535312, 1.000000000000000000, 0.9510565162951535312, 1.000000000000000000, 0.9510565162951535312, 1.000000000000000000, 0.9510565162951535312, 1.000000000000000000, 0.9510565162951535312, 1.000000000000000000, 0.9510565162951535312, 1.000000000000000000, 0.9510565162951535312, 1.000000000000000000, 0.9510565162951535312, 1.000000000000000000, 0.9510565162951535312, 1.000000000000000000, 0.9510565162951535312, 1.000000000000000000, 0.9510565162951535312, 1.000000000000000000, 0.9510565162951535312, 1.000000000000000000, 0.9510565162951535312, 1.000000000000000000, 0.9510565162951535312, 1.000000000000000000, 0.9510565162951535312, 1.000000000000000000, 0.9510565162951535312, 1.000000000000000000, 0.9510565162951535312, 1.000000000000000000, 0.9510565162951535312, 1.000000000000000000, 0.9510565162951535312, 1.000000000000000000, 0.9510565162951535312, 1.000000000000000000, 0.9510565162951535312, 1.000000000000000000, 0.9510565162951535312, 1.000000000000000000, 0.9510565162951535312, 1.000000000000000000, 0.9510565162951535312, 1.000000000000000000, 0.9510565162951535312, 1.000000000000000000, 0.9510565162951535312, 1.000000000000000000, 0.9510565162951535312, 1.000000000000000000, 0.9510565162951535312, 1.000000000000000000, 0.9510565162951535312, 1.000000000000000000, 0.9510565162951535312, 1.000000000000000000, 0.9510565162951535312, 1.000000000000000000, 0.9510565162951535312, 1.000000000000000000, 0.9510565162951535312, 1.000000000000000000, 0.9510565162951535312, 1.000000000000000000, 0.9510565162951535312, 1.000000000000000000, 0.9510565162951535312, 1.000000000000000000, 0.9510565162951535312, 1.000000000000000000, 0.9510565162951535312, 1.000000000000000000, 0.9510565162951535312, 1.000000000000000000, 0.9510565162951535312, 1.000000000000000000, 0.9510565162951535312, 1.000000000000000000, 0.9510565162951535312, 1.000000000000000000, 0.9510565162951535312, 1.000000000000000000, 0.9510565162951535312, 1.000000000000000000, 0.9510565162951535312, 1.000000000000000000, 0.9510565162951535312, 1.000000000000000000, 0.9510565162951535312, 1.000000000000000000, 0.9510565162951535312, 1.000000000000000000, 0.9510565162951535312, 1.000000000000000000, 0.9510565162951535312, 1.000000000000000000, 0.9510565162951535312, 1.000000000000000000, 0.9510565162951535312, 1.000000000000000000, 0.9510565162951535312, 1.000000000000000000, 0.9510565162951535312, 1.000000000000000000, 0.9510565162951535312, 1.000000000000000000, 0.9510565162951535312, 1.000000000000000000, 0.9510565162951535312, 1.000000000000000000, 0.9510565162951535312, 1.000000000000000000, 0.9510565162951535312, 1.000000000000000000, 0.9510565162951535312, 1.000000000000000000, 0.9510565162951535312, 1.000000000000000000, 0.9510565162951535312, 1.000000000000000000, 0.9510565162951535312, 1.000000000000000000, 0.9510565162951535312, 1.000000000000000000, 0.9510565162951535312, 1.000000000000000000, 0.9510565162951535312, 1.000000000000000000, 0.9510565162951535312, 1.000000000000000000, 0.9510565162951535312, 1.000000000000000000, 0.9510565162951535312, 1.000000000000000000, 0.9510565162951535312, 1.000000000000000000, 0.9510565162951535312, 1.000000000000000000, 0.9510565162951535312, 1.000000000000000000, 0.9510565162951535312, 1.000000000000000000, 0.9510565162951535312, 1.000000000000000000, 0.9510565162951535312, 1.000000000000000000, 0.9510565162951535312, 1.000000000000000000, 0.9510565162951535312, 1.000000000000000000, 0.9510565162951535312, 1.000000000000000000, 0.9510565162951535312, 1.000000000000000000, 0.9510565162951535312, 1.000000000000000000, 0.9510565162951535312, 1.000000000000000000, 0.9510565162951535312, 1.000000000000000000, 0.9510565162951535312, 1.000000000000000000, 0.9510565162951535312, 1.000000000000000000, 0.9510565162951535312, 1.000000000000000000, 0.9510565162951535312, 1.000000000000000000, 0.9510565162951535312, 1.000000000000000000, 0.9510565162951535312, 1.000000000000000000, 0.9510565162951535312, 1.000000000000000000, 0.9510565162951535312, 1.000000000000000000, 0.9510565162951535312, 1.000000000000000000, 0.9510565162951535312, 1.000000000000000000, 0.9510565162951535312, 1.000000000000000000, 0.9510565162951535312, 1.000000000000000000, 0.9510565162951535312, 1.000000000000000000, 0.9510565162951535312, 1.000000000000000000, 0.9510565162951535312, 1.000000000000000000, 0.9510565162951535312, 1.000000000000000000, 0.9510565162951535312, 1.000000000000000000, 0.9510565162951535312, 1.000000000000000000, 0.9510565162951535312, 1.000000000000000000, 0.9510565162951535312, 1.000000000000000000, 0.9510565162951535312, 1.000000000000000000, 0.9510565162951535312, 1.000000000000000000, 0.9510565162951535312, 1.000000000000000000, 0.9510565162951535312, 1.000000000000000000, 0.9510565162951535312, 1.000000000000000000, 0.9510565162951535312, 1.000000000000000000, 0.9510565162951535312, 1.000000000000000000, 0.9510565162951535312, 1.000000000000000000, 0.9510565162951535312, 1.000000000000000000, 0.9510565162951535312, 1.000000000000000000, 0.9510565162951535312, 1.000000000000000000, 0.9510565162951535312, 1.000000000000000000, 0.9510565162951535312, 1.000000000000000000, 0.9510565162951535312, 1.000000000000000000, 0.9510565162951535312, 1.000000000000000000, 0.9510565162951535312, 1.000000000000000000, 0.9510565162951535312, 1.000000000000000000, 0.9510565162951535312, 1.000000000000000000, 0.9510565162951535312, 1.000000000000000000, 0.9510565162951535312, 1.000000000000000000, 0.9510565162951535312, 1.000000000000000000, 0.9510565162951535312, 1.000000000000000000, 0.9510565162951535312, 1.000000000000000000, 0.9510565162951535312, 1.000000000000000000, 0.9510565162951535312, 1.000000000000000000, 0.9510565162951535312, 1.000000000000000000, 0.9510565162951535312, 1.000000000000000000, 0.9510565162951535312, 1.000000000000000000, 0.9510565162951535312, 1.000000000000000000, 0.9510565162951535312, 1.000000000000000000, 0.9510565162951535312, 1.000000000000000000, 0.9510565162951535312, 1.000000000000000000, 0.9510565162951535312, 1.000000000000000000, 0.9510565162951535312, 1.000000000000000000, 0.9510565162951535312, 1.000000000000000000, 0.9510565162951535312, 1.000000000000000000, 0.9510565162951535312, 1.000000000000000000, 0.9510565162951535312, 1.000000000000000000, 0.9510565162951535312, 1.000000000000000000, 0.9510565162951535312, 1.000000000000000000, 0.9510565162951535312, 1.000000000000000000, 0.9510565162951535312, 1.000000000000000000, 0.9510565162951535312, 1.000000000000000000, 0.9510565162951535312, 1.000000000000000000, 0.9510565162951535312, 1.000000000000000000, 0.9510565162951535312, 1.000000000000000000, 0.9510565162951535312, 1.000000000000000000, 0.9510565162951535312, 1.000000000000000000, 0.9510565162951535312, 1.000000000000000000, 0.9510565162951535312, 1.000000000000000000, 0.9510565162951535312, 1.000000000000000000, 0.9510565162951535312, 1.000000000000000000, 0.9510565162951535312, 1.000000000000000000, 0.9510565162951535312, 1.000000000000000000, 0.9510565162951535312, 1.000000000000000000, 0.9510565162951535312, 1.000000000000000000, 0.9510565162951535312, 1.000000000000000000, 0.9510565162951535312, 1.000000000000000000, 0.9510565162951535312, 1.000000000000000000, 0.9510565162951535312, 1.000000000000000000, 0.9510565162951535312, 1.000000000000000000, 0.9510565162951535312, 1.000000000000000000, 0.9510565162951535312, 1.000000000000000000, 0.9510565162951535312, 1.000000000000000000, 0.9510565162951535312, 1.000000000000000000, 0.9510565162951535312, 1.000000000000000000, 0.9510565162951535312, 1.000000000000000000, 0.9510565162951535312, 1.000000000000000000, 0.9510565162951535312, 1.000000000000000000, 0.9510565162951535312, 1.000000000000000000, 0.9510565162951535312, 1.000000000000000000, 0.9510565162951535312, 1.000000000000000000, 0.9510565162951535312, 1.000000000000000000, 0.9510565162951535312, 1.000000000000000000, 0.9510565162951535312, 1.000000000000000000, 0.9510565162951535312, 1.000000000000000000, 0.9510565162951535312, 1.000000000000000000, 0.9510565162951535312, 1.000000000000000000, 0.9510565162951535312, 1.000000000000000000, 0.9510565162951535312, 1.000000000000000000, 0.9510565162951535312, 1.000000000000000000, 0.9510565162951535312, 1.000000000000000000, 0.9510565162951535312, 1.000000000000000000, 0.9510565162951535312, 1.000000000000000000, 0.9510565162951535312, 1.000000000000000000, 0.9510565162951535312, 1.000000000000000000, 0.9510565162951535312, 1.000000000000000000, 0.9510565162951535312, 1.000000000000000000, 0.9510565162951535312, 1.000000000000000000, 0.9510565162951535312, 1.000000000000000000, 0.9510565162951535312, 1.000000000000000000, 0.9510565162951535312, 1.000000000000000000, 0.9510565162951535312, 1.000000000000000000, 0.9510565162951535312, 1.000000000000000000, 0.9510565162951535312, 1.000000000000000000, 0.9510565162951535312, 1.000000000000000000, 0.9510565162951535312, 1.000000000000000000, 0.9510565162951535312, 1.000000000000000000, 0.9510565162951535312, 1.000000000000000000, 0.9510565162951535312, 1.000000000000000000, 0.9510565162951535312, 1.000000000000000000, 0.9510565162951535312, 1.000000000000000000, 0.9510565162951535312, 1.000000000000000000, 0.9510565162951535312, 1.000000000000000000, 0.9510565162951535312, 1.000000000000000000, 0.9510565162951535312, 1.000000000000000000, 0.9510565162951535312, 1.000000000000000000, 0.9510565162951535312, 1.000000000000000000, 0.9510565162951535312, 1.000000000000000000, 0.9510565162951535312, 1.000000000000000000, 0.9510565162951535312, 1.000000000000000000, 0.9510565162951535312, 1.000000000000000000, 0.9510565162951535312, 1.000000000000000000, 0.9510565162951535312, 1.000000000000000000, 0.9510565162951535312, 1.000000000000000000, 0.9510565162951535312, 1.000000000000000000, 0.9510565162951535312, 1.000000000000000000, 0.9510565162951535312, 1.000000000000000000, 0.9510565162951535312, 1.000000000000000000, 0.9510565162951535312, 1.000000000000000000, 0.9510565162951535312, 1.000000000000000000, 0.9510565162951535312, 1.000000000000000000, 0.9510565162951535312, 1.000000000000000000, 0.9510565162951535312, 1.000000000000000000, 0.9510565162951535312, 1.000000000000000000, 0.9510565162951535312, 1.000000000000000000, 0.9510565162951535312, 1.000000000000000000, 0.9510565162951535312, 1.000000000000000000, 0.9510565162951535312, 1.000000000000000000, 0.9510565162951535312, 1.000000000000000000, 0.9510565162951535312, 1.000000000000000000, 0.9510565162951535312, 1.000000000000000000, 0.9510565162951535312, 1.000000000000000000, 0.9510565162951535312, 1.000000000000000000, 0.9510565162951535312, 1.000000000000000000, 0.9510565162951535312, 1.000000000000000000, 0.9510565162951535312, 1.000000000000000000, 0.9510565162951535312, 1.000000000000000000, 0.9510565162951535312, 1.000000000000000000, 0.9510565162951535312, 1.000000000000000000, 0.9510565162951535312, 1.000000000000000000, 0.9510565162951535312, 1.000000000000000000, 0.9510565162951535312, 1.000000000000000000, 0.9510565162951535312, 1.000000000000000000, 0.9510565162951535312, 1.000000000000000000, 0.9510565162951535312, 1.000000000000000000, 0.9510565162951535312, 1.000000000000000000, 0.9510565162951535312, 1.000000000000000000, 0.9510565162951535312, 1.000000000000000000, 0.9510565162951535312, 1.000000000000000000, 0.9510565162951535312, 1.000000000000000000, 0.9510565162951535312, 1.000000000000000000, 0.9510565162951535312, 1.000000000000000000, 0.9510565162951535312, 1.000000000000000000, 0.9510565162951535312, 1.000000000000000000, 0.9510565162951535312, 1.000000000000000000, 0.9510565162951535312, 1.000000000000000000, 0.9510565162951535312, 1.000000000000000000, 0.9510565162951535312, 1.000000000000000000, 0.9510565162951535312, 1.000000000000000000, 0.9510565162951535312, 1.000000000000000000, 0.9510565162951535312, 1.000000000000000000, 0.9510565162951535312, 1.000000000000000000, 0.9510565162951535312, 1.000000000000000000, 0.9510565162951535312, 1.000000000000000000, 0.9510565162951535312, 1.000000000000000000, 0.9510565162951535312, 1.000000000000000000, 0.9836243115514193835, 0.9782066976764483002 ) ) 
 REPRESENTATION_ITEM ( '' )  );
#7151=CARTESIAN_POINT ( 'NONE',  ( 43.01140435219951286, 75.53445800887256212, 39.46799094044489209 ) ) ;
#7153=CARTESIAN_POINT ( 'NONE',  ( 38.01140435219951996, 129.8604996726487286, 35.83527830041810347 ) ) ;
#7154=CARTESIAN_POINT ( 'NONE',  ( 41.64333658814960870, 86.51518717409399528, 30.00020018409699318 ) ) ;
#7158=CARTESIAN_POINT ( 'NONE',  ( 39.92123440845005433, 117.2344580088725792, 38.46393386101375711 ) ) ;
#7159=DIRECTION ( 'NONE',  ( 0.000000000000000000, 1.000000000000000000, 0.000000000000000000 ) ) ;
#7160=CARTESIAN_POINT ( 'NONE',  ( 41.46631938032478359, 81.38445800887257064, 38.96596240072933170 ) ) ;
#7163=CARTESIAN_POINT ( 'NONE',  ( 45.74753988029933538, 152.3297705074272699, 30.44471234641811819 ) ) ;
#7164=CARTESIAN_POINT ( 'NONE',  ( 38.58424406990784661, 105.2297705074273040, 32.77220824515698183 ) ) ;
#7166=CARTESIAN_POINT ( 'NONE',  ( 38.58424406990785371, 134.9651871740940123, 32.77220824515697473 ) ) ;
#7167=FACE_OUTER_BOUND ( 'NONE', #19414, .T. ) ;
#7172=CARTESIAN_POINT ( 'NONE',  ( 38.58424406990784661, 111.2651871740939811, 35.64915139335016647 ) ) ;
#7175=VERTEX_POINT ( 'NONE', #10814 ) ;
#7176=CARTESIAN_POINT ( 'NONE',  ( 44.55648932407425633, 103.8844580088725849, 29.45539723777780239 ) ) ;
#7177=CARTESIAN_POINT ( 'NONE',  ( 44.37947211624943833, 151.2797705074273438, 38.42115945441014446 ) ) ;
#7178=CARTESIAN_POINT ( 'NONE',  ( 38.96631938032478359, 154.0104996726487343, 37.14960608071593384 ) ) ;
#7179=CARTESIAN_POINT ( 'NONE',  ( 45.74753988029933538, 115.1651871740940010, 37.97664729208901946 ) ) ;
#7182=CARTESIAN_POINT ( 'NONE',  ( 47.05648932407426344, 68.51049967264874851, 31.27175355779120025 ) ) ;
#7184=CARTESIAN_POINT ( 'NONE',  ( 42.21948215057684450, 75.45757658655230671, 39.21067981925355639 ) ) ;
#7185=CARTESIAN_POINT ( 'NONE',  ( 41.46631938032478359, 123.1104996726487570, 29.45539723777780239 ) ) ;
#7187=CARTESIAN_POINT ( 'NONE',  ( 39.42975644700377558, 77.81518717409399244, 31.60846029578754468 ) ) ;
#7191=EDGE_CURVE ( 'NONE', #15486, #21451, #6055, .T. ) ;
#7195=ORIENTED_EDGE ( 'NONE', *, *, #18362, .T. ) ;
#7196=CARTESIAN_POINT ( 'NONE',  ( 39.42975644700377558, 143.8151871740940067, 31.60846029578754468 ) ) ;
#7197=FACE_OUTER_BOUND ( 'NONE', #742, .T. ) ;
#7198=ADVANCED_FACE ( 'NONE', ( #2750 ), #11019, .T. ) ;
#7199=CARTESIAN_POINT ( 'NONE',  ( 43.01140435219951286, 101.6297705074273239, 29.55568802177586107 ) ) ;
#7205=EDGE_CURVE ( 'NONE', #16099, #17658, #17369, .T. ) ;
#7207=CARTESIAN_POINT ( 'NONE',  ( 43.80332655382220253, 88.53738109496899256, 39.21067981925355639 ) ) ;
#7208=CARTESIAN_POINT ( 'NONE',  ( 43.01140435219951286, 83.62977050742730967, 29.55568802177586463 ) ) ;
#7209=CARTESIAN_POINT ( 'NONE',  ( 41.64333658814960870, 140.5151871740939953, 30.00020018409699318 ) ) ;
#7212=CARTESIAN_POINT ( 'NONE',  ( 46.10157429594899270, 103.7604996726487627, 38.46393386101376421 ) ) ;
#7214=CARTESIAN_POINT ( 'NONE',  ( 44.55648932407425633, 118.6104996726487570, 38.96596240072933170 ) ) ;
#7218=CARTESIAN_POINT ( 'NONE',  ( 43.80332655382220253, 151.9575765865523067, 29.21067981925356705 ) ) ;
#7219=CARTESIAN_POINT ( 'NONE',  ( 43.01140435219951996, 2.710499672648754466, 34.21067981925357060 ) ) ;
#7220=CARTESIAN_POINT ( 'NONE',  ( 39.42975644700377558, 87.67977050742732104, 36.81289934271958941 ) ) ;
#7223=CARTESIAN_POINT ( 'NONE',  ( 46.59305225739526435, 76.91518717409400097, 31.60846029578754468 ) ) ;
#7226=VERTEX_POINT ( 'NONE', #4958 ) ;
#7227=CARTESIAN_POINT ( 'NONE',  ( 43.01140435219951286, 69.53445800887257633, 39.21067981925356349 ) ) ;
#7229=CARTESIAN_POINT ( 'NONE',  ( 43.01140435219951996, 10.71049967264875491, 34.21067981925357060 ) ) ;
#7230=CARTESIAN_POINT ( 'NONE',  ( 40.27526882409969744, 129.8297705074273267, 37.97664729208901235 ) ) ;
#7235=CARTESIAN_POINT ( 'NONE',  ( 39.42975644700377558, 138.0797705074273267, 31.60846029578754468 ) ) ;
#7237=CARTESIAN_POINT ( 'NONE',  ( 39.92123440845005433, 111.2344580088725650, 38.46393386101375711 ) ) ;
#7240=CARTESIAN_POINT ( 'NONE',  ( 46.59305225739526435, 97.31518717409400665, 36.81289934271958941 ) ) ;
#7246=EDGE_CURVE ( 'NONE', #17093, #1584, #19631, .T. ) ;
#7247=CARTESIAN_POINT ( 'NONE',  ( 46.10157429594899270, 141.8344580088725593, 38.46393386101376421 ) ) ;
#7248=CARTESIAN_POINT ( 'NONE',  ( 45.74753988029933538, 115.4297705074272926, 37.97664729208901946 ) ) ;
#7251=CARTESIAN_POINT ( 'NONE',  ( 38.58424406990785371, 107.9651871740939981, 32.77220824515697473 ) ) ;
#7253=CARTESIAN_POINT ( 'NONE',  ( 46.10157429594899270, 156.8344580088725593, 38.46393386101375711 ) ) ;
#7257=CARTESIAN_POINT ( 'NONE',  ( 47.43856463449118621, 73.87977050742732388, 34.21067981925357060 ) ) ;
#7259=CARTESIAN_POINT ( 'NONE',  ( 44.55648932407425633, 67.88445800887258486, 29.45539723777780239 ) ) ;
#7261=AXIS2_PLACEMENT_3D ( 'NONE', #13926, #10316, #20665 ) ;
#7262=CARTESIAN_POINT ( 'NONE',  ( 48.01140435219951996, 131.0604996726487457, 35.83527830041810347 ) ) ;
#7263=CARTESIAN_POINT ( 'NONE',  ( 39.42975644700377558, 84.41518717409400097, 36.81289934271958941 ) ) ;
#7267=CARTESIAN_POINT ( 'NONE',  ( 38.96631938032478359, 117.0844580088725877, 37.14960608071593384 ) ) ;
#7268=CARTESIAN_POINT ( 'NONE',  ( 48.01140435219951996, 127.1344580088725706, 35.83527830041809636 ) ) ;
#7270=CARTESIAN_POINT ( 'NONE',  ( 41.46631938032478359, 93.38445800887258486, 38.96596240072933170 ) ) ;
#7271=CARTESIAN_POINT ( 'NONE',  ( 40.27526882409969033, 138.8297705074272983, 37.97664729208901946 ) ) ;
#7272=CARTESIAN_POINT ( 'NONE',  ( 39.42975644700377558, 108.0797705074273125, 31.60846029578754468 ) ) ;
#7274=CARTESIAN_POINT ( 'NONE',  ( 45.74753988029934249, 133.1651871740940010, 37.97664729208901235 ) ) ;
#7276=DIRECTION ( 'NONE',  ( 0.000000000000000000, -0.000000000000000000, 1.000000000000000000 ) ) ;
#7283=DIRECTION ( 'NONE',  ( 0.000000000000000000, 0.000000000000000000, 1.000000000000000000 ) ) ;
#7284=CARTESIAN_POINT ( 'NONE',  ( 41.64333658814960870, 117.7151871740939981, 38.42115945441014446 ) ) ;
#7285=( BOUNDED_CURVE ( )  B_SPLINE_CURVE ( 2, ( #10838, #473, #15991, #17429, #19312, #4210, #19416, #2553, #9075, #2337, #9290, #7643, #10939 ),
 .UNSPECIFIED., .F., .F. ) 
 B_SPLINE_CURVE_WITH_KNOTS ( ( 3, 2, 2, 2, 2, 2, 3 ),
 ( 0.8161764705882352811, 0.8176470588235293935, 0.8205882352941176183, 0.8235294117647058432, 0.8264705882352940680, 0.8294117647058824039, 0.8308823529411765163 ),
 .UNSPECIFIED. ) 
 CURVE ( )  GEOMETRIC_REPRESENTATION_ITEM ( )  RATIONAL_B_SPLINE_CURVE ( ( 0.9755282581475768211, 0.9755282581475768211, 1.000000000000000000, 0.9510565162951535312, 1.000000000000000000, 0.9510565162951535312, 1.000000000000000000, 0.9510565162951535312, 1.000000000000000000, 0.9510565162951535312, 1.000000000000000000, 0.9755282581475768211, 0.9755282581475768211 ) ) 
 REPRESENTATION_ITEM ( '' )  );
#7286=EDGE_LOOP ( 'NONE', ( #5962, #20428, #7396, #2232 ) ) ;
#7290=CARTESIAN_POINT ( 'NONE',  ( 43.01140435219951286, 105.5344580088725621, 39.46799094044489209 ) ) ;
#7292=CARTESIAN_POINT ( 'NONE',  ( 39.42975644700377558, 150.0797705074273267, 31.60846029578754468 ) ) ;
#7293=CARTESIAN_POINT ( 'NONE',  ( 45.74753988029933538, 61.42977050742732104, 37.97664729208901946 ) ) ;
#7294=CARTESIAN_POINT ( 'NONE',  ( 46.59305225739526435, 115.3151871740940067, 36.81289934271958941 ) ) ;
#7297=CARTESIAN_POINT ( 'NONE',  ( 39.92123440845004723, 72.26049967264870588, 29.95742577749337343 ) ) ;
#7300=CARTESIAN_POINT ( 'NONE',  ( 38.01140435219952707, 71.93445800887258201, 35.83527830041809636 ) ) ;
#7302=CARTESIAN_POINT ( 'NONE',  ( 43.01140435219951996, 10.71049967264875491, 29.21067981925357060 ) ) ;
#7305=VERTEX_POINT ( 'NONE', #13004 ) ;
#7310=CARTESIAN_POINT ( 'NONE',  ( 38.58424406990786082, 144.1151871740939896, 34.21067981925357060 ) ) ;
#7312=CARTESIAN_POINT ( 'NONE',  ( 47.43856463449117911, 101.0297705074273154, 32.77220824515697473 ) ) ;
#7314=VERTEX_POINT ( 'NONE', #13114 ) ;
#7318=CARTESIAN_POINT ( 'NONE',  ( 44.37947211624943833, 110.4797705074273324, 30.00020018409699318 ) ) ;
#7321=CARTESIAN_POINT ( 'NONE',  ( 43.01140435219951286, 147.8651871740940180, 38.86567161673127657 ) ) ;
#7322=CARTESIAN_POINT ( 'NONE',  ( 38.01140435219951996, 96.56049967264871725, 32.58608133808903773 ) ) ;
#7328=CARTESIAN_POINT ( 'NONE',  ( 47.05648932407426344, 64.58445800887258770, 31.27175355779120025 ) ) ;
#7331=CARTESIAN_POINT ( 'NONE',  ( 46.59305225739526435, 80.17977050742732104, 31.60846029578754468 ) ) ;
#7333=CARTESIAN_POINT ( 'NONE',  ( 46.59305225739526435, 82.31518717409400665, 36.81289934271958941 ) ) ;
#7337=EDGE_LOOP ( 'NONE', ( #4458, #6519, #12463, #12605 ) ) ;
#7340=CARTESIAN_POINT ( 'NONE',  ( 38.58424406990785371, 132.2297705074273040, 32.77220824515697473 ) ) ;
#7346=CARTESIAN_POINT ( 'NONE',  ( 46.10157429594899270, 121.7344580088725934, 29.95742577749336988 ) ) ;
#7349=CARTESIAN_POINT ( 'NONE',  ( 46.59305225739526435, 100.9151871740940010, 31.60846029578754468 ) ) ;
#7350=CARTESIAN_POINT ( 'NONE',  ( 47.05648932407426344, 133.5844580088725877, 31.27175355779120025 ) ) ;
#7354=CARTESIAN_POINT ( 'NONE',  ( 38.01140435219951996, 131.6344580088725991, 32.58608133808903773 ) ) ;
#7355=CARTESIAN_POINT ( 'NONE',  ( 45.74753988029933538, 112.4297705074273210, 37.97664729208901946 ) ) ;
#7358=CARTESIAN_POINT ( 'NONE',  ( 44.37947211624943833, 104.2151871740939981, 30.00020018409699318 ) ) ;
#7361=CARTESIAN_POINT ( 'NONE',  ( 44.55648932407425633, 75.68445800887258201, 38.96596240072933170 ) ) ;
#7365=DIRECTION ( 'NONE',  ( 0.000000000000000000, 0.000000000000000000, 1.000000000000000000 ) ) ;
#7366=CARTESIAN_POINT ( 'NONE',  ( 39.42975644700377558, 72.67977050742730682, 36.81289934271958941 ) ) ;
#7368=EDGE_CURVE ( 'NONE', #16674, #21451, #9082, .T. ) ;
#7370=CARTESIAN_POINT ( 'NONE',  ( 47.05648932407426344, 60.98445800887257207, 37.14960608071593384 ) ) ;
#7372=CARTESIAN_POINT ( 'NONE',  ( 41.46631938032478359, 124.3104996726487457, 38.96596240072933170 ) ) ;
#7373=CARTESIAN_POINT ( 'NONE',  ( 43.01140435219951286, 78.86518717409400381, 38.86567161673127657 ) ) ;
#7379=DIRECTION ( 'NONE',  ( 0.000000000000000000, 0.000000000000000000, 1.000000000000000000 ) ) ;
#7381=CARTESIAN_POINT ( 'NONE',  ( 44.37947211624943833, 145.2797705074273154, 38.42115945441014446 ) ) ;
#7382=CARTESIAN_POINT ( 'NONE',  ( 46.59305225739526435, 107.1797705074273352, 31.60846029578754468 ) ) ;
#7384=CARTESIAN_POINT ( 'NONE',  ( 45.74753988029934249, 139.1651871740940010, 37.97664729208901235 ) ) ;
#7392=CARTESIAN_POINT ( 'NONE',  ( 45.74753988029933538, 115.1651871740940010, 37.97664729208901946 ) ) ;
#7394=ADVANCED_FACE ( 'NONE', ( #6944 ), #13543, .T. ) ;
#7396=ORIENTED_EDGE ( 'NONE', *, *, #20255, .T. ) ;
#7397=CARTESIAN_POINT ( 'NONE',  ( 46.10157429594899270, 88.73445800887256496, 29.95742577749337343 ) ) ;
#7399=CARTESIAN_POINT ( 'NONE',  ( 48.01140435219951996, 155.2104996726487514, 34.21067981925357060 ) ) ;
#7400=CARTESIAN_POINT ( 'NONE',  ( 43.01140435219951286, 104.3651871740940038, 29.55568802177586463 ) ) ;
#7402=CARTESIAN_POINT ( 'NONE',  ( 41.46631938032478359, 76.31049967264874567, 38.96596240072933170 ) ) ;
#7407=CARTESIAN_POINT ( 'NONE',  ( 44.37947211624943833, 71.21518717409399812, 30.00020018409699318 ) ) ;
#7412=( BOUNDED_CURVE ( )  B_SPLINE_CURVE ( 2, ( #18530, #10266, #20192, #18310, #15223, #16755, #11688, #19977, #1666, #21734, #11909, #5191, #18637 ),
 .UNSPECIFIED., .F., .T. ) 
 B_SPLINE_CURVE_WITH_KNOTS ( ( 3, 2, 2, 2, 2, 2, 3 ),
 ( 0.1102941176470588203, 0.1117647058823529466, 0.1147058823529411714, 0.1176470588235294101, 0.1205882352941176489, 0.1235294117647058876, 0.1249999999999999861 ),
 .UNSPECIFIED. ) 
 CURVE ( )  GEOMETRIC_REPRESENTATION_ITEM ( )  RATIONAL_B_SPLINE_CURVE ( ( 0.9755282581475767101, 0.9755282581475765991, 1.000000000000000000, 0.9510565162951535312, 1.000000000000000000, 0.9510565162951535312, 1.000000000000000000, 0.9510565162951535312, 1.000000000000000000, 0.9510565162951535312, 1.000000000000000000, 0.9755282581475769321, 0.9755282581475765991 ) ) 
 REPRESENTATION_ITEM ( '' )  );
#7415=ORIENTED_EDGE ( 'NONE', *, *, #12686, .T. ) ;
#7416=CARTESIAN_POINT ( 'NONE',  ( 40.27526882409969033, 144.5651871740939782, 37.97664729208901946 ) ) ;
#7418=CARTESIAN_POINT ( 'NONE',  ( 39.42975644700377558, 108.0797705074273125, 31.60846029578754468 ) ) ;
#7422=VERTEX_POINT ( 'NONE', #5171 ) ;
#7423=CARTESIAN_POINT ( 'NONE',  ( 38.96631938032478359, 117.0844580088725877, 37.14960608071593384 ) ) ;
#7425=CARTESIAN_POINT ( 'NONE',  ( 38.58424406990784661, 84.22977050742730398, 32.77220824515698183 ) ) ;
#7426=CARTESIAN_POINT ( 'NONE',  ( 40.27526882409969033, 141.5651871740940067, 37.97664729208901946 ) ) ;
#7427=CARTESIAN_POINT ( 'NONE',  ( 38.01140435219952707, 102.7104996726487514, 34.21067981925357060 ) ) ;
#7434=CARTESIAN_POINT ( 'NONE',  ( 47.43856463449117200, 82.72977050742731819, 35.64915139335016647 ) ) ;
#7436=CARTESIAN_POINT ( 'NONE',  ( 44.37947211624943833, 67.01518717409399528, 38.42115945441014446 ) ) ;
#7439=VERTEX_POINT ( 'NONE', #11891 ) ;
#7441=CARTESIAN_POINT ( 'NONE',  ( 43.01140435219951996, 10.71049967264875491, 34.21067981925357060 ) ) ;
#7442=CARTESIAN_POINT ( 'NONE',  ( 38.58424406990785371, 138.2297705074273324, 32.77220824515697473 ) ) ;
#7445=DIRECTION ( 'NONE',  ( 1.000000000000000000, 0.000000000000000000, -0.000000000000000000 ) ) ;
#7447=CARTESIAN_POINT ( 'NONE',  ( 47.43856463449117200, 125.0297705074273011, 32.77220824515698183 ) ) ;
#7448=CARTESIAN_POINT ( 'NONE',  ( 47.05648932407426344, 138.9844580088725650, 37.14960608071593384 ) ) ;
#7449=CARTESIAN_POINT ( 'NONE',  ( 48.01140435219951996, 155.0604996726487457, 35.83527830041809636 ) ) ;
#7453=CARTESIAN_POINT ( 'NONE',  ( 43.01140435219951286, 101.3651871740939896, 29.55568802177586463 ) ) ;
#7454=CARTESIAN_POINT ( 'NONE',  ( 43.01140435219951286, 134.0344580088725763, 29.21067981925356705 ) ) ;
#7457=CARTESIAN_POINT ( 'NONE',  ( 46.10157429594899270, 135.8344580088725877, 38.46393386101376421 ) ) ;
#7458=CARTESIAN_POINT ( 'NONE',  ( 41.64333658814960870, 117.9797705074273182, 38.42115945441014446 ) ) ;
#7461=CARTESIAN_POINT ( 'NONE',  ( 39.42975644700377558, 98.81518717409400665, 31.60846029578754468 ) ) ;
#7464=CARTESIAN_POINT ( 'NONE',  ( 47.05648932407426344, 157.5844580088725877, 31.27175355779120025 ) ) ;
#7465=EDGE_CURVE ( 'NONE', #7175, #13745, #18832, .T. ) ;
#7468=CARTESIAN_POINT ( 'NONE',  ( 43.01140435219951996, 155.0344580088726048, 29.21067981925357060 ) ) ;
#7472=CARTESIAN_POINT ( 'NONE',  ( 41.64333658814960870, 78.97977050742731819, 38.42115945441014446 ) ) ;
#7475=VERTEX_POINT ( 'NONE', #15425 ) ;
#7479=CARTESIAN_POINT ( 'NONE',  ( 46.10157429594899270, 116.6604996726487258, 29.95742577749337343 ) ) ;
#7480=CARTESIAN_POINT ( 'NONE',  ( 44.37947211624943833, 82.01518717409400949, 38.42115945441014446 ) ) ;
#7488=CARTESIAN_POINT ( 'NONE',  ( 41.64333658814960870, 140.7797705074273154, 30.00020018409699318 ) ) ;
#7490=CARTESIAN_POINT ( 'NONE',  ( 41.64333658814960870, 138.7151871740940123, 38.42115945441014446 ) ) ;
#7492=CARTESIAN_POINT ( 'NONE',  ( 43.80332655382220253, 137.8836182503284533, 29.21067981925356705 ) ) ;
#7499=CARTESIAN_POINT ( 'NONE',  ( 44.37947211624943833, 103.0151871740939953, 38.42115945441014446 ) ) ;
#7504=CARTESIAN_POINT ( 'NONE',  ( 38.96631938032478359, 90.08445800887257349, 37.14960608071593384 ) ) ;
#7505=CARTESIAN_POINT ( 'NONE',  ( 39.42975644700377558, 147.6797705074273495, 36.81289934271958941 ) ) ;
#7506=CARTESIAN_POINT ( 'NONE',  ( 46.10157429594899270, 148.7604996726487627, 38.46393386101376421 ) ) ;
#7507=CARTESIAN_POINT ( 'NONE',  ( 46.59305225739526435, 109.3151871740939924, 36.81289934271958941 ) ) ;
#7510=CARTESIAN_POINT ( 'NONE',  ( 45.05633291560662457, 59.76197383743925684, 29.61780626570246966 ) ) ;
#7515=CARTESIAN_POINT ( 'NONE',  ( 38.58424406990784661, 66.26518717409400949, 35.64915139335016647 ) ) ;
#7516=CARTESIAN_POINT ( 'NONE',  ( 46.10157429594899270, 104.6604996726487116, 29.95742577749336988 ) ) ;
#7523=CARTESIAN_POINT ( 'NONE',  ( 47.43856463449118621, 142.6151871740939896, 34.21067981925357060 ) ) ;
#7524=CARTESIAN_POINT ( 'NONE',  ( 39.42975644700377558, 102.6797705074273210, 36.81289934271958941 ) ) ;
#7528=ORIENTED_EDGE ( 'NONE', *, *, #4813, .T. ) ;
#7529=CARTESIAN_POINT ( 'NONE',  ( 38.96631938032478359, 114.0844580088725877, 37.14960608071593384 ) ) ;
#7531=CARTESIAN_POINT ( 'NONE',  ( 46.59305225739526435, 80.17977050742732104, 31.60846029578754468 ) ) ;
#7532=CARTESIAN_POINT ( 'NONE',  ( 44.37947211624943833, 134.2151871740940123, 30.00020018409699318 ) ) ;
#7533=CARTESIAN_POINT ( 'NONE',  ( 46.10157429594899270, 100.7604996726487485, 38.46393386101376421 ) ) ;
#7537=( BOUNDED_CURVE ( )  B_SPLINE_CURVE ( 2, ( #21148, #7492, #20933, #5814, #12545, #7711, #6032, #12762, #4374, #19273, #4174, #10902, #11105 ),
 .UNSPECIFIED., .F., .F. ) 
 B_SPLINE_CURVE_WITH_KNOTS ( ( 3, 2, 2, 2, 2, 2, 3 ),
 ( 0.2132352941176470507, 0.2147058823529411631, 0.2176470588235294157, 0.2205882352941176405, 0.2235294117647058931, 0.2264705882352941180, 0.2279411764705882304 ),
 .UNSPECIFIED. ) 
 CURVE ( )  GEOMETRIC_REPRESENTATION_ITEM ( )  RATIONAL_B_SPLINE_CURVE ( ( 0.9755282581475768211, 0.9755282581475768211, 1.000000000000000000, 0.9510565162951535312, 1.000000000000000000, 0.9510565162951535312, 1.000000000000000000, 0.9510565162951535312, 1.000000000000000000, 0.9510565162951535312, 1.000000000000000000, 0.9755282581475768211, 0.9755282581475768211 ) ) 
 REPRESENTATION_ITEM ( '' )  );
#7540=EDGE_CURVE ( 'NONE', #13261, #13667, #15823, .T. ) ;
#7541=VECTOR ( 'NONE', #19248, 1000.000000000000000 ) ;
#7544=CARTESIAN_POINT ( 'NONE',  ( 47.43856463449117200, 85.72977050742731819, 35.64915139335016647 ) ) ;
#7550=AXIS2_PLACEMENT_3D ( 'NONE', #3847, #20601, #19054 ) ;
#7551=CARTESIAN_POINT ( 'NONE',  ( 39.42975644700377558, 132.6797705074273210, 36.81289934271958941 ) ) ;
#7556=CARTESIAN_POINT ( 'NONE',  ( 38.58424406990784661, 129.2297705074273324, 32.77220824515698183 ) ) ;
#7557=ADVANCED_FACE ( 'NONE', ( #10685 ), #8713, .T. ) ;
#7558=CARTESIAN_POINT ( 'NONE',  ( 44.55648932407425633, 109.6104996726487428, 38.96596240072933170 ) ) ;
#7559=LINE ( 'NONE', #14049, #7993 ) ;
#7560=CARTESIAN_POINT ( 'NONE',  ( 42.21948215057684450, 129.0373810949690210, 29.21067981925356705 ) ) ;
#7563=CARTESIAN_POINT ( 'NONE',  ( 38.58424406990786082, 99.11518717409400381, 34.21067981925357060 ) ) ;
#7564=CARTESIAN_POINT ( 'NONE',  ( 43.01140435219954838, 132.5344580088725763, 39.21067981925356349 ) ) ;
#7567=CARTESIAN_POINT ( 'NONE',  ( 38.96631938032478359, 132.0844580088725877, 37.14960608071593384 ) ) ;
#7568=CARTESIAN_POINT ( 'NONE',  ( 48.01140435219951996, 133.4344580088725820, 32.58608133808903773 ) ) ;
#7569=CARTESIAN_POINT ( 'NONE',  ( 39.42975644700377558, 117.6797705074273210, 36.81289934271958941 ) ) ;
#7572=CARTESIAN_POINT ( 'NONE',  ( 38.58424406990785371, 98.96518717409398391, 32.77220824515697473 ) ) ;
#7573=CARTESIAN_POINT ( 'NONE',  ( 38.01140435219952707, 90.86049967264872862, 35.83527830041809636 ) ) ;
#7579=CARTESIAN_POINT ( 'NONE',  ( 44.55648932407425633, 154.8844580088725991, 29.45539723777780239 ) ) ;
#7580=CARTESIAN_POINT ( 'NONE',  ( 39.42975644700377558, 75.67977050742732104, 36.81289934271958941 ) ) ;
#7581=ORIENTED_EDGE ( 'NONE', *, *, #3602, .T. ) ;
#7583=CARTESIAN_POINT ( 'NONE',  ( 40.27526882409969033, 155.9297705074273210, 30.44471234641811819 ) ) ;
#7586=CARTESIAN_POINT ( 'NONE',  ( 44.55648932407425633, 119.8104996726487457, 29.45539723777780239 ) ) ;
#7588=CARTESIAN_POINT ( 'NONE',  ( 47.43856463449117200, 73.46518717409398391, 35.64915139335016647 ) ) ;
#7594=CARTESIAN_POINT ( 'NONE',  ( 43.01140435219951286, 62.96049967264873004, 29.21067981925356705 ) ) ;
#7595=CARTESIAN_POINT ( 'NONE',  ( 46.10157429594899270, 156.8344580088725309, 38.46393386101376421 ) ) ;
#7596=CARTESIAN_POINT ( 'NONE',  ( 43.01140435219951286, 142.1297705074273097, 38.86567161673127657 ) ) ;
#7597=ADVANCED_FACE ( 'NONE', ( #7167 ), #13870, .T. ) ;
#7599=CARTESIAN_POINT ( 'NONE',  ( 40.27526882409969744, 123.5651871740939924, 37.97664729208901235 ) ) ;
#7601=CARTESIAN_POINT ( 'NONE',  ( 40.27526882409969033, 60.82977050742731961, 37.97664729208901946 ) ) ;
#7605=CARTESIAN_POINT ( 'NONE',  ( 38.01140435219952707, 120.8604996726487428, 35.83527830041809636 ) ) ;
#7606=CARTESIAN_POINT ( 'NONE',  ( 44.37947211624943833, 110.2151871740940123, 30.00020018409699318 ) ) ;
#7607=ORIENTED_EDGE ( 'NONE', *, *, #10183, .T. ) ;
#7609=VERTEX_POINT ( 'NONE', #21362 ) ;
#7610=CARTESIAN_POINT ( 'NONE',  ( 38.01140435219951996, 89.63445800887258486, 32.58608133808903773 ) ) ;
#7611=CARTESIAN_POINT ( 'NONE',  ( 38.01140435219952707, 159.7104996726487514, 34.21067981925357060 ) ) ;
#7613=CARTESIAN_POINT ( 'NONE',  ( 44.55648932407425633, 146.8104996726487457, 29.45539723777780239 ) ) ;
#7614=CARTESIAN_POINT ( 'NONE',  ( 44.37947211624943833, 106.0151871740939953, 38.42115945441014446 ) ) ;
#7620=CARTESIAN_POINT ( 'NONE',  ( 46.10157429594899270, 118.7344580088725650, 29.95742577749336988 ) ) ;
#7624=CARTESIAN_POINT ( 'NONE',  ( 46.59305225739526435, 70.91518717409398675, 31.60846029578754468 ) ) ;
#7626=CARTESIAN_POINT ( 'NONE',  ( 47.05648932407426344, 94.91049967264873999, 37.14960608071593384 ) ) ;
#7632=CARTESIAN_POINT ( 'NONE',  ( 38.58424406990784661, 138.2651871740939669, 35.64915139335016647 ) ) ;
#7633=CARTESIAN_POINT ( 'NONE',  ( 39.42975644700377558, 156.4151871740940010, 36.81289934271958941 ) ) ;
#7634=CARTESIAN_POINT ( 'NONE',  ( 39.42975644700377558, 96.67977050742732104, 36.81289934271958941 ) ) ;
#7637=ORIENTED_EDGE ( 'NONE', *, *, #6001, .F. ) ;
#7640=AXIS2_PLACEMENT_3D ( 'NONE', #2655, #11037, #4747 ) ;
#7642=CARTESIAN_POINT ( 'NONE',  ( 41.46631938032478359, 113.1844580088725820, 29.45539723777780239 ) ) ;
#7643=CARTESIAN_POINT ( 'NONE',  ( 42.21948215057684450, 75.03738109496899256, 29.21067981925356705 ) ) ;
#7646=CARTESIAN_POINT ( 'NONE',  ( 40.27526882409969033, 80.92977050742729261, 30.44471234641811819 ) ) ;
#7647=CARTESIAN_POINT ( 'NONE',  ( 40.27526882409969033, 131.6651871740939725, 30.44471234641811819 ) ) ;
#7649=CARTESIAN_POINT ( 'NONE',  ( 44.55648932407425633, 91.61049967264874283, 38.96596240072933170 ) ) ;
#7654=CARTESIAN_POINT ( 'NONE',  ( 43.01140435219951996, 153.5344580088726048, 39.21067981925357060 ) ) ;
#7657=CARTESIAN_POINT ( 'NONE',  ( 43.80332655382220253, 106.9575765865522925, 29.21067981925356705 ) ) ;
#7659=CARTESIAN_POINT ( 'NONE',  ( 47.43856463449118621, 79.87977050742732388, 34.21067981925357060 ) ) ;
#7665=CARTESIAN_POINT ( 'NONE',  ( 47.05648932407426344, 124.5844580088725735, 31.27175355779120025 ) ) ;
#7666=CARTESIAN_POINT ( 'NONE',  ( 44.37947211624943833, 127.2797705074273438, 38.42115945441014446 ) ) ;
#7671=CARTESIAN_POINT ( 'NONE',  ( 47.43856463449117200, 127.7297705074272898, 35.64915139335016647 ) ) ;
#7672=CARTESIAN_POINT ( 'NONE',  ( 44.55648932407425633, 134.8104996726487457, 29.45539723777780239 ) ) ;
#7673=EDGE_CURVE ( 'NONE', #17454, #5192, #20351, .T. ) ;
#7674=( BOUNDED_CURVE ( )  B_SPLINE_CURVE ( 2, ( #8239, #12971, #14941, #9566, #21688, #13304, #2826, #6466, #4809, #11531, #1398, #20042, #14509 ),
 .UNSPECIFIED., .F., .T. ) 
 B_SPLINE_CURVE_WITH_KNOTS ( ( 3, 2, 2, 2, 2, 2, 3 ),
 ( 0.6102941176470587648, 0.6117647058823529882, 0.6147058823529412130, 0.6176470588235294379, 0.6205882352941176627, 0.6235294117647058876, 0.6250000000000000000 ),
 .UNSPECIFIED. ) 
 CURVE ( )  GEOMETRIC_REPRESENTATION_ITEM ( )  RATIONAL_B_SPLINE_CURVE ( ( 0.9755282581475768211, 0.9755282581475758219, 1.000000000000000000, 0.9510565162951535312, 1.000000000000000000, 0.9510565162951535312, 1.000000000000000000, 0.9510565162951535312, 1.000000000000000000, 0.9510565162951535312, 1.000000000000000000, 0.9755282581475768211, 0.9755282581475768211 ) ) 
 REPRESENTATION_ITEM ( '' )  );
#7675=CARTESIAN_POINT ( 'NONE',  ( 42.21948215057684450, 99.03738109496899256, 29.21067981925356705 ) ) ;
#7676=CARTESIAN_POINT ( 'NONE',  ( 38.01140435219952707, 129.5604996726487457, 32.58608133808903773 ) ) ;
#7683=CARTESIAN_POINT ( 'NONE',  ( 47.05648932407426344, 135.9844580088725934, 37.14960608071593384 ) ) ;
#7684=CARTESIAN_POINT ( 'NONE',  ( 39.42975644700377558, 108.6797705074273352, 36.81289934271958941 ) ) ;
#7687=CARTESIAN_POINT ( 'NONE',  ( 40.27526882409969744, 99.56518717409400665, 37.97664729208901235 ) ) ;
#7690=VERTEX_POINT ( 'NONE', #12438 ) ;
#7694=CARTESIAN_POINT ( 'NONE',  ( 43.01140435219951996, 153.5344580088726048, 39.21067981925357060 ) ) ;
#7695=CARTESIAN_POINT ( 'NONE',  ( 38.58424406990785371, 78.52977050742730114, 35.64915139335015937 ) ) ;
#7696=EDGE_LOOP ( 'NONE', ( #13669, #14567, #6669, #1959 ) ) ;
#7698=CARTESIAN_POINT ( 'NONE',  ( 38.58424406990784661, 153.5297705074273154, 35.64915139335016647 ) ) ;
#7700=CARTESIAN_POINT ( 'NONE',  ( 39.92123440845004723, 124.1604996726487400, 38.46393386101376421 ) ) ;
#7701=CARTESIAN_POINT ( 'NONE',  ( 46.59305225739526435, 79.31518717409399244, 36.81289934271958941 ) ) ;
#7704=CARTESIAN_POINT ( 'NONE',  ( 43.80332655382220253, 112.5373810949689926, 39.21067981925355639 ) ) ;
#7708=CARTESIAN_POINT ( 'NONE',  ( 38.58424406990786082, 141.3797705074273381, 34.21067981925357060 ) ) ;
#7710=CARTESIAN_POINT ( 'NONE',  ( 43.01140435219951286, 126.8651871740939896, 38.86567161673127657 ) ) ;
#7711=CARTESIAN_POINT ( 'NONE',  ( 48.01140435219951996, 137.3604996726487286, 32.58608133808903773 ) ) ;
#7717=CARTESIAN_POINT ( 'NONE',  ( 41.64333658814960870, 105.7151871740940123, 38.42115945441014446 ) ) ;
#7720=EDGE_LOOP ( 'NONE', ( #6291, #20740, #16315, #20191 ) ) ;
#7721=CARTESIAN_POINT ( 'NONE',  ( 38.01140435219952707, 95.78445800887259054, 34.21067981925357060 ) ) ;
#7722=CARTESIAN_POINT ( 'NONE',  ( 47.05648932407426344, 102.9844580088725792, 37.14960608071593384 ) ) ;
#7723=CARTESIAN_POINT ( 'NONE',  ( 38.01140435219952707, 147.7104996726487514, 34.21067981925357060 ) ) ;
#7724=CARTESIAN_POINT ( 'NONE',  ( 47.43856463449117200, 109.4651871740940123, 35.64915139335016647 ) ) ;
#7726=CARTESIAN_POINT ( 'NONE',  ( 48.01140435219951996, 65.06049967264873146, 35.83527830041810347 ) ) ;
#7727=CARTESIAN_POINT ( 'NONE',  ( 43.01140435219951286, 64.46049967264873715, 39.21067981925356349 ) ) ;
#7732=( BOUNDED_CURVE ( )  B_SPLINE_CURVE ( 2, ( #3295, #21707, #6936, #13536, #3625, #13748, #8587, #3517, #10347, #8261, #1529, #17052, #18502 ),
 .UNSPECIFIED., .F., .F. ) 
 B_SPLINE_CURVE_WITH_KNOTS ( ( 3, 2, 2, 2, 2, 2, 3 ),
 ( 0.6985294117647058432, 0.6999999999999999556, 0.7029411764705881804, 0.7058823529411765163, 0.7088235294117647411, 0.7117647058823529660, 0.7132352941176470784 ),
 .UNSPECIFIED. ) 
 CURVE ( )  GEOMETRIC_REPRESENTATION_ITEM ( )  RATIONAL_B_SPLINE_CURVE ( ( 0.9755282581475768211, 0.9755282581475768211, 1.000000000000000000, 0.9510565162951535312, 1.000000000000000000, 0.9510565162951535312, 1.000000000000000000, 0.9510565162951535312, 1.000000000000000000, 0.9510565162951535312, 1.000000000000000000, 0.9755282581475768211, 0.9755282581475768211 ) ) 
 REPRESENTATION_ITEM ( '' )  );
#7733=CARTESIAN_POINT ( 'NONE',  ( 39.42975644700377558, 71.81518717409400665, 31.60846029578754468 ) ) ;
#7735=CARTESIAN_POINT ( 'NONE',  ( 42.21948215057684450, 114.0373810949690210, 29.21067981925356705 ) ) ;
#7738=ORIENTED_EDGE ( 'NONE', *, *, #9514, .T. ) ;
#7742=CARTESIAN_POINT ( 'NONE',  ( 47.43856463449117200, 130.4651871740939839, 35.64915139335016647 ) ) ;
#7743=CARTESIAN_POINT ( 'NONE',  ( 44.37947211624943833, 157.0151871740940237, 38.42115945441014446 ) ) ;
#7744=CARTESIAN_POINT ( 'NONE',  ( 43.01140435219951286, 92.62977050742732388, 29.55568802177586107 ) ) ;
#7748=EDGE_CURVE ( 'NONE', #13985, #11079, #7537, .T. ) ;
#7753=CARTESIAN_POINT ( 'NONE',  ( 38.58424406990784661, 75.52977050742732956, 35.64915139335016647 ) ) ;
#7754=CARTESIAN_POINT ( 'NONE',  ( 44.37947211624943833, 131.2151871740940123, 30.00020018409699318 ) ) ;
#7755=CARTESIAN_POINT ( 'NONE',  ( 48.01140435219951996, 89.21049967264873715, 34.21067981925357060 ) ) ;
#7760=CARTESIAN_POINT ( 'NONE',  ( 48.01140435219951996, 62.21049967264874425, 34.21067981925357060 ) ) ;
#7763=CARTESIAN_POINT ( 'NONE',  ( 43.01140435219951286, 79.12977050742732388, 38.86567161673127657 ) ) ;
#7771=CARTESIAN_POINT ( 'NONE',  ( 45.74753988029934249, 128.3297705074273267, 30.44471234641812174 ) ) ;
#7774=CARTESIAN_POINT ( 'NONE',  ( 43.01140435219951286, 130.1297705074273381, 38.86567161673127657 ) ) ;
#7776=CARTESIAN_POINT ( 'NONE',  ( 41.46631938032478359, 63.38445800887257064, 38.96596240072933170 ) ) ;
#7781=CARTESIAN_POINT ( 'NONE',  ( 43.01140435219951286, 73.46049967264872294, 39.21067981925356349 ) ) ;
#7784=CARTESIAN_POINT ( 'NONE',  ( 39.92123440845004723, 132.2344580088725650, 38.46393386101376421 ) ) ;
#7785=CARTESIAN_POINT ( 'NONE',  ( 45.74753988029933538, 101.3297705074273267, 30.44471234641811819 ) ) ;
#7788=CARTESIAN_POINT ( 'NONE',  ( 46.59305225739526435, 97.91518717409400097, 31.60846029578754468 ) ) ;
#7790=ORIENTED_EDGE ( 'NONE', *, *, #9681, .F. ) ;
#7791=DIRECTION ( 'NONE',  ( 0.000000000000000000, 1.000000000000000000, 0.000000000000000000 ) ) ;
#7795=CARTESIAN_POINT ( 'NONE',  ( 46.59305225739526435, 71.17977050742730682, 31.60846029578754468 ) ) ;
#7798=CARTESIAN_POINT ( 'NONE',  ( 41.64333658814960870, 150.9797705074273324, 38.42115945441014446 ) ) ;
#7800=CARTESIAN_POINT ( 'NONE',  ( 47.05648932407426344, 119.5104996726487343, 31.27175355779120025 ) ) ;
#7801=CARTESIAN_POINT ( 'NONE',  ( 41.64333658814960870, 75.71518717409401233, 38.42115945441014446 ) ) ;
#7803=LINE ( 'NONE', #9460, #13448 ) ;
#7808=CARTESIAN_POINT ( 'NONE',  ( 43.01140435219951996, 10.71049967264875491, 29.21067981925357060 ) ) ;
#7810=CARTESIAN_POINT ( 'NONE',  ( 38.58424406990784661, 135.5297705074273154, 35.64915139335016647 ) ) ;
#7812=CARTESIAN_POINT ( 'NONE',  ( 38.58424406990786082, 123.1151871740940038, 34.21067981925357060 ) ) ;
#7813=EDGE_CURVE ( 'NONE', #15014, #16099, #11649, .T. ) ;
#7817=CARTESIAN_POINT ( 'NONE',  ( 43.01140435219951996, 148.4604996726487798, 39.21067981925356349 ) ) ;
#7821=CARTESIAN_POINT ( 'NONE',  ( 43.01140435219951286, 107.3651871740940038, 29.55568802177586463 ) ) ;
#7822=ORIENTED_EDGE ( 'NONE', *, *, #5675, .F. ) ;
#7823=DIRECTION ( 'NONE',  ( 0.000000000000000000, 1.000000000000000000, 0.000000000000000000 ) ) ;
#7825=CARTESIAN_POINT ( 'NONE',  ( 38.96631938032478359, 83.48445800887257917, 31.27175355779120025 ) ) ;
#7829=CARTESIAN_POINT ( 'NONE',  ( 39.92123440845004723, 148.1604996726487400, 38.46393386101376421 ) ) ;
#7830=CARTESIAN_POINT ( 'NONE',  ( 43.01140435219951286, 110.3651871740939754, 29.55568802177586463 ) ) ;
#7832=CARTESIAN_POINT ( 'NONE',  ( 38.01140435219952707, 63.71049967264874425, 34.21067981925357060 ) ) ;
#7836=FACE_OUTER_BOUND ( 'NONE', #20058, .T. ) ;
#7838=CARTESIAN_POINT ( 'NONE',  ( 44.37947211624943833, 158.4797705074273040, 30.00020018409699318 ) ) ;
#7840=CARTESIAN_POINT ( 'NONE',  ( 41.64333658814960870, 152.5151871740940237, 30.00020018409699318 ) ) ;
#7841=CARTESIAN_POINT ( 'NONE',  ( 43.01140435219957681, 94.46049967264876557, 39.21067981925356349 ) ) ;
#7845=CARTESIAN_POINT ( 'NONE',  ( 38.58424406990785371, 66.26518717409400949, 35.64915139335015937 ) ) ;
#7849=CARTESIAN_POINT ( 'NONE',  ( 45.74753988029933538, 131.0651871740940067, 30.44471234641811819 ) ) ;
#7855=CARTESIAN_POINT ( 'NONE',  ( 44.55648932407425633, 115.8844580088725991, 29.45539723777780239 ) ) ;
#7856=DIRECTION ( 'NONE',  ( 0.000000000000000000, 0.000000000000000000, 1.000000000000000000 ) ) ;
#7857=CARTESIAN_POINT ( 'NONE',  ( 38.58424406990784661, 72.22977050742733240, 32.77220824515698183 ) ) ;
#7858=CARTESIAN_POINT ( 'NONE',  ( 44.37947211624943833, 140.2151871740940123, 30.00020018409699318 ) ) ;
#7860=CARTESIAN_POINT ( 'NONE',  ( 39.92123440845004723, 91.16049967264872578, 38.46393386101376421 ) ) ;
#7865=CARTESIAN_POINT ( 'NONE',  ( 46.10157429594899270, 150.8344580088725593, 38.46393386101375711 ) ) ;
#7868=CARTESIAN_POINT ( 'NONE',  ( 44.37947211624943833, 73.27977050742731535, 38.42115945441014446 ) ) ;
#7875=LINE ( 'NONE', #19437, #19778 ) ;
#7876=CARTESIAN_POINT ( 'NONE',  ( 38.58424406990785371, 120.2297705074273182, 32.77220824515697473 ) ) ;
#7879=DIRECTION ( 'NONE',  ( 0.000000000000000000, 1.000000000000000000, 0.000000000000000000 ) ) ;
#7880=ORIENTED_EDGE ( 'NONE', *, *, #11878, .F. ) ;
#7881=CARTESIAN_POINT ( 'NONE',  ( 39.42975644700377558, 126.6797705074273210, 36.81289934271958941 ) ) ;
#7883=CARTESIAN_POINT ( 'NONE',  ( 44.55648932407425633, 66.68445800887256780, 38.96596240072933170 ) ) ;
#7885=CARTESIAN_POINT ( 'NONE',  ( 39.92123440845005433, 101.3344580088725877, 29.95742577749336988 ) ) ;
#7892=CARTESIAN_POINT ( 'NONE',  ( 44.55648932407425633, 124.8844580088725706, 29.45539723777780239 ) ) ;
#7893=CARTESIAN_POINT ( 'NONE',  ( 47.43856463449118621, 100.8797705074273239, 34.21067981925357060 ) ) ;
#7896=CARTESIAN_POINT ( 'NONE',  ( 38.58424406990785371, 99.26518717409398107, 35.64915139335015937 ) ) ;
#7897=CARTESIAN_POINT ( 'NONE',  ( 41.46631938032478359, 85.31049967264874567, 38.96596240072933170 ) ) ;
#7902=CARTESIAN_POINT ( 'NONE',  ( 45.74753988029934249, 65.32977050742731251, 30.44471234641812174 ) ) ;
#7905=CARTESIAN_POINT ( 'NONE',  ( 38.58424406990784661, 156.5297705074272869, 35.64915139335016647 ) ) ;
#7910=CARTESIAN_POINT ( 'NONE',  ( 43.01140435219951286, 110.9604996726487371, 28.95336869806222779 ) ) ;
#7911=CARTESIAN_POINT ( 'NONE',  ( 38.58424406990784661, 69.26518717409398107, 35.64915139335016647 ) ) ;
#7917=CARTESIAN_POINT ( 'NONE',  ( 41.46631938032478359, 155.1844580088725820, 29.45539723777780239 ) ) ;
#7918=CARTESIAN_POINT ( 'NONE',  ( 45.74753988029933538, 137.3297705074273267, 30.44471234641811819 ) ) ;
#7920=CARTESIAN_POINT ( 'NONE',  ( 47.43856463449117911, 130.7651871740939953, 32.77220824515697473 ) ) ;
#7926=LINE ( 'NONE', #17827, #9342 ) ;
#7927=ORIENTED_EDGE ( 'NONE', *, *, #12549, .T. ) ;
#7928=CARTESIAN_POINT ( 'NONE',  ( 43.01140435219951996, 10.71049967264875491, 34.21067981925357060 ) ) ;
#7930=CARTESIAN_POINT ( 'NONE',  ( 41.46631938032478359, 84.38445800887258486, 38.96596240072933170 ) ) ;
#7931=CARTESIAN_POINT ( 'NONE',  ( 43.80332655382220253, 103.9575765865522925, 29.21067981925356705 ) ) ;
#7933=CARTESIAN_POINT ( 'NONE',  ( 38.01140435219952707, 153.7104996726487514, 34.21067981925357060 ) ) ;
#7934=CARTESIAN_POINT ( 'NONE',  ( 47.43856463449117200, 97.46518717409399812, 35.64915139335016647 ) ) ;
#7937=CARTESIAN_POINT ( 'NONE',  ( 39.92123440845004723, 61.16049967264873288, 38.46393386101376421 ) ) ;
#7939=CARTESIAN_POINT ( 'NONE',  ( 46.10157429594899270, 69.83445800887255928, 38.46393386101375711 ) ) ;
#7942=CARTESIAN_POINT ( 'NONE',  ( 47.43856463449117200, 64.76518717409400949, 32.77220824515698183 ) ) ;
#7945=CARTESIAN_POINT ( 'NONE',  ( 40.27526882409969744, 150.5651871740940067, 37.97664729208901235 ) ) ;
#7946=FACE_OUTER_BOUND ( 'NONE', #2821, .T. ) ;
#7951=CARTESIAN_POINT ( 'NONE',  ( 47.43856463449117911, 64.76518717409400949, 32.77220824515697473 ) ) ;
#7955=CARTESIAN_POINT ( 'NONE',  ( 47.43856463449117200, 133.4651871740940123, 35.64915139335016647 ) ) ;
#7959=ORIENTED_EDGE ( 'NONE', *, *, #11706, .T. ) ;
#7960=CARTESIAN_POINT ( 'NONE',  ( 43.80332655382220253, 59.88361825032847463, 29.21067981925356705 ) ) ;
#7962=CARTESIAN_POINT ( 'NONE',  ( 41.64333658814960870, 77.77977050742731535, 30.00020018409699318 ) ) ;
#7963=CARTESIAN_POINT ( 'NONE',  ( 46.59305225739526435, 139.9151871740940010, 31.60846029578754468 ) ) ;
#7965=CARTESIAN_POINT ( 'NONE',  ( 41.46631938032478359, 88.31049967264874567, 38.96596240072933170 ) ) ;
#7968=DIRECTION ( 'NONE',  ( 0.000000000000000000, 0.000000000000000000, 1.000000000000000000 ) ) ;
#7970=CARTESIAN_POINT ( 'NONE',  ( 45.74753988029933538, 92.06518717409399244, 30.44471234641811819 ) ) ;
#7972=CARTESIAN_POINT ( 'NONE',  ( 44.55648932407425633, 108.6844580088725820, 38.96596240072933170 ) ) ;
#7973=CARTESIAN_POINT ( 'NONE',  ( 46.10157429594899270, 141.8344580088725593, 38.46393386101375711 ) ) ;
#7975=CARTESIAN_POINT ( 'NONE',  ( 40.27526882409969033, 77.92977050742732104, 30.44471234641811819 ) ) ;
#7979=ORIENTED_EDGE ( 'NONE', *, *, #1718, .F. ) ;
#7980=CARTESIAN_POINT ( 'NONE',  ( 39.42975644700377558, 158.8151871740940067, 31.60846029578754468 ) ) ;
#7984=CARTESIAN_POINT ( 'NONE',  ( 47.43856463449117911, 128.0297705074273154, 32.77220824515697473 ) ) ;
#7986=CARTESIAN_POINT ( 'NONE',  ( 46.10157429594899270, 87.83445800887255928, 38.46393386101375711 ) ) ;
#7987=( BOUNDED_CURVE ( )  B_SPLINE_CURVE ( 2, ( #21214, #16342, #8206, #1474, #14907, #4438, #8093, #16449, #14800, #1362, #12717, #1037, #21541 ),
 .UNSPECIFIED., .F., .F. ) 
 B_SPLINE_CURVE_WITH_KNOTS ( ( 3, 2, 2, 2, 2, 2, 3 ),
 ( 0.2720588235294117974, 0.2735294117647059098, 0.2764705882352941346, 0.2794117647058823595, 0.2823529411764705843, 0.2852941176470588092, 0.2867647058823529216 ),
 .UNSPECIFIED. ) 
 CURVE ( )  GEOMETRIC_REPRESENTATION_ITEM ( )  RATIONAL_B_SPLINE_CURVE ( ( 0.9755282581475768211, 0.9755282581475772652, 1.000000000000000000, 0.9510565162951535312, 1.000000000000000000, 0.9510565162951535312, 1.000000000000000000, 0.9510565162951535312, 1.000000000000000000, 0.9510565162951535312, 1.000000000000000000, 0.9755282581475768211, 0.9755282581475768211 ) ) 
 REPRESENTATION_ITEM ( '' )  );
#7989=CARTESIAN_POINT ( 'NONE',  ( 43.01140435219951286, 115.1297705074272955, 38.86567161673127657 ) ) ;
#7990=CARTESIAN_POINT ( 'NONE',  ( 43.01140435219951286, 99.53445800887257633, 39.21067981925356349 ) ) ;
#7991=CARTESIAN_POINT ( 'NONE',  ( 47.43856463449117200, 88.72977050742730398, 35.64915139335016647 ) ) ;
#7992=CARTESIAN_POINT ( 'NONE',  ( 41.46631938032478359, 65.18445800887258201, 29.45539723777780239 ) ) ;
#7993=VECTOR ( 'NONE', #5993, 1000.000000000000000 ) ;
#7995=CARTESIAN_POINT ( 'NONE',  ( 38.96631938032478359, 83.48445800887257917, 31.27175355779120025 ) ) ;
#7996=CARTESIAN_POINT ( 'NONE',  ( 41.46631938032478359, 96.11049967264874283, 29.45539723777780239 ) ) ;
#7999=CARTESIAN_POINT ( 'NONE',  ( 41.46631938032478359, 103.3104996726487457, 38.96596240072933170 ) ) ;
#8002=CARTESIAN_POINT ( 'NONE',  ( 38.01140435219951996, 119.6344580088725706, 32.58608133808903773 ) ) ;
#8003=CARTESIAN_POINT ( 'NONE',  ( 38.58424406990786082, 99.37977050742732388, 34.21067981925357060 ) ) ;
#8006=CARTESIAN_POINT ( 'NONE',  ( 47.43856463449117911, 85.46518717409399812, 35.64915139335015937 ) ) ;
#8009=DIRECTION ( 'NONE',  ( 0.000000000000000000, 1.000000000000000000, 0.000000000000000000 ) ) ;
#8011=CARTESIAN_POINT ( 'NONE',  ( 38.58424406990786082, 144.3797705074273097, 34.21067981925357060 ) ) ;
#8014=CARTESIAN_POINT ( 'NONE',  ( 38.58424406990785371, 66.52977050742731535, 35.64915139335015937 ) ) ;
#8016=ORIENTED_EDGE ( 'NONE', *, *, #17394, .T. ) ;
#8017=CARTESIAN_POINT ( 'NONE',  ( 43.01140435219951286, 157.1297705074272812, 38.86567161673127657 ) ) ;
#8021=CARTESIAN_POINT ( 'NONE',  ( 38.96631938032478359, 112.0104996726487485, 37.14960608071593384 ) ) ;
#8022=CARTESIAN_POINT ( 'NONE',  ( 38.58424406990786082, 66.11518717409398960, 34.21067981925357060 ) ) ;
#8027=CARTESIAN_POINT ( 'NONE',  ( 43.01140435219951286, 149.0344580088725763, 28.95336869806222779 ) ) ;
#8028=CARTESIAN_POINT ( 'NONE',  ( 44.37947211624943833, 136.2797705074273154, 38.42115945441014446 ) ) ;
#8030=CARTESIAN_POINT ( 'NONE',  ( 45.74753988029934249, 125.0651871740939924, 30.44471234641812174 ) ) ;
#8033=DIRECTION ( 'NONE',  ( 0.000000000000000000, 1.000000000000000000, 0.000000000000000000 ) ) ;
#8034=CARTESIAN_POINT ( 'NONE',  ( 43.01140435219951996, 149.9604996726487798, 29.21067981925357060 ) ) ;
#8036=CARTESIAN_POINT ( 'NONE',  ( 48.01140435219951996, 83.06049967264873146, 35.83527830041809636 ) ) ;
#8039=ORIENTED_EDGE ( 'NONE', *, *, #11781, .F. ) ;
#8042=CARTESIAN_POINT ( 'NONE',  ( 43.01140435219951286, 78.53445800887259054, 39.46799094044489209 ) ) ;
#8043=CARTESIAN_POINT ( 'NONE',  ( 44.55648932407425633, 103.8844580088725849, 29.45539723777780239 ) ) ;
#8044=CARTESIAN_POINT ( 'NONE',  ( 48.01140435219951996, 140.0604996726487457, 35.83527830041810347 ) ) ;
#8045=CARTESIAN_POINT ( 'NONE',  ( 46.59305225739526435, 100.3151871740940067, 36.81289934271958941 ) ) ;
#8053=CARTESIAN_POINT ( 'NONE',  ( 43.01140435219951286, 158.6297705074273381, 29.55568802177586463 ) ) ;
#8059=CARTESIAN_POINT ( 'NONE',  ( 44.37947211624943833, 74.21518717409399812, 30.00020018409699318 ) ) ;
#8064=CARTESIAN_POINT ( 'NONE',  ( 39.42975644700377558, 132.4151871740940010, 36.81289934271958941 ) ) ;
#8070=ORIENTED_EDGE ( 'NONE', *, *, #21778, .F. ) ;
#8071=CARTESIAN_POINT ( 'NONE',  ( 43.01140435219951286, 66.53445800887257633, 39.21067981925356349 ) ) ;
#8073=CARTESIAN_POINT ( 'NONE',  ( 38.58424406990786082, 66.37977050742730967, 34.21067981925357060 ) ) ;
#8074=CARTESIAN_POINT ( 'NONE',  ( 43.01140435219951286, 122.3651871740939754, 29.55568802177586463 ) ) ;
#8076=CARTESIAN_POINT ( 'NONE',  ( 41.46631938032478359, 91.31049967264874567, 38.96596240072933170 ) ) ;
#8080=CARTESIAN_POINT ( 'NONE',  ( 40.27526882409969033, 89.66518717409400097, 30.44471234641811819 ) ) ;
#8081=CARTESIAN_POINT ( 'NONE',  ( 47.05648932407426344, 150.9844580088725934, 37.14960608071593384 ) ) ;
#8083=VERTEX_POINT ( 'NONE', #16030 ) ;
#8084=CARTESIAN_POINT ( 'NONE',  ( 43.01140435219951286, 77.62977050742729546, 29.55568802177586463 ) ) ;
#8090=CARTESIAN_POINT ( 'NONE',  ( 43.01140435219951996, 10.71049967264875491, 29.21067981925357060 ) ) ;
#8091=CARTESIAN_POINT ( 'NONE',  ( 41.64333658814960870, 119.7797705074273296, 30.00020018409699318 ) ) ;
#8092=VERTEX_POINT ( 'NONE', #9229 ) ;
#8093=CARTESIAN_POINT ( 'NONE',  ( 48.01140435219951996, 130.2844580088725763, 34.21067981925357060 ) ) ;
#8094=ORIENTED_EDGE ( 'NONE', *, *, #7191, .T. ) ;
#8095=CARTESIAN_POINT ( 'NONE',  ( 44.37947211624943833, 119.4797705074273182, 30.00020018409699318 ) ) ;
#8097=CARTESIAN_POINT ( 'NONE',  ( 47.43856463449117200, 151.7651871740939669, 32.77220824515698183 ) ) ;
#8100=CARTESIAN_POINT ( 'NONE',  ( 39.92123440845005433, 83.33445800887257349, 29.95742577749336988 ) ) ;
#8101=CARTESIAN_POINT ( 'NONE',  ( 38.96631938032478359, 96.41049967264873999, 31.27175355779120025 ) ) ;
#8103=CARTESIAN_POINT ( 'NONE',  ( 43.01140435219951996, 10.71049967264875491, 29.21067981925357060 ) ) ;
#8106=CARTESIAN_POINT ( 'NONE',  ( 48.01140435219951996, 127.1344580088725706, 35.83527830041810347 ) ) ;
#8107=CARTESIAN_POINT ( 'NONE',  ( 41.64333658814960870, 101.7797705074273154, 30.00020018409699318 ) ) ;
#8110=CARTESIAN_POINT ( 'NONE',  ( 43.01140435219951286, 84.86518717409400381, 38.86567161673127657 ) ) ;
#8111=CARTESIAN_POINT ( 'NONE',  ( 43.01140435219951996, 10.71049967264875491, 34.21067981925357060 ) ) ;
#8113=CARTESIAN_POINT ( 'NONE',  ( 43.01140435219951996, 10.71049967264875491, 34.21067981925357060 ) ) ;
#8116=CARTESIAN_POINT ( 'NONE',  ( 44.37947211624943833, 145.2797705074273154, 38.42115945441014446 ) ) ;
#8119=EDGE_CURVE ( 'NONE', #15219, #2955, #10768, .T. ) ;
#8120=CARTESIAN_POINT ( 'NONE',  ( 47.43856463449118621, 67.87977050742730967, 34.21067981925357060 ) ) ;
#8123=CARTESIAN_POINT ( 'NONE',  ( 47.43856463449117200, 148.7297705074273324, 35.64915139335016647 ) ) ;
#8124=CARTESIAN_POINT ( 'NONE',  ( 43.01140435219951996, 10.71049967264875491, 39.21067981925356349 ) ) ;
#8125=CARTESIAN_POINT ( 'NONE',  ( 47.05648932407426344, 112.9104996726487400, 37.14960608071593384 ) ) ;
#8126=CARTESIAN_POINT ( 'NONE',  ( 44.37947211624943833, 68.21518717409399812, 30.00020018409699318 ) ) ;
#8132=CARTESIAN_POINT ( 'NONE',  ( 44.55648932407425633, 150.6844580088725820, 38.96596240072933170 ) ) ;
#8133=CARTESIAN_POINT ( 'NONE',  ( 44.37947211624943833, 134.4797705074273324, 30.00020018409699318 ) ) ;
#8135=CARTESIAN_POINT ( 'NONE',  ( 43.01140435219951286, 120.8651871740940180, 38.86567161673127657 ) ) ;
#8137=CARTESIAN_POINT ( 'NONE',  ( 43.01140435219951996, 10.71049967264875491, 9.210679819253577705 ) ) ;
#8138=CARTESIAN_POINT ( 'NONE',  ( 45.51144763592289877, 59.40255829349017347, 29.88057779030456373 ) ) ;
#8143=CARTESIAN_POINT ( 'NONE',  ( 38.58424406990785371, 99.52977050742730114, 35.64915139335015937 ) ) ;
#8148=CARTESIAN_POINT ( 'NONE',  ( 46.10157429594899270, 85.73445800887256496, 29.95742577749337343 ) ) ;
#8150=CARTESIAN_POINT ( 'NONE',  ( 38.01140435219951996, 135.5604996726487457, 32.58608133808903773 ) ) ;
#8151=CARTESIAN_POINT ( 'NONE',  ( 44.37947211624943833, 101.2151871740939981, 30.00020018409699318 ) ) ;
#8157=CARTESIAN_POINT ( 'NONE',  ( 42.21948215057684450, 105.0373810949690210, 29.21067981925356705 ) ) ;
#8161=CARTESIAN_POINT ( 'NONE',  ( 43.01140435219951286, 157.1297705074272812, 38.86567161673127657 ) ) ;
#8164=CARTESIAN_POINT ( 'NONE',  ( 40.27526882409969744, 147.5651871740939782, 37.97664729208901235 ) ) ;
#8169=CARTESIAN_POINT ( 'NONE',  ( 41.64333658814960870, 71.51518717409399528, 30.00020018409699318 ) ) ;
#8172=CARTESIAN_POINT ( 'NONE',  ( 43.01140435219951996, 10.71049967264875491, 29.21067981925357060 ) ) ;
#8173=CARTESIAN_POINT ( 'NONE',  ( 38.58424406990786082, 120.1151871740940038, 34.21067981925357060 ) ) ;
#8177=AXIS2_PLACEMENT_3D ( 'NONE', #2454, #2666, #14354 ) ;
#8179=CARTESIAN_POINT ( 'NONE',  ( 38.01140435219952707, 113.9344580088725820, 35.83527830041809636 ) ) ;
#8181=EDGE_CURVE ( 'NONE', #17373, #5984, #4180, .T. ) ;
#8182=CARTESIAN_POINT ( 'NONE',  ( 38.96631938032478359, 110.4844580088725792, 31.27175355779120025 ) ) ;
#8185=CARTESIAN_POINT ( 'NONE',  ( 45.74753988029933538, 64.42977050742732104, 37.97664729208901946 ) ) ;
#8186=CARTESIAN_POINT ( 'NONE',  ( 44.37947211624943833, 125.2151871740939981, 30.00020018409699318 ) ) ;
#8188=CARTESIAN_POINT ( 'NONE',  ( 48.01140435219951996, 83.21049967264873715, 34.21067981925357060 ) ) ;
#8190=CARTESIAN_POINT ( 'NONE',  ( 48.01140435219951996, 98.06049967264873146, 35.83527830041809636 ) ) ;
#8192=CARTESIAN_POINT ( 'NONE',  ( 39.42975644700377558, 84.41518717409400097, 36.81289934271958941 ) ) ;
#8194=CARTESIAN_POINT ( 'NONE',  ( 43.01140435219951996, 10.71049967264875491, 34.21067981925357060 ) ) ;
#8196=CARTESIAN_POINT ( 'NONE',  ( 45.74753988029933538, 64.42977050742732104, 37.97664729208901946 ) ) ;
#8201=CARTESIAN_POINT ( 'NONE',  ( 43.01140435219951286, 150.8651871740940180, 38.86567161673127657 ) ) ;
#8203=CARTESIAN_POINT ( 'NONE',  ( 45.74753988029934249, 113.3297705074272983, 30.44471234641812174 ) ) ;
#8206=CARTESIAN_POINT ( 'NONE',  ( 44.55648932407425633, 130.8844580088725706, 29.45539723777780239 ) ) ;
#8207=ORIENTED_EDGE ( 'NONE', *, *, #2884, .F. ) ;
#8208=CARTESIAN_POINT ( 'NONE',  ( 40.27526882409969033, 114.8297705074273125, 37.97664729208901946 ) ) ;
#8209=DIRECTION ( 'NONE',  ( 0.000000000000000000, 0.000000000000000000, 1.000000000000000000 ) ) ;
#8210=CARTESIAN_POINT ( 'NONE',  ( 44.37947211624943833, 85.27977050742731535, 38.42115945441014446 ) ) ;
#8211=CARTESIAN_POINT ( 'NONE',  ( 41.64333658814960870, 158.5151871740940237, 30.00020018409699318 ) ) ;
#8212=EDGE_CURVE ( 'NONE', #7175, #16530, #511, .T. ) ;
#8218=CARTESIAN_POINT ( 'NONE',  ( 38.01140435219952707, 156.7104996726487514, 34.21067981925357060 ) ) ;
#8220=CARTESIAN_POINT ( 'NONE',  ( 38.01140435219952707, 125.7844580088725905, 34.21067981925357060 ) ) ;
#8221=CARTESIAN_POINT ( 'NONE',  ( 40.27526882409969033, 98.92977050742732104, 30.44471234641811819 ) ) ;
#8224=CARTESIAN_POINT ( 'NONE',  ( 43.01140435219951286, 86.36518717409400381, 29.55568802177586107 ) ) ;
#8225=CARTESIAN_POINT ( 'NONE',  ( 43.01140435219951996, 10.71049967264875491, 34.21067981925357060 ) ) ;
#8229=CARTESIAN_POINT ( 'NONE',  ( 45.74753988029934249, 145.4297705074273210, 37.97664729208901235 ) ) ;
#8232=CARTESIAN_POINT ( 'NONE',  ( 41.64333658814960870, 66.97977050742731819, 38.42115945441014446 ) ) ;
#8234=CARTESIAN_POINT ( 'NONE',  ( 45.74753988029933538, 142.4297705074273495, 37.97664729208901946 ) ) ;
#8235=CARTESIAN_POINT ( 'NONE',  ( 38.58424406990784661, 99.52977050742728693, 35.64915139335016647 ) ) ;
#8237=CARTESIAN_POINT ( 'NONE',  ( 44.55648932407425633, 109.6104996726487428, 38.96596240072933170 ) ) ;
#8238=CARTESIAN_POINT ( 'NONE',  ( 40.27526882409969033, 68.66518717409400097, 30.44471234641811819 ) ) ;
#8239=CARTESIAN_POINT ( 'NONE',  ( 43.01140435219957681, 96.53445800887259054, 39.21067981925356349 ) ) ;
#8243=CARTESIAN_POINT ( 'NONE',  ( 41.46631938032478359, 111.1104996726487428, 29.45539723777780239 ) ) ;
#8244=CARTESIAN_POINT ( 'NONE',  ( 47.05648932407426344, 153.9844580088725934, 37.14960608071593384 ) ) ;
#8245=CARTESIAN_POINT ( 'NONE',  ( 44.37947211624943833, 131.4797705074273040, 30.00020018409699318 ) ) ;
#8246=( BOUNDED_CURVE ( )  B_SPLINE_CURVE ( 2, ( #5622, #7184, #15448, #17301, #8622, #5510, #233, #2000, #13781, #8842, #6971, #20411, #5307 ),
 .UNSPECIFIED., .F., .F. ) 
 B_SPLINE_CURVE_WITH_KNOTS ( ( 3, 2, 2, 2, 2, 2, 3 ),
 ( 0.8161764705882352811, 0.8176470588235293935, 0.8205882352941176183, 0.8235294117647058432, 0.8264705882352940680, 0.8294117647058824039, 0.8308823529411765163 ),
 .UNSPECIFIED. ) 
 CURVE ( )  GEOMETRIC_REPRESENTATION_ITEM ( )  RATIONAL_B_SPLINE_CURVE ( ( 0.9755282581475768211, 0.9755282581475768211, 1.000000000000000000, 0.9510565162951535312, 1.000000000000000000, 0.9510565162951535312, 1.000000000000000000, 0.9510565162951535312, 1.000000000000000000, 0.9510565162951535312, 1.000000000000000000, 0.9755282581475768211, 0.9755282581475768211 ) ) 
 REPRESENTATION_ITEM ( '' )  );
#8248=CARTESIAN_POINT ( 'NONE',  ( 41.64333658814960870, 113.5151871740940095, 30.00020018409699318 ) ) ;
#8250=CARTESIAN_POINT ( 'NONE',  ( 43.01140435219951996, 10.71049967264875491, 39.21067981925356349 ) ) ;
#8254=CARTESIAN_POINT ( 'NONE',  ( 40.27526882409969744, 99.82977050742731251, 37.97664729208901235 ) ) ;
#8258=CARTESIAN_POINT ( 'NONE',  ( 43.80332655382219542, 145.9575765865523067, 29.21067981925356705 ) ) ;
#8260=CARTESIAN_POINT ( 'NONE',  ( 47.05648932407426344, 82.58445800887258770, 31.27175355779120025 ) ) ;
#8261=CARTESIAN_POINT ( 'NONE',  ( 39.92123440845005433, 86.33445800887258770, 29.95742577749336988 ) ) ;
#8262=CARTESIAN_POINT ( 'NONE',  ( 39.92123440845004723, 135.2604996726487343, 29.95742577749337343 ) ) ;
#8263=CARTESIAN_POINT ( 'NONE',  ( 40.27526882409969033, 95.66518717409398675, 30.44471234641811819 ) ) ;
#8269=CARTESIAN_POINT ( 'NONE',  ( 48.01140435219951996, 70.28445800887257633, 34.21067981925357060 ) ) ;
#8272=CARTESIAN_POINT ( 'NONE',  ( 44.55648932407425633, 114.6844580088725820, 38.96596240072933170 ) ) ;
#8273=CARTESIAN_POINT ( 'NONE',  ( 40.27526882409969033, 63.56518717409399954, 37.97664729208901946 ) ) ;
#8274=CARTESIAN_POINT ( 'NONE',  ( 43.01140435219951996, 10.71049967264875491, 39.21067981925356349 ) ) ;
#8276=CARTESIAN_POINT ( 'NONE',  ( 38.58424406990785371, 146.9651871740940123, 32.77220824515697473 ) ) ;
#8280=CARTESIAN_POINT ( 'NONE',  ( 45.22504609509771001, 59.11591859955431971, 30.37668211462113277 ) ) ;
#8283=CARTESIAN_POINT ( 'NONE',  ( 44.55648932407425633, 111.6844580088725820, 38.96596240072933170 ) ) ;
#8284=CARTESIAN_POINT ( 'NONE',  ( 47.43856463449117200, 127.7651871740940237, 32.77220824515698183 ) ) ;
#8288=ORIENTED_EDGE ( 'NONE', *, *, #18616, .F. ) ;
#8289=CARTESIAN_POINT ( 'NONE',  ( 41.64333658814960870, 153.9797705074273324, 38.42115945441014446 ) ) ;
#8290=CARTESIAN_POINT ( 'NONE',  ( 41.64333658814960870, 122.5151871740940095, 30.00020018409699318 ) ) ;
#8293=CARTESIAN_POINT ( 'NONE',  ( 43.01140435219951286, 77.96049967264873715, 28.95336869806222779 ) ) ;
#8298=CARTESIAN_POINT ( 'NONE',  ( 43.01140435219951286, 89.36518717409398960, 29.55568802177586463 ) ) ;
#8299=CARTESIAN_POINT ( 'NONE',  ( 42.21948215057684450, 82.38361825032845331, 39.21067981925355639 ) ) ;
#8302=CARTESIAN_POINT ( 'NONE',  ( 47.43856463449118621, 61.87977050742732388, 34.21067981925357060 ) ) ;
#8308=CARTESIAN_POINT ( 'NONE',  ( 45.74753988029933538, 149.0651871740940067, 30.44471234641811819 ) ) ;
#8309=CARTESIAN_POINT ( 'NONE',  ( 43.01140435219951996, 154.4604996726487798, 39.21067981925357060 ) ) ;
#8310=CARTESIAN_POINT ( 'NONE',  ( 47.43856463449117911, 112.7297705074273324, 35.64915139335015937 ) ) ;
#8311=CARTESIAN_POINT ( 'NONE',  ( 48.01140435219951996, 154.1344580088725991, 35.83527830041809636 ) ) ;
#8314=ADVANCED_FACE ( 'NONE', ( #1495 ), #4572, .T. ) ;
#8317=CARTESIAN_POINT ( 'NONE',  ( 44.37947211624943833, 118.2797705074273296, 38.42115945441014446 ) ) ;
#8319=CARTESIAN_POINT ( 'NONE',  ( 41.64333658814960870, 153.7151871740940123, 38.42115945441014446 ) ) ;
#8321=CARTESIAN_POINT ( 'NONE',  ( 43.01140435219951286, 119.9604996726487229, 29.21067981925356705 ) ) ;
#8325=DIRECTION ( 'NONE',  ( 0.000000000000000000, 1.000000000000000000, 0.000000000000000000 ) ) ;
#8326=DIRECTION ( 'NONE',  ( 0.000000000000000000, 1.000000000000000000, 0.000000000000000000 ) ) ;
#8329=CARTESIAN_POINT ( 'NONE',  ( 45.74753988029933538, 95.32977050742729830, 30.44471234641811819 ) ) ;
#8332=CARTESIAN_POINT ( 'NONE',  ( 39.42975644700377558, 89.81518717409400665, 31.60846029578754468 ) ) ;
#8336=CARTESIAN_POINT ( 'NONE',  ( 38.58424406990785371, 141.5297705074272869, 35.64915139335015937 ) ) ;
#8338=EDGE_CURVE ( 'NONE', #3067, #20247, #4794, .T. ) ;
#8342=CARTESIAN_POINT ( 'NONE',  ( 47.43856463449117200, 142.7297705074273324, 35.64915139335016647 ) ) ;
#8343=CARTESIAN_POINT ( 'NONE',  ( 40.27526882409969033, 95.92977050742732104, 30.44471234641811819 ) ) ;
#8346=CARTESIAN_POINT ( 'NONE',  ( 39.92123440845004723, 115.1604996726487542, 38.46393386101376421 ) ) ;
#8347=CARTESIAN_POINT ( 'NONE',  ( 39.42975644700377558, 66.41518717409400097, 36.81289934271958941 ) ) ;
#8348=CARTESIAN_POINT ( 'NONE',  ( 43.01140435219951286, 146.0344580088725479, 29.21067981925356705 ) ) ;
#8352=CARTESIAN_POINT ( 'NONE',  ( 38.96631938032478359, 111.4104996726487400, 31.27175355779120025 ) ) ;
#8353=CARTESIAN_POINT ( 'NONE',  ( 38.96631938032478359, 152.4844580088725934, 31.27175355779120025 ) ) ;
#8354=CARTESIAN_POINT ( 'NONE',  ( 40.27526882409969033, 122.9297705074272926, 30.44471234641811819 ) ) ;
#8356=CYLINDRICAL_SURFACE ( 'NONE', #7128, 4.999999999999997335 ) ;
#8358=CARTESIAN_POINT ( 'NONE',  ( 40.27526882409969744, 119.6651871740940010, 30.44471234641812174 ) ) ;
#8360=CARTESIAN_POINT ( 'NONE',  ( 43.01140435219951996, 10.71049967264875491, 34.21067981925357060 ) ) ;
#8364=CARTESIAN_POINT ( 'NONE',  ( 45.74753988029934249, 95.32977050742729830, 30.44471234641812174 ) ) ;
#8369=CARTESIAN_POINT ( 'NONE',  ( 47.05648932407426344, 70.58445800887257349, 31.27175355779120025 ) ) ;
#8372=CARTESIAN_POINT ( 'NONE',  ( 43.01140435219951286, 140.9604996726487514, 28.95336869806222779 ) ) ;
#8373=CARTESIAN_POINT ( 'NONE',  ( 45.74753988029933538, 95.06518717409400665, 30.44471234641811819 ) ) ;
#8375=( BOUNDED_CURVE ( )  B_SPLINE_CURVE ( 2, ( #16363, #4352, #6116, #11190, #13177, #1384, #1275, #19909, #14495, #12739, #2816, #1166, #3148 ),
 .UNSPECIFIED., .F., .F. ) 
 B_SPLINE_CURVE_WITH_KNOTS ( ( 3, 2, 2, 2, 2, 2, 3 ),
 ( 0.3014705882352941013, 0.3029411764705882137, 0.3058823529411764941, 0.3088235294117647189, 0.3117647058823529438, 0.3147058823529411686, 0.3161764705882352811 ),
 .UNSPECIFIED. ) 
 CURVE ( )  GEOMETRIC_REPRESENTATION_ITEM ( )  RATIONAL_B_SPLINE_CURVE ( ( 0.9755282581475768211, 0.9755282581475768211, 1.000000000000000000, 0.9510565162951535312, 1.000000000000000000, 0.9510565162951535312, 1.000000000000000000, 0.9510565162951535312, 1.000000000000000000, 0.9510565162951535312, 1.000000000000000000, 0.9755282581475768211, 0.9755282581475768211 ) ) 
 REPRESENTATION_ITEM ( '' )  );
#8382=CARTESIAN_POINT ( 'NONE',  ( 43.01140435219951286, 80.96049967264873715, 29.21067981925356705 ) ) ;
#8383=CARTESIAN_POINT ( 'NONE',  ( 39.42975644700377558, 147.6797705074273495, 36.81289934271958941 ) ) ;
#8384=CARTESIAN_POINT ( 'NONE',  ( 43.01140435219951996, 10.71049967264875491, 39.21067981925356349 ) ) ;
#8386=CARTESIAN_POINT ( 'NONE',  ( 45.74753988029934249, 145.1651871740940010, 37.97664729208901235 ) ) ;
#8390=CARTESIAN_POINT ( 'NONE',  ( 40.27526882409969744, 60.56518717409398533, 37.97664729208901235 ) ) ;
#8395=CARTESIAN_POINT ( 'NONE',  ( 44.37947211624943833, 125.2151871740939981, 30.00020018409699318 ) ) ;
#8396=ORIENTED_EDGE ( 'NONE', *, *, #11473, .T. ) ;
#8398=CARTESIAN_POINT ( 'NONE',  ( 39.92123440845005433, 113.3344580088725735, 29.95742577749336988 ) ) ;
#8401=CARTESIAN_POINT ( 'NONE',  ( 38.01140435219951996, 107.6344580088725706, 32.58608133808903773 ) ) ;
#8402=CARTESIAN_POINT ( 'NONE',  ( 39.42975644700377558, 153.0797705074273267, 31.60846029578754468 ) ) ;
#8403=CARTESIAN_POINT ( 'NONE',  ( 39.42975644700377558, 69.07977050742732672, 31.60846029578754468 ) ) ;
#8404=CARTESIAN_POINT ( 'NONE',  ( 40.27526882409969033, 126.5651871740940209, 37.97664729208901946 ) ) ;
#8406=CARTESIAN_POINT ( 'NONE',  ( 47.05648932407426344, 86.51049967264874851, 31.27175355779120025 ) ) ;
#8410=CARTESIAN_POINT ( 'NONE',  ( 45.74753988029933538, 79.16518717409398675, 37.97664729208901946 ) ) ;
#8412=CARTESIAN_POINT ( 'NONE',  ( 38.01140435219952707, 81.56049967264873146, 32.58608133808903773 ) ) ;
#8415=CARTESIAN_POINT ( 'NONE',  ( 38.58424406990786082, 63.37977050742732388, 34.21067981925357060 ) ) ;
#8420=CARTESIAN_POINT ( 'NONE',  ( 40.27526882409969033, 152.6651871740940010, 30.44471234641811819 ) ) ;
#8421=ADVANCED_FACE ( 'NONE', ( #9661 ), #16361, .T. ) ;
#8424=CARTESIAN_POINT ( 'NONE',  ( 40.27526882409969744, 110.9297705074273068, 30.44471234641812174 ) ) ;
#8428=VERTEX_POINT ( 'NONE', #3034 ) ;
#8429=CARTESIAN_POINT ( 'NONE',  ( 47.43856463449117200, 121.7297705074273040, 35.64915139335016647 ) ) ;
#8430=ADVANCED_FACE ( 'NONE', ( #9772 ), #16468, .T. ) ;
#8432=CARTESIAN_POINT ( 'NONE',  ( 43.01140435219951286, 150.8651871740940180, 38.86567161673127657 ) ) ;
#8438=UNCERTAINTY_MEASURE_WITH_UNIT (LENGTH_MEASURE( 1.000000000000000082E-05 ), #21622, 'distance_accuracy_value', 'NONE');
#8445=CARTESIAN_POINT ( 'NONE',  ( 39.42975644700377558, 90.67977050742732104, 36.81289934271958941 ) ) ;
#8446=( BOUNDED_CURVE ( )  B_SPLINE_CURVE ( 2, ( #5059, #15417, #11773, #10023, #13327, #13641, #20271, #313, #20487, #15306, #10242, #5377, #14961 ),
 .UNSPECIFIED., .F., .F. ) 
 B_SPLINE_CURVE_WITH_KNOTS ( ( 3, 2, 2, 2, 2, 2, 3 ),
 ( 0.9632352941176470784, 0.9647058823529411908, 0.9676470588235294157, 0.9705882352941176405, 0.9735294117647058654, 0.9764705882352940902, 0.9779411764705882026 ),
 .UNSPECIFIED. ) 
 CURVE ( )  GEOMETRIC_REPRESENTATION_ITEM ( )  RATIONAL_B_SPLINE_CURVE ( ( 0.9755282581475768211, 0.9755282581475768211, 1.000000000000000000, 0.9510565162951535312, 1.000000000000000000, 0.9510565162951535312, 1.000000000000000000, 0.9510565162951535312, 1.000000000000000000, 0.9510565162951535312, 1.000000000000000000, 0.9755282581475768211, 0.9755282581475768211 ) ) 
 REPRESENTATION_ITEM ( '' )  );
#8449=CARTESIAN_POINT ( 'NONE',  ( 44.37947211624943833, 89.21518717409399812, 30.00020018409699318 ) ) ;
#8455=CARTESIAN_POINT ( 'NONE',  ( 46.59305225739526435, 143.1797705074273210, 31.60846029578754468 ) ) ;
#8457=CARTESIAN_POINT ( 'NONE',  ( 38.01140435219952707, 119.7844580088725763, 34.21067981925357060 ) ) ;
#8459=CARTESIAN_POINT ( 'NONE',  ( 43.01140435219951286, 142.1297705074273097, 38.86567161673127657 ) ) ;
#8460=AXIS2_PLACEMENT_3D ( 'NONE', #15525, #15839, #8706 ) ;
#8461=CARTESIAN_POINT ( 'NONE',  ( 45.74753988029933538, 94.42977050742732104, 37.97664729208901946 ) ) ;
#8462=LINE ( 'NONE', #16703, #6699 ) ;
#8463=CARTESIAN_POINT ( 'NONE',  ( 39.42975644700377558, 59.81518717409399244, 31.60846029578754468 ) ) ;
#8466=CARTESIAN_POINT ( 'NONE',  ( 39.92123440845005433, 109.1604996726487400, 38.46393386101375711 ) ) ;
#8468=CARTESIAN_POINT ( 'NONE',  ( 38.01140435219952707, 111.5604996726487457, 32.58608133808903773 ) ) ;
#8469=CARTESIAN_POINT ( 'NONE',  ( 43.01140435219951286, 143.0344580088726048, 28.95336869806222779 ) ) ;
#8470=CARTESIAN_POINT ( 'NONE',  ( 43.01140435219951286, 122.6297705074273239, 29.55568802177586463 ) ) ;
#8473=CARTESIAN_POINT ( 'NONE',  ( 38.58424406990785371, 120.2651871740939953, 35.64915139335015937 ) ) ;
#8481=CARTESIAN_POINT ( 'NONE',  ( 44.37947211624943833, 85.27977050742731535, 38.42115945441014446 ) ) ;
#8484=CARTESIAN_POINT ( 'NONE',  ( 47.05648932407426344, 73.58445800887257349, 31.27175355779120025 ) ) ;
#8487=CARTESIAN_POINT ( 'NONE',  ( 41.46631938032478359, 132.1104996726487286, 29.45539723777780239 ) ) ;
#8488=CARTESIAN_POINT ( 'NONE',  ( 44.37947211624943833, 85.01518717409399528, 38.42115945441014446 ) ) ;
#8492=CARTESIAN_POINT ( 'NONE',  ( 39.92123440845005433, 93.26049967264872009, 29.95742577749336988 ) ) ;
#8493=CARTESIAN_POINT ( 'NONE',  ( 47.05648932407426344, 126.9844580088725934, 37.14960608071593384 ) ) ;
#8495=CARTESIAN_POINT ( 'NONE',  ( 39.42975644700377558, 150.0797705074273267, 31.60846029578754468 ) ) ;
#8496=CARTESIAN_POINT ( 'NONE',  ( 43.80332655382220963, 157.5373810949690494, 39.21067981925355639 ) ) ;
#8498=CARTESIAN_POINT ( 'NONE',  ( 39.42975644700377558, 143.8151871740940067, 31.60846029578754468 ) ) ;
#8501=ORIENTED_EDGE ( 'NONE', *, *, #19283, .T. ) ;
#8502=CARTESIAN_POINT ( 'NONE',  ( 43.01140435219951286, 59.36518717409399670, 29.55568802177586107 ) ) ;
#8506=CARTESIAN_POINT ( 'NONE',  ( 46.59305225739526435, 124.9151871740940010, 31.60846029578754468 ) ) ;
#8512=( BOUNDED_CURVE ( )  B_SPLINE_CURVE ( 2, ( #11973, #505, #18702, #5360, #3386, #8787, #5041, #13414, #20148, #76, #12076, #404, #15599 ),
 .UNSPECIFIED., .F., .F. ) 
 B_SPLINE_CURVE_WITH_KNOTS ( ( 3, 2, 2, 2, 2, 2, 3 ),
 ( 0.3455882352941176405, 0.3470588235294117530, 0.3499999999999999778, 0.3529411764705882582, 0.3558823529411764830, 0.3588235294117647078, 0.3602941176470588203 ),
 .UNSPECIFIED. ) 
 CURVE ( )  GEOMETRIC_REPRESENTATION_ITEM ( )  RATIONAL_B_SPLINE_CURVE ( ( 0.9755282581475768211, 0.9755282581475768211, 1.000000000000000000, 0.9510565162951535312, 1.000000000000000000, 0.9510565162951535312, 1.000000000000000000, 0.9510565162951535312, 1.000000000000000000, 0.9510565162951535312, 1.000000000000000000, 0.9755282581475768211, 0.9755282581475768211 ) ) 
 REPRESENTATION_ITEM ( '' )  );
#8513=CARTESIAN_POINT ( 'NONE',  ( 43.01140435219951286, 102.5344580088725763, 39.46799094044489209 ) ) ;
#8514=CARTESIAN_POINT ( 'NONE',  ( 40.27526882409969744, 155.9297705074273210, 30.44471234641812174 ) ) ;
#8515=CARTESIAN_POINT ( 'NONE',  ( 39.42975644700377558, 63.67977050742732104, 36.81289934271958941 ) ) ;
#8516=CARTESIAN_POINT ( 'NONE',  ( 47.43856463449117200, 115.4651871740940123, 35.64915139335016647 ) ) ;
#8518=CARTESIAN_POINT ( 'NONE',  ( 41.46631938032478359, 84.11049967264874283, 29.45539723777780239 ) ) ;
#8522=CARTESIAN_POINT ( 'NONE',  ( 45.74753988029933538, 77.06518717409399244, 30.44471234641811819 ) ) ;
#8527=CARTESIAN_POINT ( 'NONE',  ( 39.42975644700377558, 69.67977050742732104, 36.81289934271958941 ) ) ;
#8533=CARTESIAN_POINT ( 'NONE',  ( 46.59305225739526435, 154.3151871740940067, 36.81289934271958941 ) ) ;
#8535=CARTESIAN_POINT ( 'NONE',  ( 43.01140435219951996, 10.71049967264875491, 34.21067981925357060 ) ) ;
#8537=ORIENTED_EDGE ( 'NONE', *, *, #5560, .F. ) ;
#8538=PRODUCT_DEFINITION ( 'UNKNOWN', '', #6326, #5311 ) ;
#8541=CARTESIAN_POINT ( 'NONE',  ( 39.92123440845005433, 126.2604996726487343, 29.95742577749336988 ) ) ;
#8542=CARTESIAN_POINT ( 'NONE',  ( 44.37947211624943833, 158.2151871740939839, 30.00020018409699318 ) ) ;
#8545=CARTESIAN_POINT ( 'NONE',  ( 43.80332655382220253, 81.61133943119283174, 39.21067981925355639 ) ) ;
#8546=DIRECTION ( 'NONE',  ( 0.000000000000000000, 0.000000000000000000, 1.000000000000000000 ) ) ;
#8549=CARTESIAN_POINT ( 'NONE',  ( 46.10157429594899270, 101.6604996726487258, 29.95742577749336988 ) ) ;
#8551=CARTESIAN_POINT ( 'NONE',  ( 43.01140435219951286, 77.96049967264873715, 29.21067981925356705 ) ) ;
#8553=CARTESIAN_POINT ( 'NONE',  ( 47.43856463449117200, 95.02977050742730114, 32.77220824515698183 ) ) ;
#8556=CARTESIAN_POINT ( 'NONE',  ( 40.27526882409969744, 77.66518717409400097, 30.44471234641812174 ) ) ;
#8557=CARTESIAN_POINT ( 'NONE',  ( 43.01140435219951996, 10.71049967264875491, 34.21067981925357060 ) ) ;
#8558=ORIENTED_EDGE ( 'NONE', *, *, #2850, .F. ) ;
#8562=DIRECTION ( 'NONE',  ( 0.000000000000000000, 1.000000000000000000, 0.000000000000000000 ) ) ;
#8564=CARTESIAN_POINT ( 'NONE',  ( 39.42975644700377558, 147.6797705074273495, 36.81289934271958941 ) ) ;
#8566=CARTESIAN_POINT ( 'NONE',  ( 45.74753988029933538, 100.4297705074273210, 37.97664729208901946 ) ) ;
#8567=CARTESIAN_POINT ( 'NONE',  ( 48.01140435219951996, 152.2104996726487514, 34.21067981925357060 ) ) ;
#8569=CARTESIAN_POINT ( 'NONE',  ( 43.01140435219951286, 95.96049967264873715, 29.21067981925356705 ) ) ;
#8570=( BOUNDED_CURVE ( )  B_SPLINE_CURVE ( 2, ( #12241, #10386, #17087, #555, #19083, #10708, #2001, #8732, #15450, #15551, #7185, #350, #7080 ),
 .UNSPECIFIED., .F., .F. ) 
 B_SPLINE_CURVE_WITH_KNOTS ( ( 3, 2, 2, 2, 2, 2, 3 ),
 ( 0.3455882352941176405, 0.3470588235294117530, 0.3499999999999999778, 0.3529411764705882582, 0.3558823529411764830, 0.3588235294117647078, 0.3602941176470588203 ),
 .UNSPECIFIED. ) 
 CURVE ( )  GEOMETRIC_REPRESENTATION_ITEM ( )  RATIONAL_B_SPLINE_CURVE ( ( 0.9755282581475768211, 0.9755282581475768211, 1.000000000000000000, 0.9510565162951535312, 1.000000000000000000, 0.9510565162951535312, 1.000000000000000000, 0.9510565162951535312, 1.000000000000000000, 0.9510565162951535312, 1.000000000000000000, 0.9755282581475768211, 0.9755282581475768211 ) ) 
 REPRESENTATION_ITEM ( '' )  );
#8574=CARTESIAN_POINT ( 'NONE',  ( 44.55648932407425633, 139.8844580088725991, 29.45539723777780239 ) ) ;
#8575=CARTESIAN_POINT ( 'NONE',  ( 47.43856463449118621, 121.8797705074273239, 34.21067981925357060 ) ) ;
#8577=CARTESIAN_POINT ( 'NONE',  ( 40.27526882409969744, 114.5651871740939924, 37.97664729208901235 ) ) ;
#8578=DIRECTION ( 'NONE',  ( 0.000000000000000000, 0.000000000000000000, 1.000000000000000000 ) ) ;
#8580=ADVANCED_FACE ( 'NONE', ( #20345 ), #3371, .T. ) ;
#8582=CARTESIAN_POINT ( 'NONE',  ( 45.22504609509771001, 59.11591859955431971, 30.37668211462113277 ) ) ;
#8583=CARTESIAN_POINT ( 'NONE',  ( 43.01140435219951286, 82.12977050742730967, 38.86567161673127657 ) ) ;
#8586=CARTESIAN_POINT ( 'NONE',  ( 41.46631938032478359, 69.38445800887258486, 38.96596240072933170 ) ) ;
#8587=CARTESIAN_POINT ( 'NONE',  ( 38.01140435219952707, 86.78445800887257633, 34.21067981925357060 ) ) ;
#8588=CARTESIAN_POINT ( 'NONE',  ( 48.01140435219951996, 128.2104996726487514, 34.21067981925357060 ) ) ;
#8589=CARTESIAN_POINT ( 'NONE',  ( 47.43856463449117200, 85.76518717409398107, 32.77220824515698183 ) ) ;
#8593=CARTESIAN_POINT ( 'NONE',  ( 38.01140435219952707, 116.6344580088725706, 32.58608133808903773 ) ) ;
#8597=CARTESIAN_POINT ( 'NONE',  ( 41.64333658814960870, 147.9797705074273324, 38.42115945441014446 ) ) ;
#8600=CARTESIAN_POINT ( 'NONE',  ( 45.74753988029934249, 143.0651871740939782, 30.44471234641812174 ) ) ;
#8603=CARTESIAN_POINT ( 'NONE',  ( 38.58424406990786082, 63.11518717409400381, 34.21067981925357060 ) ) ;
#8605=CIRCLE ( 'NONE', #20917, 4.999999999999997335 ) ;
#8608=CARTESIAN_POINT ( 'NONE',  ( 41.64333658814960870, 125.5151871740939953, 30.00020018409699318 ) ) ;
#8610=VERTEX_POINT ( 'NONE', #5239 ) ;
#8612=ADVANCED_FACE ( 'NONE', ( #20238 ), #15156, .T. ) ;
#8613=CARTESIAN_POINT ( 'NONE',  ( 38.01140435219952707, 113.6344580088725706, 32.58608133808903773 ) ) ;
#8614=ORIENTED_EDGE ( 'NONE', *, *, #12987, .T. ) ;
#8615=CARTESIAN_POINT ( 'NONE',  ( 39.92123440845004723, 102.2344580088725650, 38.46393386101376421 ) ) ;
#8616=CARTESIAN_POINT ( 'NONE',  ( 38.58424406990785371, 156.2297705074273040, 32.77220824515697473 ) ) ;
#8617=CARTESIAN_POINT ( 'NONE',  ( 39.92123440845004723, 156.2604996726486775, 29.95742577749337343 ) ) ;
#8618=CARTESIAN_POINT ( 'NONE',  ( 45.74753988029933538, 119.0651871740939782, 30.44471234641811819 ) ) ;
#8621=CARTESIAN_POINT ( 'NONE',  ( 44.55648932407425633, 80.81049967264873146, 29.45539723777780239 ) ) ;
#8622=CARTESIAN_POINT ( 'NONE',  ( 38.96631938032478359, 75.08445800887257349, 37.14960608071593384 ) ) ;
#8623=DIRECTION ( 'NONE',  ( 0.000000000000000000, 1.000000000000000000, 0.000000000000000000 ) ) ;
#8625=AXIS2_PLACEMENT_3D ( 'NONE', #12218, #2196, #7276 ) ;
#8626=CARTESIAN_POINT ( 'NONE',  ( 38.58424406990786082, 75.11518717409400381, 34.21067981925357060 ) ) ;
#8628=CARTESIAN_POINT ( 'NONE',  ( 38.96631938032478359, 122.4844580088725934, 31.27175355779120025 ) ) ;
#8634=ORIENTED_EDGE ( 'NONE', *, *, #19108, .T. ) ;
#8635=CARTESIAN_POINT ( 'NONE',  ( 44.37947211624943833, 158.2151871740939839, 30.00020018409699318 ) ) ;
#8637=CARTESIAN_POINT ( 'NONE',  ( 46.59305225739526435, 118.5797705074273267, 36.81289934271958941 ) ) ;
#8642=CARTESIAN_POINT ( 'NONE',  ( 47.43856463449117200, 109.7297705074273040, 35.64915139335016647 ) ) ;
#8643=CARTESIAN_POINT ( 'NONE',  ( 41.46631938032478359, 158.1844580088726104, 29.45539723777780239 ) ) ;
#8646=CARTESIAN_POINT ( 'NONE',  ( 39.42975644700377558, 143.8151871740940067, 31.60846029578754468 ) ) ;
#8656=CARTESIAN_POINT ( 'NONE',  ( 45.74753988029933538, 97.42977050742730682, 37.97664729208901946 ) ) ;
#8659=CARTESIAN_POINT ( 'NONE',  ( 44.37947211624943833, 80.21518717409399812, 30.00020018409699318 ) ) ;
#8664=FACE_OUTER_BOUND ( 'NONE', #6770, .T. ) ;
#8669=CARTESIAN_POINT ( 'NONE',  ( 47.43856463449117200, 137.0297705074272869, 32.77220824515698183 ) ) ;
#8674=CARTESIAN_POINT ( 'NONE',  ( 43.01140435219951286, 102.5344580088725763, 39.21067981925356349 ) ) ;
#8676=CARTESIAN_POINT ( 'NONE',  ( 38.01140435219952707, 108.5604996726487457, 32.58608133808903773 ) ) ;
#8679=CARTESIAN_POINT ( 'NONE',  ( 44.55648932407425633, 138.6844580088725820, 38.96596240072933170 ) ) ;
#8680=CARTESIAN_POINT ( 'NONE',  ( 46.59305225739526435, 122.1797705074273210, 31.60846029578754468 ) ) ;
#8682=CARTESIAN_POINT ( 'NONE',  ( 46.10157429594899270, 99.83445800887257349, 38.46393386101375711 ) ) ;
#8683=CARTESIAN_POINT ( 'NONE',  ( 44.37947211624943833, 110.2151871740940123, 30.00020018409699318 ) ) ;
#8690=ADVANCED_FACE ( 'NONE', ( #7115 ), #17018, .T. ) ;
#8691=CARTESIAN_POINT ( 'NONE',  ( 41.64333658814960870, 86.77977050742731535, 30.00020018409699318 ) ) ;
#8692=VECTOR ( 'NONE', #5226, 1000.000000000000000 ) ;
#8694=ORIENTED_EDGE ( 'NONE', *, *, #6520, .F. ) ;
#8695=CARTESIAN_POINT ( 'NONE',  ( 48.01140435219951996, 110.3604996726487428, 32.58608133808903773 ) ) ;
#8696=( BOUNDED_CURVE ( )  B_SPLINE_CURVE ( 2, ( #5144, #403, #17033, #2055, #12075, #15501, #11863, #13620, #7133, #17246, #8897, #10655, #13837 ),
 .UNSPECIFIED., .F., .F. ) 
 B_SPLINE_CURVE_WITH_KNOTS ( ( 3, 2, 2, 2, 2, 2, 3 ),
 ( 0.05147058823529411520, 0.05294117647058823456, 0.05588235294117647328, 0.05882352941176470507, 0.06176470588235294379, 0.06470588235294118251, 0.06617647058823528106 ),
 .UNSPECIFIED. ) 
 CURVE ( )  GEOMETRIC_REPRESENTATION_ITEM ( )  RATIONAL_B_SPLINE_CURVE ( ( 0.9755282581475767101, 0.9755282581475765991, 1.000000000000000000, 0.9510565162951535312, 1.000000000000000000, 0.9510565162951535312, 1.000000000000000000, 0.9510565162951535312, 1.000000000000000000, 0.9510565162951535312, 1.000000000000000000, 0.9755282581475769321, 0.9755282581475765991 ) ) 
 REPRESENTATION_ITEM ( '' )  );
#8697=CARTESIAN_POINT ( 'NONE',  ( 46.10157429594899270, 72.83445800887257349, 38.46393386101376421 ) ) ;
#8698=CARTESIAN_POINT ( 'NONE',  ( 41.46631938032478359, 126.1104996726487570, 29.45539723777780239 ) ) ;
#8699=CARTESIAN_POINT ( 'NONE',  ( 41.64333658814960870, 84.71518717409399812, 38.42115945441014446 ) ) ;
#8706=DIRECTION ( 'NONE',  ( 0.000000000000000000, 0.000000000000000000, 1.000000000000000000 ) ) ;
#8707=CARTESIAN_POINT ( 'NONE',  ( 47.05648932407426344, 67.91049967264873999, 37.14960608071593384 ) ) ;
#8708=CARTESIAN_POINT ( 'NONE',  ( 46.10157429594899270, 142.7604996726487343, 38.46393386101375711 ) ) ;
#8709=CARTESIAN_POINT ( 'NONE',  ( 38.58424406990784661, 147.5297705074273154, 35.64915139335016647 ) ) ;
#8710=CARTESIAN_POINT ( 'NONE',  ( 46.59305225739526435, 106.5797705074273125, 36.81289934271958941 ) ) ;
#8712=CARTESIAN_POINT ( 'NONE',  ( 44.37947211624943833, 131.2151871740940123, 30.00020018409699318 ) ) ;
#8713=CYLINDRICAL_SURFACE ( 'NONE', #13876, 4.999999999999997335 ) ;
#8715=CARTESIAN_POINT ( 'NONE',  ( 41.64333658814960870, 59.51518717409400239, 30.00020018409699318 ) ) ;
#8717=CARTESIAN_POINT ( 'NONE',  ( 42.21948215057684450, 135.4575765865523067, 39.21067981925355639 ) ) ;
#8718=CARTESIAN_POINT ( 'NONE',  ( 40.27526882409969033, 114.5651871740939782, 37.97664729208901946 ) ) ;
#8722=ORIENTED_EDGE ( 'NONE', *, *, #14123, .F. ) ;
#8723=CARTESIAN_POINT ( 'NONE',  ( 48.01140435219951996, 103.2844580088725763, 34.21067981925357060 ) ) ;
#8724=CARTESIAN_POINT ( 'NONE',  ( 38.58424406990785371, 153.2297705074273324, 32.77220824515697473 ) ) ;
#8725=CARTESIAN_POINT ( 'NONE',  ( 45.74753988029933538, 62.32977050742730540, 30.44471234641811819 ) ) ;
#8726=CARTESIAN_POINT ( 'NONE',  ( 38.58424406990784661, 116.9651871740939839, 32.77220824515698183 ) ) ;
#8729=CARTESIAN_POINT ( 'NONE',  ( 38.01140435219951996, 72.56049967264874567, 32.58608133808903773 ) ) ;
#8730=DIRECTION ( 'NONE',  ( -0.000000000000000000, -1.000000000000000000, -0.000000000000000000 ) ) ;
#8731=DIRECTION ( 'NONE',  ( 0.000000000000000000, 0.000000000000000000, 1.000000000000000000 ) ) ;
#8732=CARTESIAN_POINT ( 'NONE',  ( 38.01140435219952707, 123.5604996726487173, 32.58608133808903773 ) ) ;
#8734=CARTESIAN_POINT ( 'NONE',  ( 40.27526882409969033, 81.56518717409399244, 37.97664729208901946 ) ) ;
#8740=EDGE_LOOP ( 'NONE', ( #1274, #14179, #4465, #17531 ) ) ;
#8745=CARTESIAN_POINT ( 'NONE',  ( 47.43856463449118621, 139.6151871740939896, 34.21067981925357060 ) ) ;
#8747=CARTESIAN_POINT ( 'NONE',  ( 44.37947211624943833, 101.4797705074273182, 30.00020018409699318 ) ) ;
#8751=ORIENTED_EDGE ( 'NONE', *, *, #18616, .T. ) ;
#8752=CARTESIAN_POINT ( 'NONE',  ( 38.58424406990784661, 111.5297705074273154, 35.64915139335016647 ) ) ;
#8753=CARTESIAN_POINT ( 'NONE',  ( 38.96631938032478359, 131.4844580088725934, 31.27175355779120025 ) ) ;
#8754=CARTESIAN_POINT ( 'NONE',  ( 38.01140435219952707, 126.5604996726487315, 32.58608133808903773 ) ) ;
#8755=CARTESIAN_POINT ( 'NONE',  ( 41.64333658814960870, 141.7151871740940123, 38.42115945441014446 ) ) ;
#8756=CARTESIAN_POINT ( 'NONE',  ( 41.46631938032478359, 100.3104996726487457, 38.96596240072933170 ) ) ;
#8760=CARTESIAN_POINT ( 'NONE',  ( 43.01140435219951286, 100.4604996726487371, 39.21067981925356349 ) ) ;
#8762=EDGE_CURVE ( 'NONE', #13207, #13022, #20770, .T. ) ;
#8765=CARTESIAN_POINT ( 'NONE',  ( 40.27526882409969033, 80.92977050742729261, 30.44471234641811819 ) ) ;
#8768=CARTESIAN_POINT ( 'NONE',  ( 38.58424406990785371, 74.96518717409401233, 32.77220824515697473 ) ) ;
#8769=CARTESIAN_POINT ( 'NONE',  ( 43.01140435219951286, 119.0344580088725621, 29.21067981925356705 ) ) ;
#8771=ORIENTED_EDGE ( 'NONE', *, *, #2754, .F. ) ;
#8772=CARTESIAN_POINT ( 'NONE',  ( 42.21948215057684450, 137.1113394311928175, 29.21067981925356705 ) ) ;
#8774=CARTESIAN_POINT ( 'NONE',  ( 46.59305225739526435, 136.5797705074272983, 36.81289934271958941 ) ) ;
#8779=CARTESIAN_POINT ( 'NONE',  ( 43.01140435219951286, 140.6297705074273097, 29.55568802177586463 ) ) ;
#8780=CARTESIAN_POINT ( 'NONE',  ( 39.42975644700377558, 93.07977050742731251, 31.60846029578754468 ) ) ;
#8784=CARTESIAN_POINT ( 'NONE',  ( 41.64333658814960870, 60.71518717409399102, 38.42115945441014446 ) ) ;
#8785=CARTESIAN_POINT ( 'NONE',  ( 38.01140435219952707, 159.7104996726487514, 34.21067981925357060 ) ) ;
#8786=CARTESIAN_POINT ( 'NONE',  ( 38.58424406990786082, 96.11518717409400381, 34.21067981925357060 ) ) ;
#8787=CARTESIAN_POINT ( 'NONE',  ( 38.01140435219952707, 122.9344580088725962, 35.83527830041809636 ) ) ;
#8790=CARTESIAN_POINT ( 'NONE',  ( 44.55648932407425633, 109.8844580088725849, 29.45539723777780239 ) ) ;
#8791=CARTESIAN_POINT ( 'NONE',  ( 47.05648932407426344, 141.9844580088725650, 37.14960608071593384 ) ) ;
#8792=CARTESIAN_POINT ( 'NONE',  ( 39.42975644700377558, 111.0797705074273125, 31.60846029578754468 ) ) ;
#8795=CARTESIAN_POINT ( 'NONE',  ( 44.37947211624943833, 103.0151871740939953, 38.42115945441014446 ) ) ;
#8801=CARTESIAN_POINT ( 'NONE',  ( 46.59305225739526435, 89.17977050742732104, 31.60846029578754468 ) ) ;
#8804=CARTESIAN_POINT ( 'NONE',  ( 38.01140435219951996, 77.93445800887256780, 35.83527830041810347 ) ) ;
#8806=CARTESIAN_POINT ( 'NONE',  ( 46.10157429594899270, 133.7604996726487059, 38.46393386101376421 ) ) ;
#8808=CARTESIAN_POINT ( 'NONE',  ( 38.58424406990786082, 84.11518717409400381, 34.21067981925357060 ) ) ;
#8813=CARTESIAN_POINT ( 'NONE',  ( 46.10157429594899270, 127.7344580088725934, 29.95742577749336988 ) ) ;
#8817=CARTESIAN_POINT ( 'NONE',  ( 44.37947211624943833, 154.2797705074273438, 38.42115945441014446 ) ) ;
#8818=CARTESIAN_POINT ( 'NONE',  ( 44.37947211624943833, 104.4797705074273182, 30.00020018409699318 ) ) ;
#8821=CARTESIAN_POINT ( 'NONE',  ( 47.43856463449117911, 136.7651871740939953, 32.77220824515697473 ) ) ;
#8824=CARTESIAN_POINT ( 'NONE',  ( 43.01140435219951286, 152.9604996726487798, 29.21067981925356705 ) ) ;
#8828=CARTESIAN_POINT ( 'NONE',  ( 39.42975644700377558, 113.8151871740940067, 31.60846029578754468 ) ) ;
#8834=CARTESIAN_POINT ( 'NONE',  ( 38.01140435219951996, 101.9344580088725536, 35.83527830041810347 ) ) ;
#8835=CARTESIAN_POINT ( 'NONE',  ( 47.43856463449117911, 151.7297705074273324, 35.64915139335015937 ) ) ;
#8837=CARTESIAN_POINT ( 'NONE',  ( 38.96631938032478359, 156.4104996726487400, 31.27175355779120025 ) ) ;
#8838=CARTESIAN_POINT ( 'NONE',  ( 47.43856463449118621, 118.6151871740940038, 34.21067981925357060 ) ) ;
#8840=CARTESIAN_POINT ( 'NONE',  ( 39.92123440845004723, 69.26049967264874851, 29.95742577749337343 ) ) ;
#8842=CARTESIAN_POINT ( 'NONE',  ( 39.92123440845005433, 74.33445800887255928, 29.95742577749336988 ) ) ;
#8846=CARTESIAN_POINT ( 'NONE',  ( 39.42975644700377558, 78.41518717409400097, 36.81289934271958941 ) ) ;
#8847=CARTESIAN_POINT ( 'NONE',  ( 43.80332655382220253, 104.8836182503284675, 29.21067981925356705 ) ) ;
#8854=CARTESIAN_POINT ( 'NONE',  ( 41.64333658814960870, 144.7151871740940123, 38.42115945441014446 ) ) ;
#8856=CARTESIAN_POINT ( 'NONE',  ( 43.01140435219951286, 106.1297705074273097, 38.86567161673127657 ) ) ;
#8860=ORIENTED_EDGE ( 'NONE', *, *, #17923, .F. ) ;
#8861=PLANE ( 'NONE',  #4378 ) ;
#8863=CARTESIAN_POINT ( 'NONE',  ( 38.58424406990784661, 140.9651871740939555, 32.77220824515698183 ) ) ;
#8864=CARTESIAN_POINT ( 'NONE',  ( 48.01140435219951996, 98.36049967264872862, 32.58608133808903773 ) ) ;
#8866=CARTESIAN_POINT ( 'NONE',  ( 38.96631938032478359, 61.01049967264874141, 37.14960608071593384 ) ) ;
#8868=CARTESIAN_POINT ( 'NONE',  ( 43.01140435219951286, 144.5344580088726048, 39.21067981925356349 ) ) ;
#8873=CARTESIAN_POINT ( 'NONE',  ( 39.42975644700377558, 84.07977050742732672, 31.60846029578754468 ) ) ;
#8875=CARTESIAN_POINT ( 'NONE',  ( 38.58424406990785371, 81.26518717409399528, 35.64915139335015937 ) ) ;
#8878=ORIENTED_EDGE ( 'NONE', *, *, #11790, .T. ) ;
#8879=CARTESIAN_POINT ( 'NONE',  ( 47.05648932407426344, 85.58445800887258770, 31.27175355779120025 ) ) ;
#8880=CARTESIAN_POINT ( 'NONE',  ( 43.01140435219951286, 128.0344580088725479, 29.21067981925356705 ) ) ;
#8881=CARTESIAN_POINT ( 'NONE',  ( 46.59305225739526435, 130.5797705074273267, 36.81289934271958941 ) ) ;
#8886=CARTESIAN_POINT ( 'NONE',  ( 43.01140435219951286, 131.6297705074273381, 29.55568802177586463 ) ) ;
#8888=VECTOR ( 'NONE', #486, 1000.000000000000000 ) ;
#8896=CARTESIAN_POINT ( 'NONE',  ( 39.42975644700377558, 102.4151871740940010, 36.81289934271958941 ) ) ;
#8897=CARTESIAN_POINT ( 'NONE',  ( 41.46631938032478359, 153.1104996726487570, 29.45539723777780239 ) ) ;
#8898=CARTESIAN_POINT ( 'NONE',  ( 43.01140435219951996, 10.71049967264875491, 39.21067981925356349 ) ) ;
#8900=CARTESIAN_POINT ( 'NONE',  ( 48.01140435219951996, 142.1344580088725991, 35.83527830041810347 ) ) ;
#8901=CARTESIAN_POINT ( 'NONE',  ( 46.59305225739526435, 116.1797705074273210, 31.60846029578754468 ) ) ;
#8903=CARTESIAN_POINT ( 'NONE',  ( 44.55648932407425633, 100.8844580088725849, 29.45539723777780239 ) ) ;
#8904=CARTESIAN_POINT ( 'NONE',  ( 38.58424406990786082, 108.1151871740940038, 34.21067981925357060 ) ) ;
#8906=CARTESIAN_POINT ( 'NONE',  ( 43.01140435219951286, 63.53445800887256922, 39.21067981925356349 ) ) ;
#8910=CARTESIAN_POINT ( 'NONE',  ( 39.42975644700377558, 90.07977050742732672, 31.60846029578754468 ) ) ;
#8911=ORIENTED_EDGE ( 'NONE', *, *, #11810, .F. ) ;
#8912=CARTESIAN_POINT ( 'NONE',  ( 46.10157429594899270, 61.73445800887257917, 29.95742577749337343 ) ) ;
#8913=DIRECTION ( 'NONE',  ( 0.000000000000000000, 1.000000000000000000, 0.000000000000000000 ) ) ;
#8914=CARTESIAN_POINT ( 'NONE',  ( 39.92123440845004723, 132.2604996726487627, 29.95742577749337343 ) ) ;
#8915=CARTESIAN_POINT ( 'NONE',  ( 44.37947211624943833, 86.21518717409399812, 30.00020018409699318 ) ) ;
#8921=CARTESIAN_POINT ( 'NONE',  ( 46.10157429594899270, 143.6604996726487400, 29.95742577749336988 ) ) ;
#8922=CARTESIAN_POINT ( 'NONE',  ( 40.27526882409969033, 140.9297705074273210, 30.44471234641811819 ) ) ;
#8923=CARTESIAN_POINT ( 'NONE',  ( 47.43856463449117200, 106.7297705074273324, 35.64915139335016647 ) ) ;
#8925=CARTESIAN_POINT ( 'NONE',  ( 39.42975644700377558, 135.4151871740940010, 36.81289934271958941 ) ) ;
#8928=CARTESIAN_POINT ( 'NONE',  ( 43.01140435219951286, 62.62977050742732388, 29.55568802177586463 ) ) ;
#8929=CARTESIAN_POINT ( 'NONE',  ( 43.01140435219951286, 92.03445800887257633, 29.21067981925356705 ) ) ;
#8932=CARTESIAN_POINT ( 'NONE',  ( 38.58424406990784661, 110.9651871740940123, 32.77220824515698183 ) ) ;
#8937=CARTESIAN_POINT ( 'NONE',  ( 43.01140435219951286, 99.53445800887259054, 39.46799094044489209 ) ) ;
#8938=CARTESIAN_POINT ( 'NONE',  ( 38.58424406990785371, 147.2297705074273324, 32.77220824515697473 ) ) ;
#8939=CARTESIAN_POINT ( 'NONE',  ( 38.01140435219952707, 159.7104996726487514, 34.21067981925357060 ) ) ;
#8940=CARTESIAN_POINT ( 'NONE',  ( 43.01140435219951286, 117.8651871740939754, 38.86567161673127657 ) ) ;
#8942=CARTESIAN_POINT ( 'NONE',  ( 38.01140435219951996, 75.86049967264874283, 35.83527830041810347 ) ) ;
#8944=CARTESIAN_POINT ( 'NONE',  ( 46.10157429594899270, 135.8344580088725877, 38.46393386101375711 ) ) ;
#8946=CARTESIAN_POINT ( 'NONE',  ( 43.01140435219951996, 10.71049967264875491, 34.21067981925357060 ) ) ;
#8947=CARTESIAN_POINT ( 'NONE',  ( 45.74753988029933538, 68.06518717409397823, 30.44471234641811819 ) ) ;
#8956=CARTESIAN_POINT ( 'NONE',  ( 47.43856463449117200, 142.7651871740939669, 32.77220824515698183 ) ) ;
#8958=CARTESIAN_POINT ( 'NONE',  ( 38.58424406990785371, 102.2297705074273324, 32.77220824515697473 ) ) ;
#8962=ORIENTED_EDGE ( 'NONE', *, *, #17049, .T. ) ;
#8965=CARTESIAN_POINT ( 'NONE',  ( 38.01140435219952707, 131.6344580088725706, 32.58608133808903773 ) ) ;
#8967=CARTESIAN_POINT ( 'NONE',  ( 45.74753988029933538, 82.42977050742732104, 37.97664729208901946 ) ) ;
#8968=CARTESIAN_POINT ( 'NONE',  ( 46.59305225739526435, 145.9151871740940294, 31.60846029578754468 ) ) ;
#8970=CARTESIAN_POINT ( 'NONE',  ( 43.01140435219951286, 103.4604996726487087, 39.46799094044489209 ) ) ;
#8975=CARTESIAN_POINT ( 'NONE',  ( 38.01140435219952707, 143.7844580088725763, 34.21067981925357060 ) ) ;
#8978=CARTESIAN_POINT ( 'NONE',  ( 44.37947211624943833, 85.27977050742731535, 38.42115945441014446 ) ) ;
#8980=CARTESIAN_POINT ( 'NONE',  ( 45.74753988029934249, 80.06518717409397823, 30.44471234641812174 ) ) ;
#8983=VERTEX_POINT ( 'NONE', #133 ) ;
#8985=CARTESIAN_POINT ( 'NONE',  ( 38.01140435219952707, 117.7104996726487371, 34.21067981925357060 ) ) ;
#8987=CARTESIAN_POINT ( 'NONE',  ( 40.27526882409969744, 128.9297705074272926, 30.44471234641812174 ) ) ;
#8991=ORIENTED_EDGE ( 'NONE', *, *, #5935, .T. ) ;
#8992=CARTESIAN_POINT ( 'NONE',  ( 46.59305225739526435, 140.1797705074273210, 31.60846029578754468 ) ) ;
#8993=CARTESIAN_POINT ( 'NONE',  ( 41.64333658814960870, 90.97977050742731819, 38.42115945441014446 ) ) ;
#8995=CARTESIAN_POINT ( 'NONE',  ( 43.01140435219951286, 111.5344580088725905, 39.21067981925356349 ) ) ;
#8996=CARTESIAN_POINT ( 'NONE',  ( 46.10157429594899270, 120.8344580088725593, 38.46393386101375711 ) ) ;
#8998=CARTESIAN_POINT ( 'NONE',  ( 43.01140435219951286, 96.86518717409398960, 38.86567161673127657 ) ) ;
#9003=CARTESIAN_POINT ( 'NONE',  ( 48.01140435219951996, 71.06049967264873146, 35.83527830041809636 ) ) ;
#9004=CARTESIAN_POINT ( 'NONE',  ( 38.01140435219952707, 131.7844580088725763, 34.21067981925357060 ) ) ;
#9005=CARTESIAN_POINT ( 'NONE',  ( 46.59305225739526435, 113.1797705074273210, 31.60846029578754468 ) ) ;
#9008=CARTESIAN_POINT ( 'NONE',  ( 38.58424406990785371, 105.2651871740939953, 35.64915139335015937 ) ) ;
#9009=ORIENTED_EDGE ( 'NONE', *, *, #1004, .T. ) ;
#9011=CARTESIAN_POINT ( 'NONE',  ( 44.55648932407425633, 76.88445800887257064, 29.45539723777780239 ) ) ;
#9015=CARTESIAN_POINT ( 'NONE',  ( 41.64333658814960870, 77.77977050742731535, 30.00020018409699318 ) ) ;
#9018=CARTESIAN_POINT ( 'NONE',  ( 43.01140435219951286, 68.03445800887259054, 28.95336869806222779 ) ) ;
#9021=CARTESIAN_POINT ( 'NONE',  ( 43.01140435219951286, 122.9604996726487371, 28.95336869806222779 ) ) ;
#9022=CARTESIAN_POINT ( 'NONE',  ( 38.58424406990784661, 74.96518717409401233, 32.77220824515698183 ) ) ;
#9025=CARTESIAN_POINT ( 'NONE',  ( 43.01140435219954838, 109.4604996726487371, 39.21067981925356349 ) ) ;
#9027=CARTESIAN_POINT ( 'NONE',  ( 43.01140435219951286, 81.53445800887257633, 39.21067981925356349 ) ) ;
#9029=CARTESIAN_POINT ( 'NONE',  ( 38.01140435219951996, 158.6344580088725706, 32.58608133808903773 ) ) ;
#9030=CARTESIAN_POINT ( 'NONE',  ( 45.74753988029933538, 145.4297705074273210, 37.97664729208901946 ) ) ;
#9031=CARTESIAN_POINT ( 'NONE',  ( 39.42975644700377558, 108.6797705074273352, 36.81289934271958941 ) ) ;
#9033=CARTESIAN_POINT ( 'NONE',  ( 45.74753988029934249, 137.0651871740940067, 30.44471234641812174 ) ) ;
#9037=CARTESIAN_POINT ( 'NONE',  ( 43.01140435219951996, 10.71049967264875491, 34.21067981925357060 ) ) ;
#9041=CYLINDRICAL_SURFACE ( 'NONE', #19036, 4.999999999999997335 ) ;
#9042=CARTESIAN_POINT ( 'NONE',  ( 46.59305225739526435, 115.9151871740940010, 31.60846029578754468 ) ) ;
#9045=ORIENTED_EDGE ( 'NONE', *, *, #10967, .F. ) ;
#9046=CARTESIAN_POINT ( 'NONE',  ( 38.96631938032478359, 89.48445800887257917, 31.27175355779120025 ) ) ;
#9047=CARTESIAN_POINT ( 'NONE',  ( 41.64333658814960870, 150.9797705074273324, 38.42115945441014446 ) ) ;
#9048=CARTESIAN_POINT ( 'NONE',  ( 41.46631938032478359, 159.1104996726487570, 29.45539723777780239 ) ) ;
#9049=CARTESIAN_POINT ( 'NONE',  ( 38.58424406990784661, 111.2651871740939811, 35.64915139335016647 ) ) ;
#9051=CARTESIAN_POINT ( 'NONE',  ( 38.01140435219952707, 75.71049967264873715, 34.21067981925357060 ) ) ;
#9052=CARTESIAN_POINT ( 'NONE',  ( 39.92123440845005433, 108.2344580088725792, 38.46393386101375711 ) ) ;
#9053=CARTESIAN_POINT ( 'NONE',  ( 43.01140435219951996, 149.0344580088725763, 29.21067981925357060 ) ) ;
#9056=FACE_OUTER_BOUND ( 'NONE', #9615, .T. ) ;
#9057=CARTESIAN_POINT ( 'NONE',  ( 47.43856463449118621, 67.61518717409398960, 34.21067981925357060 ) ) ;
#9058=CARTESIAN_POINT ( 'NONE',  ( 48.01140435219951996, 104.3604996726487428, 32.58608133808903773 ) ) ;
#9061=ORIENTED_EDGE ( 'NONE', *, *, #4121, .F. ) ;
#9066=CARTESIAN_POINT ( 'NONE',  ( 41.64333658814960870, 143.5151871740939953, 30.00020018409699318 ) ) ;
#9068=CARTESIAN_POINT ( 'NONE',  ( 47.43856463449117911, 104.0297705074273011, 32.77220824515697473 ) ) ;
#9070=ORIENTED_EDGE ( 'NONE', *, *, #7748, .F. ) ;
#9073=CARTESIAN_POINT ( 'NONE',  ( 41.46631938032478359, 114.3844580088725849, 38.96596240072933170 ) ) ;
#9075=CARTESIAN_POINT ( 'NONE',  ( 38.96631938032478359, 75.41049967264873999, 31.27175355779120025 ) ) ;
#9076=CARTESIAN_POINT ( 'NONE',  ( 46.59305225739526435, 145.3151871740940067, 36.81289934271958941 ) ) ;
#9077=CARTESIAN_POINT ( 'NONE',  ( 38.96631938032478359, 99.41049967264873999, 31.27175355779120025 ) ) ;
#9082=( BOUNDED_CURVE ( )  B_SPLINE_CURVE ( 2, ( #1758, #18945, #3845, #8813, #20600, #5384, #5485, #7268, #8493, #15202, #2185, #12210, #105 ),
 .UNSPECIFIED., .F., .F. ) 
 B_SPLINE_CURVE_WITH_KNOTS ( ( 3, 2, 2, 2, 2, 2, 3 ),
 ( 0.3014705882352941013, 0.3029411764705882137, 0.3058823529411764941, 0.3088235294117647189, 0.3117647058823529438, 0.3147058823529411686, 0.3161764705882352811 ),
 .UNSPECIFIED. ) 
 CURVE ( )  GEOMETRIC_REPRESENTATION_ITEM ( )  RATIONAL_B_SPLINE_CURVE ( ( 0.9755282581475768211, 0.9755282581475768211, 1.000000000000000000, 0.9510565162951535312, 1.000000000000000000, 0.9510565162951535312, 1.000000000000000000, 0.9510565162951535312, 1.000000000000000000, 0.9510565162951535312, 1.000000000000000000, 0.9755282581475768211, 0.9755282581475768211 ) ) 
 REPRESENTATION_ITEM ( '' )  );
#9087=ORIENTED_EDGE ( 'NONE', *, *, #5172, .T. ) ;
#9088=CARTESIAN_POINT ( 'NONE',  ( 40.27526882409969033, 87.82977050742732672, 37.97664729208901946 ) ) ;
#9090=EDGE_CURVE ( 'NONE', #10720, #13985, #1218, .T. ) ;
#9091=CARTESIAN_POINT ( 'NONE',  ( 43.01140435219951286, 68.36518717409400381, 29.55568802177586107 ) ) ;
#9096=CARTESIAN_POINT ( 'NONE',  ( 42.21948215057684450, 117.0373810949690210, 29.21067981925356705 ) ) ;
#9097=CARTESIAN_POINT ( 'NONE',  ( 43.01140435219951286, 122.9604996726487371, 29.21067981925356705 ) ) ;
#9098=CARTESIAN_POINT ( 'NONE',  ( 44.37947211624943833, 133.2797705074273154, 38.42115945441014446 ) ) ;
#9101=VERTEX_POINT ( 'NONE', #20098 ) ;
#9104=CARTESIAN_POINT ( 'NONE',  ( 41.64333658814960870, 137.7797705074273154, 30.00020018409699318 ) ) ;
#9105=CARTESIAN_POINT ( 'NONE',  ( 43.80332655382220253, 134.8836182503284817, 29.21067981925356705 ) ) ;
#9107=FACE_OUTER_BOUND ( 'NONE', #3695, .T. ) ;
#9108=CARTESIAN_POINT ( 'NONE',  ( 47.05648932407426344, 121.5844580088725735, 31.27175355779120025 ) ) ;
#9110=CARTESIAN_POINT ( 'NONE',  ( 41.64333658814960870, 95.51518717409400949, 30.00020018409699318 ) ) ;
#9111=CARTESIAN_POINT ( 'NONE',  ( 38.96631938032478359, 66.41049967264873999, 31.27175355779120025 ) ) ;
#9117=CARTESIAN_POINT ( 'NONE',  ( 38.96631938032478359, 128.4844580088725934, 31.27175355779120025 ) ) ;
#9118=CARTESIAN_POINT ( 'NONE',  ( 38.58424406990784661, 117.5297705074273011, 35.64915139335016647 ) ) ;
#9121=CARTESIAN_POINT ( 'NONE',  ( 40.27526882409969744, 98.66518717409400097, 30.44471234641812174 ) ) ;
#9127=CARTESIAN_POINT ( 'NONE',  ( 38.58424406990786082, 72.37977050742732388, 34.21067981925357060 ) ) ;
#9129=ORIENTED_EDGE ( 'NONE', *, *, #20457, .T. ) ;
#9133=CARTESIAN_POINT ( 'NONE',  ( 48.01140435219951996, 116.0604996726487599, 35.83527830041810347 ) ) ;
#9134=CARTESIAN_POINT ( 'NONE',  ( 45.74753988029933538, 82.16518717409400097, 37.97664729208901946 ) ) ;
#9141=CARTESIAN_POINT ( 'NONE',  ( 43.01140435219951286, 158.0344580088725763, 28.95336869806222779 ) ) ;
#9142=CARTESIAN_POINT ( 'NONE',  ( 47.43856463449117200, 145.7297705074272756, 35.64915139335016647 ) ) ;
#9144=CARTESIAN_POINT ( 'NONE',  ( 43.01140435219951286, 140.3651871740940180, 29.55568802177586107 ) ) ;
#9145=CARTESIAN_POINT ( 'NONE',  ( 42.21948215057687293, 69.03738109496899256, 29.21067981925355994 ) ) ;
#9148=CARTESIAN_POINT ( 'NONE',  ( 38.58424406990786082, 60.37977050742732388, 34.21067981925357060 ) ) ;
#9153=CARTESIAN_POINT ( 'NONE',  ( 43.01140435219951286, 116.3651871740939896, 29.55568802177586463 ) ) ;
#9157=CARTESIAN_POINT ( 'NONE',  ( 38.96631938032478359, 96.08445800887258770, 37.14960608071593384 ) ) ;
#9158=CARTESIAN_POINT ( 'NONE',  ( 40.27526882409969744, 147.8297705074272983, 37.97664729208901235 ) ) ;
#9160=CARTESIAN_POINT ( 'NONE',  ( 46.10157429594899270, 152.6604996726487400, 29.95742577749337343 ) ) ;
#9161=CARTESIAN_POINT ( 'NONE',  ( 43.01140435219951286, 102.8651871740940038, 38.86567161673127657 ) ) ;
#9163=CARTESIAN_POINT ( 'NONE',  ( 43.01140435219951286, 59.96049967264874425, 28.95336869806222779 ) ) ;
#9164=LINE ( 'NONE', #15863, #11500 ) ;
#9169=CARTESIAN_POINT ( 'NONE',  ( 44.37947211624943833, 67.01518717409399528, 38.42115945441014446 ) ) ;
#9177=CARTESIAN_POINT ( 'NONE',  ( 43.01140435219951286, 144.8651871740939612, 38.86567161673127657 ) ) ;
#9179=CARTESIAN_POINT ( 'NONE',  ( 43.01140435219951286, 103.1297705074273097, 38.86567161673127657 ) ) ;
#9181=ORIENTED_EDGE ( 'NONE', *, *, #21402, .F. ) ;
#9184=CARTESIAN_POINT ( 'NONE',  ( 39.92123440845004723, 114.2344580088725650, 38.46393386101376421 ) ) ;
#9186=CARTESIAN_POINT ( 'NONE',  ( 45.74753988029933538, 74.32977050742729830, 30.44471234641811819 ) ) ;
#9187=CARTESIAN_POINT ( 'NONE',  ( 43.01140435219951286, 138.8651871740940180, 38.86567161673127657 ) ) ;
#9188=CARTESIAN_POINT ( 'NONE',  ( 48.01140435219951996, 104.2104996726487371, 34.21067981925357060 ) ) ;
#9193=CARTESIAN_POINT ( 'NONE',  ( 42.21948215057684450, 153.4575765865523067, 39.21067981925356349 ) ) ;
#9194=CARTESIAN_POINT ( 'NONE',  ( 38.01140435219952707, 143.9344580088725536, 35.83527830041809636 ) ) ;
#9195=FACE_OUTER_BOUND ( 'NONE', #19280, .T. ) ;
#9196=ORIENTED_EDGE ( 'NONE', *, *, #5620, .F. ) ;
#9197=CARTESIAN_POINT ( 'NONE',  ( 43.01140435219951286, 88.12977050742732388, 38.86567161673127657 ) ) ;
#9203=CARTESIAN_POINT ( 'NONE',  ( 43.01140435219951286, 105.5344580088725621, 39.21067981925356349 ) ) ;
#9204=CARTESIAN_POINT ( 'NONE',  ( 47.43856463449117911, 134.0297705074273154, 32.77220824515697473 ) ) ;
#9207=ADVANCED_FACE ( 'NONE', ( #9056 ), #17195, .T. ) ;
#9211=CARTESIAN_POINT ( 'NONE',  ( 47.43856463449117200, 128.0297705074273154, 32.77220824515698183 ) ) ;
#9213=( BOUNDED_CURVE ( )  B_SPLINE_CURVE ( 2, ( #12157, #7218, #19214, #1130, #14894, #9844, #17979, #21530, #8081, #7865, #13034, #16544, #11477 ),
 .UNSPECIFIED., .F., .F. ) 
 B_SPLINE_CURVE_WITH_KNOTS ( ( 3, 2, 2, 2, 2, 2, 3 ),
 ( 0.06617647058823529493, 0.06764705882352940736, 0.07058823529411764608, 0.07352941176470588480, 0.07647058823529412352, 0.07941176470588234837, 0.08088235294117647467 ),
 .UNSPECIFIED. ) 
 CURVE ( )  GEOMETRIC_REPRESENTATION_ITEM ( )  RATIONAL_B_SPLINE_CURVE ( ( 0.9755282581475768211, 0.9755282581475768211, 1.000000000000000000, 0.9510565162951535312, 1.000000000000000000, 0.9510565162951535312, 1.000000000000000000, 0.9510565162951535312, 1.000000000000000000, 0.9510565162951535312, 1.000000000000000000, 0.9755282581475765991, 0.9755282581475767101 ) ) 
 REPRESENTATION_ITEM ( '' )  );
#9215=CARTESIAN_POINT ( 'NONE',  ( 38.96631938032478359, 111.0844580088725735, 37.14960608071593384 ) ) ;
#9216=CARTESIAN_POINT ( 'NONE',  ( 41.46631938032478359, 129.1104996726487570, 29.45539723777780239 ) ) ;
#9218=CARTESIAN_POINT ( 'NONE',  ( 39.42975644700377558, 99.41518717409400097, 36.81289934271958941 ) ) ;
#9219=CARTESIAN_POINT ( 'NONE',  ( 48.01140435219951996, 74.36049967264872862, 32.58608133808903773 ) ) ;
#9223=CARTESIAN_POINT ( 'NONE',  ( 41.46631938032478359, 132.3844580088725706, 38.96596240072933170 ) ) ;
#9224=CARTESIAN_POINT ( 'NONE',  ( 38.96631938032478359, 135.0844580088725877, 37.14960608071593384 ) ) ;
#9225=CARTESIAN_POINT ( 'NONE',  ( 47.43856463449117200, 112.7297705074273182, 35.64915139335016647 ) ) ;
#9228=CARTESIAN_POINT ( 'NONE',  ( 44.37947211624943833, 94.01518717409400949, 38.42115945441014446 ) ) ;
#9229=CARTESIAN_POINT ( 'NONE',  ( 43.01140435219951286, 89.03445800887257633, 29.21067981925356705 ) ) ;
#9236=CARTESIAN_POINT ( 'NONE',  ( 47.43856463449117911, 80.02977050742731535, 32.77220824515697473 ) ) ;
#9242=CARTESIAN_POINT ( 'NONE',  ( 47.05648932407426344, 122.5104996726487343, 31.27175355779120025 ) ) ;
#9243=CARTESIAN_POINT ( 'NONE',  ( 47.43856463449117200, 82.46518717409398391, 35.64915139335016647 ) ) ;
#9249=CARTESIAN_POINT ( 'NONE',  ( 48.01140435219951996, 157.1344580088725422, 35.83527830041810347 ) ) ;
#9250=CARTESIAN_POINT ( 'NONE',  ( 46.59305225739526435, 140.1797705074273210, 31.60846029578754468 ) ) ;
#9252=CARTESIAN_POINT ( 'NONE',  ( 46.59305225739526435, 124.3151871740940067, 36.81289934271958941 ) ) ;
#9254=CARTESIAN_POINT ( 'NONE',  ( 43.01140435219951286, 98.03445800887257633, 29.21067981925356705 ) ) ;
#9255=CARTESIAN_POINT ( 'NONE',  ( 47.05648932407426344, 91.58445800887257349, 31.27175355779120025 ) ) ;
#9258=CARTESIAN_POINT ( 'NONE',  ( 47.43856463449117200, 103.7651871740939669, 32.77220824515698183 ) ) ;
#9263=CARTESIAN_POINT ( 'NONE',  ( 48.01140435219951996, 91.13445800887257064, 35.83527830041810347 ) ) ;
#9264=CARTESIAN_POINT ( 'NONE',  ( 48.01140435219951996, 149.2104996726487514, 34.21067981925357060 ) ) ;
#9265=CARTESIAN_POINT ( 'NONE',  ( 39.42975644700377558, 110.8151871740939924, 31.60846029578754468 ) ) ;
#9267=CARTESIAN_POINT ( 'NONE',  ( 38.01140435219951996, 66.56049967264871725, 32.58608133808903773 ) ) ;
#9272=( BOUNDED_CURVE ( )  B_SPLINE_CURVE ( 1, ( #14110, #12247 ),
 .UNSPECIFIED., .F., .F. ) 
 B_SPLINE_CURVE_WITH_KNOTS ( ( 2, 2 ),
 ( 0.000000000000000000, 1.000000000000000000 ),
 .UNSPECIFIED. ) 
 CURVE ( )  GEOMETRIC_REPRESENTATION_ITEM ( )  RATIONAL_B_SPLINE_CURVE ( ( 0.9782066976764471899, 0.9782066976764471899 ) ) 
 REPRESENTATION_ITEM ( '' )  );
#9273=CARTESIAN_POINT ( 'NONE',  ( 40.27526882409969033, 69.56518717409400665, 37.97664729208901946 ) ) ;
#9275=DIRECTION ( 'NONE',  ( 0.000000000000000000, 0.000000000000000000, 1.000000000000000000 ) ) ;
#9281=VERTEX_POINT ( 'NONE', #5947 ) ;
#9282=CARTESIAN_POINT ( 'NONE',  ( 43.01140435219951286, 129.8651871740940180, 38.86567161673127657 ) ) ;
#9284=CARTESIAN_POINT ( 'NONE',  ( 47.43856463449117911, 98.02977050742731535, 32.77220824515697473 ) ) ;
#9286=ORIENTED_EDGE ( 'NONE', *, *, #13492, .F. ) ;
#9289=CARTESIAN_POINT ( 'NONE',  ( 48.01140435219951996, 112.2844580088725763, 34.21067981925357060 ) ) ;
#9290=CARTESIAN_POINT ( 'NONE',  ( 41.46631938032478359, 75.11049967264874283, 29.45539723777780239 ) ) ;
#9291=CARTESIAN_POINT ( 'NONE',  ( 44.37947211624943833, 76.27977050742731535, 38.42115945441014446 ) ) ;
#9292=CARTESIAN_POINT ( 'NONE',  ( 40.27526882409969033, 135.5651871740939782, 37.97664729208901946 ) ) ;
#9293=CARTESIAN_POINT ( 'NONE',  ( 44.55648932407425633, 95.81049967264873146, 29.45539723777780239 ) ) ;
#9300=CYLINDRICAL_SURFACE ( 'NONE', #8177, 4.999999999999997335 ) ;
#9302=CARTESIAN_POINT ( 'NONE',  ( 44.37947211624943833, 77.47977050742731819, 30.00020018409699318 ) ) ;
#9310=CARTESIAN_POINT ( 'NONE',  ( 38.58424406990785371, 126.2297705074273182, 32.77220824515697473 ) ) ;
#9311=ORIENTED_EDGE ( 'NONE', *, *, #4921, .T. ) ;
#9313=ORIENTED_EDGE ( 'NONE', *, *, #21546, .T. ) ;
#9314=CARTESIAN_POINT ( 'NONE',  ( 46.59305225739526435, 127.5797705074273267, 36.81289934271958941 ) ) ;
#9316=CARTESIAN_POINT ( 'NONE',  ( 41.46631938032478359, 100.3104996726487457, 38.96596240072933170 ) ) ;
#9317=CARTESIAN_POINT ( 'NONE',  ( 38.96631938032478359, 130.0104996726487343, 37.14960608071593384 ) ) ;
#9318=CARTESIAN_POINT ( 'NONE',  ( 38.96631938032478359, 97.01049967264874851, 37.14960608071593384 ) ) ;
#9322=DIRECTION ( 'NONE',  ( 0.000000000000000000, 1.000000000000000000, 0.000000000000000000 ) ) ;
#9323=CARTESIAN_POINT ( 'NONE',  ( 43.80332655382220253, 125.8836182503284533, 29.21067981925356705 ) ) ;
#9326=CARTESIAN_POINT ( 'NONE',  ( 41.46631938032478359, 129.3844580088725706, 38.96596240072933170 ) ) ;
#9327=CARTESIAN_POINT ( 'NONE',  ( 43.01140435219951286, 106.1297705074272955, 38.86567161673127657 ) ) ;
#9330=CARTESIAN_POINT ( 'NONE',  ( 38.58424406990785371, 92.96518717409401233, 32.77220824515697473 ) ) ;
#9336=CARTESIAN_POINT ( 'NONE',  ( 44.37947211624943833, 80.47977050742731819, 30.00020018409699318 ) ) ;
#9337=( BOUNDED_CURVE ( )  B_SPLINE_CURVE ( 1, ( #8582, #1957 ),
 .UNSPECIFIED., .F., .F. ) 
 B_SPLINE_CURVE_WITH_KNOTS ( ( 2, 2 ),
 ( 0.000000000000000000, 1.000000000000000000 ),
 .UNSPECIFIED. ) 
 CURVE ( )  GEOMETRIC_REPRESENTATION_ITEM ( )  RATIONAL_B_SPLINE_CURVE ( ( 0.9782068950532306628, 0.9782068950532306628 ) ) 
 REPRESENTATION_ITEM ( '' )  );
#9338=VERTEX_POINT ( 'NONE', #6057 ) ;
#9340=CARTESIAN_POINT ( 'NONE',  ( 40.27526882409969033, 156.8297705074272983, 37.97664729208901946 ) ) ;
#9342=VECTOR ( 'NONE', #9476, 1000.000000000000000 ) ;
#9343=CARTESIAN_POINT ( 'NONE',  ( 39.92123440845004723, 117.2604996726487485, 29.95742577749337343 ) ) ;
#9344=CARTESIAN_POINT ( 'NONE',  ( 44.37947211624943833, 79.01518717409400949, 38.42115945441014446 ) ) ;
#9347=CARTESIAN_POINT ( 'NONE',  ( 48.01140435219951996, 113.2104996726487371, 34.21067981925357060 ) ) ;
#9351=CARTESIAN_POINT ( 'NONE',  ( 44.37947211624943833, 146.4797705074273324, 30.00020018409699318 ) ) ;
#9353=CARTESIAN_POINT ( 'NONE',  ( 44.37947211624943833, 122.2151871740940123, 30.00020018409699318 ) ) ;
#9354=CARTESIAN_POINT ( 'NONE',  ( 42.21948215057684450, 70.38361825032846752, 39.21067981925355639 ) ) ;
#9357=CARTESIAN_POINT ( 'NONE',  ( 44.37947211624943833, 59.47977050742732530, 30.00020018409699318 ) ) ;
#9358=CARTESIAN_POINT ( 'NONE',  ( 44.55648932407425633, 148.6104996726487570, 38.96596240072933170 ) ) ;
#9362=CYLINDRICAL_SURFACE ( 'NONE', #16203, 24.99999999999998579 ) ;
#9363=CARTESIAN_POINT ( 'NONE',  ( 39.42975644700377558, 108.4151871740940152, 36.81289934271958941 ) ) ;
#9366=CARTESIAN_POINT ( 'NONE',  ( 48.01140435219951996, 88.13445800887258486, 35.83527830041810347 ) ) ;
#9369=CARTESIAN_POINT ( 'NONE',  ( 38.01140435219951996, 150.8604996726487286, 35.83527830041810347 ) ) ;
#9370=CARTESIAN_POINT ( 'NONE',  ( 38.58424406990784661, 101.9651871740939981, 32.77220824515698183 ) ) ;
#9373=CARTESIAN_POINT ( 'NONE',  ( 47.05648932407426344, 65.51049967264874851, 31.27175355779120025 ) ) ;
#9377=CARTESIAN_POINT ( 'NONE',  ( 43.80332655382220253, 79.95757658655229250, 29.21067981925356705 ) ) ;
#9380=CARTESIAN_POINT ( 'NONE',  ( 47.43856463449117200, 73.76518717409399528, 32.77220824515698183 ) ) ;
#9382=CARTESIAN_POINT ( 'NONE',  ( 43.01140435219951286, 153.8651871740939896, 38.86567161673127657 ) ) ;
#9383=CARTESIAN_POINT ( 'NONE',  ( 43.80332655382220253, 95.88361825032846752, 29.21067981925356705 ) ) ;
#9390=CARTESIAN_POINT ( 'NONE',  ( 43.01140435219951286, 134.3651871740939612, 29.55568802177586463 ) ) ;
#9391=CARTESIAN_POINT ( 'NONE',  ( 40.27526882409969744, 92.92977050742730682, 30.44471234641812174 ) ) ;
#9393=ORIENTED_EDGE ( 'NONE', *, *, #11753, .T. ) ;
#9398=DIRECTION ( 'NONE',  ( 0.000000000000000000, 1.000000000000000000, 0.000000000000000000 ) ) ;
#9399=CARTESIAN_POINT ( 'NONE',  ( 47.43856463449118621, 79.87977050742732388, 34.21067981925357060 ) ) ;
#9400=CARTESIAN_POINT ( 'NONE',  ( 43.01140435219951286, 134.3651871740939612, 29.55568802177586463 ) ) ;
#9401=( BOUNDED_CURVE ( )  B_SPLINE_CURVE ( 2, ( #12067, #5137, #16918, #5451, #11854, #286, #8457, #1830, #12170, #6803, #3492, #15390, #63 ),
 .UNSPECIFIED., .F., .F. ) 
 B_SPLINE_CURVE_WITH_KNOTS ( ( 3, 2, 2, 2, 2, 2, 3 ),
 ( 0.3750000000000000000, 0.3764705882352941124, 0.3794117647058823373, 0.3823529411764705621, 0.3852941176470588425, 0.3882352941176470673, 0.3897058823529411797 ),
 .UNSPECIFIED. ) 
 CURVE ( )  GEOMETRIC_REPRESENTATION_ITEM ( )  RATIONAL_B_SPLINE_CURVE ( ( 0.9755282581475768211, 0.9755282581475768211, 1.000000000000000000, 0.9510565162951535312, 1.000000000000000000, 0.9510565162951535312, 1.000000000000000000, 0.9510565162951535312, 1.000000000000000000, 0.9510565162951535312, 1.000000000000000000, 0.9755282581475768211, 0.9755282581475768211 ) ) 
 REPRESENTATION_ITEM ( '' )  );
#9402=CARTESIAN_POINT ( 'NONE',  ( 47.05648932407426344, 88.91049967264873999, 37.14960608071593384 ) ) ;
#9411=VERTEX_POINT ( 'NONE', #6158 ) ;
#9412=CARTESIAN_POINT ( 'NONE',  ( 47.43856463449117200, 80.02977050742732956, 32.77220824515698183 ) ) ;
#9415=CARTESIAN_POINT ( 'NONE',  ( 43.01140435219951996, 10.71049967264875491, 39.21067981925356349 ) ) ;
#9419=CARTESIAN_POINT ( 'NONE',  ( 38.58424406990785371, 123.2297705074273040, 32.77220824515697473 ) ) ;
#9424=CARTESIAN_POINT ( 'NONE',  ( 40.27526882409969033, 129.8297705074273267, 37.97664729208901946 ) ) ;
#9426=FACE_OUTER_BOUND ( 'NONE', #2468, .T. ) ;
#9427=CARTESIAN_POINT ( 'NONE',  ( 39.42975644700377558, 90.07977050742732672, 31.60846029578754468 ) ) ;
#9428=CARTESIAN_POINT ( 'NONE',  ( 39.92123440845004723, 65.33445800887257349, 29.95742577749337343 ) ) ;
#9433=CARTESIAN_POINT ( 'NONE',  ( 41.46631938032478359, 97.31049967264873146, 38.96596240072933170 ) ) ;
#9435=AXIS2_PLACEMENT_3D ( 'NONE', #3720, #18815, #8578 ) ;
#9436=CARTESIAN_POINT ( 'NONE',  ( 41.46631938032478359, 67.31049967264873146, 38.96596240072933170 ) ) ;
#9437=CARTESIAN_POINT ( 'NONE',  ( 48.01140435219951996, 125.0604996726487599, 35.83527830041809636 ) ) ;
#9440=AXIS2_PLACEMENT_3D ( 'NONE', #1273, #6340, #19793 ) ;
#9441=CARTESIAN_POINT ( 'NONE',  ( 48.01140435219951996, 136.4344580088725820, 32.58608133808903773 ) ) ;
#9442=CARTESIAN_POINT ( 'NONE',  ( 39.42975644700377558, 102.0797705074273267, 31.60846029578754468 ) ) ;
#9445=CARTESIAN_POINT ( 'NONE',  ( 47.43856463449117911, 100.7651871740939953, 32.77220824515697473 ) ) ;
#9449=CARTESIAN_POINT ( 'NONE',  ( 43.01140435219951996, 158.9604996726487514, 29.21067981925357060 ) ) ;
#9452=CARTESIAN_POINT ( 'NONE',  ( 46.10157429594899270, 154.7344580088725650, 29.95742577749336988 ) ) ;
#9453=CARTESIAN_POINT ( 'NONE',  ( 38.58424406990786082, 69.37977050742730967, 34.21067981925357060 ) ) ;
#9455=ORIENTED_EDGE ( 'NONE', *, *, #1610, .T. ) ;
#9456=CARTESIAN_POINT ( 'NONE',  ( 39.42975644700377558, 153.6797705074273210, 36.81289934271958941 ) ) ;
#9457=CARTESIAN_POINT ( 'NONE',  ( 38.01140435219951996, 120.5604996726487457, 32.58608133808903773 ) ) ;
#9458=CARTESIAN_POINT ( 'NONE',  ( 47.43856463449118621, 79.61518717409400381, 34.21067981925357060 ) ) ;
#9460=CARTESIAN_POINT ( 'NONE',  ( 43.01140435219951996, 10.71049967264875491, 39.21067981925356349 ) ) ;
#9465=DIRECTION ( 'NONE',  ( 0.000000000000000000, 1.000000000000000000, 0.000000000000000000 ) ) ;
#9466=CARTESIAN_POINT ( 'NONE',  ( 38.96631938032478359, 150.0844580088725593, 37.14960608071593384 ) ) ;
#9468=CARTESIAN_POINT ( 'NONE',  ( 45.74753988029933538, 131.3297705074273267, 30.44471234641811819 ) ) ;
#9470=CARTESIAN_POINT ( 'NONE',  ( 47.43856463449118621, 130.6151871740940180, 34.21067981925357060 ) ) ;
#9471=CARTESIAN_POINT ( 'NONE',  ( 39.92123440845005433, 69.26049967264874851, 29.95742577749336988 ) ) ;
#9472=CARTESIAN_POINT ( 'NONE',  ( 41.46631938032478359, 150.1104996726487570, 29.45539723777780239 ) ) ;
#9473=CARTESIAN_POINT ( 'NONE',  ( 43.80332655382220253, 64.53738109496899256, 39.21067981925355639 ) ) ;
#9476=DIRECTION ( 'NONE',  ( 0.000000000000000000, 1.000000000000000000, 0.000000000000000000 ) ) ;
#9477=CARTESIAN_POINT ( 'NONE',  ( 45.74753988029933538, 107.0651871740939640, 30.44471234641811819 ) ) ;
#9478=ORIENTED_EDGE ( 'NONE', *, *, #9514, .F. ) ;
#9481=ORIENTED_EDGE ( 'NONE', *, *, #8338, .F. ) ;
#9482=CARTESIAN_POINT ( 'NONE',  ( 41.46631938032478359, 90.38445800887258486, 38.96596240072933170 ) ) ;
#9483=CARTESIAN_POINT ( 'NONE',  ( 43.01140435219951996, 10.71049967264875491, 34.21067981925357060 ) ) ;
#9484=CARTESIAN_POINT ( 'NONE',  ( 48.01140435219951996, 152.3604996726487570, 32.58608133808903773 ) ) ;
#9485=CARTESIAN_POINT ( 'NONE',  ( 39.42975644700377558, 108.4151871740940152, 36.81289934271958941 ) ) ;
#9494=CARTESIAN_POINT ( 'NONE',  ( 41.64333658814960870, 62.51518717409400239, 30.00020018409699318 ) ) ;
#9496=EDGE_CURVE ( 'NONE', #10959, #19332, #12783, .T. ) ;
#9497=CARTESIAN_POINT ( 'NONE',  ( 47.05648932407426344, 95.51049967264873430, 31.27175355779120025 ) ) ;
#9501=CARTESIAN_POINT ( 'NONE',  ( 44.37947211624943833, 68.21518717409399812, 30.00020018409699318 ) ) ;
#9504=LINE ( 'NONE', #8172, #11980 ) ;
#9505=CARTESIAN_POINT ( 'NONE',  ( 38.58424406990784661, 135.2651871740939953, 35.64915139335016647 ) ) ;
#9512=CARTESIAN_POINT ( 'NONE',  ( 47.05648932407426344, 117.9844580088725792, 37.14960608071593384 ) ) ;
#9513=CARTESIAN_POINT ( 'NONE',  ( 44.55648932407425633, 59.81049967264874567, 29.45539723777780239 ) ) ;
#9514=EDGE_CURVE ( 'NONE', #1555, #15249, #21640, .T. ) ;
#9515=CARTESIAN_POINT ( 'NONE',  ( 45.74753988029933538, 77.32977050742729830, 30.44471234641811819 ) ) ;
#9516=CARTESIAN_POINT ( 'NONE',  ( 46.59305225739526435, 136.3151871740940351, 36.81289934271958941 ) ) ;
#9517=CARTESIAN_POINT ( 'NONE',  ( 38.01140435219951996, 87.56049967264871725, 32.58608133808903773 ) ) ;
#9521=CARTESIAN_POINT ( 'NONE',  ( 43.80332655382220253, 106.5373810949690068, 39.21067981925355639 ) ) ;
#9522=CARTESIAN_POINT ( 'NONE',  ( 48.01140435219951996, 62.36049967264873573, 32.58608133808903773 ) ) ;
#9523=( GEOMETRIC_REPRESENTATION_CONTEXT ( 3 ) GLOBAL_UNCERTAINTY_ASSIGNED_CONTEXT ( ( #8438 ) ) GLOBAL_UNIT_ASSIGNED_CONTEXT ( ( #21622, #11138, #21293 ) ) REPRESENTATION_CONTEXT ( 'NONE', 'WORKASPACE' ) );
#9525=CARTESIAN_POINT ( 'NONE',  ( 43.01140435219951286, 71.62977050742732388, 29.55568802177586463 ) ) ;
#9530=VERTEX_POINT ( 'NONE', #14972 ) ;
#9533=CARTESIAN_POINT ( 'NONE',  ( 41.64333658814960870, 125.7797705074273296, 30.00020018409699318 ) ) ;
#9536=( BOUNDED_CURVE ( )  B_SPLINE_CURVE ( 2, ( #3017, #13050, #9755, #6097, #1147 ),
 .UNSPECIFIED., .F., .T. ) 
 B_SPLINE_CURVE_WITH_KNOTS ( ( 3, 2, 3 ),
 ( 0.9779411764705882026, 0.9794117647058823151, 0.9803957504473121976 ),
 .UNSPECIFIED. ) 
 CURVE ( )  GEOMETRIC_REPRESENTATION_ITEM ( )  RATIONAL_B_SPLINE_CURVE ( ( 0.9755282581475768211, 0.9755282581475768211, 1.000000000000000000, 0.9836257053654985372, 0.9782076199944956807 ) ) 
 REPRESENTATION_ITEM ( '' )  );
#9537=ORIENTED_EDGE ( 'NONE', *, *, #13099, .T. ) ;
#9538=CARTESIAN_POINT ( 'NONE',  ( 45.74753988029933538, 131.3297705074273267, 30.44471234641811819 ) ) ;
#9539=CARTESIAN_POINT ( 'NONE',  ( 44.55648932407425633, 58.88445800887258486, 29.45539723777780239 ) ) ;
#9547=CARTESIAN_POINT ( 'NONE',  ( 39.92123440845004723, 122.3344580088725593, 29.95742577749337343 ) ) ;
#9548=CARTESIAN_POINT ( 'NONE',  ( 44.37947211624943833, 100.2797705074273154, 38.42115945441014446 ) ) ;
#9551=CARTESIAN_POINT ( 'NONE',  ( 39.42975644700377558, 101.8151871740940067, 31.60846029578754468 ) ) ;
#9557=CARTESIAN_POINT ( 'NONE',  ( 43.01140435219951286, 71.62977050742732388, 29.55568802177586107 ) ) ;
#9560=CARTESIAN_POINT ( 'NONE',  ( 39.42975644700377558, 150.6797705074273210, 36.81289934271958941 ) ) ;
#9562=EDGE_CURVE ( 'NONE', #3562, #10959, #6575, .T. ) ;
#9563=CARTESIAN_POINT ( 'NONE',  ( 48.01140435219951996, 110.2104996726487514, 34.21067981925357060 ) ) ;
#9564=CARTESIAN_POINT ( 'NONE',  ( 46.59305225739526435, 64.91518717409400097, 31.60846029578754468 ) ) ;
#9566=CARTESIAN_POINT ( 'NONE',  ( 39.92123440845005433, 96.23445800887257917, 38.46393386101375711 ) ) ;
#9571=CARTESIAN_POINT ( 'NONE',  ( 38.01140435219951996, 149.6344580088725991, 32.58608133808903773 ) ) ;
#9572=CARTESIAN_POINT ( 'NONE',  ( 43.01140435219951286, 128.6297705074273097, 29.55568802177586463 ) ) ;
#9574=CARTESIAN_POINT ( 'NONE',  ( 39.42975644700377558, 123.4151871740940010, 36.81289934271958941 ) ) ;
#9579=CARTESIAN_POINT ( 'NONE',  ( 48.01140435219951996, 65.36049967264874283, 32.58608133808903773 ) ) ;
#9583=AXIS2_PLACEMENT_3D ( 'NONE', #5789, #1053, #17472 ) ;
#9585=CARTESIAN_POINT ( 'NONE',  ( 46.10157429594899270, 85.76049967264874851, 38.46393386101375711 ) ) ;
#9587=CARTESIAN_POINT ( 'NONE',  ( 38.96631938032478359, 86.48445800887257917, 31.27175355779120025 ) ) ;
#9591=CARTESIAN_POINT ( 'NONE',  ( 46.10157429594899270, 145.7604996726487627, 38.46393386101376421 ) ) ;
#9592=CARTESIAN_POINT ( 'NONE',  ( 39.42975644700377558, 93.41518717409400097, 36.81289934271958941 ) ) ;
#9595=CARTESIAN_POINT ( 'NONE',  ( 39.92123440845004723, 64.16049967264873999, 38.46393386101376421 ) ) ;
#9597=CARTESIAN_POINT ( 'NONE',  ( 43.01140435219951996, 170.7104996726487514, 34.21067981925357060 ) ) ;
#9601=CARTESIAN_POINT ( 'NONE',  ( 47.43856463449117200, 157.7297705074273040, 35.64915139335016647 ) ) ;
#9603=CARTESIAN_POINT ( 'NONE',  ( 41.64333658814960870, 150.7151871740940123, 38.42115945441014446 ) ) ;
#9608=CARTESIAN_POINT ( 'NONE',  ( 45.74753988029934249, 65.06518717409400665, 30.44471234641812174 ) ) ;
#9613=CARTESIAN_POINT ( 'NONE',  ( 47.43856463449118621, 130.6151871740940180, 34.21067981925357060 ) ) ;
#9615=EDGE_LOOP ( 'NONE', ( #17671, #15270, #13021, #4496 ) ) ;
#9618=ORIENTED_EDGE ( 'NONE', *, *, #20429, .T. ) ;
#9619=CARTESIAN_POINT ( 'NONE',  ( 43.01140435219951286, 116.9604996726487371, 29.21067981925356705 ) ) ;
#9620=CARTESIAN_POINT ( 'NONE',  ( 39.42975644700377558, 75.67977050742732104, 36.81289934271958941 ) ) ;
#9621=CARTESIAN_POINT ( 'NONE',  ( 38.58424406990784661, 137.9651871740939839, 32.77220824515698183 ) ) ;
#9623=CARTESIAN_POINT ( 'NONE',  ( 44.55648932407425633, 94.61049967264874283, 38.96596240072933170 ) ) ;
#9627=CARTESIAN_POINT ( 'NONE',  ( 43.01140435219951286, 83.36518717409397539, 29.55568802177586463 ) ) ;
#9630=DIRECTION ( 'NONE',  ( 0.000000000000000000, 1.000000000000000000, 0.000000000000000000 ) ) ;
#9632=CARTESIAN_POINT ( 'NONE',  ( 39.42975644700377558, 78.07977050742731251, 31.60846029578754468 ) ) ;
#9636=ORIENTED_EDGE ( 'NONE', *, *, #19879, .F. ) ;
#9637=CARTESIAN_POINT ( 'NONE',  ( 38.58424406990786082, 159.1151871740940180, 34.21067981925357060 ) ) ;
#9640=CARTESIAN_POINT ( 'NONE',  ( 44.37947211624943833, 122.4797705074273182, 30.00020018409699318 ) ) ;
#9643=CARTESIAN_POINT ( 'NONE',  ( 47.43856463449117200, 124.7297705074273182, 35.64915139335016647 ) ) ;
#9644=CARTESIAN_POINT ( 'NONE',  ( 38.96631938032478359, 73.01049967264873430, 37.14960608071593384 ) ) ;
#9645=CARTESIAN_POINT ( 'NONE',  ( 46.59305225739526435, 89.17977050742732104, 31.60846029578754468 ) ) ;
#9646=CARTESIAN_POINT ( 'NONE',  ( 43.01140435219951286, 63.53445800887257633, 39.46799094044489209 ) ) ;
#9648=CARTESIAN_POINT ( 'NONE',  ( 43.01140435219951996, 10.71049967264875491, 34.21067981925357060 ) ) ;
#9649=CARTESIAN_POINT ( 'NONE',  ( 39.92123440845005433, 97.16049967264873999, 38.46393386101375711 ) ) ;
#9652=CARTESIAN_POINT ( 'NONE',  ( 42.21948215057684450, 103.3836182503284675, 39.21067981925355639 ) ) ;
#9655=EDGE_CURVE ( 'NONE', #18126, #3562, #3488, .T. ) ;
#9656=CARTESIAN_POINT ( 'NONE',  ( 47.05648932407426344, 120.9844580088725934, 37.14960608071593384 ) ) ;
#9657=CARTESIAN_POINT ( 'NONE',  ( 38.58424406990786082, 108.3797705074273239, 34.21067981925357060 ) ) ;
#9660=CARTESIAN_POINT ( 'NONE',  ( 40.27526882409969744, 86.66518717409400097, 30.44471234641812174 ) ) ;
#9661=FACE_OUTER_BOUND ( 'NONE', #11346, .T. ) ;
#9665=( BOUNDED_CURVE ( )  B_SPLINE_CURVE ( 2, ( #16969, #224, #1777, #3437, #1880, #8179, #16532, #8613, #3322, #8398, #13668, #10051, #6961 ),
 .UNSPECIFIED., .F., .F. ) 
 B_SPLINE_CURVE_WITH_KNOTS ( ( 3, 2, 2, 2, 2, 2, 3 ),
 ( 0.4338235294117647189, 0.4352941176470588314, 0.4382352941176470562, 0.4411764705882352811, 0.4441176470588235059, 0.4470588235294117863, 0.4485294117647058987 ),
 .UNSPECIFIED. ) 
 CURVE ( )  GEOMETRIC_REPRESENTATION_ITEM ( )  RATIONAL_B_SPLINE_CURVE ( ( 0.9755282581475768211, 0.9755282581475768211, 1.000000000000000000, 0.9510565162951535312, 1.000000000000000000, 0.9510565162951535312, 1.000000000000000000, 0.9510565162951535312, 1.000000000000000000, 0.9510565162951535312, 1.000000000000000000, 0.9755282581475768211, 0.9755282581475768211 ) ) 
 REPRESENTATION_ITEM ( '' )  );
#9667=CARTESIAN_POINT ( 'NONE',  ( 40.27526882409969744, 63.82977050742731961, 37.97664729208901235 ) ) ;
#9670=CARTESIAN_POINT ( 'NONE',  ( 39.42975644700377558, 153.0797705074273267, 31.60846029578754468 ) ) ;
#9673=CARTESIAN_POINT ( 'NONE',  ( 48.01140435219951996, 113.2104996726487371, 34.21067981925357060 ) ) ;
#9674=CARTESIAN_POINT ( 'NONE',  ( 41.64333658814960870, 69.71518717409399812, 38.42115945441014446 ) ) ;
#9676=VECTOR ( 'NONE', #7159, 1000.000000000000000 ) ;
#9681=EDGE_CURVE ( 'NONE', #9281, #14883, #11906, .T. ) ;
#9683=CARTESIAN_POINT ( 'NONE',  ( 39.92123440845004723, 155.3344580088725877, 29.95742577749337343 ) ) ;
#9684=CARTESIAN_POINT ( 'NONE',  ( 45.74753988029933538, 130.4297705074273210, 37.97664729208901946 ) ) ;
#9686=CARTESIAN_POINT ( 'NONE',  ( 40.27526882409969744, 126.5651871740940067, 37.97664729208901235 ) ) ;
#9689=CARTESIAN_POINT ( 'NONE',  ( 43.01140435219951996, 10.71049967264875491, 29.21067981925357060 ) ) ;
#9690=CARTESIAN_POINT ( 'NONE',  ( 47.05648932407426344, 148.9104996726487400, 37.14960608071593384 ) ) ;
#9692=DIRECTION ( 'NONE',  ( 0.000000000000000000, 1.000000000000000000, 0.000000000000000000 ) ) ;
#9696=CARTESIAN_POINT ( 'NONE',  ( 47.05648932407426344, 78.98445800887257917, 37.14960608071593384 ) ) ;
#9698=CARTESIAN_POINT ( 'NONE',  ( 38.96631938032478359, 141.4104996726487400, 31.27175355779120025 ) ) ;
#9699=CARTESIAN_POINT ( 'NONE',  ( 40.27526882409969033, 93.56518717409397823, 37.97664729208901946 ) ) ;
#9705=LINE ( 'NONE', #14755, #1630 ) ;
#9706=CARTESIAN_POINT ( 'NONE',  ( 38.01140435219952707, 105.7104996726487371, 34.21067981925357060 ) ) ;
#9708=CARTESIAN_POINT ( 'NONE',  ( 46.10157429594899270, 80.66049967264873999, 29.95742577749336988 ) ) ;
#9709=CARTESIAN_POINT ( 'NONE',  ( 39.42975644700377558, 63.41518717409400097, 36.81289934271958941 ) ) ;
#9711=AXIS2_PLACEMENT_3D ( 'NONE', #9597, #4190, #2533 ) ;
#9714=ORIENTED_EDGE ( 'NONE', *, *, #19995, .F. ) ;
#9715=CARTESIAN_POINT ( 'NONE',  ( 40.27526882409969744, 71.66518717409400097, 30.44471234641812174 ) ) ;
#9719=CARTESIAN_POINT ( 'NONE',  ( 47.43856463449117200, 133.7651871740939669, 32.77220824515698183 ) ) ;
#9726=AXIS2_PLACEMENT_3D ( 'NONE', #16803, #168, #13607 ) ;
#9728=CARTESIAN_POINT ( 'NONE',  ( 39.92123440845004723, 111.2344580088725507, 38.46393386101376421 ) ) ;
#9729=CARTESIAN_POINT ( 'NONE',  ( 48.01140435219951996, 116.2104996726487371, 34.21067981925357060 ) ) ;
#9730=CARTESIAN_POINT ( 'NONE',  ( 38.58424406990784661, 66.52977050742730114, 35.64915139335016647 ) ) ;
#9731=CARTESIAN_POINT ( 'NONE',  ( 40.27526882409969033, 122.6651871740939725, 30.44471234641811819 ) ) ;
#9733=CARTESIAN_POINT ( 'NONE',  ( 47.05648932407426344, 91.91049967264873999, 37.14960608071593384 ) ) ;
#9736=CARTESIAN_POINT ( 'NONE',  ( 38.01140435219952707, 138.5604996726487457, 32.58608133808903773 ) ) ;
#9737=CARTESIAN_POINT ( 'NONE',  ( 46.59305225739526435, 91.91518717409400097, 31.60846029578754468 ) ) ;
#9742=CARTESIAN_POINT ( 'NONE',  ( 41.64333658814960870, 78.97977050742731819, 38.42115945441014446 ) ) ;
#9750=CARTESIAN_POINT ( 'NONE',  ( 40.27526882409969744, 123.8297705074273125, 37.97664729208901235 ) ) ;
#9753=VERTEX_POINT ( 'NONE', #531 ) ;
#9754=CARTESIAN_POINT ( 'NONE',  ( 41.64333658814960870, 120.9797705074273182, 38.42115945441014446 ) ) ;
#9755=CARTESIAN_POINT ( 'NONE',  ( 44.55648932407425633, 58.88445800887258486, 29.45539723777780239 ) ) ;
#9757=CARTESIAN_POINT ( 'NONE',  ( 39.42975644700377558, 152.8151871740940067, 31.60846029578754468 ) ) ;
#9766=CARTESIAN_POINT ( 'NONE',  ( 38.96631938032478359, 126.0844580088725735, 37.14960608071593384 ) ) ;
#9767=CARTESIAN_POINT ( 'NONE',  ( 46.59305225739526435, 107.1797705074273352, 31.60846029578754468 ) ) ;
#9770=CARTESIAN_POINT ( 'NONE',  ( 40.27526882409969744, 90.56518717409400665, 37.97664729208901235 ) ) ;
#9772=FACE_OUTER_BOUND ( 'NONE', #3892, .T. ) ;
#9774=CARTESIAN_POINT ( 'NONE',  ( 42.21948215057683740, 138.4575765865523067, 39.21067981925357060 ) ) ;
#9778=CARTESIAN_POINT ( 'NONE',  ( 46.59305225739526435, 65.17977050742732104, 31.60846029578754468 ) ) ;
#9779=ORIENTED_EDGE ( 'NONE', *, *, #7673, .T. ) ;
#9781=CARTESIAN_POINT ( 'NONE',  ( 39.42975644700377558, 150.0797705074273267, 31.60846029578754468 ) ) ;
#9783=EDGE_CURVE ( 'NONE', #10801, #470, #6433, .T. ) ;
#9784=CARTESIAN_POINT ( 'NONE',  ( 39.92123440845004723, 111.2604996726487343, 29.95742577749337343 ) ) ;
#9785=CARTESIAN_POINT ( 'NONE',  ( 43.01140435219951286, 71.36518717409397539, 29.55568802177586463 ) ) ;
#9791=CYLINDRICAL_SURFACE ( 'NONE', #5442, 4.999999999999997335 ) ;
#9792=CARTESIAN_POINT ( 'NONE',  ( 38.01140435219951996, 152.6344580088725422, 32.58608133808903773 ) ) ;
#9793=CARTESIAN_POINT ( 'NONE',  ( 40.27526882409969033, 132.8297705074273267, 37.97664729208901946 ) ) ;
#9794=( BOUNDED_CURVE ( )  B_SPLINE_CURVE ( 2, ( #18350, #13392, #9982, #11841, #15263, #6892, #13599, #20338, #11949, #18679, #3582, #5869, #4007 ),
 .UNSPECIFIED., .F., .F. ) 
 B_SPLINE_CURVE_WITH_KNOTS ( ( 3, 2, 2, 2, 2, 2, 3 ),
 ( 0.5955882352941176405, 0.5970588235294117530, 0.5999999999999999778, 0.6029411764705882026, 0.6058823529411764275, 0.6088235294117646523, 0.6102941176470587648 ),
 .UNSPECIFIED. ) 
 CURVE ( )  GEOMETRIC_REPRESENTATION_ITEM ( )  RATIONAL_B_SPLINE_CURVE ( ( 0.9755282581475768211, 0.9755282581475768211, 1.000000000000000000, 0.9510565162951535312, 1.000000000000000000, 0.9510565162951535312, 1.000000000000000000, 0.9510565162951535312, 1.000000000000000000, 0.9510565162951535312, 1.000000000000000000, 0.9755282581475777093, 0.9755282581475768211 ) ) 
 REPRESENTATION_ITEM ( '' )  );
#9796=CARTESIAN_POINT ( 'NONE',  ( 47.43856463449117911, 112.7651871740940379, 32.77220824515697473 ) ) ;
#9804=CARTESIAN_POINT ( 'NONE',  ( 45.74753988029934249, 91.42977050742732104, 37.97664729208901235 ) ) ;
#9808=CARTESIAN_POINT ( 'NONE',  ( 43.01140435219951286, 104.0344580088725763, 29.21067981925356705 ) ) ;
#9809=CARTESIAN_POINT ( 'NONE',  ( 39.92123440845004723, 144.2604996726487343, 29.95742577749337343 ) ) ;
#9810=CARTESIAN_POINT ( 'NONE',  ( 39.42975644700377558, 98.81518717409400665, 31.60846029578754468 ) ) ;
#9817=CARTESIAN_POINT ( 'NONE',  ( 39.42975644700377558, 60.41518717409400097, 36.81289934271958941 ) ) ;
#9820=CARTESIAN_POINT ( 'NONE',  ( 39.42975644700377558, 141.4151871740940010, 36.81289934271958941 ) ) ;
#9824=CARTESIAN_POINT ( 'NONE',  ( 46.59305225739526435, 70.31518717409400665, 36.81289934271958941 ) ) ;
#9827=CARTESIAN_POINT ( 'NONE',  ( 45.74753988029933538, 121.1651871740939725, 37.97664729208901946 ) ) ;
#9836=CARTESIAN_POINT ( 'NONE',  ( 47.43856463449117200, 70.72977050742730398, 35.64915139335016647 ) ) ;
#9837=CARTESIAN_POINT ( 'NONE',  ( 45.74753988029933538, 127.1651871740939725, 37.97664729208901946 ) ) ;
#9839=CARTESIAN_POINT ( 'NONE',  ( 46.10157429594899270, 80.66049967264873999, 29.95742577749337343 ) ) ;
#9841=CARTESIAN_POINT ( 'NONE',  ( 38.01140435219952707, 144.5604996726487173, 32.58608133808903773 ) ) ;
#9842=CARTESIAN_POINT ( 'NONE',  ( 39.92123440845005433, 138.2604996726487343, 29.95742577749336988 ) ) ;
#9843=CARTESIAN_POINT ( 'NONE',  ( 40.27526882409969033, 84.56518717409397823, 37.97664729208901946 ) ) ;
#9844=CARTESIAN_POINT ( 'NONE',  ( 48.01140435219951996, 151.4344580088725820, 32.58608133808903773 ) ) ;
#9847=CARTESIAN_POINT ( 'NONE',  ( 44.37947211624943833, 62.47977050742731109, 30.00020018409699318 ) ) ;
#9851=ORIENTED_EDGE ( 'NONE', *, *, #12435, .T. ) ;
#9852=CARTESIAN_POINT ( 'NONE',  ( 47.43856463449118621, 151.6151871740939896, 34.21067981925357060 ) ) ;
#9854=CARTESIAN_POINT ( 'NONE',  ( 41.64333658814960870, 113.7797705074273296, 30.00020018409699318 ) ) ;
#9857=CARTESIAN_POINT ( 'NONE',  ( 48.01140435219951996, 88.43445800887258201, 32.58608133808903773 ) ) ;
#9859=CARTESIAN_POINT ( 'NONE',  ( 47.43856463449117200, 116.0297705074273154, 32.77220824515698183 ) ) ;
#9860=CARTESIAN_POINT ( 'NONE',  ( 39.92123440845005433, 72.26049967264872009, 29.95742577749336988 ) ) ;
#9861=CARTESIAN_POINT ( 'NONE',  ( 45.74753988029933538, 85.42977050742730682, 37.97664729208901946 ) ) ;
#9862=CARTESIAN_POINT ( 'NONE',  ( 44.37947211624943833, 157.0151871740940237, 38.42115945441014446 ) ) ;
#9869=CARTESIAN_POINT ( 'NONE',  ( 46.10157429594899270, 131.6604996726487400, 29.95742577749336988 ) ) ;
#9871=CARTESIAN_POINT ( 'NONE',  ( 46.10157429594899270, 121.7344580088725792, 29.95742577749337343 ) ) ;
#9872=CARTESIAN_POINT ( 'NONE',  ( 44.37947211624943833, 95.47977050742731819, 30.00020018409699318 ) ) ;
#9875=CARTESIAN_POINT ( 'NONE',  ( 40.27526882409969744, 89.66518717409400097, 30.44471234641812174 ) ) ;
#9878=FACE_OUTER_BOUND ( 'NONE', #6321, .T. ) ;
#9881=CARTESIAN_POINT ( 'NONE',  ( 47.43856463449118621, 145.8797705074273097, 34.21067981925357060 ) ) ;
#9883=CARTESIAN_POINT ( 'NONE',  ( 47.43856463449118621, 106.6151871740940038, 34.21067981925357060 ) ) ;
#9884=CARTESIAN_POINT ( 'NONE',  ( 40.27526882409969744, 69.82977050742731251, 37.97664729208901235 ) ) ;
#9887=CARTESIAN_POINT ( 'NONE',  ( 44.37947211624943833, 148.2797705074273154, 38.42115945441014446 ) ) ;
#9888=CARTESIAN_POINT ( 'NONE',  ( 43.01140435219951286, 97.12977050742732388, 38.86567161673127657 ) ) ;
#9890=CARTESIAN_POINT ( 'NONE',  ( 38.01140435219952707, 114.7104996726487371, 34.21067981925357060 ) ) ;
#9891=CARTESIAN_POINT ( 'NONE',  ( 43.01140435219951286, 72.86518717409400381, 38.86567161673127657 ) ) ;
#9896=CARTESIAN_POINT ( 'NONE',  ( 43.01140435219954838, 110.9604996726487371, 29.21067981925356705 ) ) ;
#9897=CARTESIAN_POINT ( 'NONE',  ( 48.01140435219951996, 148.2844580088725763, 34.21067981925357060 ) ) ;
#9898=CARTESIAN_POINT ( 'NONE',  ( 41.64333658814960870, 131.7797705074273154, 30.00020018409699318 ) ) ;
#9900=CARTESIAN_POINT ( 'NONE',  ( 39.42975644700377558, 113.8151871740940067, 31.60846029578754468 ) ) ;
#9902=FACE_OUTER_BOUND ( 'NONE', #5343, .T. ) ;
#9907=CARTESIAN_POINT ( 'NONE',  ( 44.37947211624943833, 95.47977050742731819, 30.00020018409699318 ) ) ;
#9908=EDGE_LOOP ( 'NONE', ( #11493, #21655, #11523, #16892 ) ) ;
#9910=VERTEX_POINT ( 'NONE', #17171 ) ;
#9911=CARTESIAN_POINT ( 'NONE',  ( 47.05648932407426344, 85.58445800887258770, 31.27175355779120025 ) ) ;
#9913=CARTESIAN_POINT ( 'NONE',  ( 41.46631938032478359, 142.3104996726487457, 38.96596240072933170 ) ) ;
#9914=CARTESIAN_POINT ( 'NONE',  ( 47.43856463449118621, 94.61518717409400381, 34.21067981925357060 ) ) ;
#9916=( BOUNDED_CURVE ( )  B_SPLINE_CURVE ( 2, ( #10249, #16948, #2184, #12209, #10141, #18724, #16844, #6943, #1757, #8492, #13649, #18944, #10571 ),
 .UNSPECIFIED., .F., .F. ) 
 B_SPLINE_CURVE_WITH_KNOTS ( ( 3, 2, 2, 2, 2, 2, 3 ),
 ( 0.6397058823529411242, 0.6411764705882353477, 0.6441176470588235725, 0.6470588235294117974, 0.6500000000000000222, 0.6529411764705882470, 0.6544117647058823595 ),
 .UNSPECIFIED. ) 
 CURVE ( )  GEOMETRIC_REPRESENTATION_ITEM ( )  RATIONAL_B_SPLINE_CURVE ( ( 0.9755282581475768211, 0.9755282581475758219, 1.000000000000000000, 0.9510565162951535312, 1.000000000000000000, 0.9510565162951535312, 1.000000000000000000, 0.9510565162951535312, 1.000000000000000000, 0.9510565162951535312, 1.000000000000000000, 0.9755282581475768211, 0.9755282581475768211 ) ) 
 REPRESENTATION_ITEM ( '' )  );
#9925=CARTESIAN_POINT ( 'NONE',  ( 38.01140435219952707, 78.71049967264875136, 34.21067981925357060 ) ) ;
#9926=CARTESIAN_POINT ( 'NONE',  ( 41.64333658814960870, 59.51518717409400239, 30.00020018409699318 ) ) ;
#9927=CARTESIAN_POINT ( 'NONE',  ( 38.01140435219952707, 62.93445800887258201, 35.83527830041809636 ) ) ;
#9929=CARTESIAN_POINT ( 'NONE',  ( 46.59305225739526435, 142.3151871740940067, 36.81289934271958941 ) ) ;
#9934=CARTESIAN_POINT ( 'NONE',  ( 44.82204145925543060, 59.16666223754088350, 30.14399968058850021 ) ) ;
#9937=CARTESIAN_POINT ( 'NONE',  ( 38.58424406990784661, 125.9651871740939697, 32.77220824515698183 ) ) ;
#9939=ORIENTED_EDGE ( 'NONE', *, *, #2982, .F. ) ;
#9942=VECTOR ( 'NONE', #11004, 1000.000000000000000 ) ;
#9945=CARTESIAN_POINT ( 'NONE',  ( 43.01140435219951286, 115.4604996726487229, 39.21067981925356349 ) ) ;
#9946=VECTOR ( 'NONE', #4296, 1000.000000000000000 ) ;
#9947=CARTESIAN_POINT ( 'NONE',  ( 46.59305225739526435, 65.17977050742732104, 31.60846029578754468 ) ) ;
#9948=CARTESIAN_POINT ( 'NONE',  ( 47.43856463449117200, 121.4651871740939839, 35.64915139335016647 ) ) ;
#9950=CARTESIAN_POINT ( 'NONE',  ( 41.46631938032478359, 79.31049967264873146, 38.96596240072933170 ) ) ;
#9952=CARTESIAN_POINT ( 'NONE',  ( 44.55648932407425633, 97.61049967264874283, 38.96596240072933170 ) ) ;
#9954=CARTESIAN_POINT ( 'NONE',  ( 39.42975644700377558, 83.81518717409400665, 31.60846029578754468 ) ) ;
#9955=CARTESIAN_POINT ( 'NONE',  ( 38.01140435219952707, 81.86049967264874283, 35.83527830041809636 ) ) ;
#9958=EDGE_CURVE ( 'NONE', #21594, #17127, #15571, .T. ) ;
#9960=CARTESIAN_POINT ( 'NONE',  ( 47.43856463449118621, 64.87977050742730967, 34.21067981925357060 ) ) ;
#9964=ORIENTED_EDGE ( 'NONE', *, *, #8119, .T. ) ;
#9965=CARTESIAN_POINT ( 'NONE',  ( 43.01140435219951286, 152.3651871740940180, 29.55568802177586463 ) ) ;
#9966=CARTESIAN_POINT ( 'NONE',  ( 43.01140435219951286, 61.46049967264873715, 39.21067981925356349 ) ) ;
#9967=CARTESIAN_POINT ( 'NONE',  ( 38.58424406990785371, 114.5297705074273296, 35.64915139335015937 ) ) ;
#9972=CARTESIAN_POINT ( 'NONE',  ( 38.58424406990786082, 114.3797705074273097, 34.21067981925357060 ) ) ;
#9974=CARTESIAN_POINT ( 'NONE',  ( 45.74753988029933538, 151.1651871740939725, 37.97664729208901946 ) ) ;
#9977=CARTESIAN_POINT ( 'NONE',  ( 48.01140435219951996, 82.28445800887257633, 34.21067981925357060 ) ) ;
#9981=CARTESIAN_POINT ( 'NONE',  ( 43.01140435219954838, 131.9604996726487229, 29.21067981925356705 ) ) ;
#9982=CARTESIAN_POINT ( 'NONE',  ( 44.55648932407425633, 97.88445800887257064, 29.45539723777780239 ) ) ;
#9984=CARTESIAN_POINT ( 'NONE',  ( 43.01140435219951286, 95.62977050742732388, 29.55568802177586463 ) ) ;
#9985=( BOUNDED_CURVE ( )  B_SPLINE_CURVE ( 2, ( #17656, #1238, #6193, #18207, #4759, #13143, #14680, #6084, #11595, #7973, #21531, #12812, #18324 ),
 .UNSPECIFIED., .F., .F. ) 
 B_SPLINE_CURVE_WITH_KNOTS ( ( 3, 2, 2, 2, 2, 2, 3 ),
 ( 0.1544117647058823595, 0.1558823529411764719, 0.1588235294117646967, 0.1617647058823529493, 0.1647058823529411742, 0.1676470588235293990, 0.1691176470588235115 ),
 .UNSPECIFIED. ) 
 CURVE ( )  GEOMETRIC_REPRESENTATION_ITEM ( )  RATIONAL_B_SPLINE_CURVE ( ( 0.9755282581475768211, 0.9755282581475768211, 1.000000000000000000, 0.9510565162951535312, 1.000000000000000000, 0.9510565162951535312, 1.000000000000000000, 0.9510565162951535312, 1.000000000000000000, 0.9510565162951535312, 1.000000000000000000, 0.9755282581475769321, 0.9755282581475765991 ) ) 
 REPRESENTATION_ITEM ( '' )  );
#9988=CARTESIAN_POINT ( 'NONE',  ( 39.42975644700377558, 83.81518717409400665, 31.60846029578754468 ) ) ;
#9992=FACE_OUTER_BOUND ( 'NONE', #2933, .T. ) ;
#9997=CARTESIAN_POINT ( 'NONE',  ( 47.43856463449117200, 145.7297705074272756, 35.64915139335016647 ) ) ;
#9998=CARTESIAN_POINT ( 'NONE',  ( 46.59305225739526435, 98.17977050742732104, 31.60846029578754468 ) ) ;
#10001=CARTESIAN_POINT ( 'NONE',  ( 48.01140435219951996, 113.0604996726487457, 35.83527830041810347 ) ) ;
#10002=CARTESIAN_POINT ( 'NONE',  ( 43.01140435219951286, 66.86518717409397539, 38.86567161673127657 ) ) ;
#10005=CARTESIAN_POINT ( 'NONE',  ( 38.96631938032478359, 155.4844580088725934, 31.27175355779120025 ) ) ;
#10007=CARTESIAN_POINT ( 'NONE',  ( 41.46631938032478359, 152.1844580088725820, 29.45539723777780239 ) ) ;
#10008=CARTESIAN_POINT ( 'NONE',  ( 43.01140435219951286, 119.6297705074272955, 29.55568802177586463 ) ) ;
#10011=CARTESIAN_POINT ( 'NONE',  ( 43.01140435219951286, 119.3651871740940038, 29.55568802177586107 ) ) ;
#10013=FACE_OUTER_BOUND ( 'NONE', #15877, .T. ) ;
#10017=CARTESIAN_POINT ( 'NONE',  ( 41.64333658814960870, 96.97977050742731819, 38.42115945441014446 ) ) ;
#10019=ORIENTED_EDGE ( 'NONE', *, *, #16809, .T. ) ;
#10022=CARTESIAN_POINT ( 'NONE',  ( 41.46631938032478359, 83.18445800887258201, 29.45539723777780239 ) ) ;
#10023=CARTESIAN_POINT ( 'NONE',  ( 39.92123440845005433, 60.23445800887256496, 38.46393386101375711 ) ) ;
#10024=CARTESIAN_POINT ( 'NONE',  ( 38.96631938032478359, 142.0104996726487627, 37.14960608071593384 ) ) ;
#10025=CARTESIAN_POINT ( 'NONE',  ( 43.01140435219951286, 101.3651871740939896, 29.55568802177586463 ) ) ;
#10031=CARTESIAN_POINT ( 'NONE',  ( 41.46631938032478359, 105.1104996726487428, 29.45539723777780239 ) ) ;
#10032=EDGE_CURVE ( 'NONE', #9411, #10505, #14406, .T. ) ;
#10034=CARTESIAN_POINT ( 'NONE',  ( 48.01140435219951996, 146.2104996726487229, 34.21067981925357060 ) ) ;
#10035=CARTESIAN_POINT ( 'NONE',  ( 40.27526882409969033, 147.8297705074272983, 37.97664729208901946 ) ) ;
#10040=CARTESIAN_POINT ( 'NONE',  ( 38.58424406990786082, 141.1151871740939896, 34.21067981925357060 ) ) ;
#10044=CARTESIAN_POINT ( 'NONE',  ( 47.43856463449118621, 61.61518717409400381, 34.21067981925357060 ) ) ;
#10048=CARTESIAN_POINT ( 'NONE',  ( 45.74753988029933538, 127.1651871740939725, 37.97664729208901946 ) ) ;
#10049=EDGE_LOOP ( 'NONE', ( #17484, #17664 ) ) ;
#10051=CARTESIAN_POINT ( 'NONE',  ( 42.21948215057684450, 113.1113394311928317, 29.21067981925356705 ) ) ;
#10053=( BOUNDED_CURVE ( )  B_SPLINE_CURVE ( 2, ( #4565, #9652, #7999, #3027, #11286, #16353, #1263, #17893, #6332, #13058, #13283, #19784, #4677 ),
 .UNSPECIFIED., .F., .F. ) 
 B_SPLINE_CURVE_WITH_KNOTS ( ( 3, 2, 2, 2, 2, 2, 3 ),
 ( 0.5514705882352941568, 0.5529411764705882693, 0.5558823529411764941, 0.5588235294117647189, 0.5617647058823529438, 0.5647058823529411686, 0.5661764705882352811 ),
 .UNSPECIFIED. ) 
 CURVE ( )  GEOMETRIC_REPRESENTATION_ITEM ( )  RATIONAL_B_SPLINE_CURVE ( ( 0.9755282581475768211, 0.9755282581475768211, 1.000000000000000000, 0.9510565162951535312, 1.000000000000000000, 0.9510565162951535312, 1.000000000000000000, 0.9510565162951535312, 1.000000000000000000, 0.9510565162951535312, 1.000000000000000000, 0.9755282581475768211, 0.9755282581475768211 ) ) 
 REPRESENTATION_ITEM ( '' )  );
#10054=CARTESIAN_POINT ( 'NONE',  ( 41.64333658814960870, 66.97977050742731819, 38.42115945441014446 ) ) ;
#10055=CARTESIAN_POINT ( 'NONE',  ( 38.58424406990786082, 123.1151871740940038, 34.21067981925357060 ) ) ;
#10057=CARTESIAN_POINT ( 'NONE',  ( 38.96631938032478359, 84.41049967264873999, 31.27175355779120025 ) ) ;
#10062=CARTESIAN_POINT ( 'NONE',  ( 38.58424406990784661, 86.96518717409398391, 32.77220824515698183 ) ) ;
#10064=CARTESIAN_POINT ( 'NONE',  ( 38.01140435219952707, 132.7104996726487514, 34.21067981925357060 ) ) ;
#10066=CARTESIAN_POINT ( 'NONE',  ( 38.58424406990784661, 66.52977050742730114, 35.64915139335016647 ) ) ;
#10071=CARTESIAN_POINT ( 'NONE',  ( 47.43856463449117200, 151.7651871740939669, 32.77220824515698183 ) ) ;
#10073=CARTESIAN_POINT ( 'NONE',  ( 46.59305225739526435, 112.5797705074273125, 36.81289934271958941 ) ) ;
#10078=CARTESIAN_POINT ( 'NONE',  ( 38.58424406990784661, 120.5297705074273154, 35.64915139335016647 ) ) ;
#10080=CARTESIAN_POINT ( 'NONE',  ( 38.58424406990784661, 153.2651871740940237, 35.64915139335016647 ) ) ;
#10082=CARTESIAN_POINT ( 'NONE',  ( 38.01140435219952707, 158.7844580088725763, 34.21067981925357060 ) ) ;
#10085=DIRECTION ( 'NONE',  ( 0.000000000000000000, 0.000000000000000000, 1.000000000000000000 ) ) ;
#10088=AXIS2_PLACEMENT_3D ( 'NONE', #21165, #6054, #19501 ) ;
#10089=CARTESIAN_POINT ( 'NONE',  ( 38.01140435219952707, 98.93445800887255359, 35.83527830041809636 ) ) ;
#10090=AXIS2_PLACEMENT_3D ( 'NONE', #14885, #9398, #7856 ) ;
#10091=CARTESIAN_POINT ( 'NONE',  ( 43.01140435219951286, 91.12977050742732388, 38.86567161673127657 ) ) ;
#10094=CARTESIAN_POINT ( 'NONE',  ( 39.42975644700377558, 87.41518717409401518, 36.81289934271958941 ) ) ;
#10099=CARTESIAN_POINT ( 'NONE',  ( 41.64333658814960870, 143.7797705074273154, 30.00020018409699318 ) ) ;
#10102=CARTESIAN_POINT ( 'NONE',  ( 38.58424406990786082, 60.37977050742732388, 34.21067981925357060 ) ) ;
#10104=VECTOR ( 'NONE', #18592, 1000.000000000000000 ) ;
#10105=CARTESIAN_POINT ( 'NONE',  ( 41.64333658814960870, 147.9797705074273324, 38.42115945441014446 ) ) ;
#10106=ADVANCED_FACE ( 'NONE', ( #12865 ), #11640, .T. ) ;
#10107=CARTESIAN_POINT ( 'NONE',  ( 42.21948215057683740, 142.3836182503285102, 39.21067981925357060 ) ) ;
#10108=CARTESIAN_POINT ( 'NONE',  ( 44.55648932407425633, 98.81049967264873146, 29.45539723777780239 ) ) ;
#10109=CARTESIAN_POINT ( 'NONE',  ( 45.74753988029933538, 61.16518717409398675, 37.97664729208901946 ) ) ;
#10112=CARTESIAN_POINT ( 'NONE',  ( 43.01140435219951286, 104.9604996726487371, 29.21067981925356705 ) ) ;
#10114=DIRECTION ( 'NONE',  ( 0.000000000000000000, 1.000000000000000000, 0.000000000000000000 ) ) ;
#10115=CARTESIAN_POINT ( 'NONE',  ( 44.55648932407425633, 142.8844580088725991, 29.45539723777780239 ) ) ;
#10116=CARTESIAN_POINT ( 'NONE',  ( 40.27526882409969033, 126.8297705074273409, 37.97664729208901946 ) ) ;
#10118=CARTESIAN_POINT ( 'NONE',  ( 38.01140435219952707, 140.6344580088725991, 32.58608133808903773 ) ) ;
#10120=CARTESIAN_POINT ( 'NONE',  ( 44.37947211624943833, 118.0151871740940095, 38.42115945441014446 ) ) ;
#10127=CARTESIAN_POINT ( 'NONE',  ( 40.27526882409969744, 86.92977050742732104, 30.44471234641812174 ) ) ;
#10132=CARTESIAN_POINT ( 'NONE',  ( 43.01140435219951286, 74.03445800887257633, 28.95336869806222779 ) ) ;
#10134=VECTOR ( 'NONE', #14810, 1000.000000000000000 ) ;
#10135=CARTESIAN_POINT ( 'NONE',  ( 47.05648932407426344, 142.9104996726487400, 37.14960608071593384 ) ) ;
#10136=CARTESIAN_POINT ( 'NONE',  ( 38.58424406990784661, 83.96518717409399812, 32.77220824515698183 ) ) ;
#10141=CARTESIAN_POINT ( 'NONE',  ( 38.96631938032478359, 94.01049967264873430, 37.14960608071593384 ) ) ;
#10143=CARTESIAN_POINT ( 'NONE',  ( 42.21948215057683740, 148.3836182503284817, 39.21067981925355639 ) ) ;
#10144=CARTESIAN_POINT ( 'NONE',  ( 41.46631938032478359, 79.31049967264873146, 38.96596240072933170 ) ) ;
#10145=CARTESIAN_POINT ( 'NONE',  ( 38.58424406990784661, 156.2297705074273040, 32.77220824515698183 ) ) ;
#10147=CARTESIAN_POINT ( 'NONE',  ( 47.43856463449117911, 145.7651871740939953, 32.77220824515697473 ) ) ;
#10153=CARTESIAN_POINT ( 'NONE',  ( 38.01140435219952707, 77.63445800887255643, 32.58608133808903773 ) ) ;
#10157=CARTESIAN_POINT ( 'NONE',  ( 47.43856463449118621, 124.6151871740940038, 34.21067981925357060 ) ) ;
#10164=CARTESIAN_POINT ( 'NONE',  ( 38.96631938032478359, 101.4844580088725792, 31.27175355779120025 ) ) ;
#10165=CARTESIAN_POINT ( 'NONE',  ( 38.58424406990785371, 159.2297705074272756, 32.77220824515697473 ) ) ;
#10166=CARTESIAN_POINT ( 'NONE',  ( 46.59305225739526435, 68.17977050742732104, 31.60846029578754468 ) ) ;
#10167=CARTESIAN_POINT ( 'NONE',  ( 47.43856463449118621, 127.6151871740940038, 34.21067981925357060 ) ) ;
#10170=CARTESIAN_POINT ( 'NONE',  ( 48.01140435219951996, 80.06049967264871725, 35.83527830041810347 ) ) ;
#10172=CARTESIAN_POINT ( 'NONE',  ( 38.01140435219952707, 144.7104996726487229, 34.21067981925357060 ) ) ;
#10174=CARTESIAN_POINT ( 'NONE',  ( 46.59305225739526435, 82.31518717409400665, 36.81289934271958941 ) ) ;
#10175=CARTESIAN_POINT ( 'NONE',  ( 41.46631938032478359, 81.11049967264874283, 29.45539723777780239 ) ) ;
#10176=CARTESIAN_POINT ( 'NONE',  ( 43.01140435219951286, 92.96049967264875136, 29.21067981925356705 ) ) ;
#10178=CARTESIAN_POINT ( 'NONE',  ( 47.43856463449117200, 68.02977050742731535, 32.77220824515698183 ) ) ;
#10183=EDGE_CURVE ( 'NONE', #18126, #7422, #17242, .T. ) ;
#10184=CARTESIAN_POINT ( 'NONE',  ( 39.42975644700377558, 149.8151871740940067, 31.60846029578754468 ) ) ;
#10186=CARTESIAN_POINT ( 'NONE',  ( 43.01140435219951286, 118.1297705074273239, 38.86567161673127657 ) ) ;
#10189=VECTOR ( 'NONE', #20433, 1000.000000000000000 ) ;
#10191=ORIENTED_EDGE ( 'NONE', *, *, #14123, .T. ) ;
#10192=CARTESIAN_POINT ( 'NONE',  ( 38.58424406990786082, 117.3797705074273097, 34.21067981925357060 ) ) ;
#10194=CARTESIAN_POINT ( 'NONE',  ( 44.37947211624943833, 155.2151871740940123, 30.00020018409699318 ) ) ;
#10196=CARTESIAN_POINT ( 'NONE',  ( 46.10157429594899270, 82.73445800887257917, 29.95742577749336988 ) ) ;
#10199=CARTESIAN_POINT ( 'NONE',  ( 43.01140435219951286, 101.9604996726487371, 29.21067981925356705 ) ) ;
#10201=CARTESIAN_POINT ( 'NONE',  ( 43.80332655382220253, 91.53738109496900677, 39.21067981925355639 ) ) ;
#10204=CARTESIAN_POINT ( 'NONE',  ( 41.64333658814960870, 92.77977050742731535, 30.00020018409699318 ) ) ;
#10207=CARTESIAN_POINT ( 'NONE',  ( 40.27526882409969744, 83.66518717409398675, 30.44471234641812174 ) ) ;
#10213=CARTESIAN_POINT ( 'NONE',  ( 38.58424406990785371, 138.5297705074273154, 35.64915139335015937 ) ) ;
#10215=CARTESIAN_POINT ( 'NONE',  ( 44.37947211624943833, 59.47977050742732530, 30.00020018409699318 ) ) ;
#10217=CARTESIAN_POINT ( 'NONE',  ( 38.58424406990786082, 150.3797705074273097, 34.21067981925357060 ) ) ;
#10219=CARTESIAN_POINT ( 'NONE',  ( 47.43856463449118621, 97.87977050742732388, 34.21067981925357060 ) ) ;
#10221=CARTESIAN_POINT ( 'NONE',  ( 40.27526882409969033, 63.56518717409399954, 37.97664729208901946 ) ) ;
#10226=CARTESIAN_POINT ( 'NONE',  ( 38.01140435219951996, 140.6344580088725706, 32.58608133808903773 ) ) ;
#10227=CARTESIAN_POINT ( 'NONE',  ( 46.59305225739526435, 121.5797705074273267, 36.81289934271958941 ) ) ;
#10229=CARTESIAN_POINT ( 'NONE',  ( 43.01140435219953417, 141.5344580088726048, 39.21067981925356349 ) ) ;
#10230=CARTESIAN_POINT ( 'NONE',  ( 41.64333658814960870, 114.7151871740940123, 38.42115945441014446 ) ) ;
#10232=FACE_OUTER_BOUND ( 'NONE', #1065, .T. ) ;
#10236=CARTESIAN_POINT ( 'NONE',  ( 47.43856463449117911, 85.72977050742731819, 35.64915139335015937 ) ) ;
#10239=CYLINDRICAL_SURFACE ( 'NONE', #19627, 4.999999999999997335 ) ;
#10240=( BOUNDED_CURVE ( )  B_SPLINE_CURVE ( 2, ( #8995, #5776, #19446, #7237, #9215, #4025, #17779, #12723, #20890, #2578, #17676, #10753, #15913 ),
 .UNSPECIFIED., .F., .T. ) 
 B_SPLINE_CURVE_WITH_KNOTS ( ( 3, 2, 2, 2, 2, 2, 3 ),
 ( 0.4632352941176470784, 0.4647058823529411908, 0.4676470588235294157, 0.4705882352941176405, 0.4735294117647058654, 0.4764705882352940902, 0.4779411764705882582 ),
 .UNSPECIFIED. ) 
 CURVE ( )  GEOMETRIC_REPRESENTATION_ITEM ( )  RATIONAL_B_SPLINE_CURVE ( ( 0.9755282581475768211, 0.9755282581475768211, 1.000000000000000000, 0.9510565162951535312, 1.000000000000000000, 0.9510565162951535312, 1.000000000000000000, 0.9510565162951535312, 1.000000000000000000, 0.9510565162951535312, 1.000000000000000000, 0.9755282581475763770, 0.9755282581475768211 ) ) 
 REPRESENTATION_ITEM ( '' )  );
#10241=CARTESIAN_POINT ( 'NONE',  ( 44.55648932407425633, 69.68445800887256780, 38.96596240072933170 ) ) ;
#10242=CARTESIAN_POINT ( 'NONE',  ( 41.46631938032478359, 59.18445800887258201, 29.45539723777780239 ) ) ;
#10244=CARTESIAN_POINT ( 'NONE',  ( 44.55648932407425633, 125.8104996726487315, 29.45539723777780239 ) ) ;
#10245=CARTESIAN_POINT ( 'NONE',  ( 44.37947211624943833, 88.01518717409399528, 38.42115945441014446 ) ) ;
#10249=CARTESIAN_POINT ( 'NONE',  ( 43.01140435219957681, 94.46049967264876557, 39.21067981925356349 ) ) ;
#10251=CARTESIAN_POINT ( 'NONE',  ( 39.92123440845005433, 93.23445800887256496, 38.46393386101375711 ) ) ;
#10253=CARTESIAN_POINT ( 'NONE',  ( 46.59305225739526435, 148.5797705074273267, 36.81289934271958941 ) ) ;
#10256=CARTESIAN_POINT ( 'NONE',  ( 45.74753988029934249, 142.1651871740940294, 37.97664729208901235 ) ) ;
#10259=CARTESIAN_POINT ( 'NONE',  ( 38.58424406990786082, 60.11518717409400381, 34.21067981925357060 ) ) ;
#10263=CARTESIAN_POINT ( 'NONE',  ( 39.42975644700377558, 125.8151871740940067, 31.60846029578754468 ) ) ;
#10266=CARTESIAN_POINT ( 'NONE',  ( 42.21948215057683740, 147.4575765865523067, 39.21067981925355639 ) ) ;
#10268=CARTESIAN_POINT ( 'NONE',  ( 38.96631938032478359, 104.4844580088725650, 31.27175355779120025 ) ) ;
#10269=CARTESIAN_POINT ( 'NONE',  ( 38.58424406990785371, 153.5297705074273438, 35.64915139335015937 ) ) ;
#10270=CARTESIAN_POINT ( 'NONE',  ( 44.82204965540746855, 59.43124467221782936, 30.14400234367972686 ) ) ;
#10271=CARTESIAN_POINT ( 'NONE',  ( 38.58424406990784661, 120.2651871740939953, 35.64915139335016647 ) ) ;
#10273=EDGE_CURVE ( 'NONE', #13896, #9910, #10240, .T. ) ;
#10274=CARTESIAN_POINT ( 'NONE',  ( 44.55648932407425633, 85.61049967264872862, 38.96596240072933170 ) ) ;
#10275=CARTESIAN_POINT ( 'NONE',  ( 48.01140435219951996, 148.1344580088725706, 35.83527830041809636 ) ) ;
#10278=CARTESIAN_POINT ( 'NONE',  ( 47.43856463449118621, 79.61518717409400381, 34.21067981925357060 ) ) ;
#10280=CARTESIAN_POINT ( 'NONE',  ( 48.01140435219951996, 127.2844580088725905, 34.21067981925357060 ) ) ;
#10282=ORIENTED_EDGE ( 'NONE', *, *, #17923, .T. ) ;
#10288=CARTESIAN_POINT ( 'NONE',  ( 38.58424406990784661, 152.9651871740940123, 32.77220824515698183 ) ) ;
#10289=AXIS2_PLACEMENT_3D ( 'NONE', #5347, #20667, #3697 ) ;
#10291=CARTESIAN_POINT ( 'NONE',  ( 38.58424406990785371, 114.2297705074273182, 32.77220824515697473 ) ) ;
#10296=ORIENTED_EDGE ( 'NONE', *, *, #1437, .F. ) ;
#10299=CARTESIAN_POINT ( 'NONE',  ( 40.27526882409969033, 86.92977050742732104, 30.44471234641811819 ) ) ;
#10300=CARTESIAN_POINT ( 'NONE',  ( 47.43856463449117200, 145.7651871740939953, 32.77220824515698183 ) ) ;
#10309=CARTESIAN_POINT ( 'NONE',  ( 43.01140435219951286, 145.4604996726487229, 39.21067981925356349 ) ) ;
#10310=EDGE_CURVE ( 'NONE', #20113, #3863, #11059, .T. ) ;
#10311=CARTESIAN_POINT ( 'NONE',  ( 43.01140435219951286, 98.62977050742730967, 29.55568802177586463 ) ) ;
#10315=CARTESIAN_POINT ( 'NONE',  ( 40.27526882409969744, 75.56518717409399244, 37.97664729208901235 ) ) ;
#10316=DIRECTION ( 'NONE',  ( 0.000000000000000000, 1.000000000000000000, 0.000000000000000000 ) ) ;
#10319=CARTESIAN_POINT ( 'NONE',  ( 43.80332655382220253, 122.8836182503284675, 29.21067981925356705 ) ) ;
#10324=CARTESIAN_POINT ( 'NONE',  ( 46.59305225739526435, 139.5797705074273267, 36.81289934271958941 ) ) ;
#10325=CARTESIAN_POINT ( 'NONE',  ( 45.74753988029933538, 98.32977050742731251, 30.44471234641811819 ) ) ;
#10326=CARTESIAN_POINT ( 'NONE',  ( 43.01140435219951996, 151.4604996726487514, 39.21067981925356349 ) ) ;
#10327=EDGE_CURVE ( 'NONE', #19429, #7439, #7559, .T. ) ;
#10331=CARTESIAN_POINT ( 'NONE',  ( 43.01140435219954838, 109.4604996726487371, 39.21067981925356349 ) ) ;
#10334=CARTESIAN_POINT ( 'NONE',  ( 41.46631938032478359, 144.3844580088725991, 38.96596240072933170 ) ) ;
#10335=CARTESIAN_POINT ( 'NONE',  ( 38.58424406990784661, 120.2297705074273182, 32.77220824515698183 ) ) ;
#10337=CARTESIAN_POINT ( 'NONE',  ( 38.96631938032478359, 140.4844580088725650, 31.27175355779120025 ) ) ;
#10338=CARTESIAN_POINT ( 'NONE',  ( 46.59305225739526435, 103.9151871740940152, 31.60846029578754468 ) ) ;
#10343=CARTESIAN_POINT ( 'NONE',  ( 43.01140435219951286, 83.62977050742730967, 29.55568802177586107 ) ) ;
#10346=CARTESIAN_POINT ( 'NONE',  ( 39.92123440845004723, 72.23445800887256496, 38.46393386101376421 ) ) ;
#10347=CARTESIAN_POINT ( 'NONE',  ( 38.96631938032478359, 86.48445800887257917, 31.27175355779120025 ) ) ;
#10349=ADVANCED_FACE ( 'NONE', ( #9107 ), #5561, .T. ) ;
#10350=CARTESIAN_POINT ( 'NONE',  ( 43.01140435219951286, 128.9604996726487514, 28.95336869806222779 ) ) ;
#10351=CARTESIAN_POINT ( 'NONE',  ( 39.42975644700377558, 89.81518717409400665, 31.60846029578754468 ) ) ;
#10359=CARTESIAN_POINT ( 'NONE',  ( 46.10157429594899270, 68.66049967264873999, 29.95742577749336988 ) ) ;
#10361=CARTESIAN_POINT ( 'NONE',  ( 45.74753988029933538, 151.4297705074273210, 37.97664729208901946 ) ) ;
#10362=CARTESIAN_POINT ( 'NONE',  ( 47.43856463449117200, 104.0297705074273011, 32.77220824515698183 ) ) ;
#10364=CARTESIAN_POINT ( 'NONE',  ( 43.01140435219951286, 135.8651871740940180, 38.86567161673127657 ) ) ;
#10367=CARTESIAN_POINT ( 'NONE',  ( 44.37947211624943833, 59.21518717409400523, 30.00020018409699318 ) ) ;
#10370=CARTESIAN_POINT ( 'NONE',  ( 38.01140435219952707, 134.9344580088725536, 35.83527830041809636 ) ) ;
#10371=CARTESIAN_POINT ( 'NONE',  ( 46.59305225739526435, 118.3151871740940067, 36.81289934271958941 ) ) ;
#10372=( BOUNDED_CURVE ( )  B_SPLINE_CURVE ( 2, ( #1526, #8258, #6605, #13323, #20059, #4946, #18392, #20888, #2576, #820, #16017, #2683, #3623 ),
 .UNSPECIFIED., .F., .F. ) 
 B_SPLINE_CURVE_WITH_KNOTS ( ( 3, 2, 2, 2, 2, 2, 3 ),
 ( 0.1249999999999999861, 0.1264705882352941124, 0.1294117647058823650, 0.1323529411764705899, 0.1352941176470588147, 0.1382352941176470673, 0.1397058823529411797 ),
 .UNSPECIFIED. ) 
 CURVE ( )  GEOMETRIC_REPRESENTATION_ITEM ( )  RATIONAL_B_SPLINE_CURVE ( ( 0.9755282581475765991, 0.9755282581475764880, 1.000000000000000000, 0.9510565162951535312, 1.000000000000000000, 0.9510565162951535312, 1.000000000000000000, 0.9510565162951535312, 1.000000000000000000, 0.9510565162951535312, 1.000000000000000000, 0.9755282581475768211, 0.9755282581475768211 ) ) 
 REPRESENTATION_ITEM ( '' )  );
#10377=CARTESIAN_POINT ( 'NONE',  ( 41.46631938032478359, 101.1844580088725678, 29.45539723777780239 ) ) ;
#10379=CARTESIAN_POINT ( 'NONE',  ( 38.58424406990786082, 156.3797705074273097, 34.21067981925357060 ) ) ;
#10380=CARTESIAN_POINT ( 'NONE',  ( 38.01140435219952707, 156.7104996726487514, 34.21067981925357060 ) ) ;
#10381=CARTESIAN_POINT ( 'NONE',  ( 44.37947211624943833, 112.0151871740940095, 38.42115945441014446 ) ) ;
#10383=CARTESIAN_POINT ( 'NONE',  ( 44.55648932407425633, 74.81049967264874567, 29.45539723777780239 ) ) ;
#10386=CARTESIAN_POINT ( 'NONE',  ( 42.21948215057684450, 124.3836182503284675, 39.21067981925355639 ) ) ;
#10388=CARTESIAN_POINT ( 'NONE',  ( 47.43856463449117200, 82.76518717409400949, 32.77220824515698183 ) ) ;
#10392=CARTESIAN_POINT ( 'NONE',  ( 41.46631938032478359, 132.1104996726487286, 29.45539723777780239 ) ) ;
#10398=CARTESIAN_POINT ( 'NONE',  ( 45.74753988029933538, 146.0651871740940067, 30.44471234641811819 ) ) ;
#10400=CARTESIAN_POINT ( 'NONE',  ( 39.42975644700377558, 105.0797705074273125, 31.60846029578754468 ) ) ;
#10402=ORIENTED_EDGE ( 'NONE', *, *, #16281, .T. ) ;
#10406=CARTESIAN_POINT ( 'NONE',  ( 38.01140435219952707, 128.9344580088726104, 35.83527830041809636 ) ) ;
#10408=CARTESIAN_POINT ( 'NONE',  ( 43.01140435219951286, 146.3651871740939896, 29.55568802177586463 ) ) ;
#10410=CARTESIAN_POINT ( 'NONE',  ( 47.05648932407426344, 118.9104996726487400, 37.14960608071593384 ) ) ;
#10412=CARTESIAN_POINT ( 'NONE',  ( 43.80332655382220253, 100.5373810949690210, 39.21067981925355639 ) ) ;
#10414=CARTESIAN_POINT ( 'NONE',  ( 43.01140435219951286, 76.46049967264873715, 39.21067981925356349 ) ) ;
#10416=CARTESIAN_POINT ( 'NONE',  ( 40.27526882409969033, 84.82977050742732672, 37.97664729208901946 ) ) ;
#10419=CARTESIAN_POINT ( 'NONE',  ( 38.58424406990785371, 77.96518717409398391, 32.77220824515697473 ) ) ;
#10425=CARTESIAN_POINT ( 'NONE',  ( 46.10157429594899270, 122.6604996726487542, 29.95742577749336988 ) ) ;
#10427=ORIENTED_EDGE ( 'NONE', *, *, #865, .F. ) ;
#10430=CARTESIAN_POINT ( 'NONE',  ( 46.59305225739526435, 133.5797705074272983, 36.81289934271958941 ) ) ;
#10432=VECTOR ( 'NONE', #15070, 1000.000000000000000 ) ;
#10434=EDGE_CURVE ( 'NONE', #16530, #19857, #4133, .T. ) ;
#10436=CARTESIAN_POINT ( 'NONE',  ( 47.43856463449117200, 61.76518717409399528, 32.77220824515698183 ) ) ;
#10440=CARTESIAN_POINT ( 'NONE',  ( 45.74753988029933538, 95.06518717409400665, 30.44471234641811819 ) ) ;
#10444=CARTESIAN_POINT ( 'NONE',  ( 46.10157429594899270, 145.7344580088725650, 29.95742577749337343 ) ) ;
#10445=CARTESIAN_POINT ( 'NONE',  ( 46.59305225739526435, 124.5797705074273267, 36.81289934271958941 ) ) ;
#10448=CARTESIAN_POINT ( 'NONE',  ( 41.64333658814960870, 108.7151871740940123, 38.42115945441014446 ) ) ;
#10449=CYLINDRICAL_SURFACE ( 'NONE', #9435, 4.999999999999997335 ) ;
#10455=CARTESIAN_POINT ( 'NONE',  ( 47.43856463449117911, 88.72977050742730398, 35.64915139335015937 ) ) ;
#10456=CIRCLE ( 'NONE', #16062, 24.99999999999998934 ) ;
#10458=DIRECTION ( 'NONE',  ( 0.000000000000000000, 1.000000000000000000, 0.000000000000000000 ) ) ;
#10459=CARTESIAN_POINT ( 'NONE',  ( 38.96631938032478359, 77.48445800887257917, 31.27175355779120025 ) ) ;
#10461=CARTESIAN_POINT ( 'NONE',  ( 48.01140435219951996, 125.3604996726487286, 32.58608133808903773 ) ) ;
#10462=CARTESIAN_POINT ( 'NONE',  ( 38.58424406990784661, 84.26518717409399528, 35.64915139335016647 ) ) ;
#10467=CARTESIAN_POINT ( 'NONE',  ( 43.01140435219951996, 10.71049967264875491, 34.21067981925357060 ) ) ;
#10469=CARTESIAN_POINT ( 'NONE',  ( 43.01140435219951996, 10.71049967264875491, 34.21067981925357060 ) ) ;
#10471=CARTESIAN_POINT ( 'NONE',  ( 44.37947211624943833, 149.4797705074273324, 30.00020018409699318 ) ) ;
#10472=CARTESIAN_POINT ( 'NONE',  ( 41.64333658814960870, 101.7797705074273154, 30.00020018409699318 ) ) ;
#10473=EDGE_CURVE ( 'NONE', #17856, #16317, #6940, .T. ) ;
#10475=CARTESIAN_POINT ( 'NONE',  ( 40.27526882409969744, 137.6651871740940010, 30.44471234641812174 ) ) ;
#10480=CARTESIAN_POINT ( 'NONE',  ( 40.27526882409969033, 111.5651871740939782, 37.97664729208901946 ) ) ;
#10482=ORIENTED_EDGE ( 'NONE', *, *, #21194, .F. ) ;
#10485=CARTESIAN_POINT ( 'NONE',  ( 43.01140435219951286, 101.0344580088725763, 28.95336869806222779 ) ) ;
#10486=CARTESIAN_POINT ( 'NONE',  ( 45.74753988029934249, 148.4297705074273210, 37.97664729208901235 ) ) ;
#10487=CARTESIAN_POINT ( 'NONE',  ( 43.01140435219951286, 154.4604996726487798, 39.46799094044489209 ) ) ;
#10488=CARTESIAN_POINT ( 'NONE',  ( 39.42975644700377558, 120.4151871740940010, 36.81289934271958941 ) ) ;
#10491=CARTESIAN_POINT ( 'NONE',  ( 47.05648932407426344, 70.91049967264873999, 37.14960608071593384 ) ) ;
#10495=CARTESIAN_POINT ( 'NONE',  ( 45.74753988029933538, 83.06518717409400665, 30.44471234641811819 ) ) ;
#10496=CARTESIAN_POINT ( 'NONE',  ( 45.22505347682923116, 59.38050100342834270, 30.37668637662395099 ) ) ;
#10500=EDGE_LOOP ( 'NONE', ( #17133, #21309, #10402, #3225, #14226, #21537, #4686, #5528 ) ) ;
#10505=VERTEX_POINT ( 'NONE', #14913 ) ;
#10506=CARTESIAN_POINT ( 'NONE',  ( 38.58424406990784661, 147.2651871740939669, 35.64915139335016647 ) ) ;
#10508=CARTESIAN_POINT ( 'NONE',  ( 46.59305225739526435, 100.5797705074273267, 36.81289934271958941 ) ) ;
#10512=ORIENTED_EDGE ( 'NONE', *, *, #9090, .T. ) ;
#10513=CARTESIAN_POINT ( 'NONE',  ( 45.74753988029933538, 113.3297705074273125, 30.44471234641811819 ) ) ;
#10517=CARTESIAN_POINT ( 'NONE',  ( 38.58424406990784661, 146.9651871740940123, 32.77220824515698183 ) ) ;
#10519=CARTESIAN_POINT ( 'NONE',  ( 38.01140435219952707, 99.71049967264875136, 34.21067981925357060 ) ) ;
#10526=CARTESIAN_POINT ( 'NONE',  ( 38.58424406990784661, 87.52977050742730114, 35.64915139335016647 ) ) ;
#10528=CARTESIAN_POINT ( 'NONE',  ( 43.01140435219951286, 80.36518717409398960, 29.55568802177586107 ) ) ;
#10532=CARTESIAN_POINT ( 'NONE',  ( 48.01140435219951996, 85.28445800887257633, 34.21067981925357060 ) ) ;
#10533=CARTESIAN_POINT ( 'NONE',  ( 43.01140435219951286, 121.4604996726487371, 39.21067981925356349 ) ) ;
#10534=CARTESIAN_POINT ( 'NONE',  ( 45.74753988029934249, 137.3297705074272983, 30.44471234641812174 ) ) ;
#10537=DIRECTION ( 'NONE',  ( 0.000000000000000000, -0.000000000000000000, 1.000000000000000000 ) ) ;
#10539=CARTESIAN_POINT ( 'NONE',  ( 47.43856463449117200, 133.7297705074273324, 35.64915139335016647 ) ) ;
#10542=CARTESIAN_POINT ( 'NONE',  ( 44.37947211624943833, 62.21518717409399102, 30.00020018409699318 ) ) ;
#10545=CARTESIAN_POINT ( 'NONE',  ( 45.74753988029933538, 98.06518717409397823, 30.44471234641811819 ) ) ;
#10549=CARTESIAN_POINT ( 'NONE',  ( 39.92123440845004723, 143.3344580088725877, 29.95742577749337343 ) ) ;
#10550=CARTESIAN_POINT ( 'NONE',  ( 39.42975644700377558, 117.0797705074273267, 31.60846029578754468 ) ) ;
#10553=CARTESIAN_POINT ( 'NONE',  ( 47.43856463449118621, 109.6151871740940038, 34.21067981925357060 ) ) ;
#10555=CARTESIAN_POINT ( 'NONE',  ( 43.01140435219951286, 88.46049967264873715, 39.21067981925356349 ) ) ;
#10562=CARTESIAN_POINT ( 'NONE',  ( 39.42975644700377558, 87.07977050742732672, 31.60846029578754468 ) ) ;
#10564=CARTESIAN_POINT ( 'NONE',  ( 39.92123440845004723, 71.33445800887258770, 29.95742577749337343 ) ) ;
#10566=CARTESIAN_POINT ( 'NONE',  ( 38.96631938032478359, 133.0104996726487343, 37.14960608071593384 ) ) ;
#10567=CARTESIAN_POINT ( 'NONE',  ( 39.42975644700377558, 87.41518717409401518, 36.81289934271958941 ) ) ;
#10571=CARTESIAN_POINT ( 'NONE',  ( 43.01140435219951286, 92.96049967264875136, 29.21067981925356705 ) ) ;
#10572=DIRECTION ( 'NONE',  ( 0.000000000000000000, 1.000000000000000000, 0.000000000000000000 ) ) ;
#10575=CARTESIAN_POINT ( 'NONE',  ( 47.43856463449117200, 140.0297705074273438, 32.77220824515698183 ) ) ;
#10576=CARTESIAN_POINT ( 'NONE',  ( 47.43856463449117200, 101.0297705074273011, 32.77220824515698183 ) ) ;
#10577=CARTESIAN_POINT ( 'NONE',  ( 39.42975644700377558, 134.8151871740940067, 31.60846029578754468 ) ) ;
#10580=CARTESIAN_POINT ( 'NONE',  ( 38.58424406990784661, 63.22977050742731109, 32.77220824515698183 ) ) ;
#10581=CARTESIAN_POINT ( 'NONE',  ( 43.01140435219951286, 136.4604996726487514, 39.21067981925356349 ) ) ;
#10585=CARTESIAN_POINT ( 'NONE',  ( 39.42975644700377558, 117.4151871740940010, 36.81289934271958941 ) ) ;
#10589=CARTESIAN_POINT ( 'NONE',  ( 41.46631938032478359, 99.38445800887258486, 38.96596240072933170 ) ) ;
#10591=CARTESIAN_POINT ( 'NONE',  ( 48.01140435219951996, 158.2104996726487514, 34.21067981925357060 ) ) ;
#10592=CARTESIAN_POINT ( 'NONE',  ( 46.59305225739526435, 118.9151871740940010, 31.60846029578754468 ) ) ;
#10594=CARTESIAN_POINT ( 'NONE',  ( 46.10157429594899270, 67.76049967264872009, 38.46393386101376421 ) ) ;
#10595=CARTESIAN_POINT ( 'NONE',  ( 38.01140435219952707, 107.7844580088725763, 34.21067981925357060 ) ) ;
#10596=CARTESIAN_POINT ( 'NONE',  ( 43.01140435219951996, 10.71049967264875491, 34.21067981925357060 ) ) ;
#10601=CARTESIAN_POINT ( 'NONE',  ( 47.43856463449117200, 79.46518717409399812, 35.64915139335016647 ) ) ;
#10605=ORIENTED_EDGE ( 'NONE', *, *, #325, .T. ) ;
#10608=ORIENTED_EDGE ( 'NONE', *, *, #4767, .T. ) ;
#10609=CARTESIAN_POINT ( 'NONE',  ( 41.64333658814960870, 147.7151871740940123, 38.42115945441014446 ) ) ;
#10611=CARTESIAN_POINT ( 'NONE',  ( 47.43856463449117911, 103.7297705074273182, 35.64915139335015937 ) ) ;
#10616=CARTESIAN_POINT ( 'NONE',  ( 39.42975644700377558, 111.0797705074273125, 31.60846029578754468 ) ) ;
#10617=DIRECTION ( 'NONE',  ( 0.000000000000000000, -0.000000000000000000, -1.000000000000000000 ) ) ;
#10619=CARTESIAN_POINT ( 'NONE',  ( 46.59305225739526435, 83.17977050742732104, 31.60846029578754468 ) ) ;
#10620=CARTESIAN_POINT ( 'NONE',  ( 39.42975644700377558, 146.8151871740940067, 31.60846029578754468 ) ) ;
#10621=CARTESIAN_POINT ( 'NONE',  ( 38.96631938032478359, 97.01049967264874851, 37.14960608071593384 ) ) ;
#10624=CARTESIAN_POINT ( 'NONE',  ( 38.01140435219952707, 60.56049967264873146, 32.58608133808903773 ) ) ;
#10626=( BOUNDED_CURVE ( )  B_SPLINE_CURVE ( 2, ( #19871, #2781, #14678, #4758, #16327, #4538, #1236, #14457, #2665, #16117, #12923, #9521, #18205 ),
 .UNSPECIFIED., .F., .F. ) 
 B_SPLINE_CURVE_WITH_KNOTS ( ( 3, 2, 2, 2, 2, 2, 3 ),
 ( 0.5073529411764705621, 0.5088235294117646745, 0.5117647058823528994, 0.5147058823529411242, 0.5176470588235294601, 0.5205882352941176849, 0.5220588235294117974 ),
 .UNSPECIFIED. ) 
 CURVE ( )  GEOMETRIC_REPRESENTATION_ITEM ( )  RATIONAL_B_SPLINE_CURVE ( ( 0.9755282581475768211, 0.9755282581475768211, 1.000000000000000000, 0.9510565162951535312, 1.000000000000000000, 0.9510565162951535312, 1.000000000000000000, 0.9510565162951535312, 1.000000000000000000, 0.9510565162951535312, 1.000000000000000000, 0.9755282581475768211, 0.9755282581475768211 ) ) 
 REPRESENTATION_ITEM ( '' )  );
#10627=DIRECTION ( 'NONE',  ( 0.000000000000000000, 1.000000000000000000, 0.000000000000000000 ) ) ;
#10634=CARTESIAN_POINT ( 'NONE',  ( 38.58424406990786082, 81.37977050742730967, 34.21067981925357060 ) ) ;
#10635=CARTESIAN_POINT ( 'NONE',  ( 47.43856463449117911, 76.46518717409401233, 35.64915139335015937 ) ) ;
#10641=CARTESIAN_POINT ( 'NONE',  ( 38.58424406990785371, 129.2297705074273040, 32.77220824515697473 ) ) ;
#10646=CARTESIAN_POINT ( 'NONE',  ( 38.58424406990786082, 138.3797705074273381, 34.21067981925357060 ) ) ;
#10649=CARTESIAN_POINT ( 'NONE',  ( 38.58424406990784661, 93.52977050742731535, 35.64915139335016647 ) ) ;
#10654=CARTESIAN_POINT ( 'NONE',  ( 45.74753988029933538, 94.16518717409400097, 37.97664729208901946 ) ) ;
#10655=CARTESIAN_POINT ( 'NONE',  ( 42.21948215057683740, 153.0373810949689926, 29.21067981925357415 ) ) ;
#10659=CARTESIAN_POINT ( 'NONE',  ( 44.55648932407425633, 133.8844580088725706, 29.45539723777780239 ) ) ;
#10660=CARTESIAN_POINT ( 'NONE',  ( 38.58424406990786082, 117.3797705074273097, 34.21067981925357060 ) ) ;
#10663=CARTESIAN_POINT ( 'NONE',  ( 47.43856463449118621, 106.6151871740940038, 34.21067981925357060 ) ) ;
#10665=DIRECTION ( 'NONE',  ( 0.000000000000000000, 0.000000000000000000, 1.000000000000000000 ) ) ;
#10669=CARTESIAN_POINT ( 'NONE',  ( 38.58424406990785371, 78.22977050742731819, 32.77220824515697473 ) ) ;
#10670=ORIENTED_EDGE ( 'NONE', *, *, #16732, .F. ) ;
#10671=CARTESIAN_POINT ( 'NONE',  ( 48.01140435219951996, 61.28445800887258343, 34.21067981925357060 ) ) ;
#10673=CARTESIAN_POINT ( 'NONE',  ( 43.01140435219951286, 133.4604996726487514, 39.46799094044489209 ) ) ;
#10674=CARTESIAN_POINT ( 'NONE',  ( 45.74753988029933538, 80.06518717409397823, 30.44471234641811819 ) ) ;
#10681=CARTESIAN_POINT ( 'NONE',  ( 41.64333658814960870, 144.9797705074273324, 38.42115945441014446 ) ) ;
#10682=CARTESIAN_POINT ( 'NONE',  ( 38.58424406990784661, 105.5297705074273011, 35.64915139335016647 ) ) ;
#10684=CARTESIAN_POINT ( 'NONE',  ( 41.64333658814960870, 135.7151871740940123, 38.42115945441014446 ) ) ;
#10685=FACE_OUTER_BOUND ( 'NONE', #5879, .T. ) ;
#10688=CARTESIAN_POINT ( 'NONE',  ( 38.01140435219952707, 135.8604996726487002, 35.83527830041809636 ) ) ;
#10691=DIRECTION ( 'NONE',  ( 0.000000000000000000, 0.000000000000000000, 1.000000000000000000 ) ) ;
#10692=CARTESIAN_POINT ( 'NONE',  ( 41.64333658814960870, 119.5151871740940095, 30.00020018409699318 ) ) ;
#10697=CARTESIAN_POINT ( 'NONE',  ( 44.55648932407425633, 91.88445800887258486, 29.45539723777780239 ) ) ;
#10698=CARTESIAN_POINT ( 'NONE',  ( 40.27526882409969744, 150.8297705074273267, 37.97664729208901235 ) ) ;
#10700=CARTESIAN_POINT ( 'NONE',  ( 48.01140435219951996, 155.3604996726487570, 32.58608133808903773 ) ) ;
#10701=CARTESIAN_POINT ( 'NONE',  ( 44.37947211624943833, 119.2151871740939981, 30.00020018409699318 ) ) ;
#10703=EDGE_CURVE ( 'NONE', #17373, #13772, #6101, .T. ) ;
#10704=CARTESIAN_POINT ( 'NONE',  ( 44.55648932407425633, 68.81049967264874567, 29.45539723777780239 ) ) ;
#10705=CARTESIAN_POINT ( 'NONE',  ( 43.01140435219951286, 77.96049967264873715, 29.21067981925356705 ) ) ;
#10706=CYLINDRICAL_SURFACE ( 'NONE', #14629, 4.999999999999997335 ) ;
#10708=CARTESIAN_POINT ( 'NONE',  ( 38.01140435219952707, 123.8604996726487570, 35.83527830041809636 ) ) ;
#10710=CARTESIAN_POINT ( 'NONE',  ( 43.01140435219951286, 69.86518717409400381, 38.86567161673127657 ) ) ;
#10718=CARTESIAN_POINT ( 'NONE',  ( 39.42975644700377558, 141.4151871740940010, 36.81289934271958941 ) ) ;
#10719=CARTESIAN_POINT ( 'NONE',  ( 41.64333658814960870, 101.7797705074273154, 30.00020018409699318 ) ) ;
#10720=VERTEX_POINT ( 'NONE', #2801 ) ;
#10724=ORIENTED_EDGE ( 'NONE', *, *, #1261, .F. ) ;
#10725=CARTESIAN_POINT ( 'NONE',  ( 48.01140435219951996, 115.2844580088725763, 34.21067981925357060 ) ) ;
#10726=AXIS2_PLACEMENT_3D ( 'NONE', #2428, #14323, #12675 ) ;
#10729=CARTESIAN_POINT ( 'NONE',  ( 46.59305225739526435, 82.57977050742731251, 36.81289934271958941 ) ) ;
#10730=CARTESIAN_POINT ( 'NONE',  ( 38.58424406990786082, 144.1151871740939896, 34.21067981925357060 ) ) ;
#10731=CARTESIAN_POINT ( 'NONE',  ( 48.01140435219951996, 101.0604996726487173, 35.83527830041810347 ) ) ;
#10735=CARTESIAN_POINT ( 'NONE',  ( 44.55648932407425633, 64.88445800887257064, 29.45539723777780239 ) ) ;
#10738=CARTESIAN_POINT ( 'NONE',  ( 47.43856463449118621, 85.87977050742730967, 34.21067981925357060 ) ) ;
#10740=CARTESIAN_POINT ( 'NONE',  ( 38.58424406990785371, 68.96518717409398391, 32.77220824515697473 ) ) ;
#10745=DIRECTION ( 'NONE',  ( 0.000000000000000000, -1.000000000000000000, 0.000000000000000000 ) ) ;
#10746=CARTESIAN_POINT ( 'NONE',  ( 47.43856463449118621, 136.8797705074273381, 34.21067981925357060 ) ) ;
#10751=CARTESIAN_POINT ( 'NONE',  ( 47.43856463449117200, 136.7297705074272756, 35.64915139335016647 ) ) ;
#10752=CARTESIAN_POINT ( 'NONE',  ( 47.05648932407426344, 154.9104996726487400, 37.14960608071593384 ) ) ;
#10753=CARTESIAN_POINT ( 'NONE',  ( 42.21948215057684450, 110.1113394311928175, 29.21067981925355994 ) ) ;
#10756=CARTESIAN_POINT ( 'NONE',  ( 40.27526882409969033, 98.66518717409400097, 30.44471234641811819 ) ) ;
#10757=CARTESIAN_POINT ( 'NONE',  ( 46.10157429594899270, 132.8344580088725593, 38.46393386101375711 ) ) ;
#10761=VECTOR ( 'NONE', #9692, 1000.000000000000000 ) ;
#10762=CARTESIAN_POINT ( 'NONE',  ( 44.55648932407425633, 71.81049967264874567, 29.45539723777780239 ) ) ;
#10763=CARTESIAN_POINT ( 'NONE',  ( 38.01140435219951996, 128.6344580088725706, 32.58608133808903773 ) ) ;
#10764=CARTESIAN_POINT ( 'NONE',  ( 45.74753988029933538, 116.3297705074272983, 30.44471234641811819 ) ) ;
#10767=CARTESIAN_POINT ( 'NONE',  ( 47.43856463449118621, 103.6151871740940038, 34.21067981925357060 ) ) ;
#10768=LINE ( 'NONE', #2591, #7541 ) ;
#10774=CARTESIAN_POINT ( 'NONE',  ( 43.01140435219954838, 108.5344580088725763, 39.21067981925356349 ) ) ;
#10775=CARTESIAN_POINT ( 'NONE',  ( 47.43856463449118621, 79.87977050742732388, 34.21067981925357060 ) ) ;
#10776=VERTEX_POINT ( 'NONE', #13053 ) ;
#10777=VERTEX_POINT ( 'NONE', #19779 ) ;
#10780=CARTESIAN_POINT ( 'NONE',  ( 43.01140435219951286, 124.4604996726487371, 39.46799094044489209 ) ) ;
#10781=CARTESIAN_POINT ( 'NONE',  ( 41.64333658814960870, 81.71518717409399812, 38.42115945441014446 ) ) ;
#10786=CARTESIAN_POINT ( 'NONE',  ( 38.01140435219952707, 80.63445800887257064, 32.58608133808903773 ) ) ;
#10788=CARTESIAN_POINT ( 'NONE',  ( 41.46631938032478359, 158.1844580088726104, 29.45539723777780239 ) ) ;
#10789=CARTESIAN_POINT ( 'NONE',  ( 39.42975644700377558, 141.6797705074273210, 36.81289934271958941 ) ) ;
#10791=CARTESIAN_POINT ( 'NONE',  ( 40.27526882409969744, 131.6651871740939725, 30.44471234641812174 ) ) ;
#10792=AXIS2_PLACEMENT_3D ( 'NONE', #11561, #104, #5590 ) ;
#10793=CARTESIAN_POINT ( 'NONE',  ( 41.46631938032478359, 70.31049967264874567, 38.96596240072933170 ) ) ;
#10796=VECTOR ( 'NONE', #20350, 1000.000000000000000 ) ;
#10797=CARTESIAN_POINT ( 'NONE',  ( 46.10157429594899270, 91.73445800887257917, 29.95742577749336988 ) ) ;
#10799=CARTESIAN_POINT ( 'NONE',  ( 43.01140435219951996, 10.71049967264875491, 34.21067981925357060 ) ) ;
#10800=CARTESIAN_POINT ( 'NONE',  ( 45.74753988029933538, 113.0651871740939924, 30.44471234641811819 ) ) ;
#10801=VERTEX_POINT ( 'NONE', #4672 ) ;
#10805=CARTESIAN_POINT ( 'NONE',  ( 43.01140435219951286, 89.03445800887256212, 28.95336869806222779 ) ) ;
#10807=CARTESIAN_POINT ( 'NONE',  ( 43.01140435219951286, 148.1297705074272812, 38.86567161673127657 ) ) ;
#10808=CARTESIAN_POINT ( 'NONE',  ( 44.55648932407425633, 148.6104996726487570, 38.96596240072933170 ) ) ;
#10809=CARTESIAN_POINT ( 'NONE',  ( 44.37947211624943833, 109.0151871740940095, 38.42115945441014446 ) ) ;
#10811=CARTESIAN_POINT ( 'NONE',  ( 38.01140435219951996, 75.56049967264871725, 32.58608133808903773 ) ) ;
#10813=CARTESIAN_POINT ( 'NONE',  ( 46.10157429594899270, 61.73445800887256496, 29.95742577749336988 ) ) ;
#10814=CARTESIAN_POINT ( 'NONE',  ( 43.01140435219951286, 85.46049967264872294, 39.21067981925356349 ) ) ;
#10818=CARTESIAN_POINT ( 'NONE',  ( 45.74753988029933538, 67.16518717409401518, 37.97664729208901946 ) ) ;
#10819=CARTESIAN_POINT ( 'NONE',  ( 47.05648932407426344, 104.5104996726487485, 31.27175355779120025 ) ) ;
#10828=CARTESIAN_POINT ( 'NONE',  ( 47.43856463449117200, 142.4651871740940123, 35.64915139335016647 ) ) ;
#10829=CARTESIAN_POINT ( 'NONE',  ( 39.42975644700377558, 155.8151871740940067, 31.60846029578754468 ) ) ;
#10831=CARTESIAN_POINT ( 'NONE',  ( 46.59305225739526435, 107.1797705074273352, 31.60846029578754468 ) ) ;
#10836=CARTESIAN_POINT ( 'NONE',  ( 48.01140435219951996, 115.1344580088725849, 35.83527830041810347 ) ) ;
#10838=CARTESIAN_POINT ( 'NONE',  ( 43.01140435219951286, 76.46049967264873715, 39.21067981925356349 ) ) ;
#10839=CARTESIAN_POINT ( 'NONE',  ( 41.64333658814960870, 81.97977050742731819, 38.42115945441014446 ) ) ;
#10840=CARTESIAN_POINT ( 'NONE',  ( 39.42975644700377558, 138.4151871740940010, 36.81289934271958941 ) ) ;
#10842=CARTESIAN_POINT ( 'NONE',  ( 38.01140435219951996, 99.56049967264873146, 32.58608133808903773 ) ) ;
#10851=CARTESIAN_POINT ( 'NONE',  ( 39.42975644700377558, 81.07977050742731251, 31.60846029578754468 ) ) ;
#10853=CARTESIAN_POINT ( 'NONE',  ( 40.27526882409969744, 65.66518717409398675, 30.44471234641812174 ) ) ;
#10857=CARTESIAN_POINT ( 'NONE',  ( 38.01140435219952707, 68.78445800887257633, 34.21067981925357060 ) ) ;
#10859=CARTESIAN_POINT ( 'NONE',  ( 38.58424406990785371, 135.5297705074273154, 35.64915139335015937 ) ) ;
#10864=CARTESIAN_POINT ( 'NONE',  ( 46.59305225739526435, 128.1797705074273210, 31.60846029578754468 ) ) ;
#10865=CARTESIAN_POINT ( 'NONE',  ( 43.01140435219954838, 110.9604996726487371, 29.21067981925356705 ) ) ;
#10868=CARTESIAN_POINT ( 'NONE',  ( 44.37947211624943833, 101.2151871740939981, 30.00020018409699318 ) ) ;
#10875=CARTESIAN_POINT ( 'NONE',  ( 46.10157429594899270, 129.8344580088725877, 38.46393386101376421 ) ) ;
#10876=CARTESIAN_POINT ( 'NONE',  ( 39.42975644700377558, 111.6797705074273210, 36.81289934271958941 ) ) ;
#10879=CARTESIAN_POINT ( 'NONE',  ( 45.74753988029934249, 94.16518717409400097, 37.97664729208901235 ) ) ;
#10881=ORIENTED_EDGE ( 'NONE', *, *, #12868, .F. ) ;
#10882=CARTESIAN_POINT ( 'NONE',  ( 43.01140435219951286, 74.96049967264873715, 29.21067981925356705 ) ) ;
#10886=CARTESIAN_POINT ( 'NONE',  ( 46.59305225739526435, 77.17977050742732104, 31.60846029578754468 ) ) ;
#10889=CARTESIAN_POINT ( 'NONE',  ( 47.43856463449117200, 151.7297705074273324, 35.64915139335016647 ) ) ;
#10891=CARTESIAN_POINT ( 'NONE',  ( 48.01140435219951996, 122.2104996726487371, 34.21067981925357060 ) ) ;
#10892=CARTESIAN_POINT ( 'NONE',  ( 45.74753988029933538, 74.06518717409399244, 30.44471234641811819 ) ) ;
#10898=CARTESIAN_POINT ( 'NONE',  ( 48.01140435219951996, 157.2844580088725763, 34.21067981925357060 ) ) ;
#10899=CARTESIAN_POINT ( 'NONE',  ( 43.01140435219951286, 145.1297705074273097, 38.86567161673127657 ) ) ;
#10901=CARTESIAN_POINT ( 'NONE',  ( 41.64333658814960870, 128.5151871740939953, 30.00020018409699318 ) ) ;
#10902=CARTESIAN_POINT ( 'NONE',  ( 43.80332655382220253, 136.5373810949690210, 39.21067981925355639 ) ) ;
#10908=CARTESIAN_POINT ( 'NONE',  ( 41.46631938032478359, 121.3104996726487457, 38.96596240072933170 ) ) ;
#10909=CARTESIAN_POINT ( 'NONE',  ( 40.27526882409969033, 102.5651871740939782, 37.97664729208901946 ) ) ;
#10912=VERTEX_POINT ( 'NONE', #8321 ) ;
#10913=CARTESIAN_POINT ( 'NONE',  ( 44.55648932407425633, 93.68445800887258201, 38.96596240072933170 ) ) ;
#10914=CARTESIAN_POINT ( 'NONE',  ( 48.01140435219951996, 149.3604996726487286, 32.58608133808903773 ) ) ;
#10915=CARTESIAN_POINT ( 'NONE',  ( 47.43856463449118621, 109.6151871740940038, 34.21067981925357060 ) ) ;
#10917=CARTESIAN_POINT ( 'NONE',  ( 45.51148226160370314, 59.71123016864975597, 29.88059778228138441 ) ) ;
#10919=CARTESIAN_POINT ( 'NONE',  ( 43.01140435219951286, 95.03445800887257633, 29.21067981925356705 ) ) ;
#10921=CARTESIAN_POINT ( 'NONE',  ( 43.01140435219951996, 10.71049967264875491, 29.21067981925357060 ) ) ;
#10922=CARTESIAN_POINT ( 'NONE',  ( 43.01140435219951286, 66.86518717409397539, 38.86567161673127657 ) ) ;
#10924=CARTESIAN_POINT ( 'NONE',  ( 41.46631938032478359, 63.11049967264874283, 29.45539723777780239 ) ) ;
#10929=FILL_AREA_STYLE ('',( #4201 ) ) ;
#10930=CARTESIAN_POINT ( 'NONE',  ( 38.58424406990786082, 132.1151871740940180, 34.21067981925357060 ) ) ;
#10932=CARTESIAN_POINT ( 'NONE',  ( 45.74753988029934249, 100.4297705074273210, 37.97664729208901235 ) ) ;
#10936=EDGE_CURVE ( 'NONE', #1013, #12255, #17110, .T. ) ;
#10938=CARTESIAN_POINT ( 'NONE',  ( 44.55648932407425633, 112.8844580088725849, 29.45539723777780239 ) ) ;
#10939=CARTESIAN_POINT ( 'NONE',  ( 43.01140435219951286, 74.96049967264873715, 29.21067981925356705 ) ) ;
#10940=CARTESIAN_POINT ( 'NONE',  ( 40.27526882409969033, 132.5651871740940067, 37.97664729208901946 ) ) ;
#10942=CARTESIAN_POINT ( 'NONE',  ( 46.10157429594899270, 89.66049967264873999, 29.95742577749337343 ) ) ;
#10947=CARTESIAN_POINT ( 'NONE',  ( 47.05648932407426344, 157.9104996726487400, 37.14960608071593384 ) ) ;
#10948=CARTESIAN_POINT ( 'NONE',  ( 41.46631938032478359, 144.3844580088725991, 38.96596240072933170 ) ) ;
#10950=ORIENTED_EDGE ( 'NONE', *, *, #19450, .F. ) ;
#10951=CARTESIAN_POINT ( 'NONE',  ( 40.27526882409969033, 71.92977050742729261, 30.44471234641811819 ) ) ;
#10956=CARTESIAN_POINT ( 'NONE',  ( 42.21948215057684450, 118.3836182503284675, 39.21067981925355639 ) ) ;
#10958=CARTESIAN_POINT ( 'NONE',  ( 41.64333658814960870, 135.9797705074273324, 38.42115945441014446 ) ) ;
#10959=VERTEX_POINT ( 'NONE', #10705 ) ;
#10962=CARTESIAN_POINT ( 'NONE',  ( 38.58424406990784661, 123.2297705074273040, 32.77220824515698183 ) ) ;
#10967=EDGE_CURVE ( 'NONE', #19975, #4691, #6676, .T. ) ;
#10970=SHAPE_DEFINITION_REPRESENTATION ( #21701, #6206 ) ;
#10971=CARTESIAN_POINT ( 'NONE',  ( 44.55648932407425633, 132.6844580088725820, 38.96596240072933170 ) ) ;
#10972=CARTESIAN_POINT ( 'NONE',  ( 40.27526882409969033, 113.9297705074273068, 30.44471234641811819 ) ) ;
#10975=CARTESIAN_POINT ( 'NONE',  ( 44.37947211624943833, 95.21518717409399812, 30.00020018409699318 ) ) ;
#10976=CARTESIAN_POINT ( 'NONE',  ( 39.92123440845005433, 90.26049967264873430, 29.95742577749336988 ) ) ;
#10977=ORIENTED_EDGE ( 'NONE', *, *, #1438, .T. ) ;
#10978=CARTESIAN_POINT ( 'NONE',  ( 38.01140435219952707, 87.71049967264873715, 34.21067981925357060 ) ) ;
#10984=CARTESIAN_POINT ( 'NONE',  ( 46.59305225739526435, 74.17977050742732104, 31.60846029578754468 ) ) ;
#10985=VERTEX_POINT ( 'NONE', #5621 ) ;
#10987=CARTESIAN_POINT ( 'NONE',  ( 45.74753988029933538, 158.3297705074273267, 30.44471234641811819 ) ) ;
#10990=CARTESIAN_POINT ( 'NONE',  ( 38.96631938032478359, 123.4104996726487542, 31.27175355779120025 ) ) ;
#10991=CARTESIAN_POINT ( 'NONE',  ( 43.01140435219951286, 81.86518717409398960, 38.86567161673127657 ) ) ;
#10998=CARTESIAN_POINT ( 'NONE',  ( 47.43856463449117200, 146.0297705074272869, 32.77220824515698183 ) ) ;
#11000=CARTESIAN_POINT ( 'NONE',  ( 38.58424406990785371, 126.2651871740940237, 35.64915139335015937 ) ) ;
#11001=CARTESIAN_POINT ( 'NONE',  ( 38.01140435219952707, 69.86049967264871441, 35.83527830041809636 ) ) ;
#11004=DIRECTION ( 'NONE',  ( 0.000000000000000000, 1.000000000000000000, 0.000000000000000000 ) ) ;
#11006=CARTESIAN_POINT ( 'NONE',  ( 39.42975644700377558, 105.4151871740940152, 36.81289934271958941 ) ) ;
#11011=CARTESIAN_POINT ( 'NONE',  ( 38.96631938032478359, 92.48445800887257917, 31.27175355779120025 ) ) ;
#11013=CARTESIAN_POINT ( 'NONE',  ( 48.01140435219951996, 152.0604996726487457, 35.83527830041810347 ) ) ;
#11014=CARTESIAN_POINT ( 'NONE',  ( 38.58424406990784661, 107.9651871740939839, 32.77220824515698183 ) ) ;
#11016=CARTESIAN_POINT ( 'NONE',  ( 41.46631938032478359, 67.31049967264873146, 38.96596240072933170 ) ) ;
#11018=CARTESIAN_POINT ( 'NONE',  ( 46.10157429594899270, 60.83445800887256638, 38.46393386101375711 ) ) ;
#11019=CYLINDRICAL_SURFACE ( 'NONE', #5554, 4.999999999999997335 ) ;
#11023=CARTESIAN_POINT ( 'NONE',  ( 43.01140435219951996, 10.71049967264875491, 29.21067981925357060 ) ) ;
#11030=CARTESIAN_POINT ( 'NONE',  ( 44.37947211624943833, 136.0151871740939953, 38.42115945441014446 ) ) ;
#11031=CARTESIAN_POINT ( 'NONE',  ( 38.58424406990785371, 93.52977050742731535, 35.64915139335015937 ) ) ;
#11035=EDGE_LOOP ( 'NONE', ( #13073, #11354, #5547, #9939 ) ) ;
#11036=CARTESIAN_POINT ( 'NONE',  ( 38.01140435219951996, 113.9344580088725820, 35.83527830041810347 ) ) ;
#11037=DIRECTION ( 'NONE',  ( 0.000000000000000000, 1.000000000000000000, 0.000000000000000000 ) ) ;
#11038=CARTESIAN_POINT ( 'NONE',  ( 40.27526882409969033, 72.82977050742732672, 37.97664729208901946 ) ) ;
#11039=CARTESIAN_POINT ( 'NONE',  ( 39.42975644700377558, 134.8151871740940067, 31.60846029578754468 ) ) ;
#11040=CARTESIAN_POINT ( 'NONE',  ( 38.01140435219952707, 90.71049967264873715, 34.21067981925357060 ) ) ;
#11046=CARTESIAN_POINT ( 'NONE',  ( 43.01140435219951996, 10.71049967264875491, 39.21067981925356349 ) ) ;
#11049=CARTESIAN_POINT ( 'NONE',  ( 43.01140435219951286, 73.12977050742729546, 38.86567161673127657 ) ) ;
#11056=CARTESIAN_POINT ( 'NONE',  ( 41.64333658814960870, 126.9797705074273182, 38.42115945441014446 ) ) ;
#11058=CARTESIAN_POINT ( 'NONE',  ( 43.80332655382220253, 87.61133943119283174, 39.21067981925355639 ) ) ;
#11059=( BOUNDED_CURVE ( )  B_SPLINE_CURVE ( 2, ( #823, #17568, #9316, #501, #15594, #16018, #17458, #15806, #11065, #930, #14372, #7675, #12508 ),
 .UNSPECIFIED., .F., .F. ) 
 B_SPLINE_CURVE_WITH_KNOTS ( ( 3, 2, 2, 2, 2, 2, 3 ),
 ( 0.5808823529411765163, 0.5823529411764706287, 0.5852941176470588536, 0.5882352941176470784, 0.5911764705882353033, 0.5941176470588235281, 0.5955882352941176405 ),
 .UNSPECIFIED. ) 
 CURVE ( )  GEOMETRIC_REPRESENTATION_ITEM ( )  RATIONAL_B_SPLINE_CURVE ( ( 0.9755282581475768211, 0.9755282581475768211, 1.000000000000000000, 0.9510565162951535312, 1.000000000000000000, 0.9510565162951535312, 1.000000000000000000, 0.9510565162951535312, 1.000000000000000000, 0.9510565162951535312, 1.000000000000000000, 0.9755282581475768211, 0.9755282581475768211 ) ) 
 REPRESENTATION_ITEM ( '' )  );
#11061=CARTESIAN_POINT ( 'NONE',  ( 46.59305225739526435, 122.1797705074273210, 31.60846029578754468 ) ) ;
#11062=CARTESIAN_POINT ( 'NONE',  ( 44.55648932407425633, 139.8844580088725991, 29.45539723777780239 ) ) ;
#11063=CARTESIAN_POINT ( 'NONE',  ( 38.01140435219951996, 59.93445800887258912, 35.83527830041810347 ) ) ;
#11065=CARTESIAN_POINT ( 'NONE',  ( 38.96631938032478359, 99.41049967264873999, 31.27175355779120025 ) ) ;
#11066=CARTESIAN_POINT ( 'NONE',  ( 42.21948215057684450, 83.11133943119283174, 29.21067981925356705 ) ) ;
#11070=CARTESIAN_POINT ( 'NONE',  ( 47.05648932407426344, 125.5104996726487343, 31.27175355779120025 ) ) ;
#11073=CARTESIAN_POINT ( 'NONE',  ( 41.46631938032478359, 135.3844580088725706, 38.96596240072933170 ) ) ;
#11074=CARTESIAN_POINT ( 'NONE',  ( 38.58424406990786082, 105.3797705074273239, 34.21067981925357060 ) ) ;
#11077=CARTESIAN_POINT ( 'NONE',  ( 38.58424406990786082, 96.11518717409400381, 34.21067981925357060 ) ) ;
#11079=VERTEX_POINT ( 'NONE', #19078 ) ;
#11080=DIRECTION ( 'NONE',  ( 0.000000000000000000, 0.000000000000000000, 1.000000000000000000 ) ) ;
#11085=CARTESIAN_POINT ( 'NONE',  ( 38.58424406990786082, 75.37977050742732388, 34.21067981925357060 ) ) ;
#11086=ORIENTED_EDGE ( 'NONE', *, *, #4103, .T. ) ;
#11089=CARTESIAN_POINT ( 'NONE',  ( 44.37947211624943833, 151.2797705074273438, 38.42115945441014446 ) ) ;
#11092=AXIS2_PLACEMENT_3D ( 'NONE', #20802, #4046, #17481 ) ;
#11093=CARTESIAN_POINT ( 'NONE',  ( 38.01140435219951996, 123.8604996726487570, 35.83527830041810347 ) ) ;
#11094=CARTESIAN_POINT ( 'NONE',  ( 39.42975644700377558, 74.81518717409399244, 31.60846029578754468 ) ) ;
#11102=CARTESIAN_POINT ( 'NONE',  ( 38.58424406990786082, 129.3797705074273381, 34.21067981925357060 ) ) ;
#11104=CARTESIAN_POINT ( 'NONE',  ( 47.43856463449118621, 121.6151871740940038, 34.21067981925357060 ) ) ;
#11105=CARTESIAN_POINT ( 'NONE',  ( 43.01140435219951286, 136.4604996726487514, 39.21067981925356349 ) ) ;
#11112=CARTESIAN_POINT ( 'NONE',  ( 44.55648932407425633, 82.61049967264874283, 38.96596240072933170 ) ) ;
#11113=CARTESIAN_POINT ( 'NONE',  ( 45.74753988029933538, 110.0651871740939782, 30.44471234641811819 ) ) ;
#11116=CARTESIAN_POINT ( 'NONE',  ( 43.01140435219951286, 86.96049967264872294, 29.21067981925356705 ) ) ;
#11117=ORIENTED_EDGE ( 'NONE', *, *, #618, .F. ) ;
#11118=CARTESIAN_POINT ( 'NONE',  ( 38.01140435219952707, 92.78445800887257633, 34.21067981925357060 ) ) ;
#11119=FACE_OUTER_BOUND ( 'NONE', #19633, .T. ) ;
#11120=CARTESIAN_POINT ( 'NONE',  ( 41.46631938032478359, 153.1104996726487570, 29.45539723777780239 ) ) ;
#11121=CARTESIAN_POINT ( 'NONE',  ( 38.58424406990786082, 111.1151871740940038, 34.21067981925357060 ) ) ;
#11123=CARTESIAN_POINT ( 'NONE',  ( 38.96631938032478359, 61.01049967264874141, 37.14960608071593384 ) ) ;
#11128=CARTESIAN_POINT ( 'NONE',  ( 47.05648932407426344, 146.5104996726487627, 31.27175355779120025 ) ) ;
#11130=CARTESIAN_POINT ( 'NONE',  ( 38.58424406990784661, 69.26518717409398107, 35.64915139335016647 ) ) ;
#11135=ORIENTED_EDGE ( 'NONE', *, *, #693, .T. ) ;
#11138=( NAMED_UNIT ( * ) PLANE_ANGLE_UNIT ( ) SI_UNIT ( $, .RADIAN. ) );
#11139=CARTESIAN_POINT ( 'NONE',  ( 39.42975644700377558, 134.8151871740940067, 31.60846029578754468 ) ) ;
#11142=ORIENTED_EDGE ( 'NONE', *, *, #11781, .T. ) ;
#11145=ORIENTED_EDGE ( 'NONE', *, *, #16232, .T. ) ;
#11146=CARTESIAN_POINT ( 'NONE',  ( 38.01140435219951996, 116.6344580088725564, 32.58608133808903773 ) ) ;
#11148=CARTESIAN_POINT ( 'NONE',  ( 38.58424406990786082, 72.37977050742732388, 34.21067981925357060 ) ) ;
#11149=CARTESIAN_POINT ( 'NONE',  ( 46.59305225739526435, 139.3151871740940067, 36.81289934271958941 ) ) ;
#11150=CARTESIAN_POINT ( 'NONE',  ( 48.01140435219951996, 95.21049967264875136, 34.21067981925357060 ) ) ;
#11154=VECTOR ( 'NONE', #19549, 1000.000000000000000 ) ;
#11159=CARTESIAN_POINT ( 'NONE',  ( 38.58424406990786082, 75.37977050742732388, 34.21067981925357060 ) ) ;
#11164=CARTESIAN_POINT ( 'NONE',  ( 43.01140435219957681, 97.46049967264875136, 39.21067981925356349 ) ) ;
#11165=CARTESIAN_POINT ( 'NONE',  ( 44.55648932407425633, 124.8844580088725706, 29.45539723777780239 ) ) ;
#11166=CARTESIAN_POINT ( 'NONE',  ( 44.37947211624943833, 125.4797705074273182, 30.00020018409699318 ) ) ;
#11169=EDGE_LOOP ( 'NONE', ( #7822, #20943, #17199, #8860 ) ) ;
#11170=CARTESIAN_POINT ( 'NONE',  ( 44.55648932407425633, 88.88445800887258486, 29.45539723777780239 ) ) ;
#11172=CARTESIAN_POINT ( 'NONE',  ( 44.37947211624943833, 124.2797705074273154, 38.42115945441014446 ) ) ;
#11174=CARTESIAN_POINT ( 'NONE',  ( 43.01140435219957681, 68.03445800887257633, 29.21067981925356705 ) ) ;
#11175=CARTESIAN_POINT ( 'NONE',  ( 41.46631938032478359, 68.18445800887256780, 29.45539723777780239 ) ) ;
#11177=CARTESIAN_POINT ( 'NONE',  ( 38.01140435219952707, 101.9344580088725678, 35.83527830041809636 ) ) ;
#11179=CARTESIAN_POINT ( 'NONE',  ( 43.01140435219951286, 60.53445800887258343, 39.21067981925356349 ) ) ;
#11180=CARTESIAN_POINT ( 'NONE',  ( 44.55648932407425633, 130.6104996726487286, 38.96596240072933170 ) ) ;
#11183=CARTESIAN_POINT ( 'NONE',  ( 46.10157429594899270, 123.8344580088725735, 38.46393386101376421 ) ) ;
#11184=CARTESIAN_POINT ( 'NONE',  ( 46.59305225739526435, 100.5797705074273267, 36.81289934271958941 ) ) ;
#11187=CARTESIAN_POINT ( 'NONE',  ( 45.74753988029934249, 101.0651871740939924, 30.44471234641812174 ) ) ;
#11189=VERTEX_POINT ( 'NONE', #7727 ) ;
#11190=CARTESIAN_POINT ( 'NONE',  ( 46.10157429594899270, 128.6604996726487400, 29.95742577749336988 ) ) ;
#11193=( BOUNDED_CURVE ( )  B_SPLINE_CURVE ( 2, ( #12413, #2490, #9011, #17583, #5575, #15722, #19143, #16032, #4252, #12633, #7361, #5793, #19354 ),
 .UNSPECIFIED., .F., .T. ) 
 B_SPLINE_CURVE_WITH_KNOTS ( ( 3, 2, 2, 2, 2, 2, 3 ),
 ( 0.8014705882352941568, 0.8029411764705882693, 0.8058823529411764941, 0.8088235294117647189, 0.8117647058823529438, 0.8147058823529411686, 0.8161764705882352811 ),
 .UNSPECIFIED. ) 
 CURVE ( )  GEOMETRIC_REPRESENTATION_ITEM ( )  RATIONAL_B_SPLINE_CURVE ( ( 0.9755282581475768211, 0.9755282581475768211, 1.000000000000000000, 0.9510565162951535312, 1.000000000000000000, 0.9510565162951535312, 1.000000000000000000, 0.9510565162951535312, 1.000000000000000000, 0.9510565162951535312, 1.000000000000000000, 0.9755282581475768211, 0.9755282581475768211 ) ) 
 REPRESENTATION_ITEM ( '' )  );
#11195=CARTESIAN_POINT ( 'NONE',  ( 40.27526882409969744, 65.92977050742732104, 30.44471234641812174 ) ) ;
#11198=CARTESIAN_POINT ( 'NONE',  ( 47.43856463449117200, 152.0297705074273438, 32.77220824515698183 ) ) ;
#11200=CARTESIAN_POINT ( 'NONE',  ( 44.55648932407425633, 121.6104996726487570, 38.96596240072933170 ) ) ;
#11201=CARTESIAN_POINT ( 'NONE',  ( 46.59305225739526435, 67.91518717409400097, 31.60846029578754468 ) ) ;
#11204=CARTESIAN_POINT ( 'NONE',  ( 38.01140435219952707, 155.9344580088725820, 35.83527830041809636 ) ) ;
#11207=CARTESIAN_POINT ( 'NONE',  ( 41.64333658814960870, 135.9797705074273324, 38.42115945441014446 ) ) ;
#11208=EDGE_CURVE ( 'NONE', #11408, #14439, #9164, .T. ) ;
#11210=CARTESIAN_POINT ( 'NONE',  ( 43.01140435219951286, 128.3651871740940180, 29.55568802177586107 ) ) ;
#11213=LINE ( 'NONE', #13093, #4490 ) ;
#11215=CARTESIAN_POINT ( 'NONE',  ( 43.80332655382220253, 82.53738109496899256, 39.21067981925355639 ) ) ;
#11216=CARTESIAN_POINT ( 'NONE',  ( 45.74753988029933538, 104.0651871740940067, 30.44471234641811819 ) ) ;
#11218=CARTESIAN_POINT ( 'NONE',  ( 43.80332655382220253, 86.88361825032846752, 29.21067981925356705 ) ) ;
#11220=CARTESIAN_POINT ( 'NONE',  ( 38.01140435219951996, 86.63445800887255643, 32.58608133808903773 ) ) ;
#11222=CARTESIAN_POINT ( 'NONE',  ( 38.96631938032478359, 148.0104996726487627, 37.14960608071593384 ) ) ;
#11223=CARTESIAN_POINT ( 'NONE',  ( 46.59305225739526435, 109.9151871740940010, 31.60846029578754468 ) ) ;
#11226=CARTESIAN_POINT ( 'NONE',  ( 44.55648932407425633, 62.81049967264873146, 29.45539723777780239 ) ) ;
#11230=CARTESIAN_POINT ( 'NONE',  ( 43.01140435219951286, 80.03445800887257633, 29.21067981925356705 ) ) ;
#11232=CARTESIAN_POINT ( 'NONE',  ( 39.42975644700377558, 59.81518717409399244, 31.60846029578754468 ) ) ;
#11235=CARTESIAN_POINT ( 'NONE',  ( 46.59305225739526435, 151.3151871740940067, 36.81289934271958941 ) ) ;
#11236=CARTESIAN_POINT ( 'NONE',  ( 43.01140435219951996, 10.71049967264875491, 34.21067981925357060 ) ) ;
#11239=ORIENTED_EDGE ( 'NONE', *, *, #5195, .T. ) ;
#11240=CARTESIAN_POINT ( 'NONE',  ( 47.43856463449117911, 70.76518717409399528, 32.77220824515697473 ) ) ;
#11243=CARTESIAN_POINT ( 'NONE',  ( 38.58424406990786082, 159.1151871740940180, 34.21067981925357060 ) ) ;
#11244=CARTESIAN_POINT ( 'NONE',  ( 45.74753988029933538, 137.0651871740940067, 30.44471234641811819 ) ) ;
#11246=ORIENTED_EDGE ( 'NONE', *, *, #10032, .T. ) ;
#11251=CARTESIAN_POINT ( 'NONE',  ( 39.42975644700377558, 78.07977050742731251, 31.60846029578754468 ) ) ;
#11252=CARTESIAN_POINT ( 'NONE',  ( 41.64333658814960870, 135.7151871740940123, 38.42115945441014446 ) ) ;
#11253=CARTESIAN_POINT ( 'NONE',  ( 38.96631938032478359, 90.41049967264875420, 31.27175355779120025 ) ) ;
#11257=CARTESIAN_POINT ( 'NONE',  ( 38.58424406990786082, 87.11518717409400381, 34.21067981925357060 ) ) ;
#11260=CARTESIAN_POINT ( 'NONE',  ( 43.80332655382220253, 61.53738109496899966, 39.21067981925355639 ) ) ;
#11264=CARTESIAN_POINT ( 'NONE',  ( 40.27526882409969033, 74.92977050742732104, 30.44471234641811819 ) ) ;
#11270=CARTESIAN_POINT ( 'NONE',  ( 41.46631938032478359, 104.1844580088725820, 29.45539723777780239 ) ) ;
#11271=CARTESIAN_POINT ( 'NONE',  ( 46.59305225739526435, 122.1797705074273210, 31.60846029578754468 ) ) ;
#11272=ORIENTED_EDGE ( 'NONE', *, *, #14155, .T. ) ;
#11275=CARTESIAN_POINT ( 'NONE',  ( 41.64333658814960870, 126.9797705074273182, 38.42115945441014446 ) ) ;
#11279=CARTESIAN_POINT ( 'NONE',  ( 45.74753988029933538, 89.32977050742732672, 30.44471234641811819 ) ) ;
#11280=CARTESIAN_POINT ( 'NONE',  ( 48.01140435219951996, 64.43445800887258201, 32.58608133808903773 ) ) ;
#11282=CARTESIAN_POINT ( 'NONE',  ( 38.96631938032478359, 102.0844580088725877, 37.14960608071593384 ) ) ;
#11286=CARTESIAN_POINT ( 'NONE',  ( 38.96631938032478359, 103.0104996726487485, 37.14960608071593384 ) ) ;
#11289=CARTESIAN_POINT ( 'NONE',  ( 44.55648932407425633, 120.6844580088725962, 38.96596240072933170 ) ) ;
#11290=CARTESIAN_POINT ( 'NONE',  ( 41.64333658814960870, 107.7797705074273154, 30.00020018409699318 ) ) ;
#11292=CARTESIAN_POINT ( 'NONE',  ( 43.01140435219951286, 101.3651871740940038, 29.55568802177586107 ) ) ;
#11294=ORIENTED_EDGE ( 'NONE', *, *, #4303, .F. ) ;
#11298=CARTESIAN_POINT ( 'NONE',  ( 41.64333658814960870, 69.97977050742731819, 38.42115945441014446 ) ) ;
#11299=VERTEX_POINT ( 'NONE', #6271 ) ;
#11301=CARTESIAN_POINT ( 'NONE',  ( 43.01140435219951286, 158.6297705074273381, 29.55568802177586463 ) ) ;
#11303=CARTESIAN_POINT ( 'NONE',  ( 38.01140435219951996, 114.5604996726487457, 32.58608133808903773 ) ) ;
#11304=CARTESIAN_POINT ( 'NONE',  ( 43.01140435219951286, 69.86518717409400381, 38.86567161673127657 ) ) ;
#11311=CARTESIAN_POINT ( 'NONE',  ( 38.01140435219951996, 155.9344580088726104, 35.83527830041810347 ) ) ;
#11312=CARTESIAN_POINT ( 'NONE',  ( 47.43856463449118621, 136.8797705074273381, 34.21067981925357060 ) ) ;
#11313=( BOUNDED_CURVE ( )  B_SPLINE_CURVE ( 2, ( #12724, #1483, #21437, #4340, #21549, #6440, #11390, #1368, #7995, #8100, #16564, #11066, #17780 ),
 .UNSPECIFIED., .F., .F. ) 
 B_SPLINE_CURVE_WITH_KNOTS ( ( 3, 2, 2, 2, 2, 2, 3 ),
 ( 0.7279411764705882026, 0.7294117647058823151, 0.7323529411764705399, 0.7352941176470588758, 0.7382352941176471006, 0.7411764705882353255, 0.7426470588235294379 ),
 .UNSPECIFIED. ) 
 CURVE ( )  GEOMETRIC_REPRESENTATION_ITEM ( )  RATIONAL_B_SPLINE_CURVE ( ( 0.9755282581475768211, 0.9755282581475768211, 1.000000000000000000, 0.9510565162951535312, 1.000000000000000000, 0.9510565162951535312, 1.000000000000000000, 0.9510565162951535312, 1.000000000000000000, 0.9510565162951535312, 1.000000000000000000, 0.9755282581475768211, 0.9755282581475768211 ) ) 
 REPRESENTATION_ITEM ( '' )  );
#11315=CARTESIAN_POINT ( 'NONE',  ( 40.27526882409969744, 125.6651871740939868, 30.44471234641812174 ) ) ;
#11316=CARTESIAN_POINT ( 'NONE',  ( 43.01140435219951996, 10.71049967264875491, 29.21067981925357060 ) ) ;
#11318=AXIS2_PLACEMENT_3D ( 'NONE', #7013, #17231, #15386 ) ;
#11319=CARTESIAN_POINT ( 'NONE',  ( 44.55648932407425633, 140.8104996726487457, 29.45539723777780239 ) ) ;
#11325=ORIENTED_EDGE ( 'NONE', *, *, #5076, .T. ) ;
#11326=CARTESIAN_POINT ( 'NONE',  ( 48.01140435219951996, 79.28445800887259054, 34.21067981925357060 ) ) ;
#11330=CARTESIAN_POINT ( 'NONE',  ( 43.01140435219951286, 142.4604996726486945, 39.46799094044489209 ) ) ;
#11331=CARTESIAN_POINT ( 'NONE',  ( 41.64333658814960870, 101.5151871740939953, 30.00020018409699318 ) ) ;
#11335=CARTESIAN_POINT ( 'NONE',  ( 41.46631938032478359, 60.11049967264874283, 29.45539723777780239 ) ) ;
#11339=CARTESIAN_POINT ( 'NONE',  ( 47.05648932407426344, 78.98445800887257917, 37.14960608071593384 ) ) ;
#11340=CARTESIAN_POINT ( 'NONE',  ( 38.01140435219952707, 78.86049967264872862, 35.83527830041809636 ) ) ;
#11341=CARTESIAN_POINT ( 'NONE',  ( 47.43856463449117200, 61.46518717409399102, 35.64915139335016647 ) ) ;
#11343=CARTESIAN_POINT ( 'NONE',  ( 38.58424406990785371, 153.2651871740940237, 35.64915139335015937 ) ) ;
#11346=EDGE_LOOP ( 'NONE', ( #1133, #4742, #12190, #1035 ) ) ;
#11347=CARTESIAN_POINT ( 'NONE',  ( 44.37947211624943833, 73.01518717409399528, 38.42115945441014446 ) ) ;
#11351=CARTESIAN_POINT ( 'NONE',  ( 39.42975644700377558, 135.4151871740940010, 36.81289934271958941 ) ) ;
#11354=ORIENTED_EDGE ( 'NONE', *, *, #5830, .T. ) ;
#11355=ORIENTED_EDGE ( 'NONE', *, *, #3754, .F. ) ;
#11358=VERTEX_POINT ( 'NONE', #19953 ) ;
#11360=CARTESIAN_POINT ( 'NONE',  ( 48.01140435219951996, 109.2844580088725905, 34.21067981925357060 ) ) ;
#11362=CARTESIAN_POINT ( 'NONE',  ( 38.58424406990784661, 69.22977050742731819, 32.77220824515698183 ) ) ;
#11363=CARTESIAN_POINT ( 'NONE',  ( 46.59305225739526435, 124.3151871740940067, 36.81289934271958941 ) ) ;
#11366=CARTESIAN_POINT ( 'NONE',  ( 44.55648932407425633, 92.81049967264874567, 29.45539723777780239 ) ) ;
#11370=CARTESIAN_POINT ( 'NONE',  ( 47.43856463449117200, 88.46518717409399812, 35.64915139335016647 ) ) ;
#11374=CARTESIAN_POINT ( 'NONE',  ( 38.58424406990784661, 75.52977050742732956, 35.64915139335016647 ) ) ;
#11382=CARTESIAN_POINT ( 'NONE',  ( 39.42975644700377558, 126.0797705074273267, 31.60846029578754468 ) ) ;
#11383=ORIENTED_EDGE ( 'NONE', *, *, #14444, .F. ) ;
#11385=DIRECTION ( 'NONE',  ( 0.000000000000000000, 0.000000000000000000, -1.000000000000000000 ) ) ;
#11388=CARTESIAN_POINT ( 'NONE',  ( 46.59305225739526435, 154.9151871740940010, 31.60846029578754468 ) ) ;
#11390=CARTESIAN_POINT ( 'NONE',  ( 38.01140435219952707, 83.78445800887257633, 34.21067981925357060 ) ) ;
#11392=CARTESIAN_POINT ( 'NONE',  ( 41.46631938032478359, 89.18445800887258201, 29.45539723777780239 ) ) ;
#11395=CARTESIAN_POINT ( 'NONE',  ( 39.92123440845004723, 119.3344580088725735, 29.95742577749337343 ) ) ;
#11396=CARTESIAN_POINT ( 'NONE',  ( 45.74753988029933538, 106.4297705074273068, 37.97664729208901946 ) ) ;
#11400=CARTESIAN_POINT ( 'NONE',  ( 47.43856463449118621, 91.61518717409400381, 34.21067981925357060 ) ) ;
#11402=ORIENTED_EDGE ( 'NONE', *, *, #4063, .T. ) ;
#11406=CARTESIAN_POINT ( 'NONE',  ( 44.37947211624943833, 64.27977050742731535, 38.42115945441014446 ) ) ;
#11408=VERTEX_POINT ( 'NONE', #13333 ) ;
#11409=CARTESIAN_POINT ( 'NONE',  ( 45.74753988029933538, 148.4297705074273210, 37.97664729208901946 ) ) ;
#11412=CARTESIAN_POINT ( 'NONE',  ( 38.01140435219952707, 108.7104996726487514, 34.21067981925357060 ) ) ;
#11413=CARTESIAN_POINT ( 'NONE',  ( 43.01140435219951286, 63.86518717409398960, 38.86567161673127657 ) ) ;
#11414=DIRECTION ( 'NONE',  ( 0.000000000000000000, 1.000000000000000000, 0.000000000000000000 ) ) ;
#11417=CARTESIAN_POINT ( 'NONE',  ( 41.46631938032478359, 156.3844580088725706, 38.96596240072933170 ) ) ;
#11421=CARTESIAN_POINT ( 'NONE',  ( 45.74753988029933538, 128.3297705074273267, 30.44471234641811819 ) ) ;
#11423=CARTESIAN_POINT ( 'NONE',  ( 40.27526882409969744, 117.5651871740940067, 37.97664729208901235 ) ) ;
#11426=CARTESIAN_POINT ( 'NONE',  ( 39.92123440845005433, 151.1604996726487116, 38.46393386101375711 ) ) ;
#11427=CARTESIAN_POINT ( 'NONE',  ( 45.51141300902961717, 59.09387774407727534, 29.88055779818149915 ) ) ;
#11431=CARTESIAN_POINT ( 'NONE',  ( 46.59305225739526435, 91.57977050742731251, 36.81289934271958941 ) ) ;
#11432=EDGE_LOOP ( 'NONE', ( #5210, #1066, #11821, #19823 ) ) ;
#11434=CARTESIAN_POINT ( 'NONE',  ( 43.01140435219951996, 10.71049967264875491, 34.21067981925357060 ) ) ;
#11436=CARTESIAN_POINT ( 'NONE',  ( 38.96631938032478359, 78.08445800887257349, 37.14960608071593384 ) ) ;
#11437=CARTESIAN_POINT ( 'NONE',  ( 43.01140435219951286, 59.96049967264874425, 29.21067981925356705 ) ) ;
#11438=CARTESIAN_POINT ( 'NONE',  ( 47.05648932407426344, 137.5104996726487627, 31.27175355779120025 ) ) ;
#11439=CARTESIAN_POINT ( 'NONE',  ( 38.58424406990784661, 93.26518717409399528, 35.64915139335016647 ) ) ;
#11441=( BOUNDED_CURVE ( )  B_SPLINE_CURVE ( 2, ( #13570, #8299, #16770, #23, #3223, #9955, #16659, #8412, #135, #1571, #10175, #18545, #16875 ),
 .UNSPECIFIED., .F., .F. ) 
 B_SPLINE_CURVE_WITH_KNOTS ( ( 3, 2, 2, 2, 2, 2, 3 ),
 ( 0.7573529411764705621, 0.7588235294117646745, 0.7617647058823528994, 0.7647058823529411242, 0.7676470588235294601, 0.7705882352941176849, 0.7720588235294117974 ),
 .UNSPECIFIED. ) 
 CURVE ( )  GEOMETRIC_REPRESENTATION_ITEM ( )  RATIONAL_B_SPLINE_CURVE ( ( 0.9755282581475768211, 0.9755282581475768211, 1.000000000000000000, 0.9510565162951535312, 1.000000000000000000, 0.9510565162951535312, 1.000000000000000000, 0.9510565162951535312, 1.000000000000000000, 0.9510565162951535312, 1.000000000000000000, 0.9755282581475768211, 0.9755282581475768211 ) ) 
 REPRESENTATION_ITEM ( '' )  );
#11448=CARTESIAN_POINT ( 'NONE',  ( 47.05648932407426344, 114.9844580088725792, 37.14960608071593384 ) ) ;
#11449=CARTESIAN_POINT ( 'NONE',  ( 45.74753988029933538, 61.16518717409398675, 37.97664729208901946 ) ) ;
#11454=ORIENTED_EDGE ( 'NONE', *, *, #12450, .F. ) ;
#11455=CARTESIAN_POINT ( 'NONE',  ( 47.43856463449117911, 70.46518717409401233, 35.64915139335015937 ) ) ;
#11458=DIRECTION ( 'NONE',  ( 0.000000000000000000, 0.000000000000000000, 1.000000000000000000 ) ) ;
#11459=CARTESIAN_POINT ( 'NONE',  ( 38.58424406990784661, 126.2651871740940237, 35.64915139335016647 ) ) ;
#11460=ADVANCED_FACE ( 'NONE', ( #16041 ), #18543, .T. ) ;
#11463=ORIENTED_EDGE ( 'NONE', *, *, #14609, .F. ) ;
#11467=AXIS2_PLACEMENT_3D ( 'NONE', #15201, #15523, #7048 ) ;
#11468=CARTESIAN_POINT ( 'NONE',  ( 45.74753988029933538, 65.32977050742732672, 30.44471234641811819 ) ) ;
#11469=CARTESIAN_POINT ( 'NONE',  ( 47.43856463449118621, 124.6151871740940038, 34.21067981925357060 ) ) ;
#11471=CARTESIAN_POINT ( 'NONE',  ( 39.92123440845004723, 82.16049967264871157, 38.46393386101376421 ) ) ;
#11473=EDGE_CURVE ( 'NONE', #7305, #13261, #12563, .T. ) ;
#11476=CARTESIAN_POINT ( 'NONE',  ( 46.59305225739526435, 85.91518717409400097, 31.60846029578754468 ) ) ;
#11477=CARTESIAN_POINT ( 'NONE',  ( 43.01140435219951996, 150.5344580088725763, 39.21067981925356349 ) ) ;
#11479=VERTEX_POINT ( 'NONE', #16186 ) ;
#11480=CARTESIAN_POINT ( 'NONE',  ( 40.27526882409969033, 62.92977050742729972, 30.44471234641811819 ) ) ;
#11487=ORIENTED_EDGE ( 'NONE', *, *, #12907, .F. ) ;
#11490=CARTESIAN_POINT ( 'NONE',  ( 43.01140435219951996, 10.71049967264875491, 39.21067981925356349 ) ) ;
#11491=CARTESIAN_POINT ( 'NONE',  ( 47.43856463449118621, 124.8797705074273239, 34.21067981925357060 ) ) ;
#11493=ORIENTED_EDGE ( 'NONE', *, *, #693, .F. ) ;
#11494=DIRECTION ( 'NONE',  ( 0.000000000000000000, 0.000000000000000000, 1.000000000000000000 ) ) ;
#11496=CARTESIAN_POINT ( 'NONE',  ( 39.42975644700377558, 117.0797705074273267, 31.60846029578754468 ) ) ;
#11498=CARTESIAN_POINT ( 'NONE',  ( 41.64333658814960870, 86.77977050742731535, 30.00020018409699318 ) ) ;
#11499=CARTESIAN_POINT ( 'NONE',  ( 45.74753988029933538, 154.1651871740939441, 37.97664729208901946 ) ) ;
#11500=VECTOR ( 'NONE', #2749, 1000.000000000000000 ) ;
#11502=CARTESIAN_POINT ( 'NONE',  ( 41.46631938032478359, 102.3844580088725849, 38.96596240072933170 ) ) ;
#11505=DIRECTION ( 'NONE',  ( 0.000000000000000000, 1.000000000000000000, 0.000000000000000000 ) ) ;
#11506=CARTESIAN_POINT ( 'NONE',  ( 48.01140435219951996, 131.3604996726487002, 32.58608133808903773 ) ) ;
#11509=CARTESIAN_POINT ( 'NONE',  ( 38.01140435219951996, 122.6344580088725849, 32.58608133808903773 ) ) ;
#11510=CARTESIAN_POINT ( 'NONE',  ( 40.27526882409969033, 105.8297705074273125, 37.97664729208901946 ) ) ;
#11514=CARTESIAN_POINT ( 'NONE',  ( 44.37947211624943833, 85.01518717409399528, 38.42115945441014446 ) ) ;
#11519=VECTOR ( 'NONE', #9322, 1000.000000000000000 ) ;
#11522=CARTESIAN_POINT ( 'NONE',  ( 43.01140435219951286, 70.12977050742730967, 38.86567161673127657 ) ) ;
#11523=ORIENTED_EDGE ( 'NONE', *, *, #20597, .T. ) ;
#11524=CARTESIAN_POINT ( 'NONE',  ( 46.59305225739526435, 148.5797705074273267, 36.81289934271958941 ) ) ;
#11525=CARTESIAN_POINT ( 'NONE',  ( 44.37947211624943833, 98.47977050742731819, 30.00020018409699318 ) ) ;
#11526=CARTESIAN_POINT ( 'NONE',  ( 41.46631938032478359, 141.1104996726487286, 29.45539723777780239 ) ) ;
#11529=CARTESIAN_POINT ( 'NONE',  ( 43.01140435219951286, 106.4604996726487371, 39.46799094044489209 ) ) ;
#11530=CARTESIAN_POINT ( 'NONE',  ( 38.58424406990784661, 65.96518717409399812, 32.77220824515698183 ) ) ;
#11531=CARTESIAN_POINT ( 'NONE',  ( 39.92123440845005433, 95.33445800887255928, 29.95742577749336988 ) ) ;
#11538=CARTESIAN_POINT ( 'NONE',  ( 41.64333658814960870, 134.7797705074273154, 30.00020018409699318 ) ) ;
#11540=CARTESIAN_POINT ( 'NONE',  ( 40.27526882409969744, 116.6651871740939868, 30.44471234641812174 ) ) ;
#11544=CARTESIAN_POINT ( 'NONE',  ( 43.80332655382220963, 140.8836182503284817, 29.21067981925357060 ) ) ;
#11548=CARTESIAN_POINT ( 'NONE',  ( 38.58424406990785371, 99.22977050742731819, 32.77220824515697473 ) ) ;
#11552=CARTESIAN_POINT ( 'NONE',  ( 46.10157429594899270, 82.73445800887257917, 29.95742577749337343 ) ) ;
#11554=EDGE_CURVE ( 'NONE', #17105, #17591, #8696, .T. ) ;
#11555=CARTESIAN_POINT ( 'NONE',  ( 43.01140435219951286, 137.9604996726487229, 28.95336869806222779 ) ) ;
#11556=CARTESIAN_POINT ( 'NONE',  ( 40.27526882409969033, 99.56518717409400665, 37.97664729208901946 ) ) ;
#11561=CARTESIAN_POINT ( 'NONE',  ( 43.01140435219951996, 10.71049967264875491, 34.21067981925357060 ) ) ;
#11563=CARTESIAN_POINT ( 'NONE',  ( 41.46631938032478359, 148.3104996726487457, 38.96596240072933170 ) ) ;
#11564=CARTESIAN_POINT ( 'NONE',  ( 47.05648932407426344, 115.5844580088725877, 31.27175355779120025 ) ) ;
#11565=CARTESIAN_POINT ( 'NONE',  ( 47.43856463449118621, 64.61518717409398960, 34.21067981925357060 ) ) ;
#11568=CARTESIAN_POINT ( 'NONE',  ( 38.58424406990785371, 144.2651871740939953, 35.64915139335015937 ) ) ;
#11571=ORIENTED_EDGE ( 'NONE', *, *, #16281, .F. ) ;
#11572=CARTESIAN_POINT ( 'NONE',  ( 39.92123440845005433, 77.33445800887257349, 29.95742577749336988 ) ) ;
#11576=CARTESIAN_POINT ( 'NONE',  ( 38.58424406990784661, 129.2651871740940237, 35.64915139335016647 ) ) ;
#11579=ORIENTED_EDGE ( 'NONE', *, *, #3982, .F. ) ;
#11581=ORIENTED_EDGE ( 'NONE', *, *, #19885, .F. ) ;
#11583=CARTESIAN_POINT ( 'NONE',  ( 38.01140435219952707, 110.7844580088725905, 34.21067981925357060 ) ) ;
#11584=CARTESIAN_POINT ( 'NONE',  ( 40.27526882409969744, 153.8297705074273267, 37.97664729208901235 ) ) ;
#11586=CARTESIAN_POINT ( 'NONE',  ( 47.43856463449117200, 64.72977050742731819, 35.64915139335016647 ) ) ;
#11587=CARTESIAN_POINT ( 'NONE',  ( 47.43856463449117200, 127.7651871740940237, 32.77220824515698183 ) ) ;
#11589=CARTESIAN_POINT ( 'NONE',  ( 38.96631938032478359, 79.01049967264873430, 37.14960608071593384 ) ) ;
#11591=CARTESIAN_POINT ( 'NONE',  ( 46.10157429594899270, 98.66049967264872578, 29.95742577749336988 ) ) ;
#11593=CARTESIAN_POINT ( 'NONE',  ( 41.64333658814960870, 92.51518717409399528, 30.00020018409699318 ) ) ;
#11595=CARTESIAN_POINT ( 'NONE',  ( 47.05648932407426344, 141.9844580088725650, 37.14960608071593384 ) ) ;
#11597=CARTESIAN_POINT ( 'NONE',  ( 47.43856463449117200, 65.02977050742732956, 32.77220824515698183 ) ) ;
#11601=ORIENTED_EDGE ( 'NONE', *, *, #13459, .T. ) ;
#11602=CARTESIAN_POINT ( 'NONE',  ( 41.64333658814960870, 149.5151871740940237, 30.00020018409699318 ) ) ;
#11606=CARTESIAN_POINT ( 'NONE',  ( 41.64333658814960870, 117.9797705074273182, 38.42115945441014446 ) ) ;
#11611=CARTESIAN_POINT ( 'NONE',  ( 43.01140435219951286, 121.1297705074273097, 38.86567161673127657 ) ) ;
#11613=CARTESIAN_POINT ( 'NONE',  ( 41.64333658814960870, 84.97977050742731819, 38.42115945441014446 ) ) ;
#11614=CARTESIAN_POINT ( 'NONE',  ( 47.43856463449118621, 157.6151871740940180, 34.21067981925357060 ) ) ;
#11617=CARTESIAN_POINT ( 'NONE',  ( 48.01140435219951996, 82.43445800887258201, 32.58608133808903773 ) ) ;
#11620=CARTESIAN_POINT ( 'NONE',  ( 38.01140435219952707, 89.78445800887257633, 34.21067981925357060 ) ) ;
#11623=CARTESIAN_POINT ( 'NONE',  ( 40.27526882409969033, 92.92977050742729261, 30.44471234641811819 ) ) ;
#11626=EDGE_LOOP ( 'NONE', ( #21266, #2759, #3589, #4257 ) ) ;
#11629=CARTESIAN_POINT ( 'NONE',  ( 47.43856463449118621, 139.8797705074273381, 34.21067981925357060 ) ) ;
#11631=CARTESIAN_POINT ( 'NONE',  ( 47.43856463449117911, 65.02977050742732956, 32.77220824515697473 ) ) ;
#11633=CARTESIAN_POINT ( 'NONE',  ( 38.58424406990784661, 141.5297705074272869, 35.64915139335016647 ) ) ;
#11635=CARTESIAN_POINT ( 'NONE',  ( 47.05648932407426344, 151.9104996726487400, 37.14960608071593384 ) ) ;
#11637=CARTESIAN_POINT ( 'NONE',  ( 43.01140435219951286, 115.4604996726487229, 39.46799094044489209 ) ) ;
#11638=CARTESIAN_POINT ( 'NONE',  ( 41.64333658814960870, 68.51518717409399528, 30.00020018409699318 ) ) ;
#11640=( BOUNDED_SURFACE ( )  B_SPLINE_SURFACE ( 1, 2, ( 
 ( #2289, #9029, #4269, #645, #10788, #9141, #15841, #17602, #4169, #12650, #10898, #9249, #859, #7595, #14294, #21039, #19926, #19702, #4592, #11311, #3277, #14946, #18264, #9683, #7917, #17922, #21801, #13416, #16380, #13311, #21693, #20047, #8244, #20151, #21357, #4934, #5043, #14620, #6592, #16599, #18036, #9792, #8353, #6361, #10007, #6248, #18375, #11644, #16486, #1403, #2941, #6472, #1292, #16712, #8132, #1621, #13084, #13193, #3168, #15064, #2832, #9571, #16277, #12978, #4814, #8027, #14734, #21470, #1183, #19813, #9897, #4702, #18146, #14835, #21581, #1515, #3503, #7137, #15505, #13841, #2060, #15602, #15177, #20577, #508, #1734, #407, #10444, #11867, #3611, #2163, #183, #18920, #79, #12185, #5463, #10334, #17037, #18599, #299, #20256, #3823, #1949, #10549, #7028, #8469, #10115, #20685, #18810, #6816, #17250, #8900, #8791, #7247, #5363, #13947, #11754, #13522, #5147, #18485, #3390, #10226, #17146, #16822, #16928, #1844, #8574, #15290, #6920, #13624, #20363, #5258, #11975, #18705, #8679, #15401, #13733, #20471, #12080, #3715, #17788, #2586, #5682, #2482, #16141, #3928, #5895, #729, #14488, #9441, #17576, #21119, #7683, #7457, #12625, #1050, #11073, #14166, #9224, #14380, #20899, #19030, #12406, #19347, #17469, #2696, #10659, #4245, #5786, #7568, #15922, #14268, #17361, #19137, #10971, #938, #6003, #7784, #21013, #5569, #9004, #7354, #12732, #12518, #19455, #4345, #19242, #17683, #12292, #2267, #4142, #834, #15715, #10875, #619, #4036, #9326, #2379, #14057, #20790, #16025, #10763, #9117, #15815, #1377, #4452, #21334, #6447, #16571, #1490, #10280, #8106, #18652, #2809, #1159, #6564, #14709, #16356, #9766, #21557, #8220, #3555, #6109, #14921, #17896, #14812, #7892, #14593, #6221, #13571, #18239, #13169, #12952, #11183, #21230, #16984, #1892, #19675, #21670, #3141, #20309, #11509, #8628, #9547, #5208, #12839, #16250, #9871, #19901, #4567, #13060, #11923, #9656, #19557, #11289, #18010, #2921, #19788, #4680, #1267, #16463, #8002, #21445, #11395, #6335, #4789, #18119, #3029, #19636, #17751, #687, #17860, #9512, #6076, #19522, #4312, #4415, #6181, #7423, #14122, #1121, #11146, #20861, #16102, #16211, #12913, #7855, #21298, #15882, #12474, #10725, #10836, #2444, #2336, #795, #17534, #9073, #9184, #7529, #11036, #14230, #5858, #12588, #19311, #7642, #4208, #10938, #2654, #17645, #2552, #9289, #21085, #15989, #5966, #12692, #19415, #4863, #9728, #6753, #11690, #11583, #6644, #8182, #19746, #4641, #6407, #4978, #14992, #14884, #18426, #11360, #4529, #13132, #19859, #16757, #4746, #18195, #3102, #1559, #1450, #1669, #8401, #18312, #13241, #13, #16534, #21630, #6521, #21736, #5301, #2205, #12232, #3865, #18963, #1990, #7290, #1882, #226, #3757, #3543, #12118, #6853, #10268, #13670, #17292, #5502, #7176, #16971, #7070, #13880, #8723, #13560, #18849, #12012, #15334, #8513, #18747, #8615, #447, #8834, #17185, #3650, #10164, #15643, #10377, #10485, #16863, #15441, #6964, #15540, #20402, #2098, #3439, #15225, #20619, #8937, #10589, #547, #20194, #5087, #124, #11801, #20296, #18532, #1779, #5193, #11911, #18640, #17078, #340, #13774, #20514, #5401, #4184, #12337, #20726, #20944, #875, #9157, #4075, #7721, #16181, #659, #16070, #5826, #14312, #3974, #19494, #12557, #983, #14422, #1094, #6044, #19285, #10913, #4281, #14205, #19071, #2307, #17617, #11118, #4386, #11011, #14098, #2523, #2743, #10697, #21057, #15858, #13989, #17832, #9263, #21158, #12772, #768, #5937, #9482, #5612, #7504, #15963, #17403, #7610, #9046, #20833, #12666, #10805, #15756, #7397, #19387, #17721, #2627, #9366, #5725, #12448, #19176, #17509, #2418, #3182, #18394, #16502, #4948, #11220, #9587, #14960, #1306, #2956, #18161, #8148, #9911, #11657, #14529, #16617, #4497, #1419, #16289, #1196, #7930, #21706, #4830, #14853, #21375, #19603, #7825, #3294, #10022, #6262, #1528, #11552, #8260, #19944, #16727, #17937, #6607, #21269, #2845, #18281, #6488, #14635, #21487, #20061, #18049, #13326, #12995, #6148, #12883, #6374, #13102, #19715, #3068, #4607, #11326, #19826, #9696, #21599, #16395, #8042, #4716, #13208, #11436, #8804, #15516, #20486, #10459, #17051, #17159, #18937, #20169, #5058, #13854, #2074, #13431, #312, #419, #3837, #5376, #7151, #6828, #3410, #7041, #11772, #15193, #15080, #13535, #6724, #13747, #10132, #12202, #1963, #8484, #15416, #20270, #20591, #18501, #8697, #18611, #3624, #13640, #10346, #16837, #1750, #12091, #18823, #3729, #10564, #5476, #1637, #97, #5161, #8369, #16940, #3516, #11987, #21816, #11882, #10241, #1855, #8586, #15305, #198, #6935, #20376, #5272, #18717, #14583, #11175, #9018, #7259, #17264, #21435, #6325, #15730, #12943, #21326, #19665, #7883, #13051, #20701, #4557, #19776, #13961, #6211, #16238, #17374, #9428, #7992, #5699, #2913, #5584, #17998, #11280, #16133, #1041, #2279, #6098, #3944, #9646, #7776, #16347, #12829, #12308, #15615, #4671, #2799, #19045, #1255, #14697, #2176, #8912, #17886, #523, #10671, #634, #7370, #14071, #20808, #12721, #1148, #19444, #4337, #11063, #17778, #2684, #14474, #21219, #19548, #4443, #9539, #16562, #16454 ),
 ( #16789, #1478, #3354, #19891, #8211, #4895, #8542, #18563, #20222, #43, #11614, #18342, #5009, #11719, #9862, #13592, #3470, #18454, #13491, #15028, #3019, #4778, #14911, #11833, #6783, #21768, #10194, #13161, #11388, #21661, #6551, #16896, #13275, #11499, #1365, #1703, #8319, #5116, #1810, #10080, #20119, #15254, #9757, #18110, #153, #20011, #3243, #6885, #20329, #8097, #14805, #6674, #21545, #9974, #16677, #8432, #1588, #15140, #18230, #13381, #6438, #3132, #12366, #14020, #2023, #13911, #20755, #15570, #13700, #3896, #12148, #372, #15367, #18880, #17109, #7321, #15674, #2235, #3788, #17002, #689, #10517, #10620, #1910, #475, #10408, #578, #5428, #8968, #10300, #260, #17328, #9076, #5646, #19105, #17431, #4001, #6996, #18996, #20435, #10730, #14125, #8646, #5227, #5329, #12047, #2339, #13807, #18777, #15783, #17213, #3574, #11942, #2128, #20649, #7101, #8755, #7426, #18671, #3679, #15472, #8863, #5532, #20545, #7209, #12261, #7858, #14559, #7963, #12916, #19418, #12696, #11149, #21088, #4105, #9187, #2657, #12592, #10840, #20864, #2882, #9621, #19314, #16214, #2776, #1125, #17862, #16320, #2447, #21301, #1229, #17537, #9516, #19526, #20974, #4315, #11252, #9292, #6185, #15885, #19640, #4532, #11039, #17755, #5862, #9400, #7532, #17973, #16109, #5751, #1017, #798, #19208, #12480, #6079, #14234, #4212, #10940, #17648, #2555, #14452, #15993, #902, #7647, #14346, #5969, #7754, #21191, #4419, #12805, #16868, #18428, #6756, #19862, #16428, #20093, #2990, #6412, #6298, #4749, #19751, #4982, #1340, #3442, #14997, #11804, #5090, #11693, #14780, #11587, #10167, #13027, #21739, #9837, #1782, #18535, #4866, #8404, #16761, #16537, #6647, #14670, #20197, #1453, #18315, #1672, #8186, #4645, #21523, #13356, #11469, #21410, #11363, #3326, #14887, #16651, #3215, #1563, #18084, #13135, #10055, #15113, #16, #9731, #8290, #8074, #18198, #3105, #13464, #21633, #6524, #9948, #13245, #19981, #12340, #15229, #3869, #5197, #10488, #10271, #16974, #1884, #15646, #5505, #2100, #2209, #10701, #8618, #10592, #15444, #8838, #20299, #13993, #345, #17297, #8940, #17405, #550, #7074, #13777, #20622, #8726, #13563, #18644, #12120, #18966, #1995, #20516, #15544, #449, #6967, #8516, #7294, #7179, #20729, #18853, #127, #15337, #13673, #5617, #19075, #3761, #3976, #229, #6856, #20406, #18750, #11914, #3653, #5304, #3546, #13883, #5403, #12016, #10381, #12235, #17188, #17081, #15758, #9049, #11121, #4187, #9265, #6151, #16184, #7830, #1096, #5940, #11223, #5828, #10915, #7724, #7507, #16075, #10809, #14207, #17621, #21273, #9485, #17836, #20946, #11014, #2746, #12670, #17512, #986, #15965, #19288, #12452, #877, #12561, #4389, #12776, #21161, #7614, #14101, #19607, #14316, #14426, #20837, #19390, #2529, #19497, #21059, #6050, #7400, #19180, #14532, #12886, #4500, #2310, #663, #5728, #4079, #2421, #9161, #15860, #773, #4287, #17725, #2630, #9370, #15083, #4719, #11331, #10025, #8151, #16293, #2848, #3072, #4833, #13106, #8045, #18661, #3297, #4952, #14750, #11556, #11660, #6491, #4610, #16621, #9810, #19829, #6265, #16505, #21491, #20065, #6613, #14963, #1422, #7934, #13434, #14856, #1531, #14638, #13211, #1310, #13329, #18164, #21710, #1199, #12998, #8263, #6728, #18397, #16730, #8373, #1640, #19719, #9914, #18052, #20172, #5062, #21379, #17942, #2960, #9699, #9592, #11439, #16399, #6377, #21602, #19948, #18284, #3186, #20489, #6938, #1859, #5480, #13964, #20273, #13857, #18720, #12094, #1753, #17268, #3627, #20594, #12205, #20704, #3840, #10351, #17054, #2077, #11990, #16840, #100, #15420, #422, #5275, #1966, #5379, #18827, #10245, #11775, #18940, #3732, #10567, #316, #3413, #5165, #16943, #2179, #7154, #7044, #8915, #13538, #18504, #8589, #200, #15618, #13645, #11886, #8488, #17163, #8699, #526, #7263, #10462, #8808, #10136, #15197, #6831, #18614, #20379, #13750, #3519, #15308, #15519, #4364, #9243, #14507, #9134, #7480, #10991, #10781, #19365, #14074, #17487, #20920, #17377, #852, #2397, #958, #5803, #2606, #10674, #15733, #4263, #9458, #21137, #7701, #17806, #9344, #7373, #17701, #20812, #14399, #5587, #2282, #12312, #5702, #12426, #2717, #14182, #19152, #19472, #17595, #3948, #19048, #12534, #14288, #745, #15834, #6021, #7801, #4053, #12752, #19261, #5915, #9022, #11094, #4163, #16159, #1071, #638, #10892, #2501, #15942, #16047, #7588, #21032, #12644, #3048, #9891, #14727, #6354, #14829, #21574, #19696, #1615, #6585, #6465, #1509, #9785, #12857, #14614, #4584, #21687, #16591, #16481, #13303, #1175, #21249, #11304, #9674, #20041, #16374, #7911, #4471, #4808, #18139, #8238, #11638, #13186, #8126, #14940, #11201, #6127, #4927, #1287, #13078, #3270, #18368, #10002, #16706, #1397, #8347, #2937, #8022, #11530, #18031, #19919, #21352, #21463, #19807, #17914, #9564, #16269, #4696, #18258, #6241, #3161, #12970, #11413, #177, #10221, #3383, #6912, #5142, #17137, #3706, #12071, #13618, #5038, #10542, #20356, #20462, #10436, #15282, #18801, #20145, #10109, #13726, #18910, #8784, #2051, #5455, #15497, #16816, #7022, #8463, #399, #2156, #11747, #15058, #15170, #73 ) ),
 .UNSPECIFIED., .F., .F., .F. ) 
 B_SPLINE_SURFACE_WITH_KNOTS ( ( 2, 2 ),
 ( 3, 2, 2, 2, 2, 2, 2, 2, 2, 2, 2, 2, 2, 2, 2, 2, 2, 2, 2, 2, 2, 2, 2, 2, 2, 2, 2, 2, 2, 2, 2, 2, 2, 2, 2, 2, 2, 2, 2, 2, 2, 2, 2, 2, 2, 2, 2, 2, 2, 2, 2, 2, 2, 2, 2, 2, 2, 2, 2, 2, 2, 2, 2, 2, 2, 2, 2, 2, 2, 2, 2, 2, 2, 2, 2, 2, 2, 2, 2, 2, 2, 2, 2, 2, 2, 2, 2, 2, 2, 2, 2, 2, 2, 2, 2, 2, 2, 2, 2, 2, 2, 2, 2, 2, 2, 2, 2, 2, 2, 2, 2, 2, 2, 2, 2, 2, 2, 2, 2, 2, 2, 2, 2, 2, 2, 2, 2, 2, 2, 2, 2, 2, 2, 2, 2, 2, 2, 2, 2, 2, 2, 2, 2, 2, 2, 2, 2, 2, 2, 2, 2, 2, 2, 2, 2, 2, 2, 2, 2, 2, 2, 2, 2, 2, 2, 2, 2, 2, 2, 2, 2, 2, 2, 2, 2, 2, 2, 2, 2, 2, 2, 2, 2, 2, 2, 2, 2, 2, 2, 2, 2, 2, 2, 2, 2, 2, 2, 2, 2, 2, 2, 2, 2, 2, 2, 2, 2, 2, 2, 2, 2, 2, 2, 2, 2, 2, 2, 2, 2, 2, 2, 2, 2, 2, 2, 2, 2, 2, 2, 2, 2, 2, 2, 2, 2, 2, 2, 2, 2, 2, 2, 2, 2, 2, 2, 2, 2, 2, 2, 2, 2, 2, 2, 2, 2, 2, 2, 2, 2, 2, 2, 2, 2, 2, 2, 2, 2, 2, 2, 2, 2, 2, 2, 2, 2, 2, 2, 2, 2, 2, 2, 2, 2, 2, 2, 2, 2, 2, 2, 2, 2, 2, 2, 2, 2, 2, 2, 2, 2, 2, 2, 2, 2, 2, 2, 2, 2, 2, 2, 2, 2, 2, 2, 2, 2, 2, 2, 2, 2, 2, 2, 2, 2, 2, 2, 2, 2, 2, 2, 2, 2, 2, 2, 2, 3 ),
 ( 0.000000000000000000, 1.000000000000000000 ),
 ( 0.000000000000000000, 0.002941176470588235253, 0.005882352941176470507, 0.008823529411764705760, 0.01176470588235294101, 0.01470588235294117627, 0.01764705882352941152, 0.02058823529411764677, 0.02352941176470588203, 0.02647058823529411728, 0.02941176470588235253, 0.03235294117647059126, 0.03529411764705882304, 0.03823529411764706176, 0.04117647058823529355, 0.04411764705882353227, 0.04705882352941176405, 0.05000000000000000278, 0.05294117647058823456, 0.05588235294117647328, 0.05882352941176470507, 0.06176470588235294379, 0.06470588235294118251, 0.06764705882352940736, 0.07058823529411764608, 0.07352941176470588480, 0.07647058823529412352, 0.07941176470588234837, 0.08235294117647058709, 0.08529411764705882582, 0.08823529411764706454, 0.09117647058823528938, 0.09411764705882352811, 0.09705882352941176683, 0.1000000000000000056, 0.1029411764705882304, 0.1058823529411764691, 0.1088235294117647078, 0.1117647058823529466, 0.1147058823529411714, 0.1176470588235294101, 0.1205882352941176489, 0.1235294117647058876, 0.1264705882352941124, 0.1294117647058823650, 0.1323529411764705899, 0.1352941176470588147, 0.1382352941176470673, 0.1411764705882352922, 0.1441176470588235170, 0.1470588235294117696, 0.1499999999999999944, 0.1529411764705882470, 0.1558823529411764719, 0.1588235294117646967, 0.1617647058823529493, 0.1647058823529411742, 0.1676470588235293990, 0.1705882352941176516, 0.1735294117647058765, 0.1764705882352941291, 0.1794117647058823539, 0.1823529411764705788, 0.1852941176470588314, 0.1882352941176470562, 0.1911764705882352811, 0.1941176470588235337, 0.1970588235294117585, 0.2000000000000000111, 0.2029411764705882359, 0.2058823529411764608, 0.2088235294117647134, 0.2117647058823529382, 0.2147058823529411631, 0.2176470588235294157, 0.2205882352941176405, 0.2235294117647058931, 0.2264705882352941180, 0.2294117647058823428, 0.2323529411764705954, 0.2352941176470588203, 0.2382352941176470451, 0.2411764705882352977, 0.2441176470588235226, 0.2470588235294117752, 0.2500000000000000000, 0.2529411764705882248, 0.2558823529411764497, 0.2588235294117647300, 0.2617647058823529549, 0.2647058823529411797, 0.2676470588235294046, 0.2705882352941176294, 0.2735294117647059098, 0.2764705882352941346, 0.2794117647058823595, 0.2823529411764705843, 0.2852941176470588092, 0.2882352941176470340, 0.2911764705882353144, 0.2941176470588235392, 0.2970588235294117641, 0.2999999999999999889, 0.3029411764705882137, 0.3058823529411764941, 0.3088235294117647189, 0.3117647058823529438, 0.3147058823529411686, 0.3176470588235293935, 0.3205882352941176738, 0.3235294117647058987, 0.3264705882352941235, 0.3294117647058823484, 0.3323529411764705732, 0.3352941176470587981, 0.3382352941176470784, 0.3411764705882353033, 0.3441176470588235281, 0.3470588235294117530, 0.3499999999999999778, 0.3529411764705882582, 0.3558823529411764830, 0.3588235294117647078, 0.3617647058823529327, 0.3647058823529411575, 0.3676470588235294379, 0.3705882352941176627, 0.3735294117647058876, 0.3764705882352941124, 0.3794117647058823373, 0.3823529411764705621, 0.3852941176470588425, 0.3882352941176470673, 0.3911764705882352922, 0.3941176470588235170, 0.3970588235294117418, 0.4000000000000000222, 0.4029411764705882470, 0.4058823529411764719, 0.4088235294117646967, 0.4117647058823529216, 0.4147058823529412019, 0.4176470588235294268, 0.4205882352941176516, 0.4235294117647058765, 0.4264705882352941013, 0.4294117647058823262, 0.4323529411764706065, 0.4352941176470588314, 0.4382352941176470562, 0.4411764705882352811, 0.4441176470588235059, 0.4470588235294117863, 0.4500000000000000111, 0.4529411764705882359, 0.4558823529411764608, 0.4588235294117646856, 0.4617647058823529660, 0.4647058823529411908, 0.4676470588235294157, 0.4705882352941176405, 0.4735294117647058654, 0.4764705882352940902, 0.4794117647058823706, 0.4823529411764705954, 0.4852941176470588203, 0.4882352941176470451, 0.4911764705882352700, 0.4941176470588235503, 0.4970588235294117752, 0.5000000000000000000, 0.5029411764705882248, 0.5058823529411764497, 0.5088235294117646745, 0.5117647058823528994, 0.5147058823529411242, 0.5176470588235294601, 0.5205882352941176849, 0.5235294117647059098, 0.5264705882352941346, 0.5294117647058823595, 0.5323529411764705843, 0.5352941176470588092, 0.5382352941176470340, 0.5411764705882352589, 0.5441176470588234837, 0.5470588235294118196, 0.5500000000000000444, 0.5529411764705882693, 0.5558823529411764941, 0.5588235294117647189, 0.5617647058823529438, 0.5647058823529411686, 0.5676470588235293935, 0.5705882352941176183, 0.5735294117647058432, 0.5764705882352940680, 0.5794117647058824039, 0.5823529411764706287, 0.5852941176470588536, 0.5882352941176470784, 0.5911764705882353033, 0.5941176470588235281, 0.5970588235294117530, 0.5999999999999999778, 0.6029411764705882026, 0.6058823529411764275, 0.6088235294117646523, 0.6117647058823529882, 0.6147058823529412130, 0.6176470588235294379, 0.6205882352941176627, 0.6235294117647058876, 0.6264705882352941124, 0.6294117647058823373, 0.6323529411764705621, 0.6352941176470587870, 0.6382352941176470118, 0.6411764705882353477, 0.6441176470588235725, 0.6470588235294117974, 0.6500000000000000222, 0.6529411764705882470, 0.6558823529411764719, 0.6588235294117646967, 0.6617647058823529216, 0.6647058823529411464, 0.6676470588235293713, 0.6705882352941175961, 0.6735294117647059320, 0.6764705882352941568, 0.6794117647058823817, 0.6823529411764706065, 0.6852941176470588314, 0.6882352941176470562, 0.6911764705882352811, 0.6941176470588235059, 0.6970588235294117307, 0.6999999999999999556, 0.7029411764705881804, 0.7058823529411765163, 0.7088235294117647411, 0.7117647058823529660, 0.7147058823529411908, 0.7176470588235294157, 0.7205882352941176405, 0.7235294117647058654, 0.7264705882352940902, 0.7294117647058823151, 0.7323529411764705399, 0.7352941176470588758, 0.7382352941176471006, 0.7411764705882353255, 0.7441176470588235503, 0.7470588235294117752, 0.7500000000000000000, 0.7529411764705882248, 0.7558823529411764497, 0.7588235294117646745, 0.7617647058823528994, 0.7647058823529411242, 0.7676470588235294601, 0.7705882352941176849, 0.7735294117647059098, 0.7764705882352941346, 0.7794117647058823595, 0.7823529411764705843, 0.7852941176470588092, 0.7882352941176470340, 0.7911764705882352589, 0.7941176470588234837, 0.7970588235294118196, 0.8000000000000000444, 0.8029411764705882693, 0.8058823529411764941, 0.8088235294117647189, 0.8117647058823529438, 0.8147058823529411686, 0.8176470588235293935, 0.8205882352941176183, 0.8235294117647058432, 0.8264705882352940680, 0.8294117647058824039, 0.8323529411764706287, 0.8352941176470588536, 0.8382352941176470784, 0.8411764705882353033, 0.8441176470588235281, 0.8470588235294117530, 0.8499999999999999778, 0.8529411764705882026, 0.8558823529411764275, 0.8588235294117646523, 0.8617647058823529882, 0.8647058823529412130, 0.8676470588235294379, 0.8705882352941176627, 0.8735294117647058876, 0.8764705882352941124, 0.8794117647058823373, 0.8823529411764705621, 0.8852941176470587870, 0.8882352941176470118, 0.8911764705882353477, 0.8941176470588235725, 0.8970588235294117974, 0.9000000000000000222, 0.9029411764705882470, 0.9058823529411764719, 0.9088235294117646967, 0.9117647058823529216, 0.9147058823529411464, 0.9176470588235293713, 0.9205882352941175961, 0.9235294117647059320, 0.9264705882352941568, 0.9294117647058823817, 0.9323529411764706065, 0.9352941176470588314, 0.9382352941176470562, 0.9411764705882352811, 0.9441176470588235059, 0.9470588235294117307, 0.9499999999999999556, 0.9529411764705881804, 0.9558823529411765163, 0.9588235294117647411, 0.9617647058823529660, 0.9647058823529411908, 0.9676470588235294157, 0.9705882352941176405, 0.9735294117647058654, 0.9764705882352940902, 0.9794117647058823151, 0.9803958162805426202 ),
 .UNSPECIFIED. ) 
 GEOMETRIC_REPRESENTATION_ITEM ( )  RATIONAL_B_SPLINE_SURFACE ( (
 ( 1.000000000000000000, 0.9510565162951535312, 1.000000000000000000, 0.9510565162951535312, 1.000000000000000000, 0.9510565162951535312, 1.000000000000000000, 0.9510565162951535312, 1.000000000000000000, 0.9510565162951535312, 1.000000000000000000, 0.9510565162951535312, 1.000000000000000000, 0.9510565162951535312, 1.000000000000000000, 0.9510565162951535312, 1.000000000000000000, 0.9510565162951535312, 1.000000000000000000, 0.9510565162951535312, 1.000000000000000000, 0.9510565162951535312, 1.000000000000000000, 0.9510565162951535312, 1.000000000000000000, 0.9510565162951535312, 1.000000000000000000, 0.9510565162951535312, 1.000000000000000000, 0.9510565162951535312, 1.000000000000000000, 0.9510565162951535312, 1.000000000000000000, 0.9510565162951535312, 1.000000000000000000, 0.9510565162951535312, 1.000000000000000000, 0.9510565162951535312, 1.000000000000000000, 0.9510565162951535312, 1.000000000000000000, 0.9510565162951535312, 1.000000000000000000, 0.9510565162951535312, 1.000000000000000000, 0.9510565162951535312, 1.000000000000000000, 0.9510565162951535312, 1.000000000000000000, 0.9510565162951535312, 1.000000000000000000, 0.9510565162951535312, 1.000000000000000000, 0.9510565162951535312, 1.000000000000000000, 0.9510565162951535312, 1.000000000000000000, 0.9510565162951535312, 1.000000000000000000, 0.9510565162951535312, 1.000000000000000000, 0.9510565162951535312, 1.000000000000000000, 0.9510565162951535312, 1.000000000000000000, 0.9510565162951535312, 1.000000000000000000, 0.9510565162951535312, 1.000000000000000000, 0.9510565162951535312, 1.000000000000000000, 0.9510565162951535312, 1.000000000000000000, 0.9510565162951535312, 1.000000000000000000, 0.9510565162951535312, 1.000000000000000000, 0.9510565162951535312, 1.000000000000000000, 0.9510565162951535312, 1.000000000000000000, 0.9510565162951535312, 1.000000000000000000, 0.9510565162951535312, 1.000000000000000000, 0.9510565162951535312, 1.000000000000000000, 0.9510565162951535312, 1.000000000000000000, 0.9510565162951535312, 1.000000000000000000, 0.9510565162951535312, 1.000000000000000000, 0.9510565162951535312, 1.000000000000000000, 0.9510565162951535312, 1.000000000000000000, 0.9510565162951535312, 1.000000000000000000, 0.9510565162951535312, 1.000000000000000000, 0.9510565162951535312, 1.000000000000000000, 0.9510565162951535312, 1.000000000000000000, 0.9510565162951535312, 1.000000000000000000, 0.9510565162951535312, 1.000000000000000000, 0.9510565162951535312, 1.000000000000000000, 0.9510565162951535312, 1.000000000000000000, 0.9510565162951535312, 1.000000000000000000, 0.9510565162951535312, 1.000000000000000000, 0.9510565162951535312, 1.000000000000000000, 0.9510565162951535312, 1.000000000000000000, 0.9510565162951535312, 1.000000000000000000, 0.9510565162951535312, 1.000000000000000000, 0.9510565162951535312, 1.000000000000000000, 0.9510565162951535312, 1.000000000000000000, 0.9510565162951535312, 1.000000000000000000, 0.9510565162951535312, 1.000000000000000000, 0.9510565162951535312, 1.000000000000000000, 0.9510565162951535312, 1.000000000000000000, 0.9510565162951535312, 1.000000000000000000, 0.9510565162951535312, 1.000000000000000000, 0.9510565162951535312, 1.000000000000000000, 0.9510565162951535312, 1.000000000000000000, 0.9510565162951535312, 1.000000000000000000, 0.9510565162951535312, 1.000000000000000000, 0.9510565162951535312, 1.000000000000000000, 0.9510565162951535312, 1.000000000000000000, 0.9510565162951535312, 1.000000000000000000, 0.9510565162951535312, 1.000000000000000000, 0.9510565162951535312, 1.000000000000000000, 0.9510565162951535312, 1.000000000000000000, 0.9510565162951535312, 1.000000000000000000, 0.9510565162951535312, 1.000000000000000000, 0.9510565162951535312, 1.000000000000000000, 0.9510565162951535312, 1.000000000000000000, 0.9510565162951535312, 1.000000000000000000, 0.9510565162951535312, 1.000000000000000000, 0.9510565162951535312, 1.000000000000000000, 0.9510565162951535312, 1.000000000000000000, 0.9510565162951535312, 1.000000000000000000, 0.9510565162951535312, 1.000000000000000000, 0.9510565162951535312, 1.000000000000000000, 0.9510565162951535312, 1.000000000000000000, 0.9510565162951535312, 1.000000000000000000, 0.9510565162951535312, 1.000000000000000000, 0.9510565162951535312, 1.000000000000000000, 0.9510565162951535312, 1.000000000000000000, 0.9510565162951535312, 1.000000000000000000, 0.9510565162951535312, 1.000000000000000000, 0.9510565162951535312, 1.000000000000000000, 0.9510565162951535312, 1.000000000000000000, 0.9510565162951535312, 1.000000000000000000, 0.9510565162951535312, 1.000000000000000000, 0.9510565162951535312, 1.000000000000000000, 0.9510565162951535312, 1.000000000000000000, 0.9510565162951535312, 1.000000000000000000, 0.9510565162951535312, 1.000000000000000000, 0.9510565162951535312, 1.000000000000000000, 0.9510565162951535312, 1.000000000000000000, 0.9510565162951535312, 1.000000000000000000, 0.9510565162951535312, 1.000000000000000000, 0.9510565162951535312, 1.000000000000000000, 0.9510565162951535312, 1.000000000000000000, 0.9510565162951535312, 1.000000000000000000, 0.9510565162951535312, 1.000000000000000000, 0.9510565162951535312, 1.000000000000000000, 0.9510565162951535312, 1.000000000000000000, 0.9510565162951535312, 1.000000000000000000, 0.9510565162951535312, 1.000000000000000000, 0.9510565162951535312, 1.000000000000000000, 0.9510565162951535312, 1.000000000000000000, 0.9510565162951535312, 1.000000000000000000, 0.9510565162951535312, 1.000000000000000000, 0.9510565162951535312, 1.000000000000000000, 0.9510565162951535312, 1.000000000000000000, 0.9510565162951535312, 1.000000000000000000, 0.9510565162951535312, 1.000000000000000000, 0.9510565162951535312, 1.000000000000000000, 0.9510565162951535312, 1.000000000000000000, 0.9510565162951535312, 1.000000000000000000, 0.9510565162951535312, 1.000000000000000000, 0.9510565162951535312, 1.000000000000000000, 0.9510565162951535312, 1.000000000000000000, 0.9510565162951535312, 1.000000000000000000, 0.9510565162951535312, 1.000000000000000000, 0.9510565162951535312, 1.000000000000000000, 0.9510565162951535312, 1.000000000000000000, 0.9510565162951535312, 1.000000000000000000, 0.9510565162951535312, 1.000000000000000000, 0.9510565162951535312, 1.000000000000000000, 0.9510565162951535312, 1.000000000000000000, 0.9510565162951535312, 1.000000000000000000, 0.9510565162951535312, 1.000000000000000000, 0.9510565162951535312, 1.000000000000000000, 0.9510565162951535312, 1.000000000000000000, 0.9510565162951535312, 1.000000000000000000, 0.9510565162951535312, 1.000000000000000000, 0.9510565162951535312, 1.000000000000000000, 0.9510565162951535312, 1.000000000000000000, 0.9510565162951535312, 1.000000000000000000, 0.9510565162951535312, 1.000000000000000000, 0.9510565162951535312, 1.000000000000000000, 0.9510565162951535312, 1.000000000000000000, 0.9510565162951535312, 1.000000000000000000, 0.9510565162951535312, 1.000000000000000000, 0.9510565162951535312, 1.000000000000000000, 0.9510565162951535312, 1.000000000000000000, 0.9510565162951535312, 1.000000000000000000, 0.9510565162951535312, 1.000000000000000000, 0.9510565162951535312, 1.000000000000000000, 0.9510565162951535312, 1.000000000000000000, 0.9510565162951535312, 1.000000000000000000, 0.9510565162951535312, 1.000000000000000000, 0.9510565162951535312, 1.000000000000000000, 0.9510565162951535312, 1.000000000000000000, 0.9510565162951535312, 1.000000000000000000, 0.9510565162951535312, 1.000000000000000000, 0.9510565162951535312, 1.000000000000000000, 0.9510565162951535312, 1.000000000000000000, 0.9510565162951535312, 1.000000000000000000, 0.9510565162951535312, 1.000000000000000000, 0.9510565162951535312, 1.000000000000000000, 0.9510565162951535312, 1.000000000000000000, 0.9510565162951535312, 1.000000000000000000, 0.9510565162951535312, 1.000000000000000000, 0.9510565162951535312, 1.000000000000000000, 0.9510565162951535312, 1.000000000000000000, 0.9510565162951535312, 1.000000000000000000, 0.9510565162951535312, 1.000000000000000000, 0.9510565162951535312, 1.000000000000000000, 0.9510565162951535312, 1.000000000000000000, 0.9510565162951535312, 1.000000000000000000, 0.9510565162951535312, 1.000000000000000000, 0.9510565162951535312, 1.000000000000000000, 0.9510565162951535312, 1.000000000000000000, 0.9510565162951535312, 1.000000000000000000, 0.9510565162951535312, 1.000000000000000000, 0.9510565162951535312, 1.000000000000000000, 0.9510565162951535312, 1.000000000000000000, 0.9510565162951535312, 1.000000000000000000, 0.9510565162951535312, 1.000000000000000000, 0.9510565162951535312, 1.000000000000000000, 0.9510565162951535312, 1.000000000000000000, 0.9510565162951535312, 1.000000000000000000, 0.9510565162951535312, 1.000000000000000000, 0.9510565162951535312, 1.000000000000000000, 0.9510565162951535312, 1.000000000000000000, 0.9510565162951535312, 1.000000000000000000, 0.9510565162951535312, 1.000000000000000000, 0.9510565162951535312, 1.000000000000000000, 0.9510565162951535312, 1.000000000000000000, 0.9510565162951535312, 1.000000000000000000, 0.9510565162951535312, 1.000000000000000000, 0.9510565162951535312, 1.000000000000000000, 0.9510565162951535312, 1.000000000000000000, 0.9510565162951535312, 1.000000000000000000, 0.9510565162951535312, 1.000000000000000000, 0.9510565162951535312, 1.000000000000000000, 0.9510565162951535312, 1.000000000000000000, 0.9510565162951535312, 1.000000000000000000, 0.9510565162951535312, 1.000000000000000000, 0.9510565162951535312, 1.000000000000000000, 0.9510565162951535312, 1.000000000000000000, 0.9510565162951535312, 1.000000000000000000, 0.9510565162951535312, 1.000000000000000000, 0.9510565162951535312, 1.000000000000000000, 0.9510565162951535312, 1.000000000000000000, 0.9510565162951535312, 1.000000000000000000, 0.9510565162951535312, 1.000000000000000000, 0.9510565162951535312, 1.000000000000000000, 0.9510565162951535312, 1.000000000000000000, 0.9510565162951535312, 1.000000000000000000, 0.9510565162951535312, 1.000000000000000000, 0.9510565162951535312, 1.000000000000000000, 0.9510565162951535312, 1.000000000000000000, 0.9510565162951535312, 1.000000000000000000, 0.9510565162951535312, 1.000000000000000000, 0.9510565162951535312, 1.000000000000000000, 0.9510565162951535312, 1.000000000000000000, 0.9510565162951535312, 1.000000000000000000, 0.9510565162951535312, 1.000000000000000000, 0.9510565162951535312, 1.000000000000000000, 0.9510565162951535312, 1.000000000000000000, 0.9510565162951535312, 1.000000000000000000, 0.9510565162951535312, 1.000000000000000000, 0.9510565162951535312, 1.000000000000000000, 0.9510565162951535312, 1.000000000000000000, 0.9510565162951535312, 1.000000000000000000, 0.9510565162951535312, 1.000000000000000000, 0.9510565162951535312, 1.000000000000000000, 0.9510565162951535312, 1.000000000000000000, 0.9510565162951535312, 1.000000000000000000, 0.9510565162951535312, 1.000000000000000000, 0.9510565162951535312, 1.000000000000000000, 0.9510565162951535312, 1.000000000000000000, 0.9510565162951535312, 1.000000000000000000, 0.9510565162951535312, 1.000000000000000000, 0.9510565162951535312, 1.000000000000000000, 0.9510565162951535312, 1.000000000000000000, 0.9510565162951535312, 1.000000000000000000, 0.9510565162951535312, 1.000000000000000000, 0.9510565162951535312, 1.000000000000000000, 0.9510565162951535312, 1.000000000000000000, 0.9510565162951535312, 1.000000000000000000, 0.9510565162951535312, 1.000000000000000000, 0.9510565162951535312, 1.000000000000000000, 0.9510565162951535312, 1.000000000000000000, 0.9510565162951535312, 1.000000000000000000, 0.9510565162951535312, 1.000000000000000000, 0.9510565162951535312, 1.000000000000000000, 0.9510565162951535312, 1.000000000000000000, 0.9510565162951535312, 1.000000000000000000, 0.9510565162951535312, 1.000000000000000000, 0.9510565162951535312, 1.000000000000000000, 0.9510565162951535312, 1.000000000000000000, 0.9510565162951535312, 1.000000000000000000, 0.9510565162951535312, 1.000000000000000000, 0.9510565162951535312, 1.000000000000000000, 0.9510565162951535312, 1.000000000000000000, 0.9510565162951535312, 1.000000000000000000, 0.9510565162951535312, 1.000000000000000000, 0.9510565162951535312, 1.000000000000000000, 0.9510565162951535312, 1.000000000000000000, 0.9510565162951535312, 1.000000000000000000, 0.9510565162951535312, 1.000000000000000000, 0.9510565162951535312, 1.000000000000000000, 0.9510565162951535312, 1.000000000000000000, 0.9510565162951535312, 1.000000000000000000, 0.9510565162951535312, 1.000000000000000000, 0.9510565162951535312, 1.000000000000000000, 0.9510565162951535312, 1.000000000000000000, 0.9510565162951535312, 1.000000000000000000, 0.9510565162951535312, 1.000000000000000000, 0.9510565162951535312, 1.000000000000000000, 0.9510565162951535312, 1.000000000000000000, 0.9510565162951535312, 1.000000000000000000, 0.9510565162951535312, 1.000000000000000000, 0.9510565162951535312, 1.000000000000000000, 0.9510565162951535312, 1.000000000000000000, 0.9510565162951535312, 1.000000000000000000, 0.9510565162951535312, 1.000000000000000000, 0.9510565162951535312, 1.000000000000000000, 0.9510565162951535312, 1.000000000000000000, 0.9510565162951535312, 1.000000000000000000, 0.9510565162951535312, 1.000000000000000000, 0.9510565162951535312, 1.000000000000000000, 0.9510565162951535312, 1.000000000000000000, 0.9510565162951535312, 1.000000000000000000, 0.9510565162951535312, 1.000000000000000000, 0.9510565162951535312, 1.000000000000000000, 0.9510565162951535312, 1.000000000000000000, 0.9510565162951535312, 1.000000000000000000, 0.9510565162951535312, 1.000000000000000000, 0.9510565162951535312, 1.000000000000000000, 0.9510565162951535312, 1.000000000000000000, 0.9510565162951535312, 1.000000000000000000, 0.9510565162951535312, 1.000000000000000000, 0.9510565162951535312, 1.000000000000000000, 0.9510565162951535312, 1.000000000000000000, 0.9510565162951535312, 1.000000000000000000, 0.9510565162951535312, 1.000000000000000000, 0.9510565162951535312, 1.000000000000000000, 0.9510565162951535312, 1.000000000000000000, 0.9510565162951535312, 1.000000000000000000, 0.9510565162951535312, 1.000000000000000000, 0.9510565162951535312, 1.000000000000000000, 0.9510565162951535312, 1.000000000000000000, 0.9510565162951535312, 1.000000000000000000, 0.9510565162951535312, 1.000000000000000000, 0.9510565162951535312, 1.000000000000000000, 0.9510565162951535312, 1.000000000000000000, 0.9510565162951535312, 1.000000000000000000, 0.9510565162951535312, 1.000000000000000000, 0.9510565162951535312, 1.000000000000000000, 0.9510565162951535312, 1.000000000000000000, 0.9510565162951535312, 1.000000000000000000, 0.9510565162951535312, 1.000000000000000000, 0.9510565162951535312, 1.000000000000000000, 0.9510565162951535312, 1.000000000000000000, 0.9510565162951535312, 1.000000000000000000, 0.9510565162951535312, 1.000000000000000000, 0.9510565162951535312, 1.000000000000000000, 0.9510565162951535312, 1.000000000000000000, 0.9510565162951535312, 1.000000000000000000, 0.9836246098489007661, 0.9782068950532306628),
 ( 1.000000000000000000, 0.9510565162951535312, 1.000000000000000000, 0.9510565162951535312, 1.000000000000000000, 0.9510565162951535312, 1.000000000000000000, 0.9510565162951535312, 1.000000000000000000, 0.9510565162951535312, 1.000000000000000000, 0.9510565162951535312, 1.000000000000000000, 0.9510565162951535312, 1.000000000000000000, 0.9510565162951535312, 1.000000000000000000, 0.9510565162951535312, 1.000000000000000000, 0.9510565162951535312, 1.000000000000000000, 0.9510565162951535312, 1.000000000000000000, 0.9510565162951535312, 1.000000000000000000, 0.9510565162951535312, 1.000000000000000000, 0.9510565162951535312, 1.000000000000000000, 0.9510565162951535312, 1.000000000000000000, 0.9510565162951535312, 1.000000000000000000, 0.9510565162951535312, 1.000000000000000000, 0.9510565162951535312, 1.000000000000000000, 0.9510565162951535312, 1.000000000000000000, 0.9510565162951535312, 1.000000000000000000, 0.9510565162951535312, 1.000000000000000000, 0.9510565162951535312, 1.000000000000000000, 0.9510565162951535312, 1.000000000000000000, 0.9510565162951535312, 1.000000000000000000, 0.9510565162951535312, 1.000000000000000000, 0.9510565162951535312, 1.000000000000000000, 0.9510565162951535312, 1.000000000000000000, 0.9510565162951535312, 1.000000000000000000, 0.9510565162951535312, 1.000000000000000000, 0.9510565162951535312, 1.000000000000000000, 0.9510565162951535312, 1.000000000000000000, 0.9510565162951535312, 1.000000000000000000, 0.9510565162951535312, 1.000000000000000000, 0.9510565162951535312, 1.000000000000000000, 0.9510565162951535312, 1.000000000000000000, 0.9510565162951535312, 1.000000000000000000, 0.9510565162951535312, 1.000000000000000000, 0.9510565162951535312, 1.000000000000000000, 0.9510565162951535312, 1.000000000000000000, 0.9510565162951535312, 1.000000000000000000, 0.9510565162951535312, 1.000000000000000000, 0.9510565162951535312, 1.000000000000000000, 0.9510565162951535312, 1.000000000000000000, 0.9510565162951535312, 1.000000000000000000, 0.9510565162951535312, 1.000000000000000000, 0.9510565162951535312, 1.000000000000000000, 0.9510565162951535312, 1.000000000000000000, 0.9510565162951535312, 1.000000000000000000, 0.9510565162951535312, 1.000000000000000000, 0.9510565162951535312, 1.000000000000000000, 0.9510565162951535312, 1.000000000000000000, 0.9510565162951535312, 1.000000000000000000, 0.9510565162951535312, 1.000000000000000000, 0.9510565162951535312, 1.000000000000000000, 0.9510565162951535312, 1.000000000000000000, 0.9510565162951535312, 1.000000000000000000, 0.9510565162951535312, 1.000000000000000000, 0.9510565162951535312, 1.000000000000000000, 0.9510565162951535312, 1.000000000000000000, 0.9510565162951535312, 1.000000000000000000, 0.9510565162951535312, 1.000000000000000000, 0.9510565162951535312, 1.000000000000000000, 0.9510565162951535312, 1.000000000000000000, 0.9510565162951535312, 1.000000000000000000, 0.9510565162951535312, 1.000000000000000000, 0.9510565162951535312, 1.000000000000000000, 0.9510565162951535312, 1.000000000000000000, 0.9510565162951535312, 1.000000000000000000, 0.9510565162951535312, 1.000000000000000000, 0.9510565162951535312, 1.000000000000000000, 0.9510565162951535312, 1.000000000000000000, 0.9510565162951535312, 1.000000000000000000, 0.9510565162951535312, 1.000000000000000000, 0.9510565162951535312, 1.000000000000000000, 0.9510565162951535312, 1.000000000000000000, 0.9510565162951535312, 1.000000000000000000, 0.9510565162951535312, 1.000000000000000000, 0.9510565162951535312, 1.000000000000000000, 0.9510565162951535312, 1.000000000000000000, 0.9510565162951535312, 1.000000000000000000, 0.9510565162951535312, 1.000000000000000000, 0.9510565162951535312, 1.000000000000000000, 0.9510565162951535312, 1.000000000000000000, 0.9510565162951535312, 1.000000000000000000, 0.9510565162951535312, 1.000000000000000000, 0.9510565162951535312, 1.000000000000000000, 0.9510565162951535312, 1.000000000000000000, 0.9510565162951535312, 1.000000000000000000, 0.9510565162951535312, 1.000000000000000000, 0.9510565162951535312, 1.000000000000000000, 0.9510565162951535312, 1.000000000000000000, 0.9510565162951535312, 1.000000000000000000, 0.9510565162951535312, 1.000000000000000000, 0.9510565162951535312, 1.000000000000000000, 0.9510565162951535312, 1.000000000000000000, 0.9510565162951535312, 1.000000000000000000, 0.9510565162951535312, 1.000000000000000000, 0.9510565162951535312, 1.000000000000000000, 0.9510565162951535312, 1.000000000000000000, 0.9510565162951535312, 1.000000000000000000, 0.9510565162951535312, 1.000000000000000000, 0.9510565162951535312, 1.000000000000000000, 0.9510565162951535312, 1.000000000000000000, 0.9510565162951535312, 1.000000000000000000, 0.9510565162951535312, 1.000000000000000000, 0.9510565162951535312, 1.000000000000000000, 0.9510565162951535312, 1.000000000000000000, 0.9510565162951535312, 1.000000000000000000, 0.9510565162951535312, 1.000000000000000000, 0.9510565162951535312, 1.000000000000000000, 0.9510565162951535312, 1.000000000000000000, 0.9510565162951535312, 1.000000000000000000, 0.9510565162951535312, 1.000000000000000000, 0.9510565162951535312, 1.000000000000000000, 0.9510565162951535312, 1.000000000000000000, 0.9510565162951535312, 1.000000000000000000, 0.9510565162951535312, 1.000000000000000000, 0.9510565162951535312, 1.000000000000000000, 0.9510565162951535312, 1.000000000000000000, 0.9510565162951535312, 1.000000000000000000, 0.9510565162951535312, 1.000000000000000000, 0.9510565162951535312, 1.000000000000000000, 0.9510565162951535312, 1.000000000000000000, 0.9510565162951535312, 1.000000000000000000, 0.9510565162951535312, 1.000000000000000000, 0.9510565162951535312, 1.000000000000000000, 0.9510565162951535312, 1.000000000000000000, 0.9510565162951535312, 1.000000000000000000, 0.9510565162951535312, 1.000000000000000000, 0.9510565162951535312, 1.000000000000000000, 0.9510565162951535312, 1.000000000000000000, 0.9510565162951535312, 1.000000000000000000, 0.9510565162951535312, 1.000000000000000000, 0.9510565162951535312, 1.000000000000000000, 0.9510565162951535312, 1.000000000000000000, 0.9510565162951535312, 1.000000000000000000, 0.9510565162951535312, 1.000000000000000000, 0.9510565162951535312, 1.000000000000000000, 0.9510565162951535312, 1.000000000000000000, 0.9510565162951535312, 1.000000000000000000, 0.9510565162951535312, 1.000000000000000000, 0.9510565162951535312, 1.000000000000000000, 0.9510565162951535312, 1.000000000000000000, 0.9510565162951535312, 1.000000000000000000, 0.9510565162951535312, 1.000000000000000000, 0.9510565162951535312, 1.000000000000000000, 0.9510565162951535312, 1.000000000000000000, 0.9510565162951535312, 1.000000000000000000, 0.9510565162951535312, 1.000000000000000000, 0.9510565162951535312, 1.000000000000000000, 0.9510565162951535312, 1.000000000000000000, 0.9510565162951535312, 1.000000000000000000, 0.9510565162951535312, 1.000000000000000000, 0.9510565162951535312, 1.000000000000000000, 0.9510565162951535312, 1.000000000000000000, 0.9510565162951535312, 1.000000000000000000, 0.9510565162951535312, 1.000000000000000000, 0.9510565162951535312, 1.000000000000000000, 0.9510565162951535312, 1.000000000000000000, 0.9510565162951535312, 1.000000000000000000, 0.9510565162951535312, 1.000000000000000000, 0.9510565162951535312, 1.000000000000000000, 0.9510565162951535312, 1.000000000000000000, 0.9510565162951535312, 1.000000000000000000, 0.9510565162951535312, 1.000000000000000000, 0.9510565162951535312, 1.000000000000000000, 0.9510565162951535312, 1.000000000000000000, 0.9510565162951535312, 1.000000000000000000, 0.9510565162951535312, 1.000000000000000000, 0.9510565162951535312, 1.000000000000000000, 0.9510565162951535312, 1.000000000000000000, 0.9510565162951535312, 1.000000000000000000, 0.9510565162951535312, 1.000000000000000000, 0.9510565162951535312, 1.000000000000000000, 0.9510565162951535312, 1.000000000000000000, 0.9510565162951535312, 1.000000000000000000, 0.9510565162951535312, 1.000000000000000000, 0.9510565162951535312, 1.000000000000000000, 0.9510565162951535312, 1.000000000000000000, 0.9510565162951535312, 1.000000000000000000, 0.9510565162951535312, 1.000000000000000000, 0.9510565162951535312, 1.000000000000000000, 0.9510565162951535312, 1.000000000000000000, 0.9510565162951535312, 1.000000000000000000, 0.9510565162951535312, 1.000000000000000000, 0.9510565162951535312, 1.000000000000000000, 0.9510565162951535312, 1.000000000000000000, 0.9510565162951535312, 1.000000000000000000, 0.9510565162951535312, 1.000000000000000000, 0.9510565162951535312, 1.000000000000000000, 0.9510565162951535312, 1.000000000000000000, 0.9510565162951535312, 1.000000000000000000, 0.9510565162951535312, 1.000000000000000000, 0.9510565162951535312, 1.000000000000000000, 0.9510565162951535312, 1.000000000000000000, 0.9510565162951535312, 1.000000000000000000, 0.9510565162951535312, 1.000000000000000000, 0.9510565162951535312, 1.000000000000000000, 0.9510565162951535312, 1.000000000000000000, 0.9510565162951535312, 1.000000000000000000, 0.9510565162951535312, 1.000000000000000000, 0.9510565162951535312, 1.000000000000000000, 0.9510565162951535312, 1.000000000000000000, 0.9510565162951535312, 1.000000000000000000, 0.9510565162951535312, 1.000000000000000000, 0.9510565162951535312, 1.000000000000000000, 0.9510565162951535312, 1.000000000000000000, 0.9510565162951535312, 1.000000000000000000, 0.9510565162951535312, 1.000000000000000000, 0.9510565162951535312, 1.000000000000000000, 0.9510565162951535312, 1.000000000000000000, 0.9510565162951535312, 1.000000000000000000, 0.9510565162951535312, 1.000000000000000000, 0.9510565162951535312, 1.000000000000000000, 0.9510565162951535312, 1.000000000000000000, 0.9510565162951535312, 1.000000000000000000, 0.9510565162951535312, 1.000000000000000000, 0.9510565162951535312, 1.000000000000000000, 0.9510565162951535312, 1.000000000000000000, 0.9510565162951535312, 1.000000000000000000, 0.9510565162951535312, 1.000000000000000000, 0.9510565162951535312, 1.000000000000000000, 0.9510565162951535312, 1.000000000000000000, 0.9510565162951535312, 1.000000000000000000, 0.9510565162951535312, 1.000000000000000000, 0.9510565162951535312, 1.000000000000000000, 0.9510565162951535312, 1.000000000000000000, 0.9510565162951535312, 1.000000000000000000, 0.9510565162951535312, 1.000000000000000000, 0.9510565162951535312, 1.000000000000000000, 0.9510565162951535312, 1.000000000000000000, 0.9510565162951535312, 1.000000000000000000, 0.9510565162951535312, 1.000000000000000000, 0.9510565162951535312, 1.000000000000000000, 0.9510565162951535312, 1.000000000000000000, 0.9510565162951535312, 1.000000000000000000, 0.9510565162951535312, 1.000000000000000000, 0.9510565162951535312, 1.000000000000000000, 0.9510565162951535312, 1.000000000000000000, 0.9510565162951535312, 1.000000000000000000, 0.9510565162951535312, 1.000000000000000000, 0.9510565162951535312, 1.000000000000000000, 0.9510565162951535312, 1.000000000000000000, 0.9510565162951535312, 1.000000000000000000, 0.9510565162951535312, 1.000000000000000000, 0.9510565162951535312, 1.000000000000000000, 0.9510565162951535312, 1.000000000000000000, 0.9510565162951535312, 1.000000000000000000, 0.9510565162951535312, 1.000000000000000000, 0.9510565162951535312, 1.000000000000000000, 0.9510565162951535312, 1.000000000000000000, 0.9510565162951535312, 1.000000000000000000, 0.9510565162951535312, 1.000000000000000000, 0.9510565162951535312, 1.000000000000000000, 0.9510565162951535312, 1.000000000000000000, 0.9510565162951535312, 1.000000000000000000, 0.9510565162951535312, 1.000000000000000000, 0.9510565162951535312, 1.000000000000000000, 0.9510565162951535312, 1.000000000000000000, 0.9510565162951535312, 1.000000000000000000, 0.9510565162951535312, 1.000000000000000000, 0.9510565162951535312, 1.000000000000000000, 0.9510565162951535312, 1.000000000000000000, 0.9510565162951535312, 1.000000000000000000, 0.9510565162951535312, 1.000000000000000000, 0.9510565162951535312, 1.000000000000000000, 0.9510565162951535312, 1.000000000000000000, 0.9510565162951535312, 1.000000000000000000, 0.9510565162951535312, 1.000000000000000000, 0.9510565162951535312, 1.000000000000000000, 0.9510565162951535312, 1.000000000000000000, 0.9510565162951535312, 1.000000000000000000, 0.9510565162951535312, 1.000000000000000000, 0.9510565162951535312, 1.000000000000000000, 0.9510565162951535312, 1.000000000000000000, 0.9510565162951535312, 1.000000000000000000, 0.9510565162951535312, 1.000000000000000000, 0.9510565162951535312, 1.000000000000000000, 0.9510565162951535312, 1.000000000000000000, 0.9510565162951535312, 1.000000000000000000, 0.9510565162951535312, 1.000000000000000000, 0.9510565162951535312, 1.000000000000000000, 0.9510565162951535312, 1.000000000000000000, 0.9510565162951535312, 1.000000000000000000, 0.9510565162951535312, 1.000000000000000000, 0.9510565162951535312, 1.000000000000000000, 0.9510565162951535312, 1.000000000000000000, 0.9510565162951535312, 1.000000000000000000, 0.9510565162951535312, 1.000000000000000000, 0.9510565162951535312, 1.000000000000000000, 0.9510565162951535312, 1.000000000000000000, 0.9510565162951535312, 1.000000000000000000, 0.9510565162951535312, 1.000000000000000000, 0.9510565162951535312, 1.000000000000000000, 0.9510565162951535312, 1.000000000000000000, 0.9510565162951535312, 1.000000000000000000, 0.9510565162951535312, 1.000000000000000000, 0.9510565162951535312, 1.000000000000000000, 0.9510565162951535312, 1.000000000000000000, 0.9510565162951535312, 1.000000000000000000, 0.9510565162951535312, 1.000000000000000000, 0.9510565162951535312, 1.000000000000000000, 0.9510565162951535312, 1.000000000000000000, 0.9510565162951535312, 1.000000000000000000, 0.9510565162951535312, 1.000000000000000000, 0.9510565162951535312, 1.000000000000000000, 0.9510565162951535312, 1.000000000000000000, 0.9510565162951535312, 1.000000000000000000, 0.9510565162951535312, 1.000000000000000000, 0.9510565162951535312, 1.000000000000000000, 0.9510565162951535312, 1.000000000000000000, 0.9510565162951535312, 1.000000000000000000, 0.9510565162951535312, 1.000000000000000000, 0.9510565162951535312, 1.000000000000000000, 0.9510565162951535312, 1.000000000000000000, 0.9510565162951535312, 1.000000000000000000, 0.9510565162951535312, 1.000000000000000000, 0.9510565162951535312, 1.000000000000000000, 0.9510565162951535312, 1.000000000000000000, 0.9510565162951535312, 1.000000000000000000, 0.9510565162951535312, 1.000000000000000000, 0.9510565162951535312, 1.000000000000000000, 0.9510565162951535312, 1.000000000000000000, 0.9510565162951535312, 1.000000000000000000, 0.9510565162951535312, 1.000000000000000000, 0.9510565162951535312, 1.000000000000000000, 0.9510565162951535312, 1.000000000000000000, 0.9510565162951535312, 1.000000000000000000, 0.9510565162951535312, 1.000000000000000000, 0.9510565162951535312, 1.000000000000000000, 0.9510565162951535312, 1.000000000000000000, 0.9510565162951535312, 1.000000000000000000, 0.9510565162951535312, 1.000000000000000000, 0.9836246098489007661, 0.9782068950532306628) ) ) 
 REPRESENTATION_ITEM ( '' )  SURFACE ( )  );
#11642=CARTESIAN_POINT ( 'NONE',  ( 42.21948215057684450, 155.1113394311928460, 29.21067981925357060 ) ) ;
#11644=CARTESIAN_POINT ( 'NONE',  ( 46.10157429594899270, 151.7344580088725934, 29.95742577749337343 ) ) ;
#11645=CARTESIAN_POINT ( 'NONE',  ( 41.64333658814960870, 120.9797705074273182, 38.42115945441014446 ) ) ;
#11647=CARTESIAN_POINT ( 'NONE',  ( 38.96631938032478359, 115.0104996726487485, 37.14960608071593384 ) ) ;
#11648=CARTESIAN_POINT ( 'NONE',  ( 39.42975644700377558, 120.4151871740940010, 36.81289934271958941 ) ) ;
#11649=LINE ( 'NONE', #11316, #10432 ) ;
#11652=CARTESIAN_POINT ( 'NONE',  ( 45.22504609509771001, 59.11591859955431971, 30.37668211462113277 ) ) ;
#11653=CARTESIAN_POINT ( 'NONE',  ( 38.58424406990785371, 96.52977050742731535, 35.64915139335015937 ) ) ;
#11655=DIRECTION ( 'NONE',  ( 0.000000000000000000, 1.000000000000000000, 0.000000000000000000 ) ) ;
#11656=ORIENTED_EDGE ( 'NONE', *, *, #11810, .T. ) ;
#11657=CARTESIAN_POINT ( 'NONE',  ( 48.01140435219951996, 85.43445800887255359, 32.58608133808903773 ) ) ;
#11659=CARTESIAN_POINT ( 'NONE',  ( 48.01140435219951996, 143.3604996726487570, 32.58608133808903773 ) ) ;
#11660=CARTESIAN_POINT ( 'NONE',  ( 39.42975644700377558, 99.41518717409400097, 36.81289934271958941 ) ) ;
#11670=CARTESIAN_POINT ( 'NONE',  ( 43.01140435219951286, 146.9604996726487229, 29.21067981925356705 ) ) ;
#11671=CARTESIAN_POINT ( 'NONE',  ( 41.46631938032478359, 78.11049967264874283, 29.45539723777780239 ) ) ;
#11672=CARTESIAN_POINT ( 'NONE',  ( 46.59305225739526435, 149.1797705074273210, 31.60846029578754468 ) ) ;
#11673=CARTESIAN_POINT ( 'NONE',  ( 42.21948215057684450, 63.45757658655229250, 39.21067981925355639 ) ) ;
#11675=CARTESIAN_POINT ( 'NONE',  ( 43.01140435219951286, 141.8651871740940180, 38.86567161673127657 ) ) ;
#11683=CARTESIAN_POINT ( 'NONE',  ( 41.46631938032478359, 134.1844580088725820, 29.45539723777780239 ) ) ;
#11684=CARTESIAN_POINT ( 'NONE',  ( 47.43856463449118621, 121.6151871740940038, 34.21067981925357060 ) ) ;
#11688=CARTESIAN_POINT ( 'NONE',  ( 38.01140435219952707, 146.7844580088725763, 34.21067981925357060 ) ) ;
#11690=CARTESIAN_POINT ( 'NONE',  ( 38.01140435219951996, 110.9344580088725678, 35.83527830041810347 ) ) ;
#11691=CARTESIAN_POINT ( 'NONE',  ( 47.43856463449118621, 154.8797705074273097, 34.21067981925357060 ) ) ;
#11692=CARTESIAN_POINT ( 'NONE',  ( 47.43856463449118621, 70.87977050742732388, 34.21067981925357060 ) ) ;
#11693=CARTESIAN_POINT ( 'NONE',  ( 45.74753988029933538, 128.0651871740940067, 30.44471234641811819 ) ) ;
#11695=CARTESIAN_POINT ( 'NONE',  ( 46.10157429594899270, 86.66049967264872578, 29.95742577749337343 ) ) ;
#11699=CARTESIAN_POINT ( 'NONE',  ( 44.37947211624943833, 91.01518717409399528, 38.42115945441014446 ) ) ;
#11703=CARTESIAN_POINT ( 'NONE',  ( 44.37947211624943833, 61.27977050742732246, 38.42115945441014446 ) ) ;
#11706=EDGE_CURVE ( 'NONE', #1555, #17127, #15286, .T. ) ;
#11709=CARTESIAN_POINT ( 'NONE',  ( 47.43856463449117200, 154.7651871740940237, 32.77220824515698183 ) ) ;
#11711=( BOUNDED_CURVE ( )  B_SPLINE_CURVE ( 1, ( #21668, #18006 ),
 .UNSPECIFIED., .F., .F. ) 
 B_SPLINE_CURVE_WITH_KNOTS ( ( 2, 2 ),
 ( 0.000000000000000000, 1.000000000000000000 ),
 .UNSPECIFIED. ) 
 CURVE ( )  GEOMETRIC_REPRESENTATION_ITEM ( )  RATIONAL_B_SPLINE_CURVE ( ( 0.9782066976764483002, 0.9782066976764483002 ) ) 
 REPRESENTATION_ITEM ( '' )  );
#11712=CARTESIAN_POINT ( 'NONE',  ( 39.42975644700377558, 111.6797705074273210, 36.81289934271958941 ) ) ;
#11716=ORIENTED_EDGE ( 'NONE', *, *, #20429, .F. ) ;
#11717=CARTESIAN_POINT ( 'NONE',  ( 40.27526882409969033, 117.8297705074273267, 37.97664729208901946 ) ) ;
#11719=CARTESIAN_POINT ( 'NONE',  ( 45.74753988029933538, 157.1651871740940010, 37.97664729208901946 ) ) ;
#11721=CARTESIAN_POINT ( 'NONE',  ( 38.01140435219952707, 107.6344580088725706, 32.58608133808903773 ) ) ;
#11725=CARTESIAN_POINT ( 'NONE',  ( 42.21948215057684450, 157.3836182503284533, 39.21067981925355639 ) ) ;
#11730=CARTESIAN_POINT ( 'NONE',  ( 46.59305225739526435, 91.57977050742731251, 36.81289934271958941 ) ) ;
#11733=CARTESIAN_POINT ( 'NONE',  ( 44.37947211624943833, 91.01518717409399528, 38.42115945441014446 ) ) ;
#11735=ORIENTED_EDGE ( 'NONE', *, *, #4729, .T. ) ;
#11738=CARTESIAN_POINT ( 'NONE',  ( 45.74753988029934249, 143.3297705074272983, 30.44471234641812174 ) ) ;
#11741=CARTESIAN_POINT ( 'NONE',  ( 45.74753988029934249, 61.42977050742731393, 37.97664729208901235 ) ) ;
#11743=CARTESIAN_POINT ( 'NONE',  ( 41.64333658814960870, 143.7797705074273154, 30.00020018409699318 ) ) ;
#11744=CARTESIAN_POINT ( 'NONE',  ( 47.43856463449117200, 95.02977050742730114, 32.77220824515698183 ) ) ;
#11746=CARTESIAN_POINT ( 'NONE',  ( 38.96631938032478359, 105.4104996726487400, 31.27175355779120025 ) ) ;
#11747=CARTESIAN_POINT ( 'NONE',  ( 43.01140435219951286, 59.36518717409399670, 29.55568802177586463 ) ) ;
#11752=CARTESIAN_POINT ( 'NONE',  ( 38.96631938032478359, 112.0104996726487485, 37.14960608071593384 ) ) ;
#11753=EDGE_CURVE ( 'NONE', #4439, #3828, #18594, .T. ) ;
#11754=CARTESIAN_POINT ( 'NONE',  ( 41.46631938032478359, 141.3844580088725991, 38.96596240072933170 ) ) ;
#11755=CARTESIAN_POINT ( 'NONE',  ( 47.43856463449117200, 125.0297705074273011, 32.77220824515698183 ) ) ;
#11758=CARTESIAN_POINT ( 'NONE',  ( 46.59305225739526435, 118.3151871740940067, 36.81289934271958941 ) ) ;
#11765=CARTESIAN_POINT ( 'NONE',  ( 39.42975644700377558, 84.07977050742732672, 31.60846029578754468 ) ) ;
#11772=CARTESIAN_POINT ( 'NONE',  ( 38.01140435219951996, 74.93445800887258201, 35.83527830041810347 ) ) ;
#11773=CARTESIAN_POINT ( 'NONE',  ( 41.46631938032478359, 60.38445800887257064, 38.96596240072933170 ) ) ;
#11774=CARTESIAN_POINT ( 'NONE',  ( 38.96631938032478359, 139.0104996726487627, 37.14960608071593384 ) ) ;
#11775=CARTESIAN_POINT ( 'NONE',  ( 43.01140435219951286, 87.86518717409397539, 38.86567161673127657 ) ) ;
#11781=EDGE_CURVE ( 'NONE', #5965, #7305, #16272, .T. ) ;
#11783=CARTESIAN_POINT ( 'NONE',  ( 46.10157429594899270, 145.7604996726487627, 38.46393386101375711 ) ) ;
#11784=CARTESIAN_POINT ( 'NONE',  ( 46.59305225739526435, 155.1797705074273210, 31.60846029578754468 ) ) ;
#11787=CARTESIAN_POINT ( 'NONE',  ( 44.37947211624943833, 146.2151871740940123, 30.00020018409699318 ) ) ;
#11790=EDGE_CURVE ( 'NONE', #4098, #11964, #20099, .T. ) ;
#11795=CARTESIAN_POINT ( 'NONE',  ( 43.01140435219951286, 134.0344580088725763, 29.21067981925356705 ) ) ;
#11796=CARTESIAN_POINT ( 'NONE',  ( 45.74753988029933538, 124.1651871740940152, 37.97664729208901946 ) ) ;
#11797=VERTEX_POINT ( 'NONE', #11179 ) ;
#11801=CARTESIAN_POINT ( 'NONE',  ( 38.01140435219951996, 98.63445800887255643, 32.58608133808903773 ) ) ;
#11802=CARTESIAN_POINT ( 'NONE',  ( 41.64333658814960870, 158.7797705074273438, 30.00020018409699318 ) ) ;
#11803=CARTESIAN_POINT ( 'NONE',  ( 38.58424406990786082, 69.37977050742730967, 34.21067981925357060 ) ) ;
#11804=CARTESIAN_POINT ( 'NONE',  ( 43.01140435219951286, 128.3651871740940180, 29.55568802177586463 ) ) ;
#11806=CARTESIAN_POINT ( 'NONE',  ( 43.01140435219951286, 80.96049967264872294, 28.95336869806222779 ) ) ;
#11809=EDGE_CURVE ( 'NONE', #14927, #13022, #14729, .T. ) ;
#11810=EDGE_CURVE ( 'NONE', #17093, #1013, #20894, .T. ) ;
#11812=CARTESIAN_POINT ( 'NONE',  ( 43.01140435219950575, 139.4604996726487514, 39.21067981925356349 ) ) ;
#11813=CARTESIAN_POINT ( 'NONE',  ( 47.43856463449117200, 82.46518717409398391, 35.64915139335016647 ) ) ;
#11817=CARTESIAN_POINT ( 'NONE',  ( 43.01140435219951286, 61.12977050742731677, 38.86567161673127657 ) ) ;
#11821=ORIENTED_EDGE ( 'NONE', *, *, #16085, .T. ) ;
#11822=CARTESIAN_POINT ( 'NONE',  ( 38.58424406990784661, 150.2651871740940237, 35.64915139335016647 ) ) ;
#11824=CARTESIAN_POINT ( 'NONE',  ( 44.37947211624943833, 115.2797705074273296, 38.42115945441014446 ) ) ;
#11830=CARTESIAN_POINT ( 'NONE',  ( 45.74753988029933538, 118.4297705074272926, 37.97664729208901946 ) ) ;
#11831=CARTESIAN_POINT ( 'NONE',  ( 42.21948215057684450, 126.0373810949690210, 29.21067981925356705 ) ) ;
#11832=CARTESIAN_POINT ( 'NONE',  ( 45.74753988029933538, 86.32977050742729830, 30.44471234641811819 ) ) ;
#11833=CARTESIAN_POINT ( 'NONE',  ( 40.27526882409969033, 155.6651871740940010, 30.44471234641811819 ) ) ;
#11841=CARTESIAN_POINT ( 'NONE',  ( 46.10157429594899270, 97.73445800887256496, 29.95742577749336988 ) ) ;
#11844=CARTESIAN_POINT ( 'NONE',  ( 46.59305225739526435, 98.17977050742732104, 31.60846029578754468 ) ) ;
#11848=CARTESIAN_POINT ( 'NONE',  ( 41.64333658814960870, 86.51518717409399528, 30.00020018409699318 ) ) ;
#11850=EDGE_LOOP ( 'NONE', ( #17237, #5349, #3753, #9045 ) ) ;
#11854=CARTESIAN_POINT ( 'NONE',  ( 38.96631938032478359, 120.0844580088725735, 37.14960608071593384 ) ) ;
#11855=ORIENTED_EDGE ( 'NONE', *, *, #2604, .F. ) ;
#11857=CARTESIAN_POINT ( 'NONE',  ( 45.74753988029933538, 149.3297705074273267, 30.44471234641811819 ) ) ;
#11858=CARTESIAN_POINT ( 'NONE',  ( 40.27526882409969033, 98.92977050742732104, 30.44471234641811819 ) ) ;
#11860=CARTESIAN_POINT ( 'NONE',  ( 43.80332655382219542, 152.8836182503285102, 29.21067981925356705 ) ) ;
#11863=CARTESIAN_POINT ( 'NONE',  ( 38.01140435219952707, 153.7104996726487514, 34.21067981925357060 ) ) ;
#11864=CARTESIAN_POINT ( 'NONE',  ( 41.46631938032478359, 109.3104996726487457, 38.96596240072933170 ) ) ;
#11867=CARTESIAN_POINT ( 'NONE',  ( 47.05648932407426344, 145.5844580088725877, 31.27175355779120025 ) ) ;
#11868=CARTESIAN_POINT ( 'NONE',  ( 38.58424406990784661, 126.2297705074273040, 32.77220824515698183 ) ) ;
#11872=CARTESIAN_POINT ( 'NONE',  ( 41.64333658814960870, 120.7151871740939981, 38.42115945441014446 ) ) ;
#11877=CARTESIAN_POINT ( 'NONE',  ( 47.43856463449117911, 89.02977050742731535, 32.77220824515697473 ) ) ;
#11878=EDGE_CURVE ( 'NONE', #6509, #8092, #640, .T. ) ;
#11882=CARTESIAN_POINT ( 'NONE',  ( 46.10157429594899270, 69.83445800887255928, 38.46393386101376421 ) ) ;
#11885=CARTESIAN_POINT ( 'NONE',  ( 39.92123440845004723, 127.1604996726487542, 38.46393386101376421 ) ) ;
#11886=CARTESIAN_POINT ( 'NONE',  ( 45.74753988029933538, 85.16518717409400097, 37.97664729208901946 ) ) ;
#11890=CARTESIAN_POINT ( 'NONE',  ( 43.01140435219951286, 117.5344580088725763, 39.21067981925356349 ) ) ;
#11891=CARTESIAN_POINT ( 'NONE',  ( 43.01140435219951286, 105.5344580088725621, 39.21067981925356349 ) ) ;
#11892=CARTESIAN_POINT ( 'NONE',  ( 43.01140435219951286, 67.46049967264873715, 39.21067981925356349 ) ) ;
#11894=CARTESIAN_POINT ( 'NONE',  ( 47.43856463449118621, 151.8797705074273097, 34.21067981925357060 ) ) ;
#11897=CARTESIAN_POINT ( 'NONE',  ( 46.59305225739526435, 142.9151871740940294, 31.60846029578754468 ) ) ;
#11901=CARTESIAN_POINT ( 'NONE',  ( 38.58424406990785371, 62.96518717409399812, 32.77220824515697473 ) ) ;
#11904=CARTESIAN_POINT ( 'NONE',  ( 43.01140435219951286, 123.5344580088725621, 39.21067981925356349 ) ) ;
#11905=CARTESIAN_POINT ( 'NONE',  ( 46.59305225739526435, 127.9151871740940010, 31.60846029578754468 ) ) ;
#11906=( BOUNDED_CURVE ( )  B_SPLINE_CURVE ( 2, ( #6275, #14758, #13007, #19727, #11564, #3195, #21500, #1540, #11448, #3306, #8272, #18175, #6621 ),
 .UNSPECIFIED., .F., .F. ) 
 B_SPLINE_CURVE_WITH_KNOTS ( ( 3, 2, 2, 2, 2, 2, 3 ),
 ( 0.4191176470588235392, 0.4205882352941176516, 0.4235294117647058765, 0.4264705882352941013, 0.4294117647058823262, 0.4323529411764706065, 0.4338235294117647189 ),
 .UNSPECIFIED. ) 
 CURVE ( )  GEOMETRIC_REPRESENTATION_ITEM ( )  RATIONAL_B_SPLINE_CURVE ( ( 0.9755282581475768211, 0.9755282581475768211, 1.000000000000000000, 0.9510565162951535312, 1.000000000000000000, 0.9510565162951535312, 1.000000000000000000, 0.9510565162951535312, 1.000000000000000000, 0.9510565162951535312, 1.000000000000000000, 0.9755282581475768211, 0.9755282581475768211 ) ) 
 REPRESENTATION_ITEM ( '' )  );
#11909=CARTESIAN_POINT ( 'NONE',  ( 41.46631938032478359, 146.1844580088725820, 29.45539723777780239 ) ) ;
#11911=CARTESIAN_POINT ( 'NONE',  ( 44.55648932407425633, 97.88445800887257064, 29.45539723777780239 ) ) ;
#11912=CARTESIAN_POINT ( 'NONE',  ( 39.42975644700377558, 156.6797705074273210, 36.81289934271958941 ) ) ;
#11913=CARTESIAN_POINT ( 'NONE',  ( 43.01140435219951286, 157.4604996726487229, 39.46799094044489209 ) ) ;
#11914=CARTESIAN_POINT ( 'NONE',  ( 45.74753988029933538, 113.0651871740939924, 30.44471234641811819 ) ) ;
#11917=CARTESIAN_POINT ( 'NONE',  ( 43.01140435219951286, 79.46049967264873715, 39.46799094044489209 ) ) ;
#11918=CARTESIAN_POINT ( 'NONE',  ( 48.01140435219951996, 148.4344580088725536, 32.58608133808903773 ) ) ;
#11919=CARTESIAN_POINT ( 'NONE',  ( 43.01140435219951286, 98.96049967264873715, 29.21067981925356705 ) ) ;
#11921=CARTESIAN_POINT ( 'NONE',  ( 38.58424406990784661, 80.96518717409399812, 32.77220824515698183 ) ) ;
#11922=DIRECTION ( 'NONE',  ( 0.000000000000000000, 1.000000000000000000, 0.000000000000000000 ) ) ;
#11923=CARTESIAN_POINT ( 'NONE',  ( 48.01140435219951996, 121.1344580088725564, 35.83527830041810347 ) ) ;
#11924=CARTESIAN_POINT ( 'NONE',  ( 43.01140435219951286, 107.9604996726487229, 29.21067981925356705 ) ) ;
#11930=CARTESIAN_POINT ( 'NONE',  ( 41.64333658814960870, 156.7151871740939839, 38.42115945441014446 ) ) ;
#11932=CARTESIAN_POINT ( 'NONE',  ( 47.43856463449118621, 118.8797705074273239, 34.21067981925357060 ) ) ;
#11942=CARTESIAN_POINT ( 'NONE',  ( 46.59305225739526435, 142.3151871740940067, 36.81289934271958941 ) ) ;
#11947=CARTESIAN_POINT ( 'NONE',  ( 47.05648932407426344, 101.5104996726487485, 31.27175355779120025 ) ) ;
#11948=LINE ( 'NONE', #12156, #20971 ) ;
#11949=CARTESIAN_POINT ( 'NONE',  ( 47.05648932407426344, 96.98445800887257917, 37.14960608071593384 ) ) ;
#11951=CARTESIAN_POINT ( 'NONE',  ( 47.43856463449117200, 98.02977050742731535, 32.77220824515698183 ) ) ;
#11954=CARTESIAN_POINT ( 'NONE',  ( 44.37947211624943833, 76.01518717409399528, 38.42115945441014446 ) ) ;
#11956=DIRECTION ( 'NONE',  ( 0.000000000000000000, 0.000000000000000000, 1.000000000000000000 ) ) ;
#11959=CYLINDRICAL_SURFACE ( 'NONE', #18364, 4.999999999999997335 ) ;
#11963=CARTESIAN_POINT ( 'NONE',  ( 38.58424406990785371, 60.22977050742731109, 32.77220824515697473 ) ) ;
#11964=VERTEX_POINT ( 'NONE', #18115 ) ;
#11965=CARTESIAN_POINT ( 'NONE',  ( 44.37947211624943833, 139.2797705074273154, 38.42115945441014446 ) ) ;
#11968=CARTESIAN_POINT ( 'NONE',  ( 43.01140435219953417, 142.4604996726487514, 39.21067981925356349 ) ) ;
#11973=CARTESIAN_POINT ( 'NONE',  ( 43.01140435219951286, 123.5344580088725621, 39.21067981925356349 ) ) ;
#11975=CARTESIAN_POINT ( 'NONE',  ( 47.05648932407426344, 138.9844580088725650, 37.14960608071593384 ) ) ;
#11976=CARTESIAN_POINT ( 'NONE',  ( 39.42975644700377558, 120.0797705074273267, 31.60846029578754468 ) ) ;
#11978=CARTESIAN_POINT ( 'NONE',  ( 41.46631938032478359, 141.3844580088725991, 38.96596240072933170 ) ) ;
#11979=CARTESIAN_POINT ( 'NONE',  ( 43.01140435219951286, 108.8651871740939896, 38.86567161673127657 ) ) ;
#11980=VECTOR ( 'NONE', #16201, 1000.000000000000000 ) ;
#11981=CARTESIAN_POINT ( 'NONE',  ( 38.01140435219952707, 125.7844580088725905, 34.21067981925357060 ) ) ;
#11984=CARTESIAN_POINT ( 'NONE',  ( 46.59305225739526435, 86.17977050742732104, 31.60846029578754468 ) ) ;
#11985=ORIENTED_EDGE ( 'NONE', *, *, #4984, .F. ) ;
#11986=CYLINDRICAL_SURFACE ( 'NONE', #572, 4.999999999999997335 ) ;
#11987=CARTESIAN_POINT ( 'NONE',  ( 48.01140435219951996, 70.13445800887255643, 35.83527830041810347 ) ) ;
#11989=CARTESIAN_POINT ( 'NONE',  ( 46.10157429594899270, 127.7604996726487485, 38.46393386101376421 ) ) ;
#11990=CARTESIAN_POINT ( 'NONE',  ( 43.01140435219951286, 89.36518717409398960, 29.55568802177586463 ) ) ;
#11994=CARTESIAN_POINT ( 'NONE',  ( 38.01140435219952707, 116.9344580088725820, 35.83527830041809636 ) ) ;
#11996=DIRECTION ( 'NONE',  ( 0.000000000000000000, 1.000000000000000000, 0.000000000000000000 ) ) ;
#11998=CARTESIAN_POINT ( 'NONE',  ( 38.58424406990784661, 153.2297705074273608, 32.77220824515698183 ) ) ;
#11999=CARTESIAN_POINT ( 'NONE',  ( 47.43856463449117200, 107.0297705074273154, 32.77220824515698183 ) ) ;
#12001=CARTESIAN_POINT ( 'NONE',  ( 44.37947211624943833, 137.2151871740940123, 30.00020018409699318 ) ) ;
#12002=DIRECTION ( 'NONE',  ( 0.000000000000000000, 0.000000000000000000, 1.000000000000000000 ) ) ;
#12004=CARTESIAN_POINT ( 'NONE',  ( 38.58424406990785371, 60.26518717409400239, 35.64915139335015937 ) ) ;
#12006=CARTESIAN_POINT ( 'NONE',  ( 41.64333658814960870, 113.5151871740940095, 30.00020018409699318 ) ) ;
#12012=CARTESIAN_POINT ( 'NONE',  ( 46.10157429594899270, 102.8344580088725877, 38.46393386101376421 ) ) ;
#12014=CARTESIAN_POINT ( 'NONE',  ( 38.58424406990786082, 159.3797705074273381, 34.21067981925357060 ) ) ;
#12015=CARTESIAN_POINT ( 'NONE',  ( 47.43856463449117200, 62.02977050742732246, 32.77220824515698183 ) ) ;
#12016=CARTESIAN_POINT ( 'NONE',  ( 45.74753988029933538, 112.1651871740939868, 37.97664729208901946 ) ) ;
#12018=CARTESIAN_POINT ( 'NONE',  ( 44.55648932407425633, 76.61049967264874283, 38.96596240072933170 ) ) ;
#12021=DIRECTION ( 'NONE',  ( 0.000000000000000000, 1.000000000000000000, 0.000000000000000000 ) ) ;
#12022=CARTESIAN_POINT ( 'NONE',  ( 40.27526882409969033, 74.66518717409397254, 30.44471234641811819 ) ) ;
#12026=EDGE_CURVE ( 'NONE', #11964, #711, #6217, .T. ) ;
#12028=( BOUNDED_CURVE ( )  B_SPLINE_CURVE ( 2, ( #7082, #8847, #20631, #7516, #10819, #9058, #14217, #17197, #15454, #12244, #17306, #12571, #2218 ),
 .UNSPECIFIED., .F., .F. ) 
 B_SPLINE_CURVE_WITH_KNOTS ( ( 3, 2, 2, 2, 2, 2, 3 ),
 ( 0.5367647058823529216, 0.5382352941176470340, 0.5411764705882352589, 0.5441176470588234837, 0.5470588235294118196, 0.5500000000000000444, 0.5514705882352941568 ),
 .UNSPECIFIED. ) 
 CURVE ( )  GEOMETRIC_REPRESENTATION_ITEM ( )  RATIONAL_B_SPLINE_CURVE ( ( 0.9755282581475768211, 0.9755282581475768211, 1.000000000000000000, 0.9510565162951535312, 1.000000000000000000, 0.9510565162951535312, 1.000000000000000000, 0.9510565162951535312, 1.000000000000000000, 0.9510565162951535312, 1.000000000000000000, 0.9755282581475768211, 0.9755282581475768211 ) ) 
 REPRESENTATION_ITEM ( '' )  );
#12034=CARTESIAN_POINT ( 'NONE',  ( 41.64333658814960870, 153.7151871740940123, 38.42115945441014446 ) ) ;
#12038=CARTESIAN_POINT ( 'NONE',  ( 38.58424406990785371, 102.5297705074273154, 35.64915139335015937 ) ) ;
#12044=EDGE_CURVE ( 'NONE', #14006, #11408, #18672, .T. ) ;
#12046=CARTESIAN_POINT ( 'NONE',  ( 38.01140435219952707, 128.7844580088725763, 34.21067981925357060 ) ) ;
#12047=CARTESIAN_POINT ( 'NONE',  ( 43.01140435219951286, 143.3651871740939896, 29.55568802177586463 ) ) ;
#12054=CARTESIAN_POINT ( 'NONE',  ( 45.74753988029933538, 82.42977050742732104, 37.97664729208901946 ) ) ;
#12057=CARTESIAN_POINT ( 'NONE',  ( 39.42975644700377558, 81.41518717409400097, 36.81289934271958941 ) ) ;
#12058=LINE ( 'NONE', #6478, #8888 ) ;
#12062=EDGE_CURVE ( 'NONE', #3065, #8092, #1371, .T. ) ;
#12063=CARTESIAN_POINT ( 'NONE',  ( 44.55648932407425633, 122.8104996726487457, 29.45539723777780239 ) ) ;
#12064=CARTESIAN_POINT ( 'NONE',  ( 46.59305225739526435, 142.5797705074273267, 36.81289934271958941 ) ) ;
#12067=CARTESIAN_POINT ( 'NONE',  ( 43.01140435219951286, 120.5344580088725763, 39.21067981925356349 ) ) ;
#12069=CARTESIAN_POINT ( 'NONE',  ( 47.43856463449118621, 133.8797705074273381, 34.21067981925357060 ) ) ;
#12070=EDGE_CURVE ( 'NONE', #15353, #9281, #6443, .T. ) ;
#12071=CARTESIAN_POINT ( 'NONE',  ( 40.27526882409969033, 62.66518717409400097, 30.44471234641811819 ) ) ;
#12073=CARTESIAN_POINT ( 'NONE',  ( 43.01140435219951286, 126.5344580088725621, 39.21067981925356349 ) ) ;
#12074=CARTESIAN_POINT ( 'NONE',  ( 47.43856463449118621, 100.6151871740940180, 34.21067981925357060 ) ) ;
#12075=CARTESIAN_POINT ( 'NONE',  ( 38.96631938032478359, 154.0104996726487343, 37.14960608071593384 ) ) ;
#12076=CARTESIAN_POINT ( 'NONE',  ( 41.46631938032478359, 122.1844580088725962, 29.45539723777780239 ) ) ;
#12080=CARTESIAN_POINT ( 'NONE',  ( 38.96631938032478359, 138.0844580088725877, 37.14960608071593384 ) ) ;
#12081=CARTESIAN_POINT ( 'NONE',  ( 47.43856463449118621, 124.8797705074273239, 34.21067981925357060 ) ) ;
#12083=CARTESIAN_POINT ( 'NONE',  ( 39.92123440845005433, 140.3344580088725877, 29.95742577749336988 ) ) ;
#12084=CARTESIAN_POINT ( 'NONE',  ( 46.59305225739526435, 103.3151871740940067, 36.81289934271958941 ) ) ;
#12085=CARTESIAN_POINT ( 'NONE',  ( 38.96631938032478359, 126.0844580088725735, 37.14960608071593384 ) ) ;
#12089=CARTESIAN_POINT ( 'NONE',  ( 41.64333658814960870, 84.97977050742731819, 38.42115945441014446 ) ) ;
#12090=CARTESIAN_POINT ( 'NONE',  ( 43.80332655382221674, 110.8836182503284675, 29.21067981925357060 ) ) ;
#12091=CARTESIAN_POINT ( 'NONE',  ( 38.01140435219952707, 71.78445800887257633, 34.21067981925357060 ) ) ;
#12093=CARTESIAN_POINT ( 'NONE',  ( 47.05648932407426344, 134.5104996726487343, 31.27175355779120025 ) ) ;
#12094=CARTESIAN_POINT ( 'NONE',  ( 44.37947211624943833, 91.01518717409399528, 38.42115945441014446 ) ) ;
#12102=CARTESIAN_POINT ( 'NONE',  ( 41.46631938032478359, 92.18445800887258201, 29.45539723777780239 ) ) ;
#12103=CARTESIAN_POINT ( 'NONE',  ( 43.01140435219953417, 142.4604996726487514, 39.21067981925356349 ) ) ;
#12104=CARTESIAN_POINT ( 'NONE',  ( 40.27526882409969033, 149.9297705074272926, 30.44471234641811819 ) ) ;
#12105=CARTESIAN_POINT ( 'NONE',  ( 43.01140435219951286, 106.1297705074272955, 38.86567161673127657 ) ) ;
#12107=CARTESIAN_POINT ( 'NONE',  ( 47.43856463449117911, 139.4651871740940123, 35.64915139335015937 ) ) ;
#12108=CARTESIAN_POINT ( 'NONE',  ( 43.80332655382220253, 66.61133943119283174, 39.21067981925355639 ) ) ;
#12110=CARTESIAN_POINT ( 'NONE',  ( 47.05648932407426344, 90.98445800887257917, 37.14960608071593384 ) ) ;
#12111=AXIS2_PLACEMENT_3D ( 'NONE', #5282, #11996, #3956 ) ;
#12114=CARTESIAN_POINT ( 'NONE',  ( 46.59305225739526435, 115.3151871740940067, 36.81289934271958941 ) ) ;
#12115=ORIENTED_EDGE ( 'NONE', *, *, #20597, .F. ) ;
#12117=ORIENTED_EDGE ( 'NONE', *, *, #13885, .F. ) ;
#12118=CARTESIAN_POINT ( 'NONE',  ( 38.01140435219952707, 104.7844580088725763, 34.21067981925357060 ) ) ;
#12119=CARTESIAN_POINT ( 'NONE',  ( 43.01140435219951286, 155.9604996726487229, 28.95336869806222779 ) ) ;
#12120=CARTESIAN_POINT ( 'NONE',  ( 41.64333658814960870, 116.5151871740940095, 30.00020018409699318 ) ) ;
#12122=AXIS2_PLACEMENT_3D ( 'NONE', #20046, #10114, #18263 ) ;
#12123=CARTESIAN_POINT ( 'NONE',  ( 38.01140435219951996, 69.86049967264871441, 35.83527830041810347 ) ) ;
#12125=CARTESIAN_POINT ( 'NONE',  ( 47.05648932407426344, 135.9844580088725934, 37.14960608071593384 ) ) ;
#12128=CARTESIAN_POINT ( 'NONE',  ( 40.27526882409969033, 78.56518717409399244, 37.97664729208901946 ) ) ;
#12129=CARTESIAN_POINT ( 'NONE',  ( 42.21948215057684450, 64.38361825032846752, 39.21067981925355639 ) ) ;
#12132=VERTEX_POINT ( 'NONE', #8868 ) ;
#12136=CARTESIAN_POINT ( 'NONE',  ( 44.37947211624943833, 145.0151871740939953, 38.42115945441014446 ) ) ;
#12138=CARTESIAN_POINT ( 'NONE',  ( 47.43856463449118621, 103.8797705074273239, 34.21067981925357060 ) ) ;
#12143=CARTESIAN_POINT ( 'NONE',  ( 38.58424406990784661, 111.2297705074273324, 32.77220824515698183 ) ) ;
#12145=CARTESIAN_POINT ( 'NONE',  ( 42.21948215057684450, 127.3836182503284533, 39.21067981925355639 ) ) ;
#12148=CARTESIAN_POINT ( 'NONE',  ( 47.43856463449118621, 148.6151871740939896, 34.21067981925357060 ) ) ;
#12149=CARTESIAN_POINT ( 'NONE',  ( 38.96631938032478359, 103.0104996726487485, 37.14960608071593384 ) ) ;
#12155=CARTESIAN_POINT ( 'NONE',  ( 43.01140435219951996, 10.71049967264875491, 34.21067981925357060 ) ) ;
#12156=CARTESIAN_POINT ( 'NONE',  ( 43.01140435219951996, 10.71049967264875491, 39.21067981925356349 ) ) ;
#12157=CARTESIAN_POINT ( 'NONE',  ( 43.01140435219951286, 152.0344580088725763, 29.21067981925356705 ) ) ;
#12159=CARTESIAN_POINT ( 'NONE',  ( 47.43856463449117200, 83.02977050742730114, 32.77220824515698183 ) ) ;
#12165=CARTESIAN_POINT ( 'NONE',  ( 39.92123440845005433, 68.33445800887258770, 29.95742577749336988 ) ) ;
#12166=CARTESIAN_POINT ( 'NONE',  ( 43.80332655382220253, 121.5373810949690068, 39.21067981925355639 ) ) ;
#12167=CARTESIAN_POINT ( 'NONE',  ( 43.01140435219951286, 131.6297705074273381, 29.55568802177586107 ) ) ;
#12169=ORIENTED_EDGE ( 'NONE', *, *, #192, .T. ) ;
#12170=CARTESIAN_POINT ( 'NONE',  ( 38.96631938032478359, 119.4844580088725792, 31.27175355779120025 ) ) ;
#12171=ORIENTED_EDGE ( 'NONE', *, *, #21718, .T. ) ;
#12172=CARTESIAN_POINT ( 'NONE',  ( 39.42975644700377558, 132.0797705074273267, 31.60846029578754468 ) ) ;
#12173=CARTESIAN_POINT ( 'NONE',  ( 45.74753988029933538, 91.42977050742732104, 37.97664729208901946 ) ) ;
#12174=CARTESIAN_POINT ( 'NONE',  ( 47.05648932407426344, 155.5104996726487343, 31.27175355779120025 ) ) ;
#12180=CARTESIAN_POINT ( 'NONE',  ( 38.58424406990784661, 93.26518717409399528, 35.64915139335016647 ) ) ;
#12182=CARTESIAN_POINT ( 'NONE',  ( 43.01140435219951286, 146.9604996726487229, 29.21067981925356705 ) ) ;
#12185=CARTESIAN_POINT ( 'NONE',  ( 44.55648932407425633, 144.6844580088725820, 38.96596240072933170 ) ) ;
#12186=CARTESIAN_POINT ( 'NONE',  ( 43.01140435219951286, 109.1297705074273239, 38.86567161673127657 ) ) ;
#12189=CARTESIAN_POINT ( 'NONE',  ( 47.43856463449117911, 109.7651871740940095, 32.77220824515697473 ) ) ;
#12190=ORIENTED_EDGE ( 'NONE', *, *, #14444, .T. ) ;
#12193=ADVANCED_FACE ( 'NONE', ( #3360 ), #17009, .T. ) ;
#12197=CARTESIAN_POINT ( 'NONE',  ( 43.01140435219951286, 88.12977050742732388, 38.86567161673127657 ) ) ;
#12202=CARTESIAN_POINT ( 'NONE',  ( 44.55648932407425633, 73.88445800887258486, 29.45539723777780239 ) ) ;
#12204=CARTESIAN_POINT ( 'NONE',  ( 48.01140435219951996, 128.3604996726487286, 32.58608133808903773 ) ) ;
#12205=CARTESIAN_POINT ( 'NONE',  ( 38.58424406990784661, 90.26518717409398107, 35.64915139335016647 ) ) ;
#12209=CARTESIAN_POINT ( 'NONE',  ( 39.92123440845005433, 94.16049967264872578, 38.46393386101375711 ) ) ;
#12210=CARTESIAN_POINT ( 'NONE',  ( 43.80332655382220253, 126.6113394311928460, 39.21067981925355639 ) ) ;
#12214=CARTESIAN_POINT ( 'NONE',  ( 40.27526882409969033, 146.9297705074273210, 30.44471234641811819 ) ) ;
#12215=CARTESIAN_POINT ( 'NONE',  ( 39.42975644700377558, 102.0797705074273267, 31.60846029578754468 ) ) ;
#12217=CARTESIAN_POINT ( 'NONE',  ( 45.74753988029934249, 134.0651871740939498, 30.44471234641812174 ) ) ;
#12218=CARTESIAN_POINT ( 'NONE',  ( 43.01140435219951996, 170.7104996726487514, 34.21067981925357060 ) ) ;
#12220=CARTESIAN_POINT ( 'NONE',  ( 47.43856463449117200, 64.72977050742731819, 35.64915139335016647 ) ) ;
#12222=( BOUNDED_CURVE ( )  B_SPLINE_CURVE ( 2, ( #6866, #16660, #24, #20205, #15456, #5098, #10064, #15007, #15347, #13572, #10392, #356, #1893 ),
 .UNSPECIFIED., .F., .F. ) 
 B_SPLINE_CURVE_WITH_KNOTS ( ( 3, 2, 2, 2, 2, 2, 3 ),
 ( 0.2573529411764705621, 0.2588235294117647300, 0.2617647058823529549, 0.2647058823529411797, 0.2676470588235294046, 0.2705882352941176294, 0.2720588235294117974 ),
 .UNSPECIFIED. ) 
 CURVE ( )  GEOMETRIC_REPRESENTATION_ITEM ( )  RATIONAL_B_SPLINE_CURVE ( ( 0.9755282581475768211, 0.9755282581475763770, 1.000000000000000000, 0.9510565162951535312, 1.000000000000000000, 0.9510565162951535312, 1.000000000000000000, 0.9510565162951535312, 1.000000000000000000, 0.9510565162951535312, 1.000000000000000000, 0.9755282581475763770, 0.9755282581475768211 ) ) 
 REPRESENTATION_ITEM ( '' )  );
#12226=CARTESIAN_POINT ( 'NONE',  ( 47.43856463449118621, 118.6151871740940038, 34.21067981925357060 ) ) ;
#12230=CARTESIAN_POINT ( 'NONE',  ( 43.01140435219951286, 76.46049967264873715, 39.21067981925356349 ) ) ;
#12232=CARTESIAN_POINT ( 'NONE',  ( 48.01140435219951996, 106.1344580088725849, 35.83527830041810347 ) ) ;
#12233=CARTESIAN_POINT ( 'NONE',  ( 38.58424406990785371, 150.5297705074272869, 35.64915139335015937 ) ) ;
#12234=CARTESIAN_POINT ( 'NONE',  ( 45.22505347682931642, 59.38050100342833559, 30.37668637662400073 ) ) ;
#12235=CARTESIAN_POINT ( 'NONE',  ( 43.01140435219951286, 111.8651871740939896, 38.86567161673127657 ) ) ;
#12238=CARTESIAN_POINT ( 'NONE',  ( 47.05648932407426344, 71.51049967264873430, 31.27175355779120025 ) ) ;
#12240=CARTESIAN_POINT ( 'NONE',  ( 47.05648932407426344, 136.5844580088725877, 31.27175355779120025 ) ) ;
#12241=CARTESIAN_POINT ( 'NONE',  ( 43.01140435219951286, 124.4604996726487371, 39.21067981925356349 ) ) ;
#12243=CARTESIAN_POINT ( 'NONE',  ( 38.58424406990784661, 81.26518717409398107, 35.64915139335016647 ) ) ;
#12244=CARTESIAN_POINT ( 'NONE',  ( 46.10157429594899270, 103.7604996726487485, 38.46393386101375711 ) ) ;
#12245=VECTOR ( 'NONE', #16083, 1000.000000000000000 ) ;
#12247=CARTESIAN_POINT ( 'NONE',  ( 45.22505347682923116, 59.38050100342834270, 30.37668637662395099 ) ) ;
#12251=CARTESIAN_POINT ( 'NONE',  ( 39.42975644700377558, 146.8151871740940067, 31.60846029578754468 ) ) ;
#12253=CARTESIAN_POINT ( 'NONE',  ( 44.37947211624943833, 103.2797705074273154, 38.42115945441014446 ) ) ;
#12255=VERTEX_POINT ( 'NONE', #18780 ) ;
#12258=CARTESIAN_POINT ( 'NONE',  ( 47.43856463449117200, 112.7297705074273182, 35.64915139335016647 ) ) ;
#12261=CARTESIAN_POINT ( 'NONE',  ( 43.01140435219951286, 140.3651871740940180, 29.55568802177586463 ) ) ;
#12262=CARTESIAN_POINT ( 'NONE',  ( 47.05648932407426344, 101.5104996726487485, 31.27175355779120025 ) ) ;
#12267=CARTESIAN_POINT ( 'NONE',  ( 44.55648932407425633, 63.68445800887258201, 38.96596240072933170 ) ) ;
#12268=CARTESIAN_POINT ( 'NONE',  ( 43.01140435219951996, 10.71049967264875491, 29.21067981925357060 ) ) ;
#12269=CARTESIAN_POINT ( 'NONE',  ( 41.64333658814960870, 84.97977050742731819, 38.42115945441014446 ) ) ;
#12271=CARTESIAN_POINT ( 'NONE',  ( 39.42975644700377558, 78.41518717409400097, 36.81289934271958941 ) ) ;
#12275=CARTESIAN_POINT ( 'NONE',  ( 46.10157429594899270, 84.83445800887258770, 38.46393386101375711 ) ) ;
#12277=CARTESIAN_POINT ( 'NONE',  ( 38.58424406990785371, 129.5297705074273154, 35.64915139335015937 ) ) ;
#12280=CARTESIAN_POINT ( 'NONE',  ( 47.05648932407426344, 72.98445800887257917, 37.14960608071593384 ) ) ;
#12282=CARTESIAN_POINT ( 'NONE',  ( 44.37947211624943833, 134.4797705074273324, 30.00020018409699318 ) ) ;
#12284=DIRECTION ( 'NONE',  ( 0.000000000000000000, 0.000000000000000000, 1.000000000000000000 ) ) ;
#12285=CARTESIAN_POINT ( 'NONE',  ( 38.96631938032478359, 129.4104996726487684, 31.27175355779120025 ) ) ;
#12286=LINE ( 'NONE', #15808, #1394 ) ;
#12287=CARTESIAN_POINT ( 'NONE',  ( 47.43856463449117200, 94.76518717409398107, 32.77220824515698183 ) ) ;
#12292=CARTESIAN_POINT ( 'NONE',  ( 47.05648932407426344, 130.5844580088725877, 31.27175355779120025 ) ) ;
#12293=CARTESIAN_POINT ( 'NONE',  ( 47.43856463449118621, 109.8797705074273239, 34.21067981925357060 ) ) ;
#12295=CARTESIAN_POINT ( 'NONE',  ( 43.01140435219951286, 101.0344580088725621, 29.21067981925356705 ) ) ;
#12296=CARTESIAN_POINT ( 'NONE',  ( 40.27526882409969744, 108.5651871740939924, 37.97664729208901235 ) ) ;
#12298=CARTESIAN_POINT ( 'NONE',  ( 48.01140435219951996, 157.1344580088725422, 35.83527830041809636 ) ) ;
#12305=CARTESIAN_POINT ( 'NONE',  ( 45.74753988029934249, 76.42977050742730682, 37.97664729208901235 ) ) ;
#12308=CARTESIAN_POINT ( 'NONE',  ( 38.01140435219951996, 62.93445800887258201, 35.83527830041810347 ) ) ;
#12310=EDGE_CURVE ( 'NONE', #495, #20113, #20792, .T. ) ;
#12311=CARTESIAN_POINT ( 'NONE',  ( 46.10157429594899270, 128.6604996726487400, 29.95742577749337343 ) ) ;
#12312=CARTESIAN_POINT ( 'NONE',  ( 38.58424406990784661, 77.96518717409396970, 32.77220824515698183 ) ) ;
#12315=CARTESIAN_POINT ( 'NONE',  ( 39.92123440845005433, 116.3344580088725735, 29.95742577749336988 ) ) ;
#12317=CARTESIAN_POINT ( 'NONE',  ( 38.96631938032478359, 81.08445800887258770, 37.14960608071593384 ) ) ;
#12321=CARTESIAN_POINT ( 'NONE',  ( 38.58424406990784661, 138.5297705074273154, 35.64915139335016647 ) ) ;
#12322=CARTESIAN_POINT ( 'NONE',  ( 47.43856463449118621, 106.8797705074273239, 34.21067981925357060 ) ) ;
#12324=CARTESIAN_POINT ( 'NONE',  ( 46.59305225739526435, 139.3151871740940067, 36.81289934271958941 ) ) ;
#12325=CARTESIAN_POINT ( 'NONE',  ( 46.10157429594899270, 67.73445800887256496, 29.95742577749336988 ) ) ;
#12328=CARTESIAN_POINT ( 'NONE',  ( 41.46631938032478359, 136.3104996726487457, 38.96596240072933170 ) ) ;
#12331=CARTESIAN_POINT ( 'NONE',  ( 43.01140435219951286, 113.3651871740939754, 29.55568802177586463 ) ) ;
#12334=AXIS2_PLACEMENT_3D ( 'NONE', #10799, #976, #20720 ) ;
#12337=CARTESIAN_POINT ( 'NONE',  ( 44.55648932407425633, 96.68445800887258201, 38.96596240072933170 ) ) ;
#12338=CARTESIAN_POINT ( 'NONE',  ( 44.37947211624943833, 146.4797705074273324, 30.00020018409699318 ) ) ;
#12339=CARTESIAN_POINT ( 'NONE',  ( 43.01140435219951286, 158.9604996726487514, 28.95336869806222779 ) ) ;
#12340=CARTESIAN_POINT ( 'NONE',  ( 44.37947211624943833, 121.0151871740940095, 38.42115945441014446 ) ) ;
#12342=CARTESIAN_POINT ( 'NONE',  ( 39.92123440845004723, 76.16049967264872578, 38.46393386101376421 ) ) ;
#12343=CARTESIAN_POINT ( 'NONE',  ( 42.21948215057684450, 108.4575765865522925, 39.21067981925356349 ) ) ;
#12345=CARTESIAN_POINT ( 'NONE',  ( 47.05648932407426344, 82.58445800887258770, 31.27175355779120025 ) ) ;
#12346=CARTESIAN_POINT ( 'NONE',  ( 43.01140435219957681, 71.03445800887256212, 29.21067981925356705 ) ) ;
#12349=CARTESIAN_POINT ( 'NONE',  ( 47.43856463449117200, 70.76518717409399528, 32.77220824515698183 ) ) ;
#12356=ORIENTED_EDGE ( 'NONE', *, *, #17652, .F. ) ;
#12357=CARTESIAN_POINT ( 'NONE',  ( 47.43856463449117200, 145.7651871740939953, 32.77220824515698183 ) ) ;
#12359=CARTESIAN_POINT ( 'NONE',  ( 43.01140435219951286, 109.1297705074273239, 38.86567161673127657 ) ) ;
#12364=CARTESIAN_POINT ( 'NONE',  ( 41.64333658814960870, 110.7797705074273154, 30.00020018409699318 ) ) ;
#12366=CARTESIAN_POINT ( 'NONE',  ( 39.42975644700377558, 149.8151871740940067, 31.60846029578754468 ) ) ;
#12367=CARTESIAN_POINT ( 'NONE',  ( 47.05648932407426344, 103.9104996726487400, 37.14960608071593384 ) ) ;
#12371=LINE ( 'NONE', #17436, #4855 ) ;
#12374=CARTESIAN_POINT ( 'NONE',  ( 43.01140435219951286, 143.0344580088726048, 29.21067981925356705 ) ) ;
#12380=CARTESIAN_POINT ( 'NONE',  ( 44.37947211624943833, 88.27977050742731535, 38.42115945441014446 ) ) ;
#12382=CARTESIAN_POINT ( 'NONE',  ( 41.64333658814960870, 68.51518717409399528, 30.00020018409699318 ) ) ;
#12387=CARTESIAN_POINT ( 'NONE',  ( 39.92123440845005433, 69.23445800887257917, 38.46393386101375711 ) ) ;
#12389=CARTESIAN_POINT ( 'NONE',  ( 45.74753988029934249, 131.3297705074273267, 30.44471234641812174 ) ) ;
#12393=EDGE_LOOP ( 'NONE', ( #9636, #11246, #14393, #12582 ) ) ;
#12394=CARTESIAN_POINT ( 'NONE',  ( 38.58424406990784661, 138.5297705074273154, 35.64915139335016647 ) ) ;
#12397=CARTESIAN_POINT ( 'NONE',  ( 41.64333658814960870, 92.77977050742731535, 30.00020018409699318 ) ) ;
#12399=DIRECTION ( 'NONE',  ( 0.000000000000000000, 1.000000000000000000, 0.000000000000000000 ) ) ;
#12400=CARTESIAN_POINT ( 'NONE',  ( 45.74753988029933538, 101.0651871740939924, 30.44471234641811819 ) ) ;
#12401=CARTESIAN_POINT ( 'NONE',  ( 42.21948215057684450, 66.03738109496899256, 29.21067981925356705 ) ) ;
#12406=CARTESIAN_POINT ( 'NONE',  ( 38.96631938032478359, 134.4844580088725934, 31.27175355779120025 ) ) ;
#12407=CARTESIAN_POINT ( 'NONE',  ( 40.27526882409969033, 110.9297705074272926, 30.44471234641811819 ) ) ;
#12410=CARTESIAN_POINT ( 'NONE',  ( 43.01140435219951286, 107.3651871740940038, 29.55568802177586107 ) ) ;
#12413=CARTESIAN_POINT ( 'NONE',  ( 43.01140435219951286, 77.03445800887257633, 29.21067981925356705 ) ) ;
#12418=CARTESIAN_POINT ( 'NONE',  ( 43.01140435219953417, 138.5344580088726048, 39.21067981925356349 ) ) ;
#12419=CARTESIAN_POINT ( 'NONE',  ( 41.64333658814960870, 80.77977050742732956, 30.00020018409699318 ) ) ;
#12420=ORIENTED_EDGE ( 'NONE', *, *, #12044, .T. ) ;
#12424=CARTESIAN_POINT ( 'NONE',  ( 44.55648932407425633, 118.6104996726487570, 38.96596240072933170 ) ) ;
#12426=CARTESIAN_POINT ( 'NONE',  ( 40.27526882409969033, 77.66518717409400097, 30.44471234641811819 ) ) ;
#12431=CARTESIAN_POINT ( 'NONE',  ( 38.96631938032478359, 80.48445800887257917, 31.27175355779120025 ) ) ;
#12432=LINE ( 'NONE', #7808, #15301 ) ;
#12434=CARTESIAN_POINT ( 'NONE',  ( 45.74753988029933538, 142.4297705074273495, 37.97664729208901946 ) ) ;
#12435=EDGE_CURVE ( 'NONE', #10777, #1337, #2761, .T. ) ;
#12437=CARTESIAN_POINT ( 'NONE',  ( 38.58424406990785371, 135.2651871740939953, 35.64915139335015937 ) ) ;
#12438=CARTESIAN_POINT ( 'NONE',  ( 43.01140435219957681, 94.46049967264876557, 39.21067981925356349 ) ) ;
#12440=CARTESIAN_POINT ( 'NONE',  ( 41.64333658814960870, 59.77977050742731535, 30.00020018409699318 ) ) ;
#12441=CARTESIAN_POINT ( 'NONE',  ( 43.80332655382220253, 91.95757658655229250, 29.21067981925356705 ) ) ;
#12444=CARTESIAN_POINT ( 'NONE',  ( 39.42975644700377558, 119.8151871740940067, 31.60846029578754468 ) ) ;
#12448=CARTESIAN_POINT ( 'NONE',  ( 46.10157429594899270, 87.83445800887255928, 38.46393386101376421 ) ) ;
#12449=CARTESIAN_POINT ( 'NONE',  ( 47.43856463449117911, 148.7297705074273324, 35.64915139335015937 ) ) ;
#12450=EDGE_CURVE ( 'NONE', #9101, #20743, #12371, .T. ) ;
#12451=CARTESIAN_POINT ( 'NONE',  ( 38.01140435219952707, 150.7104996726487514, 34.21067981925357060 ) ) ;
#12452=CARTESIAN_POINT ( 'NONE',  ( 46.59305225739526435, 106.9151871740940152, 31.60846029578754468 ) ) ;
#12454=CARTESIAN_POINT ( 'NONE',  ( 41.46631938032478359, 72.11049967264874283, 29.45539723777780239 ) ) ;
#12459=CARTESIAN_POINT ( 'NONE',  ( 46.59305225739526435, 67.31518717409400665, 36.81289934271958941 ) ) ;
#12460=CARTESIAN_POINT ( 'NONE',  ( 38.01140435219952707, 63.56049967264873146, 32.58608133808903773 ) ) ;
#12463=ORIENTED_EDGE ( 'NONE', *, *, #2025, .T. ) ;
#12467=CARTESIAN_POINT ( 'NONE',  ( 46.59305225739526435, 142.3151871740940067, 36.81289934271958941 ) ) ;
#12469=CARTESIAN_POINT ( 'NONE',  ( 45.74753988029934249, 109.4297705074273352, 37.97664729208901235 ) ) ;
#12474=CARTESIAN_POINT ( 'NONE',  ( 48.01140435219951996, 115.4344580088725678, 32.58608133808903773 ) ) ;
#12477=EDGE_CURVE ( 'NONE', #4439, #14006, #1347, .T. ) ;
#12479=CARTESIAN_POINT ( 'NONE',  ( 38.58424406990784661, 81.22977050742731819, 32.77220824515698183 ) ) ;
#12480=CARTESIAN_POINT ( 'NONE',  ( 45.74753988029933538, 133.1651871740940010, 37.97664729208901946 ) ) ;
#12482=CARTESIAN_POINT ( 'NONE',  ( 47.05648932407426344, 100.9104996726487400, 37.14960608071593384 ) ) ;
#12487=CARTESIAN_POINT ( 'NONE',  ( 39.92123440845005433, 144.2344580088725934, 38.46393386101375711 ) ) ;
#12490=CARTESIAN_POINT ( 'NONE',  ( 45.74753988029933538, 86.32977050742729830, 30.44471234641811819 ) ) ;
#12492=CARTESIAN_POINT ( 'NONE',  ( 40.27526882409969744, 72.56518717409399244, 37.97664729208901235 ) ) ;
#12494=ADVANCED_FACE ( 'NONE', ( #108 ), #6623, .T. ) ;
#12496=ORIENTED_EDGE ( 'NONE', *, *, #18992, .T. ) ;
#12497=CARTESIAN_POINT ( 'NONE',  ( 43.80332655382220253, 84.61133943119283174, 39.21067981925355639 ) ) ;
#12499=CARTESIAN_POINT ( 'NONE',  ( 45.74753988029934249, 136.4297705074273210, 37.97664729208901235 ) ) ;
#12504=CARTESIAN_POINT ( 'NONE',  ( 44.37947211624943833, 130.2797705074273154, 38.42115945441014446 ) ) ;
#12505=EDGE_CURVE ( 'NONE', #10720, #3622, #18295, .T. ) ;
#12506=CARTESIAN_POINT ( 'NONE',  ( 48.01140435219951996, 110.0604996726487315, 35.83527830041809636 ) ) ;
#12508=CARTESIAN_POINT ( 'NONE',  ( 43.01140435219951286, 98.96049967264873715, 29.21067981925356705 ) ) ;
#12511=CARTESIAN_POINT ( 'NONE',  ( 41.64333658814960870, 99.71518717409399812, 38.42115945441014446 ) ) ;
#12512=CARTESIAN_POINT ( 'NONE',  ( 43.01140435219951996, 10.71049967264875491, 39.21067981925356349 ) ) ;
#12517=CARTESIAN_POINT ( 'NONE',  ( 43.80332655382220253, 70.53738109496900677, 39.21067981925355639 ) ) ;
#12518=CARTESIAN_POINT ( 'NONE',  ( 39.92123440845004723, 131.3344580088725593, 29.95742577749337343 ) ) ;
#12519=CARTESIAN_POINT ( 'NONE',  ( 38.58424406990784661, 117.2297705074273040, 32.77220824515698183 ) ) ;
#12521=CARTESIAN_POINT ( 'NONE',  ( 45.74753988029934249, 97.16518717409398675, 37.97664729208901235 ) ) ;
#12524=CARTESIAN_POINT ( 'NONE',  ( 44.55648932407425633, 157.8844580088725706, 29.45539723777780239 ) ) ;
#12527=CARTESIAN_POINT ( 'NONE',  ( 43.01140435219951996, 10.71049967264875491, 34.21067981925357060 ) ) ;
#12529=CARTESIAN_POINT ( 'NONE',  ( 45.74753988029934249, 77.32977050742729830, 30.44471234641812174 ) ) ;
#12532=CARTESIAN_POINT ( 'NONE',  ( 43.01140435219951996, 10.71049967264875491, 29.21067981925357060 ) ) ;
#12533=CARTESIAN_POINT ( 'NONE',  ( 47.05648932407426344, 124.9104996726487542, 37.14960608071593384 ) ) ;
#12534=CARTESIAN_POINT ( 'NONE',  ( 47.43856463449117200, 76.46518717409401233, 35.64915139335016647 ) ) ;
#12540=CARTESIAN_POINT ( 'NONE',  ( 43.01140435219951286, 88.46049967264873715, 39.21067981925356349 ) ) ;
#12542=CARTESIAN_POINT ( 'NONE',  ( 39.42975644700377558, 138.0797705074273267, 31.60846029578754468 ) ) ;
#12544=CARTESIAN_POINT ( 'NONE',  ( 38.58424406990785371, 129.2651871740940237, 35.64915139335015937 ) ) ;
#12545=CARTESIAN_POINT ( 'NONE',  ( 47.05648932407426344, 137.5104996726487627, 31.27175355779120025 ) ) ;
#12549=EDGE_CURVE ( 'NONE', #4204, #11358, #2063, .T. ) ;
#12550=CARTESIAN_POINT ( 'NONE',  ( 44.55648932407425633, 91.88445800887258486, 29.45539723777780239 ) ) ;
#12553=CARTESIAN_POINT ( 'NONE',  ( 38.58424406990784661, 107.9651871740939839, 32.77220824515698183 ) ) ;
#12556=EDGE_LOOP ( 'NONE', ( #14041, #20646, #3836, #16667 ) ) ;
#12557=CARTESIAN_POINT ( 'NONE',  ( 47.05648932407426344, 94.58445800887257349, 31.27175355779120025 ) ) ;
#12559=CARTESIAN_POINT ( 'NONE',  ( 44.37947211624943833, 152.4797705074273324, 30.00020018409699318 ) ) ;
#12560=CARTESIAN_POINT ( 'NONE',  ( 38.01140435219951996, 144.5604996726487173, 32.58608133808903773 ) ) ;
#12561=CARTESIAN_POINT ( 'NONE',  ( 47.43856463449118621, 106.6151871740940038, 34.21067981925357060 ) ) ;
#12563=LINE ( 'NONE', #2531, #605 ) ;
#12569=CARTESIAN_POINT ( 'NONE',  ( 39.42975644700377558, 65.81518717409400665, 31.60846029578754468 ) ) ;
#12571=CARTESIAN_POINT ( 'NONE',  ( 43.80332655382220253, 103.5373810949689926, 39.21067981925355639 ) ) ;
#12578=DIRECTION ( 'NONE',  ( 0.000000000000000000, 0.000000000000000000, 1.000000000000000000 ) ) ;
#12579=CARTESIAN_POINT ( 'NONE',  ( 38.58424406990784661, 143.9651871740940123, 32.77220824515698183 ) ) ;
#12580=CARTESIAN_POINT ( 'NONE',  ( 47.43856463449117911, 157.4651871740939839, 35.64915139335015937 ) ) ;
#12581=CARTESIAN_POINT ( 'NONE',  ( 40.27526882409969744, 93.82977050742731251, 37.97664729208901235 ) ) ;
#12582=ORIENTED_EDGE ( 'NONE', *, *, #6177, .F. ) ;
#12588=CARTESIAN_POINT ( 'NONE',  ( 38.96631938032478359, 113.4844580088725792, 31.27175355779120025 ) ) ;
#12591=CARTESIAN_POINT ( 'NONE',  ( 46.59305225739526435, 73.57977050742732672, 36.81289934271958941 ) ) ;
#12592=CARTESIAN_POINT ( 'NONE',  ( 40.27526882409969033, 138.5651871740939498, 37.97664729208901946 ) ) ;
#12593=VECTOR ( 'NONE', #15078, 1000.000000000000000 ) ;
#12594=CARTESIAN_POINT ( 'NONE',  ( 38.01140435219951996, 90.86049967264871441, 35.83527830041810347 ) ) ;
#12598=CARTESIAN_POINT ( 'NONE',  ( 48.01140435219951996, 158.3604996726487286, 32.58608133808903773 ) ) ;
#12599=CARTESIAN_POINT ( 'NONE',  ( 48.01140435219951996, 64.28445800887257633, 34.21067981925357060 ) ) ;
#12600=ORIENTED_EDGE ( 'NONE', *, *, #10936, .T. ) ;
#12601=CARTESIAN_POINT ( 'NONE',  ( 46.59305225739526435, 74.17977050742732104, 31.60846029578754468 ) ) ;
#12605=ORIENTED_EDGE ( 'NONE', *, *, #10273, .T. ) ;
#12609=CARTESIAN_POINT ( 'NONE',  ( 38.58424406990786082, 138.3797705074273381, 34.21067981925357060 ) ) ;
#12610=ORIENTED_EDGE ( 'NONE', *, *, #9562, .F. ) ;
#12612=( BOUNDED_CURVE ( )  B_SPLINE_CURVE ( 2, ( #11116, #11218, #17830, #19282, #15961, #19601, #2741, #12881, #17934, #9585, #873, #21373, #19713 ),
 .UNSPECIFIED., .F., .F. ) 
 B_SPLINE_CURVE_WITH_KNOTS ( ( 3, 2, 2, 2, 2, 2, 3 ),
 ( 0.7132352941176470784, 0.7147058823529411908, 0.7176470588235294157, 0.7205882352941176405, 0.7235294117647058654, 0.7264705882352940902, 0.7279411764705882026 ),
 .UNSPECIFIED. ) 
 CURVE ( )  GEOMETRIC_REPRESENTATION_ITEM ( )  RATIONAL_B_SPLINE_CURVE ( ( 0.9755282581475768211, 0.9755282581475768211, 1.000000000000000000, 0.9510565162951535312, 1.000000000000000000, 0.9510565162951535312, 1.000000000000000000, 0.9510565162951535312, 1.000000000000000000, 0.9510565162951535312, 1.000000000000000000, 0.9755282581475768211, 0.9755282581475768211 ) ) 
 REPRESENTATION_ITEM ( '' )  );
#12613=ORIENTED_EDGE ( 'NONE', *, *, #12992, .F. ) ;
#12614=CARTESIAN_POINT ( 'NONE',  ( 46.59305225739526435, 124.5797705074273267, 36.81289934271958941 ) ) ;
#12617=CARTESIAN_POINT ( 'NONE',  ( 43.01140435219951286, 130.4604996726487229, 39.21067981925356349 ) ) ;
#12618=CARTESIAN_POINT ( 'NONE',  ( 38.96631938032478359, 159.4104996726487400, 31.27175355779120025 ) ) ;
#12620=CARTESIAN_POINT ( 'NONE',  ( 44.55648932407425633, 132.6844580088725820, 38.96596240072933170 ) ) ;
#12621=CARTESIAN_POINT ( 'NONE',  ( 48.01140435219951996, 125.2104996726487514, 34.21067981925357060 ) ) ;
#12624=CARTESIAN_POINT ( 'NONE',  ( 46.10157429594899270, 109.7344580088725650, 29.95742577749336988 ) ) ;
#12625=CARTESIAN_POINT ( 'NONE',  ( 44.55648932407425633, 135.6844580088725820, 38.96596240072933170 ) ) ;
#12626=CARTESIAN_POINT ( 'NONE',  ( 44.37947211624943833, 113.4797705074273324, 30.00020018409699318 ) ) ;
#12628=CARTESIAN_POINT ( 'NONE',  ( 43.01140435219951996, 10.71049967264875491, 29.21067981925357060 ) ) ;
#12629=CARTESIAN_POINT ( 'NONE',  ( 40.27526882409969744, 95.66518717409398675, 30.44471234641812174 ) ) ;
#12630=CARTESIAN_POINT ( 'NONE',  ( 38.01140435219952707, 90.56049967264874567, 32.58608133808903773 ) ) ;
#12633=CARTESIAN_POINT ( 'NONE',  ( 46.10157429594899270, 75.83445800887257349, 38.46393386101375711 ) ) ;
#12637=CARTESIAN_POINT ( 'NONE',  ( 43.01140435219951286, 76.12977050742732388, 38.86567161673127657 ) ) ;
#12640=CARTESIAN_POINT ( 'NONE',  ( 40.27526882409969033, 158.9297705074272642, 30.44471234641811819 ) ) ;
#12642=CARTESIAN_POINT ( 'NONE',  ( 43.01140435219951286, 120.5344580088725763, 39.21067981925356349 ) ) ;
#12643=CARTESIAN_POINT ( 'NONE',  ( 48.01140435219951996, 119.3604996726487570, 32.58608133808903773 ) ) ;
#12644=CARTESIAN_POINT ( 'NONE',  ( 45.74753988029933538, 73.16518717409400097, 37.97664729208901946 ) ) ;
#12647=CARTESIAN_POINT ( 'NONE',  ( 48.01140435219951996, 113.0604996726487315, 35.83527830041809636 ) ) ;
#12650=CARTESIAN_POINT ( 'NONE',  ( 48.01140435219951996, 157.4344580088725536, 32.58608133808903773 ) ) ;
#12651=CARTESIAN_POINT ( 'NONE',  ( 39.42975644700377558, 144.0797705074273267, 31.60846029578754468 ) ) ;
#12653=CARTESIAN_POINT ( 'NONE',  ( 45.74753988029934249, 124.1651871740940152, 37.97664729208901235 ) ) ;
#12657=AXIS2_PLACEMENT_3D ( 'NONE', #2403, #7050, #17169 ) ;
#12662=CARTESIAN_POINT ( 'NONE',  ( 43.01140435219951286, 105.8651871740939754, 38.86567161673127657 ) ) ;
#12664=FACE_OUTER_BOUND ( 'NONE', #19201, .T. ) ;
#12665=ORIENTED_EDGE ( 'NONE', *, *, #21546, .F. ) ;
#12666=CARTESIAN_POINT ( 'NONE',  ( 41.46631938032478359, 89.18445800887258201, 29.45539723777780239 ) ) ;
#12669=CARTESIAN_POINT ( 'NONE',  ( 39.92123440845004723, 153.2604996726487343, 29.95742577749337343 ) ) ;
#12670=CARTESIAN_POINT ( 'NONE',  ( 40.27526882409969033, 107.6651871740940152, 30.44471234641811819 ) ) ;
#12672=CARTESIAN_POINT ( 'NONE',  ( 41.46631938032478359, 66.11049967264874283, 29.45539723777780239 ) ) ;
#12674=CARTESIAN_POINT ( 'NONE',  ( 48.01140435219951996, 61.43445800887257491, 32.58608133808903773 ) ) ;
#12675=DIRECTION ( 'NONE',  ( 0.000000000000000000, 0.000000000000000000, 1.000000000000000000 ) ) ;
#12684=CARTESIAN_POINT ( 'NONE',  ( 46.59305225739526435, 136.9151871740940010, 31.60846029578754468 ) ) ;
#12686=EDGE_CURVE ( 'NONE', #6094, #310, #16632, .T. ) ;
#12687=CARTESIAN_POINT ( 'NONE',  ( 47.43856463449118621, 97.87977050742732388, 34.21067981925357060 ) ) ;
#12689=ORIENTED_EDGE ( 'NONE', *, *, #19108, .F. ) ;
#12692=CARTESIAN_POINT ( 'NONE',  ( 44.55648932407425633, 111.6844580088725820, 38.96596240072933170 ) ) ;
#12694=CARTESIAN_POINT ( 'NONE',  ( 43.80332655382220253, 89.88361825032846752, 29.21067981925356705 ) ) ;
#12695=CARTESIAN_POINT ( 'NONE',  ( 41.64333658814960870, 74.77977050742731535, 30.00020018409699318 ) ) ;
#12696=CARTESIAN_POINT ( 'NONE',  ( 47.43856463449117200, 139.4651871740940123, 35.64915139335016647 ) ) ;
#12697=CARTESIAN_POINT ( 'NONE',  ( 39.92123440845004723, 90.26049967264873430, 29.95742577749337343 ) ) ;
#12703=DIRECTION ( 'NONE',  ( 0.000000000000000000, 1.000000000000000000, 0.000000000000000000 ) ) ;
#12706=CARTESIAN_POINT ( 'NONE',  ( 47.43856463449117200, 73.72977050742731819, 35.64915139335016647 ) ) ;
#12714=CARTESIAN_POINT ( 'NONE',  ( 47.43856463449118621, 127.8797705074273239, 34.21067981925357060 ) ) ;
#12717=CARTESIAN_POINT ( 'NONE',  ( 44.55648932407425633, 129.6844580088725820, 38.96596240072933170 ) ) ;
#12719=CARTESIAN_POINT ( 'NONE',  ( 45.74753988029933538, 122.3297705074273267, 30.44471234641811819 ) ) ;
#12720=CARTESIAN_POINT ( 'NONE',  ( 43.80332655382221674, 109.5373810949689926, 39.21067981925355639 ) ) ;
#12721=CARTESIAN_POINT ( 'NONE',  ( 43.01140435219951286, 60.53445800887259054, 39.46799094044489209 ) ) ;
#12723=CARTESIAN_POINT ( 'NONE',  ( 38.01140435219952707, 110.6344580088725849, 32.58608133808903773 ) ) ;
#12724=CARTESIAN_POINT ( 'NONE',  ( 43.01140435219951286, 84.53445800887256212, 39.21067981925356349 ) ) ;
#12727=CARTESIAN_POINT ( 'NONE',  ( 38.01140435219952707, 66.86049967264872862, 35.83527830041809636 ) ) ;
#12732=CARTESIAN_POINT ( 'NONE',  ( 38.96631938032478359, 131.4844580088725934, 31.27175355779120025 ) ) ;
#12733=CARTESIAN_POINT ( 'NONE',  ( 41.64333658814960870, 102.9797705074273182, 38.42115945441014446 ) ) ;
#12736=CARTESIAN_POINT ( 'NONE',  ( 38.58424406990785371, 95.96518717409396970, 32.77220824515697473 ) ) ;
#12739=CARTESIAN_POINT ( 'NONE',  ( 46.10157429594899270, 127.7604996726487485, 38.46393386101375711 ) ) ;
#12745=CARTESIAN_POINT ( 'NONE',  ( 38.58424406990785371, 81.22977050742731819, 32.77220824515697473 ) ) ;
#12746=ORIENTED_EDGE ( 'NONE', *, *, #5154, .T. ) ;
#12748=CARTESIAN_POINT ( 'NONE',  ( 45.74753988029933538, 152.3297705074272699, 30.44471234641811819 ) ) ;
#12750=EDGE_CURVE ( 'NONE', #15251, #872, #16451, .T. ) ;
#12751=CARTESIAN_POINT ( 'NONE',  ( 38.96631938032478359, 118.0104996726487485, 37.14960608071593384 ) ) ;
#12752=CARTESIAN_POINT ( 'NONE',  ( 39.42975644700377558, 75.41518717409400097, 36.81289934271958941 ) ) ;
#12757=DIRECTION ( 'NONE',  ( 0.000000000000000000, 1.000000000000000000, 0.000000000000000000 ) ) ;
#12758=CARTESIAN_POINT ( 'NONE',  ( 43.01140435219951996, 149.0344580088725763, 29.21067981925357060 ) ) ;
#12759=CARTESIAN_POINT ( 'NONE',  ( 47.43856463449117200, 133.7297705074273324, 35.64915139335016647 ) ) ;
#12761=CARTESIAN_POINT ( 'NONE',  ( 41.64333658814960870, 126.7151871740939981, 38.42115945441014446 ) ) ;
#12762=CARTESIAN_POINT ( 'NONE',  ( 48.01140435219951996, 137.0604996726487457, 35.83527830041809636 ) ) ;
#12764=CARTESIAN_POINT ( 'NONE',  ( 38.58424406990784661, 60.22977050742731109, 32.77220824515698183 ) ) ;
#12765=CARTESIAN_POINT ( 'NONE',  ( 43.01140435219951286, 134.9604996726487514, 29.21067981925356705 ) ) ;
#12768=CARTESIAN_POINT ( 'NONE',  ( 38.58424406990786082, 105.1151871740940038, 34.21067981925357060 ) ) ;
#12771=ORIENTED_EDGE ( 'NONE', *, *, #3662, .T. ) ;
#12772=CARTESIAN_POINT ( 'NONE',  ( 46.10157429594899270, 90.83445800887255928, 38.46393386101376421 ) ) ;
#12775=CARTESIAN_POINT ( 'NONE',  ( 44.55648932407425633, 149.8104996726487457, 29.45539723777780239 ) ) ;
#12776=CARTESIAN_POINT ( 'NONE',  ( 46.59305225739526435, 106.3151871740939924, 36.81289934271958941 ) ) ;
#12778=CARTESIAN_POINT ( 'NONE',  ( 47.05648932407426344, 61.91049967264873288, 37.14960608071593384 ) ) ;
#12781=CARTESIAN_POINT ( 'NONE',  ( 43.80332655382220253, 118.9575765865522925, 29.21067981925356705 ) ) ;
#12783=LINE ( 'NONE', #10921, #12245 ) ;
#12784=CARTESIAN_POINT ( 'NONE',  ( 41.64333658814960870, 69.71518717409399812, 38.42115945441014446 ) ) ;
#12787=CARTESIAN_POINT ( 'NONE',  ( 38.58424406990786082, 153.1151871740939896, 34.21067981925357060 ) ) ;
#12795=CARTESIAN_POINT ( 'NONE',  ( 41.64333658814960870, 134.5151871740939953, 30.00020018409699318 ) ) ;
#12796=CARTESIAN_POINT ( 'NONE',  ( 46.59305225739526435, 154.9151871740940010, 31.60846029578754468 ) ) ;
#12797=CARTESIAN_POINT ( 'NONE',  ( 47.43856463449117911, 92.02977050742730114, 32.77220824515697473 ) ) ;
#12799=ORIENTED_EDGE ( 'NONE', *, *, #4984, .T. ) ;
#12804=CARTESIAN_POINT ( 'NONE',  ( 45.74753988029933538, 79.42977050742732104, 37.97664729208901946 ) ) ;
#12805=CARTESIAN_POINT ( 'NONE',  ( 47.43856463449117200, 130.7651871740939953, 32.77220824515698183 ) ) ;
#12806=CARTESIAN_POINT ( 'NONE',  ( 38.01140435219951996, 87.86049967264871441, 35.83527830041810347 ) ) ;
#12810=ADVANCED_FACE ( 'NONE', ( #4714 ), #10239, .T. ) ;
#12812=CARTESIAN_POINT ( 'NONE',  ( 43.80332655382221674, 141.6113394311928744, 39.21067981925356349 ) ) ;
#12814=CARTESIAN_POINT ( 'NONE',  ( 45.74753988029933538, 73.42977050742732104, 37.97664729208901946 ) ) ;
#12820=CARTESIAN_POINT ( 'NONE',  ( 43.01140435219951286, 104.0344580088725763, 29.21067981925356705 ) ) ;
#12821=VECTOR ( 'NONE', #1430, 1000.000000000000000 ) ;
#12822=CARTESIAN_POINT ( 'NONE',  ( 40.27526882409969744, 122.9297705074273068, 30.44471234641812174 ) ) ;
#12826=CARTESIAN_POINT ( 'NONE',  ( 38.58424406990786082, 126.3797705074273239, 34.21067981925357060 ) ) ;
#12828=CARTESIAN_POINT ( 'NONE',  ( 43.01140435219951286, 89.62977050742729546, 29.55568802177586463 ) ) ;
#12829=CARTESIAN_POINT ( 'NONE',  ( 38.96631938032478359, 63.08445800887258059, 37.14960608071593384 ) ) ;
#12831=CARTESIAN_POINT ( 'NONE',  ( 43.01140435219951996, 10.71049967264875491, 39.21067981925356349 ) ) ;
#12833=CARTESIAN_POINT ( 'NONE',  ( 43.01140435219957681, 97.46049967264875136, 39.21067981925356349 ) ) ;
#12835=CARTESIAN_POINT ( 'NONE',  ( 38.96631938032478359, 67.01049967264874851, 37.14960608071593384 ) ) ;
#12836=CARTESIAN_POINT ( 'NONE',  ( 46.10157429594899270, 93.83445800887257349, 38.46393386101375711 ) ) ;
#12839=CARTESIAN_POINT ( 'NONE',  ( 43.01140435219951286, 122.0344580088725621, 28.95336869806222779 ) ) ;
#12840=CARTESIAN_POINT ( 'NONE',  ( 38.58424406990784661, 105.5297705074273011, 35.64915139335016647 ) ) ;
#12843=CARTESIAN_POINT ( 'NONE',  ( 43.01140435219951286, 96.86518717409398960, 38.86567161673127657 ) ) ;
#12849=CARTESIAN_POINT ( 'NONE',  ( 39.42975644700377558, 66.07977050742731251, 31.60846029578754468 ) ) ;
#12852=CARTESIAN_POINT ( 'NONE',  ( 43.01140435219951286, 152.6297705074272812, 29.55568802177586463 ) ) ;
#12856=CARTESIAN_POINT ( 'NONE',  ( 39.92123440845004723, 118.1604996726487542, 38.46393386101376421 ) ) ;
#12857=CARTESIAN_POINT ( 'NONE',  ( 44.37947211624943833, 71.21518717409399812, 30.00020018409699318 ) ) ;
#12859=CARTESIAN_POINT ( 'NONE',  ( 38.01140435219952707, 65.78445800887257633, 34.21067981925357060 ) ) ;
#12865=FACE_OUTER_BOUND ( 'NONE', #16208, .T. ) ;
#12866=CARTESIAN_POINT ( 'NONE',  ( 40.27526882409969033, 134.9297705074272926, 30.44471234641811819 ) ) ;
#12867=( BOUNDED_CURVE ( )  B_SPLINE_CURVE ( 2, ( #10555, #3829, #5903, #20798, #4043, #945, #10978, #2593, #17691, #737, #6010, #626, #5690 ),
 .UNSPECIFIED., .F., .F. ) 
 B_SPLINE_CURVE_WITH_KNOTS ( ( 3, 2, 2, 2, 2, 2, 3 ),
 ( 0.6985294117647058432, 0.6999999999999999556, 0.7029411764705881804, 0.7058823529411765163, 0.7088235294117647411, 0.7117647058823529660, 0.7132352941176470784 ),
 .UNSPECIFIED. ) 
 CURVE ( )  GEOMETRIC_REPRESENTATION_ITEM ( )  RATIONAL_B_SPLINE_CURVE ( ( 0.9755282581475768211, 0.9755282581475768211, 1.000000000000000000, 0.9510565162951535312, 1.000000000000000000, 0.9510565162951535312, 1.000000000000000000, 0.9510565162951535312, 1.000000000000000000, 0.9510565162951535312, 1.000000000000000000, 0.9755282581475768211, 0.9755282581475768211 ) ) 
 REPRESENTATION_ITEM ( '' )  );
#12868=EDGE_CURVE ( 'NONE', #6293, #12132, #10372, .T. ) ;
#12870=CARTESIAN_POINT ( 'NONE',  ( 40.27526882409969744, 129.5651871740940067, 37.97664729208901235 ) ) ;
#12871=CARTESIAN_POINT ( 'NONE',  ( 38.01140435219952707, 69.56049967264874567, 32.58608133808903773 ) ) ;
#12874=CARTESIAN_POINT ( 'NONE',  ( 43.80332655382220963, 149.8836182503285102, 29.21067981925357060 ) ) ;
#12877=CARTESIAN_POINT ( 'NONE',  ( 43.01140435219951996, 10.71049967264875491, 29.21067981925357060 ) ) ;
#12878=CARTESIAN_POINT ( 'NONE',  ( 46.59305225739526435, 109.3151871740939924, 36.81289934271958941 ) ) ;
#12881=CARTESIAN_POINT ( 'NONE',  ( 48.01140435219951996, 86.06049967264874567, 35.83527830041809636 ) ) ;
#12883=CARTESIAN_POINT ( 'NONE',  ( 41.46631938032478359, 80.18445800887258201, 29.45539723777780239 ) ) ;
#12884=CARTESIAN_POINT ( 'NONE',  ( 43.01140435219951286, 128.9604996726487229, 29.21067981925356705 ) ) ;
#12885=CARTESIAN_POINT ( 'NONE',  ( 38.01140435219951996, 153.5604996726487173, 32.58608133808903773 ) ) ;
#12886=CARTESIAN_POINT ( 'NONE',  ( 46.59305225739526435, 103.9151871740940152, 31.60846029578754468 ) ) ;
#12888=CARTESIAN_POINT ( 'NONE',  ( 47.05648932407426344, 62.51049967264874141, 31.27175355779120025 ) ) ;
#12890=CARTESIAN_POINT ( 'NONE',  ( 43.80332655382220963, 147.6113394311928744, 39.21067981925356349 ) ) ;
#12891=CARTESIAN_POINT ( 'NONE',  ( 46.10157429594899270, 117.8344580088725593, 38.46393386101375711 ) ) ;
#12895=CARTESIAN_POINT ( 'NONE',  ( 47.43856463449118621, 157.8797705074273381, 34.21067981925357060 ) ) ;
#12897=CARTESIAN_POINT ( 'NONE',  ( 46.59305225739526435, 151.9151871740940010, 31.60846029578754468 ) ) ;
#12902=CARTESIAN_POINT ( 'NONE',  ( 44.37947211624943833, 65.21518717409399812, 30.00020018409699318 ) ) ;
#12906=CARTESIAN_POINT ( 'NONE',  ( 46.59305225739526435, 130.9151871740940010, 31.60846029578754468 ) ) ;
#12907=EDGE_CURVE ( 'NONE', #8083, #8428, #13188, .T. ) ;
#12910=VERTEX_POINT ( 'NONE', #5884 ) ;
#12913=CARTESIAN_POINT ( 'NONE',  ( 43.01140435219951286, 116.0344580088725763, 28.95336869806222779 ) ) ;
#12915=CARTESIAN_POINT ( 'NONE',  ( 43.01140435219951286, 79.12977050742732388, 38.86567161673127657 ) ) ;
#12916=CARTESIAN_POINT ( 'NONE',  ( 47.43856463449117200, 139.7651871740939953, 32.77220824515698183 ) ) ;
#12917=CARTESIAN_POINT ( 'NONE',  ( 38.01140435219951996, 93.56049967264873146, 32.58608133808903773 ) ) ;
#12921=CARTESIAN_POINT ( 'NONE',  ( 38.58424406990784661, 90.26518717409398107, 35.64915139335016647 ) ) ;
#12923=CARTESIAN_POINT ( 'NONE',  ( 44.55648932407425633, 106.6104996726487428, 38.96596240072933170 ) ) ;
#12924=CARTESIAN_POINT ( 'NONE',  ( 48.01140435219951996, 62.06049967264872436, 35.83527830041809636 ) ) ;
#12926=CARTESIAN_POINT ( 'NONE',  ( 46.59305225739526435, 70.57977050742732672, 36.81289934271958941 ) ) ;
#12931=ORIENTED_EDGE ( 'NONE', *, *, #13492, .T. ) ;
#12933=CARTESIAN_POINT ( 'NONE',  ( 42.21948215057684450, 105.4575765865522925, 39.21067981925355639 ) ) ;
#12936=ORIENTED_EDGE ( 'NONE', *, *, #4121, .T. ) ;
#12939=CARTESIAN_POINT ( 'NONE',  ( 43.01140435219951286, 124.1297705074272955, 38.86567161673127657 ) ) ;
#12942=CARTESIAN_POINT ( 'NONE',  ( 44.37947211624943833, 89.47977050742731819, 30.00020018409699318 ) ) ;
#12943=CARTESIAN_POINT ( 'NONE',  ( 48.01140435219951996, 67.13445800887258486, 35.83527830041810347 ) ) ;
#12944=DIRECTION ( 'NONE',  ( 0.000000000000000000, -1.000000000000000000, 0.000000000000000000 ) ) ;
#12950=CARTESIAN_POINT ( 'NONE',  ( 43.80332655382220253, 94.95757658655229250, 29.21067981925356705 ) ) ;
#12952=CARTESIAN_POINT ( 'NONE',  ( 47.05648932407426344, 123.9844580088725934, 37.14960608071593384 ) ) ;
#12953=CARTESIAN_POINT ( 'NONE',  ( 47.43856463449117200, 106.7297705074273324, 35.64915139335016647 ) ) ;
#12956=CARTESIAN_POINT ( 'NONE',  ( 47.43856463449117911, 94.76518717409399528, 32.77220824515697473 ) ) ;
#12961=CARTESIAN_POINT ( 'NONE',  ( 39.42975644700377558, 144.6797705074273495, 36.81289934271958941 ) ) ;
#12963=ADVANCED_FACE ( 'NONE', ( #9426 ), #11986, .T. ) ;
#12964=CARTESIAN_POINT ( 'NONE',  ( 47.43856463449117911, 71.02977050742730114, 32.77220824515697473 ) ) ;
#12967=CARTESIAN_POINT ( 'NONE',  ( 41.64333658814960870, 155.7797705074273438, 30.00020018409699318 ) ) ;
#12969=CARTESIAN_POINT ( 'NONE',  ( 43.01140435219951286, 107.9604996726487371, 28.95336869806222779 ) ) ;
#12970=CARTESIAN_POINT ( 'NONE',  ( 44.37947211624943833, 64.01518717409400949, 38.42115945441014446 ) ) ;
#12971=CARTESIAN_POINT ( 'NONE',  ( 42.21948215057687293, 96.45757658655232092, 39.21067981925357060 ) ) ;
#12978=CARTESIAN_POINT ( 'NONE',  ( 39.92123440845004723, 149.3344580088725877, 29.95742577749337343 ) ) ;
#12979=CARTESIAN_POINT ( 'NONE',  ( 43.01140435219951286, 134.6297705074273097, 29.55568802177586463 ) ) ;
#12981=CARTESIAN_POINT ( 'NONE',  ( 45.74753988029934249, 131.0651871740940067, 30.44471234641812174 ) ) ;
#12983=DIRECTION ( 'NONE',  ( 0.000000000000000000, 1.000000000000000000, 0.000000000000000000 ) ) ;
#12984=EDGE_CURVE ( 'NONE', #15219, #1195, #15452, .T. ) ;
#12987=EDGE_CURVE ( 'NONE', #9753, #1056, #5029, .T. ) ;
#12989=CARTESIAN_POINT ( 'NONE',  ( 48.01140435219951996, 83.21049967264873715, 34.21067981925357060 ) ) ;
#12992=EDGE_CURVE ( 'NONE', #9338, #8983, #9536, .T. ) ;
#12994=ORIENTED_EDGE ( 'NONE', *, *, #1961, .F. ) ;
#12995=CARTESIAN_POINT ( 'NONE',  ( 38.96631938032478359, 80.48445800887257917, 31.27175355779120025 ) ) ;
#12997=CARTESIAN_POINT ( 'NONE',  ( 39.92123440845004723, 138.2604996726487059, 29.95742577749337343 ) ) ;
#12998=CARTESIAN_POINT ( 'NONE',  ( 39.42975644700377558, 95.81518717409399244, 31.60846029578754468 ) ) ;
#13001=CARTESIAN_POINT ( 'NONE',  ( 38.96631938032478359, 67.01049967264874851, 37.14960608071593384 ) ) ;
#13004=CARTESIAN_POINT ( 'NONE',  ( 43.01140435219951286, 65.96049967264873715, 29.21067981925356705 ) ) ;
#13007=CARTESIAN_POINT ( 'NONE',  ( 44.55648932407425633, 115.8844580088725991, 29.45539723777780239 ) ) ;
#13008=CARTESIAN_POINT ( 'NONE',  ( 46.59305225739526435, 64.91518717409400097, 31.60846029578754468 ) ) ;
#13014=ORIENTED_EDGE ( 'NONE', *, *, #5195, .F. ) ;
#13015=CARTESIAN_POINT ( 'NONE',  ( 38.58424406990785371, 71.96518717409399812, 32.77220824515697473 ) ) ;
#13018=PRESENTATION_STYLE_ASSIGNMENT (( #1113 ) ) ;
#13019=CARTESIAN_POINT ( 'NONE',  ( 44.37947211624943833, 134.2151871740940123, 30.00020018409699318 ) ) ;
#13021=ORIENTED_EDGE ( 'NONE', *, *, #8338, .T. ) ;
#13022=VERTEX_POINT ( 'NONE', #16452 ) ;
#13026=CARTESIAN_POINT ( 'NONE',  ( 46.10157429594899270, 116.6604996726487258, 29.95742577749336988 ) ) ;
#13027=CARTESIAN_POINT ( 'NONE',  ( 47.43856463449117200, 127.4651871740940123, 35.64915139335016647 ) ) ;
#13029=CARTESIAN_POINT ( 'NONE',  ( 43.01140435219951286, 95.96049967264876557, 28.95336869806222779 ) ) ;
#13031=DIRECTION ( 'NONE',  ( 0.000000000000000000, 1.000000000000000000, 0.000000000000000000 ) ) ;
#13033=CARTESIAN_POINT ( 'NONE',  ( 41.64333658814960870, 90.71518717409401233, 38.42115945441014446 ) ) ;
#13034=CARTESIAN_POINT ( 'NONE',  ( 44.55648932407425633, 150.6844580088725820, 38.96596240072933170 ) ) ;
#13035=CARTESIAN_POINT ( 'NONE',  ( 47.05648932407426344, 71.51049967264873430, 31.27175355779120025 ) ) ;
#13037=ORIENTED_EDGE ( 'NONE', *, *, #2773, .T. ) ;
#13038=CARTESIAN_POINT ( 'NONE',  ( 46.59305225739526435, 79.57977050742731251, 36.81289934271958941 ) ) ;
#13045=CARTESIAN_POINT ( 'NONE',  ( 41.64333658814960870, 123.9797705074273324, 38.42115945441014446 ) ) ;
#13048=EDGE_LOOP ( 'NONE', ( #12665, #9286, #1333, #14693 ) ) ;
#13049=CARTESIAN_POINT ( 'NONE',  ( 38.58424406990784661, 120.2297705074273182, 32.77220824515698183 ) ) ;
#13050=CARTESIAN_POINT ( 'NONE',  ( 43.80332655382220253, 58.95757658655231381, 29.21067981925356705 ) ) ;
#13051=CARTESIAN_POINT ( 'NONE',  ( 43.01140435219951286, 66.53445800887256212, 39.46799094044489209 ) ) ;
#13053=CARTESIAN_POINT ( 'NONE',  ( 43.01140435219954838, 131.0344580088725479, 29.21067981925356705 ) ) ;
#13054=DIRECTION ( 'NONE',  ( 0.000000000000000000, 0.000000000000000000, 1.000000000000000000 ) ) ;
#13057=CARTESIAN_POINT ( 'NONE',  ( 43.01140435219951996, 155.9604996726487514, 29.21067981925357060 ) ) ;
#13058=CARTESIAN_POINT ( 'NONE',  ( 39.92123440845005433, 102.2604996726487485, 29.95742577749336988 ) ) ;
#13060=CARTESIAN_POINT ( 'NONE',  ( 48.01140435219951996, 121.2844580088725763, 34.21067981925357060 ) ) ;
#13061=CARTESIAN_POINT ( 'NONE',  ( 38.58424406990786082, 102.3797705074273381, 34.21067981925357060 ) ) ;
#13062=( BOUNDED_CURVE ( )  B_SPLINE_CURVE ( 2, ( #8929, #12441, #12550, #10797, #9255, #17500, #2411, #20718, #12110, #331, #13980, #7060, #18842 ),
 .UNSPECIFIED., .F., .F. ) 
 B_SPLINE_CURVE_WITH_KNOTS ( ( 3, 2, 2, 2, 2, 2, 3 ),
 ( 0.6544117647058823595, 0.6558823529411764719, 0.6588235294117646967, 0.6617647058823529216, 0.6647058823529411464, 0.6676470588235293713, 0.6691176470588234837 ),
 .UNSPECIFIED. ) 
 CURVE ( )  GEOMETRIC_REPRESENTATION_ITEM ( )  RATIONAL_B_SPLINE_CURVE ( ( 0.9755282581475768211, 0.9755282581475768211, 1.000000000000000000, 0.9510565162951535312, 1.000000000000000000, 0.9510565162951535312, 1.000000000000000000, 0.9510565162951535312, 1.000000000000000000, 0.9510565162951535312, 1.000000000000000000, 0.9755282581475768211, 0.9755282581475768211 ) ) 
 REPRESENTATION_ITEM ( '' )  );
#13065=CARTESIAN_POINT ( 'NONE',  ( 44.37947211624943833, 86.21518717409399812, 30.00020018409699318 ) ) ;
#13066=DIRECTION ( 'NONE',  ( 0.000000000000000000, 1.000000000000000000, 0.000000000000000000 ) ) ;
#13072=CARTESIAN_POINT ( 'NONE',  ( 39.42975644700377558, 63.07977050742731251, 31.60846029578754468 ) ) ;
#13073=ORIENTED_EDGE ( 'NONE', *, *, #21212, .F. ) ;
#13074=EDGE_LOOP ( 'NONE', ( #18094, #19126, #20778, #15567 ) ) ;
#13075=CARTESIAN_POINT ( 'NONE',  ( 46.59305225739526435, 152.1797705074273210, 31.60846029578754468 ) ) ;
#13077=CARTESIAN_POINT ( 'NONE',  ( 39.92123440845004723, 112.1604996726487258, 38.46393386101376421 ) ) ;
#13078=CARTESIAN_POINT ( 'NONE',  ( 46.59305225739526435, 67.31518717409400665, 36.81289934271958941 ) ) ;
#13081=DIRECTION ( 'NONE',  ( 0.000000000000000000, 1.000000000000000000, 0.000000000000000000 ) ) ;
#13084=CARTESIAN_POINT ( 'NONE',  ( 41.46631938032478359, 150.3844580088725991, 38.96596240072933170 ) ) ;
#13086=CARTESIAN_POINT ( 'NONE',  ( 39.42975644700377558, 129.6797705074273210, 36.81289934271958941 ) ) ;
#13088=CARTESIAN_POINT ( 'NONE',  ( 38.58424406990786082, 114.1151871740939896, 34.21067981925357060 ) ) ;
#13090=VECTOR ( 'NONE', #2037, 1000.000000000000000 ) ;
#13091=CARTESIAN_POINT ( 'NONE',  ( 39.92123440845005433, 150.2604996726487911, 29.95742577749336988 ) ) ;
#13093=CARTESIAN_POINT ( 'NONE',  ( 43.01140435219951996, 10.71049967264875491, 29.21067981925357060 ) ) ;
#13096=CARTESIAN_POINT ( 'NONE',  ( 39.92123440845005433, 120.2604996726487485, 29.95742577749336988 ) ) ;
#13097=VECTOR ( 'NONE', #16028, 1000.000000000000000 ) ;
#13099=EDGE_CURVE ( 'NONE', #11964, #9411, #390, .T. ) ;
#13101=ORIENTED_EDGE ( 'NONE', *, *, #7205, .F. ) ;
#13102=CARTESIAN_POINT ( 'NONE',  ( 44.55648932407425633, 79.88445800887257064, 29.45539723777780239 ) ) ;
#13103=CARTESIAN_POINT ( 'NONE',  ( 47.05648932407426344, 103.5844580088725877, 31.27175355779120025 ) ) ;
#13105=CARTESIAN_POINT ( 'NONE',  ( 43.01140435219951286, 136.4604996726487229, 39.46799094044489209 ) ) ;
#13106=CARTESIAN_POINT ( 'NONE',  ( 47.43856463449117200, 100.4651871740939839, 35.64915139335016647 ) ) ;
#13113=CARTESIAN_POINT ( 'NONE',  ( 43.80332655382220253, 69.61133943119284595, 39.21067981925355639 ) ) ;
#13114=CARTESIAN_POINT ( 'NONE',  ( 43.01140435219951286, 143.0344580088726048, 29.21067981925356705 ) ) ;
#13116=CARTESIAN_POINT ( 'NONE',  ( 44.37947211624943833, 59.21518717409400523, 30.00020018409699318 ) ) ;
#13119=CARTESIAN_POINT ( 'NONE',  ( 43.01140435219951286, 152.3651871740939896, 29.55568802177586107 ) ) ;
#13122=VERTEX_POINT ( 'NONE', #7990 ) ;
#13123=CARTESIAN_POINT ( 'NONE',  ( 41.64333658814960870, 69.71518717409399812, 38.42115945441014446 ) ) ;
#13127=CARTESIAN_POINT ( 'NONE',  ( 43.01140435219951286, 128.3651871740940180, 29.55568802177586463 ) ) ;
#13132=CARTESIAN_POINT ( 'NONE',  ( 47.05648932407426344, 108.9844580088725792, 37.14960608071593384 ) ) ;
#13134=CARTESIAN_POINT ( 'NONE',  ( 40.27526882409969033, 62.92977050742729972, 30.44471234641811819 ) ) ;
#13135=CARTESIAN_POINT ( 'NONE',  ( 38.58424406990784661, 123.2651871740939953, 35.64915139335016647 ) ) ;
#13137=CARTESIAN_POINT ( 'NONE',  ( 48.01140435219951996, 80.36049967264874283, 32.58608133808903773 ) ) ;
#13139=DIRECTION ( 'NONE',  ( 0.000000000000000000, 0.000000000000000000, 1.000000000000000000 ) ) ;
#13140=CARTESIAN_POINT ( 'NONE',  ( 39.92123440845005433, 139.1604996726487400, 38.46393386101375711 ) ) ;
#13141=CARTESIAN_POINT ( 'NONE',  ( 45.74753988029933538, 88.16518717409397254, 37.97664729208901946 ) ) ;
#13143=CARTESIAN_POINT ( 'NONE',  ( 48.01140435219951996, 142.4344580088725820, 32.58608133808903773 ) ) ;
#13145=CARTESIAN_POINT ( 'NONE',  ( 38.58424406990786082, 66.37977050742730967, 34.21067981925357060 ) ) ;
#13149=EDGE_LOOP ( 'NONE', ( #361, #9313, #12936, #1548 ) ) ;
#13152=CARTESIAN_POINT ( 'NONE',  ( 40.27526882409969744, 126.8297705074273125, 37.97664729208901235 ) ) ;
#13157=CARTESIAN_POINT ( 'NONE',  ( 48.01140435219951996, 88.13445800887258486, 35.83527830041809636 ) ) ;
#13159=CARTESIAN_POINT ( 'NONE',  ( 47.43856463449117200, 119.0297705074273296, 32.77220824515698183 ) ) ;
#13160=CARTESIAN_POINT ( 'NONE',  ( 42.21948215057687293, 72.03738109496900677, 29.21067981925355994 ) ) ;
#13161=CARTESIAN_POINT ( 'NONE',  ( 45.74753988029933538, 155.0651871740940067, 30.44471234641811819 ) ) ;
#13169=CARTESIAN_POINT ( 'NONE',  ( 48.01140435219951996, 124.1344580088725706, 35.83527830041810347 ) ) ;
#13170=CARTESIAN_POINT ( 'NONE',  ( 40.27526882409969033, 107.9297705074273352, 30.44471234641811819 ) ) ;
#13174=CARTESIAN_POINT ( 'NONE',  ( 40.27526882409969744, 84.56518717409399244, 37.97664729208901235 ) ) ;
#13177=CARTESIAN_POINT ( 'NONE',  ( 47.05648932407426344, 128.5104996726487343, 31.27175355779120025 ) ) ;
#13180=CARTESIAN_POINT ( 'NONE',  ( 46.59305225739526435, 70.57977050742732672, 36.81289934271958941 ) ) ;
#13182=CARTESIAN_POINT ( 'NONE',  ( 41.64333658814960870, 144.9797705074273324, 38.42115945441014446 ) ) ;
#13185=CARTESIAN_POINT ( 'NONE',  ( 47.05648932407426344, 107.5104996726487485, 31.27175355779120025 ) ) ;
#13186=CARTESIAN_POINT ( 'NONE',  ( 43.01140435219951286, 68.36518717409400381, 29.55568802177586463 ) ) ;
#13188=( BOUNDED_CURVE ( )  B_SPLINE_CURVE ( 2, ( #927, #9105, #7672, #15415, #19443, #6934, #19232, #14371, #716, #20375, #13746, #20999, #18822 ),
 .UNSPECIFIED., .F., .F. ) 
 B_SPLINE_CURVE_WITH_KNOTS ( ( 3, 2, 2, 2, 2, 2, 3 ),
 ( 0.2426470588235294101, 0.2441176470588235226, 0.2470588235294117752, 0.2500000000000000000, 0.2529411764705882248, 0.2558823529411764497, 0.2573529411764705621 ),
 .UNSPECIFIED. ) 
 CURVE ( )  GEOMETRIC_REPRESENTATION_ITEM ( )  RATIONAL_B_SPLINE_CURVE ( ( 0.9755282581475768211, 0.9755282581475768211, 1.000000000000000000, 0.9510565162951535312, 1.000000000000000000, 0.9510565162951535312, 1.000000000000000000, 0.9510565162951535312, 1.000000000000000000, 0.9510565162951535312, 1.000000000000000000, 0.9755282581475772652, 0.9755282581475768211 ) ) 
 REPRESENTATION_ITEM ( '' )  );
#13193=CARTESIAN_POINT ( 'NONE',  ( 39.92123440845004723, 150.2344580088725365, 38.46393386101376421 ) ) ;
#13194=CARTESIAN_POINT ( 'NONE',  ( 47.43856463449117200, 137.0297705074272869, 32.77220824515698183 ) ) ;
#13196=CARTESIAN_POINT ( 'NONE',  ( 41.64333658814960870, 116.5151871740940095, 30.00020018409699318 ) ) ;
#13199=CARTESIAN_POINT ( 'NONE',  ( 48.01140435219951996, 65.21049967264873715, 34.21067981925357060 ) ) ;
#13203=CARTESIAN_POINT ( 'NONE',  ( 43.01140435219951286, 100.1297705074273239, 38.86567161673127657 ) ) ;
#13204=ORIENTED_EDGE ( 'NONE', *, *, #12987, .F. ) ;
#13205=VECTOR ( 'NONE', #18917, 1000.000000000000000 ) ;
#13207=VERTEX_POINT ( 'NONE', #6323 ) ;
#13208=CARTESIAN_POINT ( 'NONE',  ( 39.92123440845004723, 78.23445800887257917, 38.46393386101376421 ) ) ;
#13210=CARTESIAN_POINT ( 'NONE',  ( 48.01140435219951996, 143.2104996726487514, 34.21067981925357060 ) ) ;
#13211=CARTESIAN_POINT ( 'NONE',  ( 41.64333658814960870, 96.71518717409399812, 38.42115945441014446 ) ) ;
#13217=CARTESIAN_POINT ( 'NONE',  ( 46.10157429594899270, 70.73445800887257917, 29.95742577749336988 ) ) ;
#13219=CARTESIAN_POINT ( 'NONE',  ( 38.01140435219952707, 147.7104996726487514, 34.21067981925357060 ) ) ;
#13221=EDGE_CURVE ( 'NONE', #3828, #12910, #16763, .T. ) ;
#13222=CARTESIAN_POINT ( 'NONE',  ( 43.01140435219951286, 59.36518717409399670, 29.55568802177586463 ) ) ;
#13225=CARTESIAN_POINT ( 'NONE',  ( 39.42975644700377558, 149.8151871740940067, 31.60846029578754468 ) ) ;
#13230=CARTESIAN_POINT ( 'NONE',  ( 38.01140435219952707, 77.93445800887255359, 35.83527830041809636 ) ) ;
#13233=CARTESIAN_POINT ( 'NONE',  ( 46.10157429594899270, 112.7344580088725792, 29.95742577749336988 ) ) ;
#13234=CARTESIAN_POINT ( 'NONE',  ( 38.58424406990784661, 123.2651871740939953, 35.64915139335016647 ) ) ;
#13240=ORIENTED_EDGE ( 'NONE', *, *, #18752, .F. ) ;
#13241=CARTESIAN_POINT ( 'NONE',  ( 39.92123440845004723, 107.3344580088725877, 29.95742577749337343 ) ) ;
#13244=CARTESIAN_POINT ( 'NONE',  ( 39.42975644700377558, 66.07977050742731251, 31.60846029578754468 ) ) ;
#13245=CARTESIAN_POINT ( 'NONE',  ( 46.59305225739526435, 121.3151871740940067, 36.81289934271958941 ) ) ;
#13248=CARTESIAN_POINT ( 'NONE',  ( 41.46631938032478359, 82.31049967264873146, 38.96596240072933170 ) ) ;
#13251=CARTESIAN_POINT ( 'NONE',  ( 44.37947211624943833, 85.01518717409399528, 38.42115945441014446 ) ) ;
#13254=DIRECTION ( 'NONE',  ( 0.000000000000000000, 0.000000000000000000, 1.000000000000000000 ) ) ;
#13256=CARTESIAN_POINT ( 'NONE',  ( 46.59305225739526435, 62.17977050742732104, 31.60846029578754468 ) ) ;
#13261=VERTEX_POINT ( 'NONE', #11174 ) ;
#13262=CARTESIAN_POINT ( 'NONE',  ( 39.42975644700377558, 150.4151871740940010, 36.81289934271958941 ) ) ;
#13267=CARTESIAN_POINT ( 'NONE',  ( 41.64333658814960870, 116.7797705074273296, 30.00020018409699318 ) ) ;
#13272=CARTESIAN_POINT ( 'NONE',  ( 44.37947211624943833, 116.4797705074273324, 30.00020018409699318 ) ) ;
#13273=CARTESIAN_POINT ( 'NONE',  ( 41.46631938032478359, 72.11049967264874283, 29.45539723777780239 ) ) ;
#13274=CARTESIAN_POINT ( 'NONE',  ( 38.58424406990786082, 87.37977050742732388, 34.21067981925357060 ) ) ;
#13275=CARTESIAN_POINT ( 'NONE',  ( 46.59305225739526435, 154.3151871740940067, 36.81289934271958941 ) ) ;
#13282=CARTESIAN_POINT ( 'NONE',  ( 39.92123440845005433, 156.2604996726487059, 29.95742577749336988 ) ) ;
#13283=CARTESIAN_POINT ( 'NONE',  ( 41.46631938032478359, 102.1104996726487286, 29.45539723777780239 ) ) ;
#13286=CARTESIAN_POINT ( 'NONE',  ( 41.64333658814960870, 95.77977050742732956, 30.00020018409699318 ) ) ;
#13291=CARTESIAN_POINT ( 'NONE',  ( 38.01140435219952707, 137.9344580088725820, 35.83527830041809636 ) ) ;
#13293=CARTESIAN_POINT ( 'NONE',  ( 46.59305225739526435, 140.1797705074273210, 31.60846029578754468 ) ) ;
#13297=CARTESIAN_POINT ( 'NONE',  ( 38.58424406990785371, 66.22977050742730398, 32.77220824515697473 ) ) ;
#13299=CARTESIAN_POINT ( 'NONE',  ( 38.58424406990784661, 144.2297705074273324, 32.77220824515698183 ) ) ;
#13302=CARTESIAN_POINT ( 'NONE',  ( 41.46631938032478359, 115.3104996726487599, 38.96596240072933170 ) ) ;
#13303=CARTESIAN_POINT ( 'NONE',  ( 46.59305225739526435, 70.31518717409400665, 36.81289934271958941 ) ) ;
#13304=CARTESIAN_POINT ( 'NONE',  ( 38.01140435219952707, 95.93445800887258201, 35.83527830041809636 ) ) ;
#13309=EDGE_CURVE ( 'NONE', #4102, #16674, #2623, .T. ) ;
#13311=CARTESIAN_POINT ( 'NONE',  ( 48.01140435219951996, 154.4344580088725820, 32.58608133808903773 ) ) ;
#13312=CARTESIAN_POINT ( 'NONE',  ( 45.74753988029933538, 122.3297705074273267, 30.44471234641811819 ) ) ;
#13314=CARTESIAN_POINT ( 'NONE',  ( 38.58424406990785371, 117.2651871740940095, 35.64915139335015937 ) ) ;
#13320=CARTESIAN_POINT ( 'NONE',  ( 47.43856463449117911, 95.02977050742730114, 32.77220824515697473 ) ) ;
#13323=CARTESIAN_POINT ( 'NONE',  ( 46.10157429594899270, 145.7344580088725650, 29.95742577749336988 ) ) ;
#13324=ORIENTED_EDGE ( 'NONE', *, *, #588, .F. ) ;
#13326=CARTESIAN_POINT ( 'NONE',  ( 38.01140435219951996, 80.63445800887258486, 32.58608133808903773 ) ) ;
#13327=CARTESIAN_POINT ( 'NONE',  ( 38.96631938032478359, 60.08445800887257349, 37.14960608071593384 ) ) ;
#13328=CARTESIAN_POINT ( 'NONE',  ( 39.92123440845004723, 141.2604996726487627, 29.95742577749337343 ) ) ;
#13329=CARTESIAN_POINT ( 'NONE',  ( 39.42975644700377558, 96.41518717409400097, 36.81289934271958941 ) ) ;
#13333=CARTESIAN_POINT ( 'NONE',  ( 43.01140435219951996, 155.9604996726487514, 29.21067981925357060 ) ) ;
#13335=CARTESIAN_POINT ( 'NONE',  ( 42.21948215057684450, 147.0373810949689926, 29.21067981925356705 ) ) ;
#13336=CARTESIAN_POINT ( 'NONE',  ( 48.01140435219951996, 80.06049967264871725, 35.83527830041809636 ) ) ;
#13337=CARTESIAN_POINT ( 'NONE',  ( 44.37947211624943833, 62.21518717409399102, 30.00020018409699318 ) ) ;
#13338=DIRECTION ( 'NONE',  ( 0.000000000000000000, 0.000000000000000000, 1.000000000000000000 ) ) ;
#13340=CARTESIAN_POINT ( 'NONE',  ( 39.42975644700377558, 147.4151871740940294, 36.81289934271958941 ) ) ;
#13343=ORIENTED_EDGE ( 'NONE', *, *, #16951, .T. ) ;
#13344=CARTESIAN_POINT ( 'NONE',  ( 41.46631938032478359, 78.38445800887257064, 38.96596240072933170 ) ) ;
#13347=CYLINDRICAL_SURFACE ( 'NONE', #6345, 4.999999999999997335 ) ;
#13348=CARTESIAN_POINT ( 'NONE',  ( 47.43856463449117200, 124.7651871740939811, 32.77220824515698183 ) ) ;
#13350=ORIENTED_EDGE ( 'NONE', *, *, #1837, .T. ) ;
#13353=VERTEX_POINT ( 'NONE', #17107 ) ;
#13355=CARTESIAN_POINT ( 'NONE',  ( 40.27526882409969033, 63.82977050742731961, 37.97664729208901946 ) ) ;
#13356=CARTESIAN_POINT ( 'NONE',  ( 47.43856463449117200, 124.7651871740939811, 32.77220824515698183 ) ) ;
#13358=CARTESIAN_POINT ( 'NONE',  ( 44.55648932407425633, 79.61049967264874283, 38.96596240072933170 ) ) ;
#13360=CYLINDRICAL_SURFACE ( 'NONE', #2603, 4.999999999999997335 ) ;
#13362=CARTESIAN_POINT ( 'NONE',  ( 40.27526882409969033, 87.56518717409400665, 37.97664729208901946 ) ) ;
#13367=CARTESIAN_POINT ( 'NONE',  ( 47.43856463449117200, 67.72977050742731819, 35.64915139335016647 ) ) ;
#13372=CARTESIAN_POINT ( 'NONE',  ( 46.59305225739526435, 154.9151871740940010, 31.60846029578754468 ) ) ;
#13374=CARTESIAN_POINT ( 'NONE',  ( 43.01140435219951286, 112.1297705074272812, 38.86567161673127657 ) ) ;
#13375=CARTESIAN_POINT ( 'NONE',  ( 47.05648932407426344, 154.5844580088725877, 31.27175355779120025 ) ) ;
#13379=CARTESIAN_POINT ( 'NONE',  ( 38.01140435219952707, 126.8604996726487002, 35.83527830041809636 ) ) ;
#13381=CARTESIAN_POINT ( 'NONE',  ( 38.58424406990784661, 150.2651871740940237, 35.64915139335016647 ) ) ;
#13389=EDGE_CURVE ( 'NONE', #11299, #7475, #14149, .T. ) ;
#13390=CARTESIAN_POINT ( 'NONE',  ( 43.01140435219951286, 89.03445800887257633, 29.21067981925356705 ) ) ;
#13392=CARTESIAN_POINT ( 'NONE',  ( 43.80332655382220253, 97.95757658655229250, 29.21067981925356705 ) ) ;
#13393=CARTESIAN_POINT ( 'NONE',  ( 47.43856463449117200, 92.02977050742730114, 32.77220824515698183 ) ) ;
#13396=CARTESIAN_POINT ( 'NONE',  ( 47.43856463449117911, 88.76518717409399528, 32.77220824515697473 ) ) ;
#13401=CARTESIAN_POINT ( 'NONE',  ( 44.37947211624943833, 139.2797705074273154, 38.42115945441014446 ) ) ;
#13405=CARTESIAN_POINT ( 'NONE',  ( 45.22505347682923116, 59.38050100342834270, 30.37668637662395099 ) ) ;
#13407=CARTESIAN_POINT ( 'NONE',  ( 40.27526882409969033, 149.9297705074272926, 30.44471234641811819 ) ) ;
#13410=CARTESIAN_POINT ( 'NONE',  ( 38.96631938032478359, 108.4104996726487400, 31.27175355779120025 ) ) ;
#13414=CARTESIAN_POINT ( 'NONE',  ( 38.01140435219952707, 122.6344580088725849, 32.58608133808903773 ) ) ;
#13416=CARTESIAN_POINT ( 'NONE',  ( 46.10157429594899270, 154.7344580088725650, 29.95742577749337343 ) ) ;
#13417=CARTESIAN_POINT ( 'NONE',  ( 46.59305225739526435, 118.5797705074273267, 36.81289934271958941 ) ) ;
#13420=CARTESIAN_POINT ( 'NONE',  ( 44.37947211624943833, 112.0151871740940095, 38.42115945441014446 ) ) ;
#13422=CARTESIAN_POINT ( 'NONE',  ( 43.01140435219951996, 10.71049967264875491, 29.21067981925357060 ) ) ;
#13426=CARTESIAN_POINT ( 'NONE',  ( 38.58424406990785371, 84.22977050742730398, 32.77220824515697473 ) ) ;
#13431=CARTESIAN_POINT ( 'NONE',  ( 48.01140435219951996, 76.28445800887257633, 34.21067981925357060 ) ) ;
#13433=CARTESIAN_POINT ( 'NONE',  ( 48.01140435219951996, 137.3604996726487570, 32.58608133808903773 ) ) ;
#13434=CARTESIAN_POINT ( 'NONE',  ( 46.59305225739526435, 97.31518717409400665, 36.81289934271958941 ) ) ;
#13438=CARTESIAN_POINT ( 'NONE',  ( 43.01140435219951286, 69.53445800887257633, 39.21067981925356349 ) ) ;
#13443=CARTESIAN_POINT ( 'NONE',  ( 43.80332655382220253, 79.53738109496900677, 39.21067981925355639 ) ) ;
#13444=CARTESIAN_POINT ( 'NONE',  ( 41.64333658814960870, 153.9797705074273324, 38.42115945441014446 ) ) ;
#13445=CARTESIAN_POINT ( 'NONE',  ( 38.96631938032478359, 62.48445800887257917, 31.27175355779120025 ) ) ;
#13447=CARTESIAN_POINT ( 'NONE',  ( 46.59305225739526435, 148.3151871740940067, 36.81289934271958941 ) ) ;
#13448=VECTOR ( 'NONE', #11414, 1000.000000000000000 ) ;
#13452=CARTESIAN_POINT ( 'NONE',  ( 44.37947211624943833, 62.21518717409399102, 30.00020018409699318 ) ) ;
#13455=CARTESIAN_POINT ( 'NONE',  ( 41.64333658814960870, 123.7151871740940123, 38.42115945441014446 ) ) ;
#13456=( BOUNDED_CURVE ( )  B_SPLINE_CURVE ( 2, ( #9053, #18647, #20303, #17192, #453, #11918, #3549, #10275, #16977, #1887, #4083, #12890, #16188 ),
 .UNSPECIFIED., .F., .F. ) 
 B_SPLINE_CURVE_WITH_KNOTS ( ( 3, 2, 2, 2, 2, 2, 3 ),
 ( 0.09558823529411764053, 0.09705882352941176683, 0.1000000000000000056, 0.1029411764705882304, 0.1058823529411764691, 0.1088235294117647078, 0.1102941176470588203 ),
 .UNSPECIFIED. ) 
 CURVE ( )  GEOMETRIC_REPRESENTATION_ITEM ( )  RATIONAL_B_SPLINE_CURVE ( ( 0.9755282581475767101, 0.9755282581475765991, 1.000000000000000000, 0.9510565162951535312, 1.000000000000000000, 0.9510565162951535312, 1.000000000000000000, 0.9510565162951535312, 1.000000000000000000, 0.9510565162951535312, 1.000000000000000000, 0.9755282581475768211, 0.9755282581475767101 ) ) 
 REPRESENTATION_ITEM ( '' )  );
#13459=EDGE_CURVE ( 'NONE', #17105, #5159, #16895, .T. ) ;
#13463=CARTESIAN_POINT ( 'NONE',  ( 43.01140435219951286, 70.12977050742732388, 38.86567161673127657 ) ) ;
#13464=CARTESIAN_POINT ( 'NONE',  ( 46.59305225739526435, 121.9151871740940010, 31.60846029578754468 ) ) ;
#13467=CARTESIAN_POINT ( 'NONE',  ( 48.01140435219951996, 83.36049967264872862, 32.58608133808903773 ) ) ;
#13469=CARTESIAN_POINT ( 'NONE',  ( 47.05648932407426344, 97.91049967264873999, 37.14960608071593384 ) ) ;
#13471=CARTESIAN_POINT ( 'NONE',  ( 40.27526882409969033, 77.66518717409400097, 30.44471234641811819 ) ) ;
#13475=CARTESIAN_POINT ( 'NONE',  ( 40.27526882409969033, 66.82977050742732672, 37.97664729208901946 ) ) ;
#13481=CARTESIAN_POINT ( 'NONE',  ( 44.37947211624943833, 155.2151871740940123, 30.00020018409699318 ) ) ;
#13483=CARTESIAN_POINT ( 'NONE',  ( 45.74753988029934249, 110.3297705074273125, 30.44471234641812174 ) ) ;
#13488=CARTESIAN_POINT ( 'NONE',  ( 41.64333658814960870, 117.9797705074273182, 38.42115945441014446 ) ) ;
#13490=CARTESIAN_POINT ( 'NONE',  ( 38.58424406990784661, 87.52977050742730114, 35.64915139335016647 ) ) ;
#13491=CARTESIAN_POINT ( 'NONE',  ( 39.42975644700377558, 156.4151871740940010, 36.81289934271958941 ) ) ;
#13492=EDGE_CURVE ( 'NONE', #14908, #4098, #7285, .T. ) ;
#13499=CARTESIAN_POINT ( 'NONE',  ( 48.01140435219951996, 77.36049967264874283, 32.58608133808903773 ) ) ;
#13501=CARTESIAN_POINT ( 'NONE',  ( 39.42975644700377558, 90.07977050742732672, 31.60846029578754468 ) ) ;
#13504=CARTESIAN_POINT ( 'NONE',  ( 39.42975644700377558, 86.81518717409400665, 31.60846029578754468 ) ) ;
#13507=CARTESIAN_POINT ( 'NONE',  ( 38.01140435219952707, 137.7844580088726048, 34.21067981925357060 ) ) ;
#13510=CARTESIAN_POINT ( 'NONE',  ( 41.64333658814960870, 138.9797705074273324, 38.42115945441014446 ) ) ;
#13513=VERTEX_POINT ( 'NONE', #17325 ) ;
#13514=CARTESIAN_POINT ( 'NONE',  ( 38.58424406990784661, 150.2297705074273040, 32.77220824515698183 ) ) ;
#13515=CARTESIAN_POINT ( 'NONE',  ( 41.64333658814960870, 93.97977050742733240, 38.42115945441014446 ) ) ;
#13516=CARTESIAN_POINT ( 'NONE',  ( 46.10157429594899270, 152.6604996726487400, 29.95742577749336988 ) ) ;
#13522=CARTESIAN_POINT ( 'NONE',  ( 39.92123440845004723, 141.2344580088725365, 38.46393386101376421 ) ) ;
#13523=CARTESIAN_POINT ( 'NONE',  ( 45.74753988029933538, 121.4297705074273068, 37.97664729208901946 ) ) ;
#13526=CARTESIAN_POINT ( 'NONE',  ( 41.64333658814960870, 119.5151871740940095, 30.00020018409699318 ) ) ;
#13531=CARTESIAN_POINT ( 'NONE',  ( 44.37947211624943833, 82.27977050742732956, 38.42115945441014446 ) ) ;
#13534=DIRECTION ( 'NONE',  ( 0.000000000000000000, -1.000000000000000000, 0.000000000000000000 ) ) ;
#13535=CARTESIAN_POINT ( 'NONE',  ( 38.96631938032478359, 74.48445800887257917, 31.27175355779120025 ) ) ;
#13536=CARTESIAN_POINT ( 'NONE',  ( 39.92123440845005433, 87.23445800887257917, 38.46393386101375711 ) ) ;
#13537=CARTESIAN_POINT ( 'NONE',  ( 44.55648932407425633, 134.8104996726487457, 29.45539723777780239 ) ) ;
#13538=CARTESIAN_POINT ( 'NONE',  ( 45.74753988029933538, 86.06518717409400665, 30.44471234641811819 ) ) ;
#13543=CYLINDRICAL_SURFACE ( 'NONE', #6863, 4.999999999999997335 ) ;
#13544=CARTESIAN_POINT ( 'NONE',  ( 44.55648932407425633, 142.6104996726487570, 38.96596240072933170 ) ) ;
#13545=CARTESIAN_POINT ( 'NONE',  ( 47.43856463449117200, 149.0297705074273438, 32.77220824515698183 ) ) ;
#13548=CARTESIAN_POINT ( 'NONE',  ( 43.01140435219951286, 143.3651871740940180, 29.55568802177586107 ) ) ;
#13553=CARTESIAN_POINT ( 'NONE',  ( 38.58424406990785371, 59.96518717409398391, 32.77220824515697473 ) ) ;
#13556=CARTESIAN_POINT ( 'NONE',  ( 38.58424406990786082, 129.1151871740940180, 34.21067981925357060 ) ) ;
#13560=CARTESIAN_POINT ( 'NONE',  ( 48.01140435219951996, 103.1344580088725706, 35.83527830041810347 ) ) ;
#13561=CARTESIAN_POINT ( 'NONE',  ( 39.42975644700377558, 153.6797705074273210, 36.81289934271958941 ) ) ;
#13562=CARTESIAN_POINT ( 'NONE',  ( 46.59305225739526435, 70.57977050742732672, 36.81289934271958941 ) ) ;
#13563=CARTESIAN_POINT ( 'NONE',  ( 39.42975644700377558, 116.8151871740940067, 31.60846029578754468 ) ) ;
#13565=CARTESIAN_POINT ( 'NONE',  ( 46.10157429594899270, 82.76049967264874851, 38.46393386101376421 ) ) ;
#13566=VECTOR ( 'NONE', #13621, 1000.000000000000000 ) ;
#13567=CARTESIAN_POINT ( 'NONE',  ( 44.55648932407425633, 98.81049967264873146, 29.45539723777780239 ) ) ;
#13569=CARTESIAN_POINT ( 'NONE',  ( 44.37947211624943833, 76.01518717409399528, 38.42115945441014446 ) ) ;
#13570=CARTESIAN_POINT ( 'NONE',  ( 43.01140435219951286, 82.46049967264873715, 39.21067981925356349 ) ) ;
#13571=CARTESIAN_POINT ( 'NONE',  ( 48.01140435219951996, 124.4344580088725536, 32.58608133808903773 ) ) ;
#13572=CARTESIAN_POINT ( 'NONE',  ( 39.92123440845005433, 132.2604996726487343, 29.95742577749336988 ) ) ;
#13574=ORIENTED_EDGE ( 'NONE', *, *, #10434, .F. ) ;
#13575=CARTESIAN_POINT ( 'NONE',  ( 44.37947211624943833, 65.47977050742731819, 30.00020018409699318 ) ) ;
#13576=( BOUNDED_CURVE ( )  B_SPLINE_CURVE ( 2, ( #20261, #18605, #16718, #17151, #12085, #5153, #11981, #2067, #13630, #15295, #20368, #18491, #21807 ),
 .UNSPECIFIED., .F., .T. ) 
 B_SPLINE_CURVE_WITH_KNOTS ( ( 3, 2, 2, 2, 2, 2, 3 ),
 ( 0.3161764705882352811, 0.3176470588235293935, 0.3205882352941176738, 0.3235294117647058987, 0.3264705882352941235, 0.3294117647058823484, 0.3308823529411764608 ),
 .UNSPECIFIED. ) 
 CURVE ( )  GEOMETRIC_REPRESENTATION_ITEM ( )  RATIONAL_B_SPLINE_CURVE ( ( 0.9755282581475768211, 0.9755282581475768211, 1.000000000000000000, 0.9510565162951535312, 1.000000000000000000, 0.9510565162951535312, 1.000000000000000000, 0.9510565162951535312, 1.000000000000000000, 0.9510565162951535312, 1.000000000000000000, 0.9755282581475768211, 0.9755282581475768211 ) ) 
 REPRESENTATION_ITEM ( '' )  );
#13580=ORIENTED_EDGE ( 'NONE', *, *, #9496, .F. ) ;
#13581=CARTESIAN_POINT ( 'NONE',  ( 40.27526882409969033, 150.5651871740940067, 37.97664729208901946 ) ) ;
#13582=CARTESIAN_POINT ( 'NONE',  ( 40.27526882409969744, 158.6651871740939725, 30.44471234641812174 ) ) ;
#13583=CARTESIAN_POINT ( 'NONE',  ( 47.43856463449117911, 118.7297705074273040, 35.64915139335015937 ) ) ;
#13587=ORIENTED_EDGE ( 'NONE', *, *, #12505, .T. ) ;
#13588=CARTESIAN_POINT ( 'NONE',  ( 46.59305225739526435, 113.1797705074273210, 31.60846029578754468 ) ) ;
#13589=DIRECTION ( 'NONE',  ( 0.000000000000000000, -1.000000000000000000, 0.000000000000000000 ) ) ;
#13590=CARTESIAN_POINT ( 'NONE',  ( 43.01140435219951996, 10.71049967264875491, 39.21067981925356349 ) ) ;
#13591=CARTESIAN_POINT ( 'NONE',  ( 46.59305225739526435, 85.57977050742732672, 36.81289934271958941 ) ) ;
#13592=CARTESIAN_POINT ( 'NONE',  ( 43.01140435219951286, 156.8651871740940180, 38.86567161673127657 ) ) ;
#13595=FACE_OUTER_BOUND ( 'NONE', #19142, .T. ) ;
#13599=CARTESIAN_POINT ( 'NONE',  ( 48.01140435219951996, 97.28445800887259054, 34.21067981925357060 ) ) ;
#13601=CIRCLE ( 'NONE', #1283, 4.999999999999997335 ) ;
#13602=CARTESIAN_POINT ( 'NONE',  ( 43.01140435219951286, 94.12977050742730967, 38.86567161673127657 ) ) ;
#13605=CARTESIAN_POINT ( 'NONE',  ( 43.01140435219951286, 78.86518717409400381, 38.86567161673127657 ) ) ;
#13607=DIRECTION ( 'NONE',  ( 0.000000000000000000, 0.000000000000000000, 1.000000000000000000 ) ) ;
#13610=CARTESIAN_POINT ( 'NONE',  ( 47.05648932407426344, 121.9104996726487542, 37.14960608071593384 ) ) ;
#13612=CARTESIAN_POINT ( 'NONE',  ( 40.27526882409969744, 59.92977050742730682, 30.44471234641812174 ) ) ;
#13615=CARTESIAN_POINT ( 'NONE',  ( 43.01140435219951286, 134.6297705074273097, 29.55568802177586463 ) ) ;
#13616=CARTESIAN_POINT ( 'NONE',  ( 44.37947211624943833, 100.2797705074273154, 38.42115945441014446 ) ) ;
#13618=CARTESIAN_POINT ( 'NONE',  ( 41.64333658814960870, 62.51518717409400239, 30.00020018409699318 ) ) ;
#13620=CARTESIAN_POINT ( 'NONE',  ( 38.01140435219952707, 153.5604996726487457, 32.58608133808903773 ) ) ;
#13621=DIRECTION ( 'NONE',  ( 0.000000000000000000, 1.000000000000000000, 0.000000000000000000 ) ) ;
#13624=CARTESIAN_POINT ( 'NONE',  ( 48.01140435219951996, 139.4344580088725252, 32.58608133808903773 ) ) ;
#13625=CARTESIAN_POINT ( 'NONE',  ( 39.42975644700377558, 123.0797705074273267, 31.60846029578754468 ) ) ;
#13629=CARTESIAN_POINT ( 'NONE',  ( 46.59305225739526435, 109.3151871740939924, 36.81289934271958941 ) ) ;
#13630=CARTESIAN_POINT ( 'NONE',  ( 38.96631938032478359, 125.4844580088725934, 31.27175355779120025 ) ) ;
#13631=EDGE_CURVE ( 'NONE', #5984, #19572, #19244, .T. ) ;
#13635=CARTESIAN_POINT ( 'NONE',  ( 43.01140435219951286, 89.62977050742730967, 29.55568802177586107 ) ) ;
#13637=ORIENTED_EDGE ( 'NONE', *, *, #5906, .F. ) ;
#13638=AXIS2_PLACEMENT_3D ( 'NONE', #5206, #11922, #18651 ) ;
#13640=CARTESIAN_POINT ( 'NONE',  ( 41.46631938032478359, 72.38445800887258486, 38.96596240072933170 ) ) ;
#13641=CARTESIAN_POINT ( 'NONE',  ( 38.01140435219952707, 59.93445800887258201, 35.83527830041809636 ) ) ;
#13642=VECTOR ( 'NONE', #4963, 1000.000000000000000 ) ;
#13643=CARTESIAN_POINT ( 'NONE',  ( 38.96631938032478359, 132.4104996726487684, 31.27175355779120025 ) ) ;
#13645=CARTESIAN_POINT ( 'NONE',  ( 46.59305225739526435, 85.31518717409400665, 36.81289934271958941 ) ) ;
#13649=CARTESIAN_POINT ( 'NONE',  ( 41.46631938032478359, 93.11049967264874283, 29.45539723777780239 ) ) ;
#13653=CARTESIAN_POINT ( 'NONE',  ( 40.27526882409969033, 155.9297705074273210, 30.44471234641811819 ) ) ;
#13654=CARTESIAN_POINT ( 'NONE',  ( 44.37947211624943833, 103.2797705074273154, 38.42115945441014446 ) ) ;
#13657=CARTESIAN_POINT ( 'NONE',  ( 47.43856463449117911, 142.4651871740940123, 35.64915139335015937 ) ) ;
#13660=CARTESIAN_POINT ( 'NONE',  ( 43.01140435219951286, 62.36518717409398960, 29.55568802177586107 ) ) ;
#13665=CARTESIAN_POINT ( 'NONE',  ( 45.74753988029933538, 118.1651871740939725, 37.97664729208901946 ) ) ;
#13667=VERTEX_POINT ( 'NONE', #8071 ) ;
#13668=CARTESIAN_POINT ( 'NONE',  ( 41.46631938032478359, 113.1844580088725820, 29.45539723777780239 ) ) ;
#13669=ORIENTED_EDGE ( 'NONE', *, *, #17350, .F. ) ;
#13670=CARTESIAN_POINT ( 'NONE',  ( 39.92123440845004723, 104.3344580088725735, 29.95742577749337343 ) ) ;
#13672=CARTESIAN_POINT ( 'NONE',  ( 41.64333658814960870, 60.97977050742731109, 38.42115945441014446 ) ) ;
#13673=CARTESIAN_POINT ( 'NONE',  ( 39.42975644700377558, 114.4151871740940010, 36.81289934271958941 ) ) ;
#13675=CARTESIAN_POINT ( 'NONE',  ( 48.01140435219951996, 77.06049967264874567, 35.83527830041810347 ) ) ;
#13678=CARTESIAN_POINT ( 'NONE',  ( 39.92123440845005433, 71.33445800887257349, 29.95742577749336988 ) ) ;
#13680=CARTESIAN_POINT ( 'NONE',  ( 43.01140435219951286, 75.86518717409398960, 38.86567161673127657 ) ) ;
#13684=ORIENTED_EDGE ( 'NONE', *, *, #10273, .F. ) ;
#13688=ORIENTED_EDGE ( 'NONE', *, *, #719, .T. ) ;
#13689=CARTESIAN_POINT ( 'NONE',  ( 38.58424406990784661, 155.9651871740939555, 32.77220824515698183 ) ) ;
#13690=CARTESIAN_POINT ( 'NONE',  ( 43.01140435219951286, 158.3651871740939896, 29.55568802177586107 ) ) ;
#13691=ADVANCED_FACE ( 'NONE', ( #1338 ), #16318, .T. ) ;
#13692=CARTESIAN_POINT ( 'NONE',  ( 47.43856463449117911, 116.0297705074273296, 32.77220824515697473 ) ) ;
#13697=ORIENTED_EDGE ( 'NONE', *, *, #14599, .T. ) ;
#13698=CARTESIAN_POINT ( 'NONE',  ( 43.01140435219951996, 10.71049967264875491, 29.21067981925357060 ) ) ;
#13699=CARTESIAN_POINT ( 'NONE',  ( 43.01140435219951286, 129.5344580088725763, 39.21067981925356349 ) ) ;
#13700=CARTESIAN_POINT ( 'NONE',  ( 46.59305225739526435, 148.9151871740940294, 31.60846029578754468 ) ) ;
#13702=CARTESIAN_POINT ( 'NONE',  ( 48.01140435219951996, 82.13445800887255643, 35.83527830041809636 ) ) ;
#13706=CARTESIAN_POINT ( 'NONE',  ( 47.05648932407426344, 100.9104996726487400, 37.14960608071593384 ) ) ;
#13709=CARTESIAN_POINT ( 'NONE',  ( 47.43856463449118621, 97.87977050742732388, 34.21067981925357060 ) ) ;
#13712=CARTESIAN_POINT ( 'NONE',  ( 47.43856463449118621, 79.61518717409400381, 34.21067981925357060 ) ) ;
#13714=DIRECTION ( 'NONE',  ( 0.000000000000000000, 1.000000000000000000, 0.000000000000000000 ) ) ;
#13718=CARTESIAN_POINT ( 'NONE',  ( 40.27526882409969744, 141.8297705074273267, 37.97664729208901235 ) ) ;
#13723=CARTESIAN_POINT ( 'NONE',  ( 45.74753988029933538, 134.3297705074273267, 30.44471234641811819 ) ) ;
#13725=EDGE_CURVE ( 'NONE', #470, #12132, #2988, .T. ) ;
#13726=CARTESIAN_POINT ( 'NONE',  ( 44.37947211624943833, 61.01518717409400239, 38.42115945441014446 ) ) ;
#13733=CARTESIAN_POINT ( 'NONE',  ( 41.46631938032478359, 138.3844580088725991, 38.96596240072933170 ) ) ;
#13734=CARTESIAN_POINT ( 'NONE',  ( 41.64333658814960870, 126.9797705074273182, 38.42115945441014446 ) ) ;
#13737=CARTESIAN_POINT ( 'NONE',  ( 39.42975644700377558, 110.8151871740939924, 31.60846029578754468 ) ) ;
#13744=CARTESIAN_POINT ( 'NONE',  ( 38.58424406990785371, 87.52977050742730114, 35.64915139335015937 ) ) ;
#13745=VERTEX_POINT ( 'NONE', #1014 ) ;
#13746=CARTESIAN_POINT ( 'NONE',  ( 44.55648932407425633, 133.6104996726487286, 38.96596240072933170 ) ) ;
#13747=CARTESIAN_POINT ( 'NONE',  ( 41.46631938032478359, 74.18445800887258201, 29.45539723777780239 ) ) ;
#13748=CARTESIAN_POINT ( 'NONE',  ( 38.01140435219952707, 86.93445800887258201, 35.83527830041809636 ) ) ;
#13749=CARTESIAN_POINT ( 'NONE',  ( 47.05648932407426344, 125.5104996726487343, 31.27175355779120025 ) ) ;
#13750=CARTESIAN_POINT ( 'NONE',  ( 44.37947211624943833, 83.21518717409399812, 30.00020018409699318 ) ) ;
#13751=ADVANCED_FACE ( 'NONE', ( #3103 ), #1228, .T. ) ;
#13756=FACE_OUTER_BOUND ( 'NONE', #9908, .T. ) ;
#13757=CARTESIAN_POINT ( 'NONE',  ( 38.96631938032478359, 92.48445800887257917, 31.27175355779120025 ) ) ;
#13759=CARTESIAN_POINT ( 'NONE',  ( 47.43856463449117200, 154.7297705074273040, 35.64915139335016647 ) ) ;
#13760=CARTESIAN_POINT ( 'NONE',  ( 40.27526882409969033, 102.8297705074272983, 37.97664729208901946 ) ) ;
#13762=CARTESIAN_POINT ( 'NONE',  ( 45.74753988029934249, 140.0651871740940067, 30.44471234641812174 ) ) ;
#13767=CARTESIAN_POINT ( 'NONE',  ( 43.01140435219951286, 119.3651871740939896, 29.55568802177586463 ) ) ;
#13772=VERTEX_POINT ( 'NONE', #14778 ) ;
#13774=CARTESIAN_POINT ( 'NONE',  ( 48.01140435219951996, 97.28445800887259054, 34.21067981925357060 ) ) ;
#13776=CARTESIAN_POINT ( 'NONE',  ( 38.01140435219951996, 156.8604996726487855, 35.83527830041810347 ) ) ;
#13777=CARTESIAN_POINT ( 'NONE',  ( 38.58424406990784661, 117.2651871740940095, 35.64915139335016647 ) ) ;
#13779=CARTESIAN_POINT ( 'NONE',  ( 46.10157429594899270, 70.76049967264873430, 38.46393386101376421 ) ) ;
#13781=CARTESIAN_POINT ( 'NONE',  ( 38.96631938032478359, 74.48445800887257917, 31.27175355779120025 ) ) ;
#13784=CARTESIAN_POINT ( 'NONE',  ( 44.37947211624943833, 77.21518717409399812, 30.00020018409699318 ) ) ;
#13794=CARTESIAN_POINT ( 'NONE',  ( 38.58424406990784661, 140.9651871740939555, 32.77220824515698183 ) ) ;
#13796=CARTESIAN_POINT ( 'NONE',  ( 47.43856463449117911, 157.7651871740940237, 32.77220824515697473 ) ) ;
#13797=CARTESIAN_POINT ( 'NONE',  ( 47.43856463449118621, 106.8797705074273239, 34.21067981925357060 ) ) ;
#13804=CARTESIAN_POINT ( 'NONE',  ( 38.01140435219952707, 128.6344580088725706, 32.58608133808903773 ) ) ;
#13806=CARTESIAN_POINT ( 'NONE',  ( 45.74753988029933538, 83.32977050742732672, 30.44471234641811819 ) ) ;
#13807=CARTESIAN_POINT ( 'NONE',  ( 45.74753988029933538, 143.0651871740939782, 30.44471234641811819 ) ) ;
#13808=CARTESIAN_POINT ( 'NONE',  ( 44.55648932407425633, 101.8104996726487457, 29.45539723777780239 ) ) ;
#13814=CARTESIAN_POINT ( 'NONE',  ( 44.55648932407425633, 91.61049967264874283, 38.96596240072933170 ) ) ;
#13815=CARTESIAN_POINT ( 'NONE',  ( 46.59305225739526435, 88.57977050742732672, 36.81289934271958941 ) ) ;
#13818=CARTESIAN_POINT ( 'NONE',  ( 43.01140435219951286, 74.36518717409400381, 29.55568802177586107 ) ) ;
#13824=CARTESIAN_POINT ( 'NONE',  ( 47.05648932407426344, 84.98445800887257917, 37.14960608071593384 ) ) ;
#13826=CARTESIAN_POINT ( 'NONE',  ( 40.27526882409969744, 132.8297705074272983, 37.97664729208901235 ) ) ;
#13831=CARTESIAN_POINT ( 'NONE',  ( 38.58424406990784661, 132.5297705074272869, 35.64915139335016647 ) ) ;
#13832=CARTESIAN_POINT ( 'NONE',  ( 46.59305225739526435, 91.57977050742731251, 36.81289934271958941 ) ) ;
#13833=( BOUNDED_CURVE ( )  B_SPLINE_CURVE ( 2, ( #21036, #17381, #14077, #15737, #642, #20815, #9347, #12647, #19369, #14403, #16051, #7704, #748 ),
 .UNSPECIFIED., .F., .T. ) 
 B_SPLINE_CURVE_WITH_KNOTS ( ( 3, 2, 2, 2, 2, 2, 3 ),
 ( 0.4485294117647058987, 0.4500000000000000111, 0.4529411764705882359, 0.4558823529411764608, 0.4588235294117646856, 0.4617647058823529660, 0.4632352941176470784 ),
 .UNSPECIFIED. ) 
 CURVE ( )  GEOMETRIC_REPRESENTATION_ITEM ( )  RATIONAL_B_SPLINE_CURVE ( ( 0.9755282581475768211, 0.9755282581475768211, 1.000000000000000000, 0.9510565162951535312, 1.000000000000000000, 0.9510565162951535312, 1.000000000000000000, 0.9510565162951535312, 1.000000000000000000, 0.9510565162951535312, 1.000000000000000000, 0.9755282581475768211, 0.9755282581475768211 ) ) 
 REPRESENTATION_ITEM ( '' )  );
#13836=CARTESIAN_POINT ( 'NONE',  ( 44.37947211624943833, 98.21518717409399812, 30.00020018409699318 ) ) ;
#13837=CARTESIAN_POINT ( 'NONE',  ( 43.01140435219951286, 152.9604996726487798, 29.21067981925356705 ) ) ;
#13838=CARTESIAN_POINT ( 'NONE',  ( 38.01140435219952707, 108.7104996726487514, 34.21067981925357060 ) ) ;
#13841=CARTESIAN_POINT ( 'NONE',  ( 38.01140435219951996, 146.9344580088726104, 35.83527830041810347 ) ) ;
#13842=CARTESIAN_POINT ( 'NONE',  ( 44.37947211624943833, 118.2797705074273296, 38.42115945441014446 ) ) ;
#13844=CARTESIAN_POINT ( 'NONE',  ( 43.80332655382220253, 99.61133943119284595, 39.21067981925355639 ) ) ;
#13845=CARTESIAN_POINT ( 'NONE',  ( 40.27526882409969744, 102.5651871740939924, 37.97664729208901235 ) ) ;
#13846=EDGE_LOOP ( 'NONE', ( #8537, #8288, #5032, #13697 ) ) ;
#13852=CARTESIAN_POINT ( 'NONE',  ( 38.58424406990786082, 90.37977050742732388, 34.21067981925357060 ) ) ;
#13853=ORIENTED_EDGE ( 'NONE', *, *, #18788, .F. ) ;
#13854=CARTESIAN_POINT ( 'NONE',  ( 47.05648932407426344, 76.58445800887257349, 31.27175355779120025 ) ) ;
#13856=CARTESIAN_POINT ( 'NONE',  ( 43.01140435219951286, 130.4604996726487514, 39.46799094044489209 ) ) ;
#13857=CARTESIAN_POINT ( 'NONE',  ( 46.59305225739526435, 91.31518717409399244, 36.81289934271958941 ) ) ;
#13861=CARTESIAN_POINT ( 'NONE',  ( 43.01140435219951286, 116.0344580088725763, 29.21067981925356705 ) ) ;
#13863=CARTESIAN_POINT ( 'NONE',  ( 39.92123440845005433, 80.33445800887258770, 29.95742577749336988 ) ) ;
#13866=CARTESIAN_POINT ( 'NONE',  ( 43.01140435219951286, 151.1297705074273097, 38.86567161673127657 ) ) ;
#13867=CARTESIAN_POINT ( 'NONE',  ( 38.58424406990784661, 102.2297705074273182, 32.77220824515698183 ) ) ;
#13869=CARTESIAN_POINT ( 'NONE',  ( 41.64333658814960870, 134.5151871740939953, 30.00020018409699318 ) ) ;
#13870=PLANE ( 'NONE',  #8625 ) ;
#13875=CARTESIAN_POINT ( 'NONE',  ( 45.74753988029933538, 119.0651871740939782, 30.44471234641811819 ) ) ;
#13876=AXIS2_PLACEMENT_3D ( 'NONE', #3532, #5288, #12002 ) ;
#13877=ORIENTED_EDGE ( 'NONE', *, *, #10327, .T. ) ;
#13878=CARTESIAN_POINT ( 'NONE',  ( 43.01140435219951286, 125.0344580088725905, 29.21067981925356705 ) ) ;
#13880=CARTESIAN_POINT ( 'NONE',  ( 48.01140435219951996, 103.4344580088725536, 32.58608133808903773 ) ) ;
#13881=CARTESIAN_POINT ( 'NONE',  ( 46.59305225739526435, 151.5797705074273267, 36.81289934271958941 ) ) ;
#13882=CARTESIAN_POINT ( 'NONE',  ( 44.55648932407425633, 155.8104996726487741, 29.45539723777780239 ) ) ;
#13883=CARTESIAN_POINT ( 'NONE',  ( 47.43856463449117200, 112.4651871740939839, 35.64915139335016647 ) ) ;
#13885=EDGE_CURVE ( 'NONE', #20293, #11479, #17685, .T. ) ;
#13887=CARTESIAN_POINT ( 'NONE',  ( 48.01140435219951996, 68.36049967264872862, 32.58608133808903773 ) ) ;
#13892=( BOUNDED_CURVE ( )  B_SPLINE_CURVE ( 2, ( #8034, #12874, #14305, #14627, #19820, #19595, #16387, #6036, #9690, #18154, #9358, #18043, #7817 ),
 .UNSPECIFIED., .F., .F. ) 
 B_SPLINE_CURVE_WITH_KNOTS ( ( 3, 2, 2, 2, 2, 2, 3 ),
 ( 0.09558823529411765441, 0.09705882352941176683, 0.1000000000000000056, 0.1029411764705882304, 0.1058823529411764691, 0.1088235294117647078, 0.1102941176470588203 ),
 .UNSPECIFIED. ) 
 CURVE ( )  GEOMETRIC_REPRESENTATION_ITEM ( )  RATIONAL_B_SPLINE_CURVE ( ( 0.9755282581475767101, 0.9755282581475768211, 1.000000000000000000, 0.9510565162951535312, 1.000000000000000000, 0.9510565162951535312, 1.000000000000000000, 0.9510565162951535312, 1.000000000000000000, 0.9510565162951535312, 1.000000000000000000, 0.9755282581475768211, 0.9755282581475767101 ) ) 
 REPRESENTATION_ITEM ( '' )  );
#13893=CARTESIAN_POINT ( 'NONE',  ( 47.43856463449117200, 76.76518717409398107, 32.77220824515698183 ) ) ;
#13896=VERTEX_POINT ( 'NONE', #6182 ) ;
#13899=ORIENTED_EDGE ( 'NONE', *, *, #16655, .T. ) ;
#13900=CARTESIAN_POINT ( 'NONE',  ( 45.74753988029933538, 143.0651871740939782, 30.44471234641811819 ) ) ;
#13902=CARTESIAN_POINT ( 'NONE',  ( 43.01140435219951286, 104.6297705074273239, 29.55568802177586107 ) ) ;
#13904=ORIENTED_EDGE ( 'NONE', *, *, #15318, .T. ) ;
#13907=CARTESIAN_POINT ( 'NONE',  ( 47.43856463449118621, 112.8797705074273097, 34.21067981925357060 ) ) ;
#13909=CARTESIAN_POINT ( 'NONE',  ( 43.01140435219951286, 88.46049967264873715, 39.21067981925356349 ) ) ;
#13911=CARTESIAN_POINT ( 'NONE',  ( 43.01140435219951286, 149.3651871740939612, 29.55568802177586463 ) ) ;
#13912=CARTESIAN_POINT ( 'NONE',  ( 38.96631938032478359, 106.0104996726487485, 37.14960608071593384 ) ) ;
#13914=CARTESIAN_POINT ( 'NONE',  ( 38.01140435219952707, 60.71049967264874425, 34.21067981925357060 ) ) ;
#13919=DIRECTION ( 'NONE',  ( -0.000000000000000000, 1.000000000000000000, -0.000000000000000000 ) ) ;
#13921=CARTESIAN_POINT ( 'NONE',  ( 40.27526882409969033, 86.92977050742732104, 30.44471234641811819 ) ) ;
#13923=EDGE_CURVE ( 'NONE', #15014, #19018, #4889, .T. ) ;
#13924=CARTESIAN_POINT ( 'NONE',  ( 40.27526882409969744, 78.56518717409399244, 37.97664729208901235 ) ) ;
#13926=CARTESIAN_POINT ( 'NONE',  ( 43.01140435219951996, 10.71049967264875491, 34.21067981925357060 ) ) ;
#13928=CARTESIAN_POINT ( 'NONE',  ( 48.01140435219951996, 85.13445800887258486, 35.83527830041809636 ) ) ;
#13930=CARTESIAN_POINT ( 'NONE',  ( 44.37947211624943833, 130.2797705074273154, 38.42115945441014446 ) ) ;
#13933=CARTESIAN_POINT ( 'NONE',  ( 43.01140435219951286, 72.53445800887256212, 39.21067981925356349 ) ) ;
#13934=ORIENTED_EDGE ( 'NONE', *, *, #3727, .T. ) ;
#13935=CARTESIAN_POINT ( 'NONE',  ( 45.74753988029933538, 140.3297705074272983, 30.44471234641811819 ) ) ;
#13936=CARTESIAN_POINT ( 'NONE',  ( 38.58424406990784661, 93.22977050742730398, 32.77220824515698183 ) ) ;
#13939=CARTESIAN_POINT ( 'NONE',  ( 43.01140435219951286, 90.53445800887257633, 39.21067981925356349 ) ) ;
#13942=CARTESIAN_POINT ( 'NONE',  ( 46.59305225739526435, 97.91518717409400097, 31.60846029578754468 ) ) ;
#13947=CARTESIAN_POINT ( 'NONE',  ( 43.01140435219951286, 141.5344580088725763, 39.46799094044489209 ) ) ;
#13948=CARTESIAN_POINT ( 'NONE',  ( 47.43856463449117200, 113.0297705074273011, 32.77220824515698183 ) ) ;
#13951=CARTESIAN_POINT ( 'NONE',  ( 39.42975644700377558, 108.4151871740940152, 36.81289934271958941 ) ) ;
#13953=FACE_OUTER_BOUND ( 'NONE', #17131, .T. ) ;
#13958=CARTESIAN_POINT ( 'NONE',  ( 47.43856463449118621, 76.87977050742732388, 34.21067981925357060 ) ) ;
#13961=CARTESIAN_POINT ( 'NONE',  ( 38.01140435219951996, 65.93445800887258201, 35.83527830041810347 ) ) ;
#13963=CARTESIAN_POINT ( 'NONE',  ( 38.96631938032478359, 127.0104996726487343, 37.14960608071593384 ) ) ;
#13964=CARTESIAN_POINT ( 'NONE',  ( 47.43856463449118621, 91.61518717409400381, 34.21067981925357060 ) ) ;
#13968=CARTESIAN_POINT ( 'NONE',  ( 38.01140435219952707, 116.7844580088725763, 34.21067981925357060 ) ) ;
#13970=CARTESIAN_POINT ( 'NONE',  ( 43.01140435219951286, 80.03445800887257633, 29.21067981925356705 ) ) ;
#13972=CARTESIAN_POINT ( 'NONE',  ( 43.01140435219951286, 143.9604996726487229, 29.21067981925356705 ) ) ;
#13973=CARTESIAN_POINT ( 'NONE',  ( 39.42975644700377558, 144.6797705074273495, 36.81289934271958941 ) ) ;
#13974=CARTESIAN_POINT ( 'NONE',  ( 40.27526882409969033, 107.9297705074273352, 30.44471234641811819 ) ) ;
#13976=CARTESIAN_POINT ( 'NONE',  ( 41.64333658814960870, 140.5151871740939953, 30.00020018409699318 ) ) ;
#13980=CARTESIAN_POINT ( 'NONE',  ( 44.55648932407425633, 90.68445800887258201, 38.96596240072933170 ) ) ;
#13982=VECTOR ( 'NONE', #5759, 1000.000000000000000 ) ;
#13984=CARTESIAN_POINT ( 'NONE',  ( 40.27526882409969033, 116.6651871740939868, 30.44471234641811819 ) ) ;
#13985=VERTEX_POINT ( 'NONE', #3544 ) ;
#13989=CARTESIAN_POINT ( 'NONE',  ( 48.01140435219951996, 91.43445800887258201, 32.58608133808903773 ) ) ;
#13990=EDGE_CURVE ( 'NONE', #137, #17423, #15184, .T. ) ;
#13991=CARTESIAN_POINT ( 'NONE',  ( 41.64333658814960870, 146.7797705074273154, 30.00020018409699318 ) ) ;
#13992=CARTESIAN_POINT ( 'NONE',  ( 38.58424406990786082, 60.37977050742732388, 34.21067981925357060 ) ) ;
#13993=CARTESIAN_POINT ( 'NONE',  ( 46.59305225739526435, 118.3151871740940067, 36.81289934271958941 ) ) ;
#13996=CARTESIAN_POINT ( 'NONE',  ( 48.01140435219951996, 68.21049967264873715, 34.21067981925357060 ) ) ;
#13997=CARTESIAN_POINT ( 'NONE',  ( 41.46631938032478359, 108.3844580088725849, 38.96596240072933170 ) ) ;
#13998=CYLINDRICAL_SURFACE ( 'NONE', #6183, 4.999999999999997335 ) ;
#14002=CARTESIAN_POINT ( 'NONE',  ( 38.58424406990786082, 72.11518717409400381, 34.21067981925357060 ) ) ;
#14003=CARTESIAN_POINT ( 'NONE',  ( 39.92123440845005433, 64.16049967264873999, 38.46393386101375711 ) ) ;
#14006=VERTEX_POINT ( 'NONE', #15335 ) ;
#14011=CARTESIAN_POINT ( 'NONE',  ( 41.64333658814960870, 141.7151871740940123, 38.42115945441014446 ) ) ;
#14013=CARTESIAN_POINT ( 'NONE',  ( 44.37947211624943833, 107.4797705074273182, 30.00020018409699318 ) ) ;
#14018=CARTESIAN_POINT ( 'NONE',  ( 43.01140435219951286, 112.1297705074272812, 38.86567161673127657 ) ) ;
#14020=CARTESIAN_POINT ( 'NONE',  ( 40.27526882409969033, 149.6651871740939725, 30.44471234641811819 ) ) ;
#14022=CARTESIAN_POINT ( 'NONE',  ( 44.55648932407425633, 103.6104996726487428, 38.96596240072933170 ) ) ;
#14025=EDGE_CURVE ( 'NONE', #17423, #5662, #7150, .T. ) ;
#14027=CARTESIAN_POINT ( 'NONE',  ( 38.01140435219952707, 152.7844580088725763, 34.21067981925357060 ) ) ;
#14029=DIRECTION ( 'NONE',  ( 0.000000000000000000, 0.000000000000000000, 1.000000000000000000 ) ) ;
#14030=ORIENTED_EDGE ( 'NONE', *, *, #11809, .F. ) ;
#14031=CARTESIAN_POINT ( 'NONE',  ( 41.64333658814960870, 83.77977050742732956, 30.00020018409699318 ) ) ;
#14033=CARTESIAN_POINT ( 'NONE',  ( 38.58424406990785371, 78.26518717409402370, 35.64915139335015937 ) ) ;
#14039=CARTESIAN_POINT ( 'NONE',  ( 39.42975644700377558, 132.0797705074273267, 31.60846029578754468 ) ) ;
#14041=ORIENTED_EDGE ( 'NONE', *, *, #11706, .F. ) ;
#14045=CARTESIAN_POINT ( 'NONE',  ( 40.27526882409969033, 137.9297705074273210, 30.44471234641811819 ) ) ;
#14049=CARTESIAN_POINT ( 'NONE',  ( 43.01140435219951996, 10.71049967264875491, 39.21067981925356349 ) ) ;
#14050=CARTESIAN_POINT ( 'NONE',  ( 48.01140435219951996, 121.2844580088725763, 34.21067981925357060 ) ) ;
#14053=CARTESIAN_POINT ( 'NONE',  ( 45.74753988029933538, 97.16518717409398675, 37.97664729208901946 ) ) ;
#14054=CARTESIAN_POINT ( 'NONE',  ( 48.01140435219951996, 133.2844580088726048, 34.21067981925357060 ) ) ;
#14057=CARTESIAN_POINT ( 'NONE',  ( 38.96631938032478359, 129.0844580088725877, 37.14960608071593384 ) ) ;
#14058=CARTESIAN_POINT ( 'NONE',  ( 38.58424406990784661, 111.5297705074273154, 35.64915139335016647 ) ) ;
#14061=CARTESIAN_POINT ( 'NONE',  ( 43.01140435219951286, 105.8651871740939896, 38.86567161673127657 ) ) ;
#14064=CARTESIAN_POINT ( 'NONE',  ( 43.80332655382220963, 157.9575765865523351, 29.21067981925357060 ) ) ;
#14068=CARTESIAN_POINT ( 'NONE',  ( 47.43856463449117911, 77.02977050742731535, 32.77220824515697473 ) ) ;
#14071=CARTESIAN_POINT ( 'NONE',  ( 46.10157429594899270, 60.83445800887256638, 38.46393386101376421 ) ) ;
#14073=CARTESIAN_POINT ( 'NONE',  ( 38.01140435219951996, 117.5604996726487315, 32.58608133808903773 ) ) ;
#14074=CARTESIAN_POINT ( 'NONE',  ( 39.42975644700377558, 81.41518717409400097, 36.81289934271958941 ) ) ;
#14077=CARTESIAN_POINT ( 'NONE',  ( 44.55648932407425633, 113.8104996726487457, 29.45539723777780239 ) ) ;
#14080=CARTESIAN_POINT ( 'NONE',  ( 46.10157429594899270, 67.76049967264873430, 38.46393386101375711 ) ) ;
#14082=CARTESIAN_POINT ( 'NONE',  ( 43.01140435219951286, 140.6297705074273097, 29.55568802177586463 ) ) ;
#14083=EDGE_CURVE ( 'NONE', #20743, #16099, #9401, .T. ) ;
#14084=CARTESIAN_POINT ( 'NONE',  ( 45.74753988029933538, 104.3297705074272983, 30.44471234641811819 ) ) ;
#14085=CARTESIAN_POINT ( 'NONE',  ( 39.42975644700377558, 132.4151871740940010, 36.81289934271958941 ) ) ;
#14091=DIRECTION ( 'NONE',  ( 0.000000000000000000, 1.000000000000000000, 0.000000000000000000 ) ) ;
#14092=CARTESIAN_POINT ( 'NONE',  ( 44.37947211624943833, 116.2151871740940123, 30.00020018409699318 ) ) ;
#14094=ORIENTED_EDGE ( 'NONE', *, *, #7191, .F. ) ;
#14098=CARTESIAN_POINT ( 'NONE',  ( 39.92123440845004723, 92.33445800887255928, 29.95742577749337343 ) ) ;
#14099=CARTESIAN_POINT ( 'NONE',  ( 39.42975644700377558, 150.6797705074273210, 36.81289934271958941 ) ) ;
#14100=CARTESIAN_POINT ( 'NONE',  ( 46.10157429594899270, 157.7604996726487343, 38.46393386101376421 ) ) ;
#14101=CARTESIAN_POINT ( 'NONE',  ( 43.01140435219951286, 105.8651871740939754, 38.86567161673127657 ) ) ;
#14103=CARTESIAN_POINT ( 'NONE',  ( 47.05648932407426344, 74.51049967264873430, 31.27175355779120025 ) ) ;
#14107=CARTESIAN_POINT ( 'NONE',  ( 46.59305225739526435, 70.31518717409400665, 36.81289934271958941 ) ) ;
#14110=CARTESIAN_POINT ( 'NONE',  ( 45.51148226160370314, 59.71123016864974176, 29.88059778228138086 ) ) ;
#14116=CARTESIAN_POINT ( 'NONE',  ( 39.42975644700377558, 140.8151871740940067, 31.60846029578754468 ) ) ;
#14117=CARTESIAN_POINT ( 'NONE',  ( 38.58424406990785371, 108.5297705074273011, 35.64915139335015937 ) ) ;
#14118=ORIENTED_EDGE ( 'NONE', *, *, #17825, .T. ) ;
#14122=CARTESIAN_POINT ( 'NONE',  ( 38.01140435219951996, 116.9344580088725820, 35.83527830041810347 ) ) ;
#14123=EDGE_CURVE ( 'NONE', #19018, #17658, #3595, .T. ) ;
#14125=CARTESIAN_POINT ( 'NONE',  ( 38.58424406990784661, 143.9651871740940123, 32.77220824515698183 ) ) ;
#14126=CARTESIAN_POINT ( 'NONE',  ( 41.46631938032478359, 105.1104996726487428, 29.45539723777780239 ) ) ;
#14130=CARTESIAN_POINT ( 'NONE',  ( 43.80332655382220963, 158.8836182503284533, 29.21067981925357060 ) ) ;
#14132=CARTESIAN_POINT ( 'NONE',  ( 42.21948215057684450, 143.1113394311928460, 29.21067981925356705 ) ) ;
#14133=AXIS2_PLACEMENT_3D ( 'NONE', #16171, #12983, #21475 ) ;
#14134=CARTESIAN_POINT ( 'NONE',  ( 46.10157429594899270, 105.8344580088725735, 38.46393386101375711 ) ) ;
#14137=CARTESIAN_POINT ( 'NONE',  ( 46.59305225739526435, 86.17977050742732104, 31.60846029578754468 ) ) ;
#14139=CARTESIAN_POINT ( 'NONE',  ( 41.64333658814960870, 66.71518717409399812, 38.42115945441014446 ) ) ;
#14143=ORIENTED_EDGE ( 'NONE', *, *, #4945, .F. ) ;
#14145=CARTESIAN_POINT ( 'NONE',  ( 38.01140435219952707, 104.7844580088725763, 34.21067981925357060 ) ) ;
#14146=CARTESIAN_POINT ( 'NONE',  ( 45.74753988029934249, 130.4297705074273210, 37.97664729208901235 ) ) ;
#14149=( BOUNDED_CURVE ( )  B_SPLINE_CURVE ( 2, ( #6995, #12145, #20117, #2022, #18879, #13379, #5328, #8754, #20221, #8541, #3787, #11831, #15471 ),
 .UNSPECIFIED., .F., .F. ) 
 B_SPLINE_CURVE_WITH_KNOTS ( ( 3, 2, 2, 2, 2, 2, 3 ),
 ( 0.3161764705882352811, 0.3176470588235293935, 0.3205882352941176738, 0.3235294117647058987, 0.3264705882352941235, 0.3294117647058823484, 0.3308823529411764608 ),
 .UNSPECIFIED. ) 
 CURVE ( )  GEOMETRIC_REPRESENTATION_ITEM ( )  RATIONAL_B_SPLINE_CURVE ( ( 0.9755282581475768211, 0.9755282581475768211, 1.000000000000000000, 0.9510565162951535312, 1.000000000000000000, 0.9510565162951535312, 1.000000000000000000, 0.9510565162951535312, 1.000000000000000000, 0.9510565162951535312, 1.000000000000000000, 0.9755282581475768211, 0.9755282581475768211 ) ) 
 REPRESENTATION_ITEM ( '' )  );
#14151=CARTESIAN_POINT ( 'NONE',  ( 40.27526882409969033, 126.8297705074273409, 37.97664729208901946 ) ) ;
#14154=CARTESIAN_POINT ( 'NONE',  ( 44.55648932407425633, 154.6104996726487570, 38.96596240072933170 ) ) ;
#14155=EDGE_CURVE ( 'NONE', #17073, #1468, #13601, .T. ) ;
#14157=CARTESIAN_POINT ( 'NONE',  ( 47.05648932407426344, 120.9844580088725934, 37.14960608071593384 ) ) ;
#14160=CARTESIAN_POINT ( 'NONE',  ( 47.43856463449117200, 97.46518717409399812, 35.64915139335016647 ) ) ;
#14161=CARTESIAN_POINT ( 'NONE',  ( 46.10157429594899270, 73.76049967264873430, 38.46393386101375711 ) ) ;
#14162=CARTESIAN_POINT ( 'NONE',  ( 44.55648932407425633, 125.8104996726487315, 29.45539723777780239 ) ) ;
#14165=CARTESIAN_POINT ( 'NONE',  ( 48.01140435219951996, 109.4344580088725820, 32.58608133808903773 ) ) ;
#14166=CARTESIAN_POINT ( 'NONE',  ( 39.92123440845004723, 135.2344580088725650, 38.46393386101376421 ) ) ;
#14167=CARTESIAN_POINT ( 'NONE',  ( 46.59305225739526435, 112.5797705074273125, 36.81289934271958941 ) ) ;
#14170=CARTESIAN_POINT ( 'NONE',  ( 47.43856463449117911, 97.76518717409398107, 32.77220824515697473 ) ) ;
#14173=CARTESIAN_POINT ( 'NONE',  ( 48.01140435219951996, 157.2844580088725763, 34.21067981925357060 ) ) ;
#14176=DIRECTION ( 'NONE',  ( 0.000000000000000000, 1.000000000000000000, 0.000000000000000000 ) ) ;
#14177=CARTESIAN_POINT ( 'NONE',  ( 39.42975644700377558, 72.07977050742732672, 31.60846029578754468 ) ) ;
#14179=ORIENTED_EDGE ( 'NONE', *, *, #5560, .T. ) ;
#14181=CARTESIAN_POINT ( 'NONE',  ( 48.01140435219951996, 125.0604996726487741, 35.83527830041810347 ) ) ;
#14182=CARTESIAN_POINT ( 'NONE',  ( 43.01140435219951286, 77.36518717409400381, 29.55568802177586463 ) ) ;
#14189=CARTESIAN_POINT ( 'NONE',  ( 41.46631938032478359, 149.1844580088725820, 29.45539723777780239 ) ) ;
#14190=CARTESIAN_POINT ( 'NONE',  ( 43.01140435219951286, 143.6297705074272812, 29.55568802177586463 ) ) ;
#14192=CARTESIAN_POINT ( 'NONE',  ( 47.43856463449118621, 136.6151871740940180, 34.21067981925357060 ) ) ;
#14196=CARTESIAN_POINT ( 'NONE',  ( 45.22505347682923826, 59.38050100342834270, 30.37668637662395099 ) ) ;
#14198=EDGE_CURVE ( 'NONE', #10505, #15773, #2889, .T. ) ;
#14201=CARTESIAN_POINT ( 'NONE',  ( 46.59305225739526435, 103.9151871740940152, 31.60846029578754468 ) ) ;
#14204=ORIENTED_EDGE ( 'NONE', *, *, #4893, .T. ) ;
#14205=CARTESIAN_POINT ( 'NONE',  ( 41.46631938032478359, 93.38445800887258486, 38.96596240072933170 ) ) ;
#14206=CARTESIAN_POINT ( 'NONE',  ( 38.01140435219951996, 150.5604996726487741, 32.58608133808903773 ) ) ;
#14207=CARTESIAN_POINT ( 'NONE',  ( 43.01140435219951286, 108.8651871740939896, 38.86567161673127657 ) ) ;
#14209=CARTESIAN_POINT ( 'NONE',  ( 38.01140435219952707, 60.71049967264874425, 34.21067981925357060 ) ) ;
#14213=CARTESIAN_POINT ( 'NONE',  ( 46.10157429594899270, 79.73445800887257917, 29.95742577749336988 ) ) ;
#14215=CARTESIAN_POINT ( 'NONE',  ( 47.43856463449117200, 67.76518717409399528, 32.77220824515698183 ) ) ;
#14217=CARTESIAN_POINT ( 'NONE',  ( 48.01140435219951996, 104.2104996726487371, 34.21067981925357060 ) ) ;
#14223=CARTESIAN_POINT ( 'NONE',  ( 43.01140435219951996, 10.71049967264875491, 34.21067981925357060 ) ) ;
#14224=CARTESIAN_POINT ( 'NONE',  ( 43.01140435219951286, 140.3651871740940180, 29.55568802177586463 ) ) ;
#14225=CARTESIAN_POINT ( 'NONE',  ( 45.74753988029934249, 107.3297705074272983, 30.44471234641812174 ) ) ;
#14226=ORIENTED_EDGE ( 'NONE', *, *, #11753, .F. ) ;
#14227=ORIENTED_EDGE ( 'NONE', *, *, #12984, .T. ) ;
#14230=CARTESIAN_POINT ( 'NONE',  ( 38.01140435219952707, 113.7844580088725763, 34.21067981925357060 ) ) ;
#14233=CARTESIAN_POINT ( 'NONE',  ( 46.59305225739526435, 79.57977050742731251, 36.81289934271958941 ) ) ;
#14234=CARTESIAN_POINT ( 'NONE',  ( 43.01140435219951286, 132.8651871740940180, 38.86567161673127657 ) ) ;
#14235=CARTESIAN_POINT ( 'NONE',  ( 46.10157429594899270, 98.66049967264872578, 29.95742577749337343 ) ) ;
#14238=CARTESIAN_POINT ( 'NONE',  ( 48.01140435219951996, 119.3604996726487570, 32.58608133808903773 ) ) ;
#14240=CARTESIAN_POINT ( 'NONE',  ( 38.01140435219952707, 152.6344580088725706, 32.58608133808903773 ) ) ;
#14241=CARTESIAN_POINT ( 'NONE',  ( 47.05648932407426344, 106.5844580088725877, 31.27175355779120025 ) ) ;
#14243=CARTESIAN_POINT ( 'NONE',  ( 38.58424406990784661, 84.22977050742730398, 32.77220824515698183 ) ) ;
#14247=CARTESIAN_POINT ( 'NONE',  ( 38.01140435219952707, 104.6344580088725564, 32.58608133808903773 ) ) ;
#14248=CARTESIAN_POINT ( 'NONE',  ( 40.27526882409969744, 131.9297705074273210, 30.44471234641812174 ) ) ;
#14250=EDGE_LOOP ( 'NONE', ( #18300, #18874, #1987, #9851 ) ) ;
#14252=CARTESIAN_POINT ( 'NONE',  ( 43.01140435219951286, 74.03445800887257633, 29.21067981925356705 ) ) ;
#14254=CARTESIAN_POINT ( 'NONE',  ( 47.43856463449118621, 130.8797705074273381, 34.21067981925357060 ) ) ;
#14256=CARTESIAN_POINT ( 'NONE',  ( 47.43856463449117200, 89.02977050742731535, 32.77220824515698183 ) ) ;
#14258=CARTESIAN_POINT ( 'NONE',  ( 43.01140435219951286, 128.9604996726487229, 29.21067981925356705 ) ) ;
#14261=CARTESIAN_POINT ( 'NONE',  ( 41.64333658814960870, 84.71518717409399812, 38.42115945441014446 ) ) ;
#14263=CARTESIAN_POINT ( 'NONE',  ( 46.10157429594899270, 124.7604996726487343, 38.46393386101375711 ) ) ;
#14267=CARTESIAN_POINT ( 'NONE',  ( 38.01140435219952707, 131.9344580088725820, 35.83527830041809636 ) ) ;
#14268=CARTESIAN_POINT ( 'NONE',  ( 48.01140435219951996, 133.1344580088725991, 35.83527830041810347 ) ) ;
#14269=CARTESIAN_POINT ( 'NONE',  ( 40.27526882409969033, 117.8297705074273267, 37.97664729208901946 ) ) ;
#14272=CARTESIAN_POINT ( 'NONE',  ( 40.27526882409969744, 93.56518717409397823, 37.97664729208901235 ) ) ;
#14277=( BOUNDED_CURVE ( )  B_SPLINE_CURVE ( 2, ( #10229, #513, #11978, #18602, #17253, #15404, #1737, #10118, #10337, #12083, #5261, #186, #3826 ),
 .UNSPECIFIED., .F., .F. ) 
 B_SPLINE_CURVE_WITH_KNOTS ( ( 3, 2, 2, 2, 2, 2, 3 ),
 ( 0.1691176470588235115, 0.1705882352941176516, 0.1735294117647058765, 0.1764705882352941291, 0.1794117647058823539, 0.1823529411764705788, 0.1838235294117646912 ),
 .UNSPECIFIED. ) 
 CURVE ( )  GEOMETRIC_REPRESENTATION_ITEM ( )  RATIONAL_B_SPLINE_CURVE ( ( 0.9755282581475765991, 0.9755282581475764880, 1.000000000000000000, 0.9510565162951535312, 1.000000000000000000, 0.9510565162951535312, 1.000000000000000000, 0.9510565162951535312, 1.000000000000000000, 0.9510565162951535312, 1.000000000000000000, 0.9755282581475769321, 0.9755282581475765991 ) ) 
 REPRESENTATION_ITEM ( '' )  );
#14281=CARTESIAN_POINT ( 'NONE',  ( 41.64333658814960870, 75.97977050742731819, 38.42115945441014446 ) ) ;
#14282=ORIENTED_EDGE ( 'NONE', *, *, #5172, .F. ) ;
#14283=EDGE_LOOP ( 'NONE', ( #11117, #16852, #11735, #9481 ) ) ;
#14284=CARTESIAN_POINT ( 'NONE',  ( 44.37947211624943833, 155.4797705074273324, 30.00020018409699318 ) ) ;
#14286=LINE ( 'NONE', #12532, #2790 ) ;
#14287=CARTESIAN_POINT ( 'NONE',  ( 47.05648932407426344, 118.9104996726487400, 37.14960608071593384 ) ) ;
#14288=CARTESIAN_POINT ( 'NONE',  ( 46.59305225739526435, 76.31518717409399244, 36.81289934271958941 ) ) ;
#14294=CARTESIAN_POINT ( 'NONE',  ( 44.55648932407425633, 156.6844580088725820, 38.96596240072933170 ) ) ;
#14296=CARTESIAN_POINT ( 'NONE',  ( 40.27526882409969033, 143.9297705074273210, 30.44471234641811819 ) ) ;
#14299=CARTESIAN_POINT ( 'NONE',  ( 40.27526882409969744, 128.6651871740940010, 30.44471234641812174 ) ) ;
#14303=CYLINDRICAL_SURFACE ( 'NONE', #3401, 4.999999999999997335 ) ;
#14305=CARTESIAN_POINT ( 'NONE',  ( 44.55648932407425633, 149.8104996726487457, 29.45539723777780239 ) ) ;
#14307=CARTESIAN_POINT ( 'NONE',  ( 38.01140435219952707, 120.7104996726487371, 34.21067981925357060 ) ) ;
#14308=CARTESIAN_POINT ( 'NONE',  ( 47.43856463449117200, 109.7651871740939953, 32.77220824515698183 ) ) ;
#14312=CARTESIAN_POINT ( 'NONE',  ( 43.01140435219951286, 95.03445800887259054, 28.95336869806222779 ) ) ;
#14313=DIRECTION ( 'NONE',  ( 0.000000000000000000, 0.000000000000000000, -1.000000000000000000 ) ) ;
#14315=CARTESIAN_POINT ( 'NONE',  ( 48.01140435219951996, 152.2104996726487514, 34.21067981925357060 ) ) ;
#14316=CARTESIAN_POINT ( 'NONE',  ( 40.27526882409969033, 105.5651871740939782, 37.97664729208901946 ) ) ;
#14319=CARTESIAN_POINT ( 'NONE',  ( 41.46631938032478359, 61.31049967264873146, 38.96596240072933170 ) ) ;
#14321=CARTESIAN_POINT ( 'NONE',  ( 43.80332655382220253, 61.95757658655229960, 29.21067981925356705 ) ) ;
#14323=DIRECTION ( 'NONE',  ( 0.000000000000000000, 1.000000000000000000, 0.000000000000000000 ) ) ;
#14324=CARTESIAN_POINT ( 'NONE',  ( 44.55648932407425633, 146.8104996726487457, 29.45539723777780239 ) ) ;
#14325=CARTESIAN_POINT ( 'NONE',  ( 44.37947211624943833, 70.01518717409399528, 38.42115945441014446 ) ) ;
#14335=ORIENTED_EDGE ( 'NONE', *, *, #16732, .T. ) ;
#14336=CARTESIAN_POINT ( 'NONE',  ( 41.64333658814960870, 129.7151871740940123, 38.42115945441014446 ) ) ;
#14337=CARTESIAN_POINT ( 'NONE',  ( 44.37947211624943833, 155.2151871740940123, 30.00020018409699318 ) ) ;
#14339=VERTEX_POINT ( 'NONE', #713 ) ;
#14340=ADVANCED_FACE ( 'NONE', ( #18904 ), #2255, .F. ) ;
#14345=CARTESIAN_POINT ( 'NONE',  ( 43.01140435219951286, 74.62977050742732388, 29.55568802177586463 ) ) ;
#14346=CARTESIAN_POINT ( 'NONE',  ( 41.64333658814960870, 131.5151871740939953, 30.00020018409699318 ) ) ;
#14348=CARTESIAN_POINT ( 'NONE',  ( 46.10157429594899270, 94.76049967264873430, 38.46393386101376421 ) ) ;
#14350=CARTESIAN_POINT ( 'NONE',  ( 42.21948215057684450, 60.03738109496900677, 29.21067981925356705 ) ) ;
#14353=CARTESIAN_POINT ( 'NONE',  ( 48.01140435219951996, 64.13445800887257064, 35.83527830041809636 ) ) ;
#14354=DIRECTION ( 'NONE',  ( 0.000000000000000000, 0.000000000000000000, 1.000000000000000000 ) ) ;
#14356=CARTESIAN_POINT ( 'NONE',  ( 47.43856463449117200, 74.02977050742730114, 32.77220824515698183 ) ) ;
#14362=CARTESIAN_POINT ( 'NONE',  ( 43.01140435219951286, 101.0344580088725621, 29.21067981925356705 ) ) ;
#14363=CARTESIAN_POINT ( 'NONE',  ( 43.01140435219951286, 122.6297705074273239, 29.55568802177586107 ) ) ;
#14367=CARTESIAN_POINT ( 'NONE',  ( 38.29782421105369394, 159.5451350900380305, 34.21067981925357060 ) ) ;
#14368=EDGE_LOOP ( 'NONE', ( #11294, #11402, #3918, #12115 ) ) ;
#14369=CARTESIAN_POINT ( 'NONE',  ( 41.64333658814960870, 122.7797705074273296, 30.00020018409699318 ) ) ;
#14371=CARTESIAN_POINT ( 'NONE',  ( 48.01140435219951996, 134.0604996726486888, 35.83527830041809636 ) ) ;
#14372=CARTESIAN_POINT ( 'NONE',  ( 41.46631938032478359, 99.11049967264872862, 29.45539723777780239 ) ) ;
#14380=CARTESIAN_POINT ( 'NONE',  ( 38.01140435219951996, 134.9344580088725536, 35.83527830041810347 ) ) ;
#14381=CARTESIAN_POINT ( 'NONE',  ( 39.42975644700377558, 102.6797705074273210, 36.81289934271958941 ) ) ;
#14384=CARTESIAN_POINT ( 'NONE',  ( 38.58424406990786082, 93.11518717409400381, 34.21067981925357060 ) ) ;
#14385=CARTESIAN_POINT ( 'NONE',  ( 41.46631938032478359, 90.11049967264874283, 29.45539723777780239 ) ) ;
#14387=CARTESIAN_POINT ( 'NONE',  ( 43.01140435219951996, 158.0344580088725763, 29.21067981925357060 ) ) ;
#14392=CARTESIAN_POINT ( 'NONE',  ( 38.58424406990785371, 75.52977050742732956, 35.64915139335015937 ) ) ;
#14393=ORIENTED_EDGE ( 'NONE', *, *, #14198, .T. ) ;
#14395=CARTESIAN_POINT ( 'NONE',  ( 46.59305225739526435, 154.5797705074273267, 36.81289934271958941 ) ) ;
#14398=CARTESIAN_POINT ( 'NONE',  ( 39.92123440845004723, 121.1604996726487400, 38.46393386101376421 ) ) ;
#14399=CARTESIAN_POINT ( 'NONE',  ( 39.42975644700377558, 78.41518717409400097, 36.81289934271958941 ) ) ;
#14401=EDGE_CURVE ( 'NONE', #10776, #4102, #7987, .T. ) ;
#14403=CARTESIAN_POINT ( 'NONE',  ( 46.10157429594899270, 112.7604996726487485, 38.46393386101375711 ) ) ;
#14406=LINE ( 'NONE', #16166, #4801 ) ;
#14407=CARTESIAN_POINT ( 'NONE',  ( 46.59305225739526435, 145.5797705074273267, 36.81289934271958941 ) ) ;
#14408=( BOUNDED_CURVE ( )  B_SPLINE_CURVE ( 2, ( #8551, #16686, #3253, #1818, #5233, #13499, #6792, #18783, #20553, #20230, #15479, #5124, #10414 ),
 .UNSPECIFIED., .F., .F. ) 
 B_SPLINE_CURVE_WITH_KNOTS ( ( 3, 2, 2, 2, 2, 2, 3 ),
 ( 0.8014705882352941568, 0.8029411764705882693, 0.8058823529411764941, 0.8088235294117647189, 0.8117647058823529438, 0.8147058823529411686, 0.8161764705882352811 ),
 .UNSPECIFIED. ) 
 CURVE ( )  GEOMETRIC_REPRESENTATION_ITEM ( )  RATIONAL_B_SPLINE_CURVE ( ( 0.9755282581475768211, 0.9755282581475768211, 1.000000000000000000, 0.9510565162951535312, 1.000000000000000000, 0.9510565162951535312, 1.000000000000000000, 0.9510565162951535312, 1.000000000000000000, 0.9510565162951535312, 1.000000000000000000, 0.9755282581475768211, 0.9755282581475768211 ) ) 
 REPRESENTATION_ITEM ( '' )  );
#14410=CARTESIAN_POINT ( 'NONE',  ( 41.64333658814960870, 125.5151871740939953, 30.00020018409699318 ) ) ;
#14412=CARTESIAN_POINT ( 'NONE',  ( 42.21948215057683740, 151.3836182503284817, 39.21067981925355639 ) ) ;
#14418=CARTESIAN_POINT ( 'NONE',  ( 40.27526882409969033, 108.5651871740939924, 37.97664729208901946 ) ) ;
#14422=CARTESIAN_POINT ( 'NONE',  ( 48.01140435219951996, 94.28445800887259054, 34.21067981925357060 ) ) ;
#14425=CARTESIAN_POINT ( 'NONE',  ( 47.05648932407426344, 151.9104996726487400, 37.14960608071593384 ) ) ;
#14426=CARTESIAN_POINT ( 'NONE',  ( 39.42975644700377558, 105.4151871740940152, 36.81289934271958941 ) ) ;
#14428=CARTESIAN_POINT ( 'NONE',  ( 38.01140435219951996, 63.56049967264873146, 32.58608133808903773 ) ) ;
#14430=CYLINDRICAL_SURFACE ( 'NONE', #10088, 4.999999999999997335 ) ;
#14431=DIRECTION ( 'NONE',  ( 0.000000000000000000, 1.000000000000000000, 0.000000000000000000 ) ) ;
#14432=CYLINDRICAL_SURFACE ( 'NONE', #10726, 4.999999999999997335 ) ;
#14434=CARTESIAN_POINT ( 'NONE',  ( 39.42975644700377558, 72.41518717409400097, 36.81289934271958941 ) ) ;
#14436=CARTESIAN_POINT ( 'NONE',  ( 48.01140435219951996, 95.36049967264872862, 32.58608133808903773 ) ) ;
#14439=VERTEX_POINT ( 'NONE', #6432 ) ;
#14443=CARTESIAN_POINT ( 'NONE',  ( 47.43856463449117200, 136.7651871740939953, 32.77220824515698183 ) ) ;
#14444=EDGE_CURVE ( 'NONE', #8092, #13745, #5149, .T. ) ;
#14445=CARTESIAN_POINT ( 'NONE',  ( 44.37947211624943833, 92.47977050742731819, 30.00020018409699318 ) ) ;
#14449=ORIENTED_EDGE ( 'NONE', *, *, #10032, .F. ) ;
#14451=CARTESIAN_POINT ( 'NONE',  ( 47.43856463449118621, 73.87977050742732388, 34.21067981925357060 ) ) ;
#14452=CARTESIAN_POINT ( 'NONE',  ( 38.58424406990786082, 132.1151871740940180, 34.21067981925357060 ) ) ;
#14453=CARTESIAN_POINT ( 'NONE',  ( 44.55648932407425633, 88.61049967264874283, 38.96596240072933170 ) ) ;
#14455=CYLINDRICAL_SURFACE ( 'NONE', #5092, 4.999999999999997335 ) ;
#14457=CARTESIAN_POINT ( 'NONE',  ( 48.01140435219951996, 107.0604996726487457, 35.83527830041809636 ) ) ;
#14458=CARTESIAN_POINT ( 'NONE',  ( 46.10157429594899270, 61.76049967264874141, 38.46393386101375711 ) ) ;
#14459=ORIENTED_EDGE ( 'NONE', *, *, #1943, .F. ) ;
#14460=CARTESIAN_POINT ( 'NONE',  ( 45.74753988029933538, 74.32977050742729830, 30.44471234641811819 ) ) ;
#14464=ORIENTED_EDGE ( 'NONE', *, *, #1391, .F. ) ;
#14466=CARTESIAN_POINT ( 'NONE',  ( 44.55648932407425633, 123.6844580088725820, 38.96596240072933170 ) ) ;
#14468=ADVANCED_FACE ( 'NONE', ( #1144 ), #4553, .T. ) ;
#14469=CARTESIAN_POINT ( 'NONE',  ( 45.74753988029934249, 127.4297705074273352, 37.97664729208901235 ) ) ;
#14472=CARTESIAN_POINT ( 'NONE',  ( 39.42975644700377558, 129.0797705074273267, 31.60846029578754468 ) ) ;
#14473=CARTESIAN_POINT ( 'NONE',  ( 43.01140435219951286, 73.46049967264872294, 39.21067981925356349 ) ) ;
#14474=CARTESIAN_POINT ( 'NONE',  ( 38.96631938032478359, 59.48445800887257207, 31.27175355779120025 ) ) ;
#14476=VECTOR ( 'NONE', #2015, 1000.000000000000000 ) ;
#14481=CARTESIAN_POINT ( 'NONE',  ( 43.80332655382220253, 133.9575765865523067, 29.21067981925356705 ) ) ;
#14482=CARTESIAN_POINT ( 'NONE',  ( 43.01140435219951286, 130.4604996726487229, 39.21067981925356349 ) ) ;
#14484=PRODUCT_CONTEXT ( 'NONE', #4779, 'mechanical' ) ;
#14488=CARTESIAN_POINT ( 'NONE',  ( 47.05648932407426344, 136.5844580088725877, 31.27175355779120025 ) ) ;
#14489=CARTESIAN_POINT ( 'NONE',  ( 46.59305225739526435, 101.1797705074273210, 31.60846029578754468 ) ) ;
#14492=CARTESIAN_POINT ( 'NONE',  ( 47.43856463449117911, 100.4651871740939981, 35.64915139335015937 ) ) ;
#14495=CARTESIAN_POINT ( 'NONE',  ( 47.05648932407426344, 127.9104996726487542, 37.14960608071593384 ) ) ;
#14500=CARTESIAN_POINT ( 'NONE',  ( 39.42975644700377558, 63.67977050742732104, 36.81289934271958941 ) ) ;
#14502=ORIENTED_EDGE ( 'NONE', *, *, #15611, .T. ) ;
#14506=CARTESIAN_POINT ( 'NONE',  ( 38.01140435219952707, 123.7104996726487371, 34.21067981925357060 ) ) ;
#14507=CARTESIAN_POINT ( 'NONE',  ( 46.59305225739526435, 82.31518717409400665, 36.81289934271958941 ) ) ;
#14509=CARTESIAN_POINT ( 'NONE',  ( 43.01140435219951286, 95.03445800887257633, 29.21067981925356705 ) ) ;
#14513=EDGE_CURVE ( 'NONE', #872, #15251, #10456, .T. ) ;
#14516=CARTESIAN_POINT ( 'NONE',  ( 46.59305225739526435, 137.1797705074273210, 31.60846029578754468 ) ) ;
#14518=CARTESIAN_POINT ( 'NONE',  ( 44.37947211624943833, 130.0151871740939953, 38.42115945441014446 ) ) ;
#14520=CARTESIAN_POINT ( 'NONE',  ( 38.96631938032478359, 150.4104996726487400, 31.27175355779120025 ) ) ;
#14524=CARTESIAN_POINT ( 'NONE',  ( 41.46631938032478359, 120.1104996726487570, 29.45539723777780239 ) ) ;
#14525=CARTESIAN_POINT ( 'NONE',  ( 45.74753988029933538, 109.1651871740939868, 37.97664729208901946 ) ) ;
#14529=CARTESIAN_POINT ( 'NONE',  ( 48.01140435219951996, 85.28445800887257633, 34.21067981925357060 ) ) ;
#14531=CARTESIAN_POINT ( 'NONE',  ( 38.01140435219951996, 147.5604996726487457, 32.58608133808903773 ) ) ;
#14532=CARTESIAN_POINT ( 'NONE',  ( 45.74753988029933538, 104.0651871740940067, 30.44471234641811819 ) ) ;
#14534=CARTESIAN_POINT ( 'NONE',  ( 44.55648932407425633, 65.81049967264873146, 29.45539723777780239 ) ) ;
#14537=CARTESIAN_POINT ( 'NONE',  ( 48.01140435219951996, 118.1344580088725849, 35.83527830041809636 ) ) ;
#14538=CARTESIAN_POINT ( 'NONE',  ( 47.05648932407426344, 79.58445800887257349, 31.27175355779120025 ) ) ;
#14540=CARTESIAN_POINT ( 'NONE',  ( 43.01140435219951286, 62.36518717409399670, 29.55568802177586463 ) ) ;
#14542=CARTESIAN_POINT ( 'NONE',  ( 44.37947211624943833, 152.2151871740940123, 30.00020018409699318 ) ) ;
#14547=CARTESIAN_POINT ( 'NONE',  ( 41.64333658814960870, 65.51518717409400949, 30.00020018409699318 ) ) ;
#14552=CARTESIAN_POINT ( 'NONE',  ( 45.74753988029933538, 139.1651871740940010, 37.97664729208901946 ) ) ;
#14558=CARTESIAN_POINT ( 'NONE',  ( 44.37947211624943833, 80.47977050742731819, 30.00020018409699318 ) ) ;
#14559=CARTESIAN_POINT ( 'NONE',  ( 45.74753988029933538, 140.0651871740940067, 30.44471234641811819 ) ) ;
#14560=CARTESIAN_POINT ( 'NONE',  ( 38.96631938032478359, 87.41049967264873999, 31.27175355779120025 ) ) ;
#14565=FACE_OUTER_BOUND ( 'NONE', #13846, .T. ) ;
#14567=ORIENTED_EDGE ( 'NONE', *, *, #14513, .F. ) ;
#14568=CARTESIAN_POINT ( 'NONE',  ( 44.37947211624943833, 71.47977050742731819, 30.00020018409699318 ) ) ;
#14574=CARTESIAN_POINT ( 'NONE',  ( 48.01140435219951996, 124.2844580088725905, 34.21067981925357060 ) ) ;
#14576=CARTESIAN_POINT ( 'NONE',  ( 47.43856463449117911, 122.0297705074273154, 32.77220824515697473 ) ) ;
#14580=CARTESIAN_POINT ( 'NONE',  ( 47.43856463449118621, 127.8797705074273239, 34.21067981925357060 ) ) ;
#14583=CARTESIAN_POINT ( 'NONE',  ( 39.92123440845004723, 68.33445800887258770, 29.95742577749337343 ) ) ;
#14585=CARTESIAN_POINT ( 'NONE',  ( 43.01140435219951996, 10.71049967264875491, 34.21067981925357060 ) ) ;
#14586=CARTESIAN_POINT ( 'NONE',  ( 42.21948215057684450, 101.1113394311928460, 29.21067981925356705 ) ) ;
#14591=CARTESIAN_POINT ( 'NONE',  ( 43.80332655382220253, 130.5373810949689926, 39.21067981925355639 ) ) ;
#14593=CARTESIAN_POINT ( 'NONE',  ( 46.10157429594899270, 124.7344580088725792, 29.95742577749337343 ) ) ;
#14594=CARTESIAN_POINT ( 'NONE',  ( 47.43856463449117200, 100.7297705074273040, 35.64915139335016647 ) ) ;
#14598=CARTESIAN_POINT ( 'NONE',  ( 38.58424406990785371, 96.26518717409400949, 35.64915139335015937 ) ) ;
#14599=EDGE_CURVE ( 'NONE', #13513, #6293, #7412, .T. ) ;
#14600=DIRECTION ( 'NONE',  ( 0.000000000000000000, 0.000000000000000000, 1.000000000000000000 ) ) ;
#14605=CARTESIAN_POINT ( 'NONE',  ( 41.64333658814960870, 63.97977050742731109, 38.42115945441014446 ) ) ;
#14608=CARTESIAN_POINT ( 'NONE',  ( 45.74753988029933538, 155.3297705074273267, 30.44471234641811819 ) ) ;
#14609=EDGE_CURVE ( 'NONE', #14883, #2955, #9665, .T. ) ;
#14613=CARTESIAN_POINT ( 'NONE',  ( 41.46631938032478359, 114.1104996726487428, 29.45539723777780239 ) ) ;
#14614=CARTESIAN_POINT ( 'NONE',  ( 45.74753988029933538, 71.06518717409400665, 30.44471234641811819 ) ) ;
#14615=CARTESIAN_POINT ( 'NONE',  ( 41.46631938032478359, 65.18445800887258201, 29.45539723777780239 ) ) ;
#14617=CARTESIAN_POINT ( 'NONE',  ( 43.01140435219951286, 152.0344580088725763, 29.21067981925356705 ) ) ;
#14619=CARTESIAN_POINT ( 'NONE',  ( 43.01140435219951996, 10.71049967264875491, 34.21067981925357060 ) ) ;
#14620=CARTESIAN_POINT ( 'NONE',  ( 39.92123440845004723, 153.2344580088725934, 38.46393386101376421 ) ) ;
#14621=CARTESIAN_POINT ( 'NONE',  ( 46.59305225739526435, 130.5797705074273267, 36.81289934271958941 ) ) ;
#14623=CARTESIAN_POINT ( 'NONE',  ( 45.74753988029934249, 128.0651871740940067, 30.44471234641812174 ) ) ;
#14624=CARTESIAN_POINT ( 'NONE',  ( 43.01140435219957681, 68.96049967264870872, 29.21067981925356705 ) ) ;
#14627=CARTESIAN_POINT ( 'NONE',  ( 46.10157429594899270, 149.6604996726486831, 29.95742577749336988 ) ) ;
#14629=AXIS2_PLACEMENT_3D ( 'NONE', #20733, #15651, #3657 ) ;
#14630=CARTESIAN_POINT ( 'NONE',  ( 47.05648932407426344, 83.51049967264874851, 31.27175355779120025 ) ) ;
#14631=VERTEX_POINT ( 'NONE', #6518 ) ;
#14635=CARTESIAN_POINT ( 'NONE',  ( 39.92123440845004723, 81.23445800887256496, 38.46393386101376421 ) ) ;
#14636=CARTESIAN_POINT ( 'NONE',  ( 43.80332655382220253, 102.6113394311928317, 39.21067981925355639 ) ) ;
#14637=CARTESIAN_POINT ( 'NONE',  ( 43.01140435219951286, 139.4604996726487514, 39.46799094044489209 ) ) ;
#14638=CARTESIAN_POINT ( 'NONE',  ( 43.01140435219951286, 96.86518717409398960, 38.86567161673127657 ) ) ;
#14641=CARTESIAN_POINT ( 'NONE',  ( 38.01140435219951996, 60.86049967264872862, 35.83527830041810347 ) ) ;
#14643=CARTESIAN_POINT ( 'NONE',  ( 44.55648932407425633, 69.68445800887256780, 38.96596240072933170 ) ) ;
#14644=CARTESIAN_POINT ( 'NONE',  ( 39.92123440845005433, 106.1604996726487400, 38.46393386101375711 ) ) ;
#14649=CARTESIAN_POINT ( 'NONE',  ( 44.37947211624943833, 157.2797705074273438, 38.42115945441014446 ) ) ;
#14651=CARTESIAN_POINT ( 'NONE',  ( 39.42975644700377558, 150.4151871740940010, 36.81289934271958941 ) ) ;
#14652=CYLINDRICAL_SURFACE ( 'NONE', #19434, 4.999999999999997335 ) ;
#14656=CARTESIAN_POINT ( 'NONE',  ( 46.59305225739526435, 67.31518717409400665, 36.81289934271958941 ) ) ;
#14659=CARTESIAN_POINT ( 'NONE',  ( 43.01140435219951286, 138.8651871740940180, 38.86567161673127657 ) ) ;
#14663=VERTEX_POINT ( 'NONE', #6751 ) ;
#14667=ORIENTED_EDGE ( 'NONE', *, *, #16951, .F. ) ;
#14668=CARTESIAN_POINT ( 'NONE',  ( 43.80332655382220253, 116.8836182503284817, 29.21067981925356705 ) ) ;
#14669=CARTESIAN_POINT ( 'NONE',  ( 43.01140435219951286, 76.12977050742732388, 38.86567161673127657 ) ) ;
#14670=CARTESIAN_POINT ( 'NONE',  ( 38.58424406990784661, 125.9651871740939697, 32.77220824515698183 ) ) ;
#14672=CARTESIAN_POINT ( 'NONE',  ( 41.46631938032478359, 94.31049967264874567, 38.96596240072933170 ) ) ;
#14674=FACE_OUTER_BOUND ( 'NONE', #14283, .T. ) ;
#14676=CARTESIAN_POINT ( 'NONE',  ( 47.43856463449117200, 91.46518717409398391, 35.64915139335016647 ) ) ;
#14678=CARTESIAN_POINT ( 'NONE',  ( 44.55648932407425633, 107.8104996726487457, 29.45539723777780239 ) ) ;
#14679=CARTESIAN_POINT ( 'NONE',  ( 43.01140435219951286, 86.03445800887256212, 29.21067981925356705 ) ) ;
#14680=CARTESIAN_POINT ( 'NONE',  ( 48.01140435219951996, 142.2844580088725763, 34.21067981925357060 ) ) ;
#14682=CARTESIAN_POINT ( 'NONE',  ( 45.74753988029933538, 77.32977050742729830, 30.44471234641811819 ) ) ;
#14687=CARTESIAN_POINT ( 'NONE',  ( 40.27526882409969033, 158.6651871740939725, 30.44471234641811819 ) ) ;
#14688=LINE ( 'NONE', #11490, #3599 ) ;
#14689=CARTESIAN_POINT ( 'NONE',  ( 43.01140435219951286, 127.1297705074273097, 38.86567161673127657 ) ) ;
#14691=EDGE_LOOP ( 'NONE', ( #17097, #15771, #13587, #195 ) ) ;
#14693=ORIENTED_EDGE ( 'NONE', *, *, #17399, .T. ) ;
#14696=CARTESIAN_POINT ( 'NONE',  ( 41.64333658814960870, 87.97977050742731819, 38.42115945441014446 ) ) ;
#14697=CARTESIAN_POINT ( 'NONE',  ( 43.01140435219951286, 62.03445800887257633, 28.95336869806222779 ) ) ;
#14700=CARTESIAN_POINT ( 'NONE',  ( 41.46631938032478359, 101.1844580088725678, 29.45539723777780239 ) ) ;
#14709=CARTESIAN_POINT ( 'NONE',  ( 41.46631938032478359, 126.3844580088725706, 38.96596240072933170 ) ) ;
#14710=CARTESIAN_POINT ( 'NONE',  ( 44.37947211624943833, 103.2797705074273154, 38.42115945441014446 ) ) ;
#14713=CARTESIAN_POINT ( 'NONE',  ( 46.59305225739526435, 88.31518717409400665, 36.81289934271958941 ) ) ;
#14716=FACE_OUTER_BOUND ( 'NONE', #20666, .T. ) ;
#14720=CARTESIAN_POINT ( 'NONE',  ( 38.58424406990786082, 63.37977050742732388, 34.21067981925357060 ) ) ;
#14721=ORIENTED_EDGE ( 'NONE', *, *, #9655, .F. ) ;
#14723=ORIENTED_EDGE ( 'NONE', *, *, #268, .F. ) ;
#14724=CARTESIAN_POINT ( 'NONE',  ( 41.64333658814960870, 156.9797705074273040, 38.42115945441014446 ) ) ;
#14726=CARTESIAN_POINT ( 'NONE',  ( 48.01140435219951996, 107.2104996726487371, 34.21067981925357060 ) ) ;
#14727=CARTESIAN_POINT ( 'NONE',  ( 41.64333658814960870, 72.71518717409399812, 38.42115945441014446 ) ) ;
#14728=CARTESIAN_POINT ( 'NONE',  ( 38.01140435219952707, 65.93445800887258201, 35.83527830041809636 ) ) ;
#14729=( BOUNDED_CURVE ( )  B_SPLINE_CURVE ( 2, ( #7454, #14481, #5890, #21225, #7350, #17571, #14054, #2374, #19133, #10757, #12620, #15811, #7564 ),
 .UNSPECIFIED., .F., .F. ) 
 B_SPLINE_CURVE_WITH_KNOTS ( ( 3, 2, 2, 2, 2, 2, 3 ),
 ( 0.2426470588235294101, 0.2441176470588235226, 0.2470588235294117752, 0.2500000000000000000, 0.2529411764705882248, 0.2558823529411764497, 0.2573529411764705621 ),
 .UNSPECIFIED. ) 
 CURVE ( )  GEOMETRIC_REPRESENTATION_ITEM ( )  RATIONAL_B_SPLINE_CURVE ( ( 0.9755282581475768211, 0.9755282581475768211, 1.000000000000000000, 0.9510565162951535312, 1.000000000000000000, 0.9510565162951535312, 1.000000000000000000, 0.9510565162951535312, 1.000000000000000000, 0.9510565162951535312, 1.000000000000000000, 0.9755282581475772652, 0.9755282581475768211 ) ) 
 REPRESENTATION_ITEM ( '' )  );
#14731=CARTESIAN_POINT ( 'NONE',  ( 43.01140435219951996, 2.710499672648754466, 59.21067981925355639 ) ) ;
#14734=CARTESIAN_POINT ( 'NONE',  ( 44.55648932407425633, 148.8844580088725991, 29.45539723777780239 ) ) ;
#14735=CARTESIAN_POINT ( 'NONE',  ( 40.27526882409969033, 129.8297705074273267, 37.97664729208901946 ) ) ;
#14737=CARTESIAN_POINT ( 'NONE',  ( 47.43856463449118621, 124.6151871740940038, 34.21067981925357060 ) ) ;
#14741=CARTESIAN_POINT ( 'NONE',  ( 43.01140435219951286, 64.46049967264873715, 39.21067981925356349 ) ) ;
#14744=LINE ( 'NONE', #12877, #10761 ) ;
#14745=AXIS2_PLACEMENT_3D ( 'NONE', #9483, #17833, #2744 ) ;
#14749=CARTESIAN_POINT ( 'NONE',  ( 41.46631938032478359, 139.3104996726487457, 38.96596240072933170 ) ) ;
#14750=CARTESIAN_POINT ( 'NONE',  ( 41.64333658814960870, 99.71518717409399812, 38.42115945441014446 ) ) ;
#14755=CARTESIAN_POINT ( 'NONE',  ( 43.01140435219951996, 10.71049967264875491, 39.21067981925356349 ) ) ;
#14758=CARTESIAN_POINT ( 'NONE',  ( 43.80332655382220253, 115.9575765865522925, 29.21067981925356705 ) ) ;
#14759=CARTESIAN_POINT ( 'NONE',  ( 46.59305225739526435, 157.5797705074273267, 36.81289934271958941 ) ) ;
#14764=ADVANCED_FACE ( 'NONE', ( #1988 ), #19069, .T. ) ;
#14766=ORIENTED_EDGE ( 'NONE', *, *, #4303, .T. ) ;
#14767=CARTESIAN_POINT ( 'NONE',  ( 46.59305225739526435, 73.91518717409400097, 31.60846029578754468 ) ) ;
#14770=CARTESIAN_POINT ( 'NONE',  ( 43.01140435219951286, 113.0344580088725763, 29.21067981925356705 ) ) ;
#14771=CARTESIAN_POINT ( 'NONE',  ( 39.42975644700377558, 131.8151871740940067, 31.60846029578754468 ) ) ;
#14778=CARTESIAN_POINT ( 'NONE',  ( 43.01140435219957681, 93.53445800887259054, 39.21067981925356349 ) ) ;
#14779=CARTESIAN_POINT ( 'NONE',  ( 38.58424406990784661, 63.22977050742731109, 32.77220824515698183 ) ) ;
#14780=CARTESIAN_POINT ( 'NONE',  ( 46.59305225739526435, 127.9151871740940010, 31.60846029578754468 ) ) ;
#14782=CARTESIAN_POINT ( 'NONE',  ( 38.01140435219952707, 93.71049967264875136, 34.21067981925357060 ) ) ;
#14785=CARTESIAN_POINT ( 'NONE',  ( 41.46631938032478359, 138.1104996726487286, 29.45539723777780239 ) ) ;
#14786=CARTESIAN_POINT ( 'NONE',  ( 41.64333658814960870, 86.51518717409399528, 30.00020018409699318 ) ) ;
#14789=VECTOR ( 'NONE', #3537, 1000.000000000000000 ) ;
#14791=CARTESIAN_POINT ( 'NONE',  ( 46.59305225739526435, 77.17977050742732104, 31.60846029578754468 ) ) ;
#14798=CARTESIAN_POINT ( 'NONE',  ( 38.58424406990786082, 126.3797705074273239, 34.21067981925357060 ) ) ;
#14799=ORIENTED_EDGE ( 'NONE', *, *, #4767, .F. ) ;
#14800=CARTESIAN_POINT ( 'NONE',  ( 47.05648932407426344, 129.9844580088725934, 37.14960608071593384 ) ) ;
#14802=CARTESIAN_POINT ( 'NONE',  ( 45.74753988029933538, 119.3297705074273267, 30.44471234641811819 ) ) ;
#14804=CARTESIAN_POINT ( 'NONE',  ( 39.42975644700377558, 87.07977050742732672, 31.60846029578754468 ) ) ;
#14805=CARTESIAN_POINT ( 'NONE',  ( 47.43856463449118621, 151.6151871740939896, 34.21067981925357060 ) ) ;
#14810=DIRECTION ( 'NONE',  ( 0.000000000000000000, 1.000000000000000000, 0.000000000000000000 ) ) ;
#14812=CARTESIAN_POINT ( 'NONE',  ( 43.01140435219951286, 125.0344580088725763, 28.95336869806222779 ) ) ;
#14813=CARTESIAN_POINT ( 'NONE',  ( 39.42975644700377558, 105.6797705074273352, 36.81289934271958941 ) ) ;
#14816=CARTESIAN_POINT ( 'NONE',  ( 38.58424406990785371, 90.26518717409398107, 35.64915139335015937 ) ) ;
#14817=DIRECTION ( 'NONE',  ( 0.000000000000000000, 1.000000000000000000, 0.000000000000000000 ) ) ;
#14819=DIRECTION ( 'NONE',  ( 0.000000000000000000, 0.000000000000000000, 1.000000000000000000 ) ) ;
#14822=CARTESIAN_POINT ( 'NONE',  ( 44.37947211624943833, 62.47977050742731109, 30.00020018409699318 ) ) ;
#14825=CARTESIAN_POINT ( 'NONE',  ( 45.74753988029933538, 143.3297705074272699, 30.44471234641811819 ) ) ;
#14828=CARTESIAN_POINT ( 'NONE',  ( 46.10157429594899270, 109.7604996726487485, 38.46393386101376421 ) ) ;
#14829=CARTESIAN_POINT ( 'NONE',  ( 39.42975644700377558, 72.41518717409400097, 36.81289934271958941 ) ) ;
#14835=CARTESIAN_POINT ( 'NONE',  ( 46.10157429594899270, 147.8344580088725309, 38.46393386101376421 ) ) ;
#14836=CARTESIAN_POINT ( 'NONE',  ( 40.27526882409969033, 135.8297705074273551, 37.97664729208901946 ) ) ;
#14838=CARTESIAN_POINT ( 'NONE',  ( 44.37947211624943833, 119.2151871740939981, 30.00020018409699318 ) ) ;
#14848=CARTESIAN_POINT ( 'NONE',  ( 44.37947211624943833, 98.47977050742731819, 30.00020018409699318 ) ) ;
#14851=ORIENTED_EDGE ( 'NONE', *, *, #12435, .F. ) ;
#14852=( BOUNDED_CURVE ( )  B_SPLINE_CURVE ( 2, ( #2139, #15264, #15579, #15150, #3365, #10089, #18680, #16797, #6893, #1710, #20232, #20444, #3479 ),
 .UNSPECIFIED., .F., .F. ) 
 B_SPLINE_CURVE_WITH_KNOTS ( ( 3, 2, 2, 2, 2, 2, 3 ),
 ( 0.5808823529411765163, 0.5823529411764706287, 0.5852941176470588536, 0.5882352941176470784, 0.5911764705882353033, 0.5941176470588235281, 0.5955882352941176405 ),
 .UNSPECIFIED. ) 
 CURVE ( )  GEOMETRIC_REPRESENTATION_ITEM ( )  RATIONAL_B_SPLINE_CURVE ( ( 0.9755282581475768211, 0.9755282581475768211, 1.000000000000000000, 0.9510565162951535312, 1.000000000000000000, 0.9510565162951535312, 1.000000000000000000, 0.9510565162951535312, 1.000000000000000000, 0.9510565162951535312, 1.000000000000000000, 0.9755282581475768211, 0.9755282581475768211 ) ) 
 REPRESENTATION_ITEM ( '' )  );
#14853=CARTESIAN_POINT ( 'NONE',  ( 38.01140435219951996, 83.93445800887258201, 35.83527830041810347 ) ) ;
#14854=CARTESIAN_POINT ( 'NONE',  ( 46.10157429594899270, 102.8344580088725877, 38.46393386101375711 ) ) ;
#14855=CARTESIAN_POINT ( 'NONE',  ( 38.01140435219951996, 141.8604996726487286, 35.83527830041810347 ) ) ;
#14856=CARTESIAN_POINT ( 'NONE',  ( 45.74753988029933538, 97.16518717409398675, 37.97664729208901946 ) ) ;
#14865=CARTESIAN_POINT ( 'NONE',  ( 39.92123440845005433, 78.26049967264873430, 29.95742577749336988 ) ) ;
#14866=CARTESIAN_POINT ( 'NONE',  ( 39.42975644700377558, 156.6797705074273210, 36.81289934271958941 ) ) ;
#14870=CARTESIAN_POINT ( 'NONE',  ( 38.58424406990785371, 143.9651871740940123, 32.77220824515697473 ) ) ;
#14874=CARTESIAN_POINT ( 'NONE',  ( 40.27526882409969744, 68.66518717409400097, 30.44471234641812174 ) ) ;
#14878=CARTESIAN_POINT ( 'NONE',  ( 41.64333658814960870, 128.5151871740939953, 30.00020018409699318 ) ) ;
#14880=VERTEX_POINT ( 'NONE', #13878 ) ;
#14883=VERTEX_POINT ( 'NONE', #20617 ) ;
#14884=CARTESIAN_POINT ( 'NONE',  ( 47.05648932407426344, 109.5844580088725735, 31.27175355779120025 ) ) ;
#14885=CARTESIAN_POINT ( 'NONE',  ( 43.01140435219951996, 10.71049967264875491, 34.21067981925357060 ) ) ;
#14886=CARTESIAN_POINT ( 'NONE',  ( 47.43856463449118621, 64.87977050742730967, 34.21067981925357060 ) ) ;
#14887=CARTESIAN_POINT ( 'NONE',  ( 44.37947211624943833, 124.0151871740939953, 38.42115945441014446 ) ) ;
#14889=CARTESIAN_POINT ( 'NONE',  ( 48.01140435219951996, 83.06049967264873146, 35.83527830041810347 ) ) ;
#14891=CARTESIAN_POINT ( 'NONE',  ( 41.46631938032478359, 145.3104996726487457, 38.96596240072933170 ) ) ;
#14893=CARTESIAN_POINT ( 'NONE',  ( 39.42975644700377558, 92.81518717409399244, 31.60846029578754468 ) ) ;
#14894=CARTESIAN_POINT ( 'NONE',  ( 47.05648932407426344, 151.5844580088725877, 31.27175355779120025 ) ) ;
#14895=CARTESIAN_POINT ( 'NONE',  ( 43.01140435219951286, 62.96049967264873004, 29.21067981925356705 ) ) ;
#14897=CARTESIAN_POINT ( 'NONE',  ( 38.58424406990784661, 66.22977050742728977, 32.77220824515698183 ) ) ;
#14902=CARTESIAN_POINT ( 'NONE',  ( 47.43856463449117200, 157.7651871740939953, 32.77220824515698183 ) ) ;
#14904=CARTESIAN_POINT ( 'NONE',  ( 46.59305225739526435, 113.1797705074273210, 31.60846029578754468 ) ) ;
#14907=CARTESIAN_POINT ( 'NONE',  ( 47.05648932407426344, 130.5844580088725877, 31.27175355779120025 ) ) ;
#14908=VERTEX_POINT ( 'NONE', #12230 ) ;
#14909=CARTESIAN_POINT ( 'NONE',  ( 46.59305225739526435, 121.5797705074273267, 36.81289934271958941 ) ) ;
#14911=CARTESIAN_POINT ( 'NONE',  ( 39.42975644700377558, 155.8151871740940067, 31.60846029578754468 ) ) ;
#14913=CARTESIAN_POINT ( 'NONE',  ( 43.01140435219951286, 74.03445800887257633, 29.21067981925356705 ) ) ;
#14918=CARTESIAN_POINT ( 'NONE',  ( 48.01140435219951996, 131.2104996726487514, 34.21067981925357060 ) ) ;
#14921=CARTESIAN_POINT ( 'NONE',  ( 39.92123440845004723, 125.3344580088725735, 29.95742577749337343 ) ) ;
#14922=CARTESIAN_POINT ( 'NONE',  ( 47.43856463449117200, 97.72977050742730398, 35.64915139335016647 ) ) ;
#14925=CARTESIAN_POINT ( 'NONE',  ( 43.01140435219951286, 92.36518717409398960, 29.55568802177586107 ) ) ;
#14926=CARTESIAN_POINT ( 'NONE',  ( 42.21948215057684450, 90.03738109496902098, 29.21067981925356705 ) ) ;
#14927=VERTEX_POINT ( 'NONE', #3862 ) ;
#14928=CARTESIAN_POINT ( 'NONE',  ( 43.01140435219951996, 10.71049967264875491, 34.21067981925357060 ) ) ;
#14931=CARTESIAN_POINT ( 'NONE',  ( 44.37947211624943833, 140.4797705074273324, 30.00020018409699318 ) ) ;
#14933=CARTESIAN_POINT ( 'NONE',  ( 41.64333658814960870, 65.77977050742732956, 30.00020018409699318 ) ) ;
#14934=ORIENTED_EDGE ( 'NONE', *, *, #192, .F. ) ;
#14935=CARTESIAN_POINT ( 'NONE',  ( 46.59305225739526435, 146.1797705074273495, 31.60846029578754468 ) ) ;
#14937=CARTESIAN_POINT ( 'NONE',  ( 47.43856463449117200, 97.72977050742730398, 35.64915139335016647 ) ) ;
#14939=CARTESIAN_POINT ( 'NONE',  ( 38.96631938032478359, 115.0104996726487485, 37.14960608071593384 ) ) ;
#14940=CARTESIAN_POINT ( 'NONE',  ( 45.74753988029933538, 68.06518717409397823, 30.44471234641811819 ) ) ;
#14941=CARTESIAN_POINT ( 'NONE',  ( 41.46631938032478359, 96.38445800887257064, 38.96596240072933170 ) ) ;
#14946=CARTESIAN_POINT ( 'NONE',  ( 38.01140435219951996, 155.6344580088725706, 32.58608133808903773 ) ) ;
#14947=CARTESIAN_POINT ( 'NONE',  ( 45.74753988029933538, 127.4297705074273068, 37.97664729208901946 ) ) ;
#14949=CARTESIAN_POINT ( 'NONE',  ( 38.58424406990786082, 120.1151871740940038, 34.21067981925357060 ) ) ;
#14951=CARTESIAN_POINT ( 'NONE',  ( 43.01140435219951996, 10.71049967264875491, 34.21067981925357060 ) ) ;
#14952=CARTESIAN_POINT ( 'NONE',  ( 48.01140435219951996, 140.3604996726487002, 32.58608133808903773 ) ) ;
#14955=CARTESIAN_POINT ( 'NONE',  ( 46.59305225739526435, 97.57977050742731251, 36.81289934271958941 ) ) ;
#14958=DIRECTION ( 'NONE',  ( 0.000000000000000000, 0.000000000000000000, -1.000000000000000000 ) ) ;
#14960=CARTESIAN_POINT ( 'NONE',  ( 39.92123440845004723, 86.33445800887258770, 29.95742577749337343 ) ) ;
#14961=CARTESIAN_POINT ( 'NONE',  ( 43.01140435219951286, 59.03445800887258343, 29.21067981925356705 ) ) ;
#14962=CARTESIAN_POINT ( 'NONE',  ( 44.55648932407425633, 136.6104996726487286, 38.96596240072933170 ) ) ;
#14963=CARTESIAN_POINT ( 'NONE',  ( 47.43856463449117200, 97.76518717409398107, 32.77220824515698183 ) ) ;
#14972=CARTESIAN_POINT ( 'NONE',  ( 43.01140435219951996, 151.4604996726487514, 39.21067981925356349 ) ) ;
#14973=CARTESIAN_POINT ( 'NONE',  ( 44.82204965540741171, 59.16666133888451640, 30.14400234367970910 ) ) ;
#14974=CARTESIAN_POINT ( 'NONE',  ( 39.92123440845005433, 62.33445800887258059, 29.95742577749336988 ) ) ;
#14976=CARTESIAN_POINT ( 'NONE',  ( 43.01140435219951286, 144.8651871740939612, 38.86567161673127657 ) ) ;
#14981=CARTESIAN_POINT ( 'NONE',  ( 44.37947211624943833, 61.01518717409400239, 38.42115945441014446 ) ) ;
#14984=CARTESIAN_POINT ( 'NONE',  ( 40.27526882409969033, 123.5651871740939924, 37.97664729208901946 ) ) ;
#14987=( BOUNDED_CURVE ( )  B_SPLINE_CURVE ( 2, ( #7227, #18898, #17230, #12387, #19011, #5876, #10857, #19224, #19121, #12165, #17665, #4016, #17553 ),
 .UNSPECIFIED., .F., .F. ) 
 B_SPLINE_CURVE_WITH_KNOTS ( ( 3, 2, 2, 2, 2, 2, 3 ),
 ( 0.8750000000000000000, 0.8764705882352941124, 0.8794117647058823373, 0.8823529411764705621, 0.8852941176470587870, 0.8882352941176470118, 0.8897058823529412352 ),
 .UNSPECIFIED. ) 
 CURVE ( )  GEOMETRIC_REPRESENTATION_ITEM ( )  RATIONAL_B_SPLINE_CURVE ( ( 0.9755282581475768211, 0.9755282581475768211, 1.000000000000000000, 0.9510565162951535312, 1.000000000000000000, 0.9510565162951535312, 1.000000000000000000, 0.9510565162951535312, 1.000000000000000000, 0.9510565162951535312, 1.000000000000000000, 0.9755282581475758219, 0.9755282581475768211 ) ) 
 REPRESENTATION_ITEM ( '' )  );
#14988=ORIENTED_EDGE ( 'NONE', *, *, #1943, .T. ) ;
#14992=CARTESIAN_POINT ( 'NONE',  ( 46.10157429594899270, 109.7344580088725650, 29.95742577749337343 ) ) ;
#14994=CARTESIAN_POINT ( 'NONE',  ( 41.64333658814960870, 152.7797705074273438, 30.00020018409699318 ) ) ;
#14996=CARTESIAN_POINT ( 'NONE',  ( 43.01140435219951286, 71.62977050742732388, 29.55568802177586463 ) ) ;
#14997=CARTESIAN_POINT ( 'NONE',  ( 41.64333658814960870, 128.5151871740939953, 30.00020018409699318 ) ) ;
#15001=CARTESIAN_POINT ( 'NONE',  ( 38.01140435219952707, 84.71049967264873715, 34.21067981925357060 ) ) ;
#15003=CARTESIAN_POINT ( 'NONE',  ( 43.01140435219951286, 143.9604996726487229, 29.21067981925356705 ) ) ;
#15004=CARTESIAN_POINT ( 'NONE',  ( 42.21948215057683029, 139.3836182503284533, 39.21067981925354928 ) ) ;
#15005=CARTESIAN_POINT ( 'NONE',  ( 43.01140435219951286, 87.86518717409397539, 38.86567161673127657 ) ) ;
#15006=FACE_OUTER_BOUND ( 'NONE', #11626, .T. ) ;
#15007=CARTESIAN_POINT ( 'NONE',  ( 38.01140435219952707, 132.5604996726487457, 32.58608133808903773 ) ) ;
#15009=CARTESIAN_POINT ( 'NONE',  ( 47.43856463449118621, 67.87977050742730967, 34.21067981925357060 ) ) ;
#15014=VERTEX_POINT ( 'NONE', #21054 ) ;
#15015=ADVANCED_FACE ( 'NONE', ( #12664 ), #5934, .T. ) ;
#15016=CARTESIAN_POINT ( 'NONE',  ( 47.43856463449117200, 154.4651871740940123, 35.64915139335016647 ) ) ;
#15019=CARTESIAN_POINT ( 'NONE',  ( 45.74753988029934249, 112.4297705074273210, 37.97664729208901235 ) ) ;
#15025=CARTESIAN_POINT ( 'NONE',  ( 38.58424406990784661, 114.5297705074273296, 35.64915139335016647 ) ) ;
#15027=CARTESIAN_POINT ( 'NONE',  ( 38.58424406990784661, 84.52977050742731535, 35.64915139335016647 ) ) ;
#15028=CARTESIAN_POINT ( 'NONE',  ( 38.58424406990784661, 156.2651871740939953, 35.64915139335016647 ) ) ;
#15031=CARTESIAN_POINT ( 'NONE',  ( 41.46631938032478359, 107.1844580088725820, 29.45539723777780239 ) ) ;
#15037=CARTESIAN_POINT ( 'NONE',  ( 43.80332655382220253, 92.88361825032846752, 29.21067981925356705 ) ) ;
#15038=CARTESIAN_POINT ( 'NONE',  ( 41.64333658814960870, 93.97977050742733240, 38.42115945441014446 ) ) ;
#15041=CARTESIAN_POINT ( 'NONE',  ( 43.01140435219951286, 89.36518717409398960, 29.55568802177586107 ) ) ;
#15046=CARTESIAN_POINT ( 'NONE',  ( 43.01140435219951286, 137.0344580088725763, 29.21067981925356705 ) ) ;
#15048=CARTESIAN_POINT ( 'NONE',  ( 43.01140435219951286, 140.6297705074273097, 29.55568802177586107 ) ) ;
#15052=CARTESIAN_POINT ( 'NONE',  ( 39.42975644700377558, 141.0797705074273267, 31.60846029578754468 ) ) ;
#15054=CARTESIAN_POINT ( 'NONE',  ( 43.01140435219951286, 95.62977050742732388, 29.55568802177586463 ) ) ;
#15057=CARTESIAN_POINT ( 'NONE',  ( 47.05648932407426344, 113.5104996726487485, 31.27175355779120025 ) ) ;
#15058=CARTESIAN_POINT ( 'NONE',  ( 44.37947211624943833, 59.21518717409400523, 30.00020018409699318 ) ) ;
#15061=CARTESIAN_POINT ( 'NONE',  ( 41.46631938032478359, 155.1844580088725820, 29.45539723777780239 ) ) ;
#15064=CARTESIAN_POINT ( 'NONE',  ( 38.01140435219951996, 149.9344580088725820, 35.83527830041810347 ) ) ;
#15065=CARTESIAN_POINT ( 'NONE',  ( 43.01140435219951286, 121.1297705074273097, 38.86567161673127657 ) ) ;
#15067=CARTESIAN_POINT ( 'NONE',  ( 42.21948215057684450, 115.3836182503284533, 39.21067981925355639 ) ) ;
#15068=CARTESIAN_POINT ( 'NONE',  ( 46.59305225739526435, 112.3151871740940067, 36.81289934271958941 ) ) ;
#15070=DIRECTION ( 'NONE',  ( 0.000000000000000000, 1.000000000000000000, 0.000000000000000000 ) ) ;
#15071=LINE ( 'NONE', #13422, #1695 ) ;
#15075=CARTESIAN_POINT ( 'NONE',  ( 47.43856463449118621, 94.87977050742732388, 34.21067981925357060 ) ) ;
#15078=DIRECTION ( 'NONE',  ( 0.000000000000000000, 1.000000000000000000, 0.000000000000000000 ) ) ;
#15080=CARTESIAN_POINT ( 'NONE',  ( 38.01140435219951996, 74.63445800887258486, 32.58608133808903773 ) ) ;
#15082=CARTESIAN_POINT ( 'NONE',  ( 47.05648932407426344, 140.5104996726487627, 31.27175355779120025 ) ) ;
#15083=CARTESIAN_POINT ( 'NONE',  ( 39.42975644700377558, 101.8151871740940067, 31.60846029578754468 ) ) ;
#15089=CARTESIAN_POINT ( 'NONE',  ( 38.01140435219952707, 105.5604996726487173, 32.58608133808903773 ) ) ;
#15091=CARTESIAN_POINT ( 'NONE',  ( 48.01140435219951996, 80.36049967264874283, 32.58608133808903773 ) ) ;
#15092=CARTESIAN_POINT ( 'NONE',  ( 43.01140435219951286, 154.1297705074273097, 38.86567161673127657 ) ) ;
#15093=CARTESIAN_POINT ( 'NONE',  ( 41.46631938032478359, 62.18445800887258201, 29.45539723777780239 ) ) ;
#15095=CARTESIAN_POINT ( 'NONE',  ( 47.43856463449117911, 148.4651871740940123, 35.64915139335015937 ) ) ;
#15103=CARTESIAN_POINT ( 'NONE',  ( 41.64333658814960870, 122.5151871740940095, 30.00020018409699318 ) ) ;
#15104=EDGE_CURVE ( 'NONE', #3065, #7175, #12612, .T. ) ;
#15110=CARTESIAN_POINT ( 'NONE',  ( 44.37947211624943833, 158.4797705074273040, 30.00020018409699318 ) ) ;
#15112=CARTESIAN_POINT ( 'NONE',  ( 44.37947211624943833, 65.47977050742731819, 30.00020018409699318 ) ) ;
#15113=CARTESIAN_POINT ( 'NONE',  ( 38.58424406990784661, 122.9651871740939981, 32.77220824515698183 ) ) ;
#15115=CARTESIAN_POINT ( 'NONE',  ( 43.01140435219951286, 85.46049967264870872, 39.46799094044489209 ) ) ;
#15119=CARTESIAN_POINT ( 'NONE',  ( 38.58424406990786082, 81.11518717409398960, 34.21067981925357060 ) ) ;
#15123=CARTESIAN_POINT ( 'NONE',  ( 46.59305225739526435, 67.57977050742732672, 36.81289934271958941 ) ) ;
#15124=( BOUNDED_CURVE ( )  B_SPLINE_CURVE ( 2, ( #19893, #21329, #11502, #6102, #11282, #11177, #2802, #16242, #1150, #7885, #14700, #14586, #18002 ),
 .UNSPECIFIED., .F., .T. ) 
 B_SPLINE_CURVE_WITH_KNOTS ( ( 3, 2, 2, 2, 2, 2, 3 ),
 ( 0.5514705882352941568, 0.5529411764705882693, 0.5558823529411764941, 0.5588235294117647189, 0.5617647058823529438, 0.5647058823529411686, 0.5661764705882352811 ),
 .UNSPECIFIED. ) 
 CURVE ( )  GEOMETRIC_REPRESENTATION_ITEM ( )  RATIONAL_B_SPLINE_CURVE ( ( 0.9755282581475768211, 0.9755282581475768211, 1.000000000000000000, 0.9510565162951535312, 1.000000000000000000, 0.9510565162951535312, 1.000000000000000000, 0.9510565162951535312, 1.000000000000000000, 0.9510565162951535312, 1.000000000000000000, 0.9755282581475768211, 0.9755282581475768211 ) ) 
 REPRESENTATION_ITEM ( '' )  );
#15129=ORIENTED_EDGE ( 'NONE', *, *, #15195, .F. ) ;
#15130=CARTESIAN_POINT ( 'NONE',  ( 45.74753988029933538, 151.1651871740939725, 37.97664729208901946 ) ) ;
#15133=CARTESIAN_POINT ( 'NONE',  ( 41.64333658814960870, 110.7797705074273154, 30.00020018409699318 ) ) ;
#15138=CARTESIAN_POINT ( 'NONE',  ( 39.42975644700377558, 120.0797705074273267, 31.60846029578754468 ) ) ;
#15140=CARTESIAN_POINT ( 'NONE',  ( 40.27526882409969033, 150.5651871740940067, 37.97664729208901946 ) ) ;
#15147=CARTESIAN_POINT ( 'NONE',  ( 43.01140435219951996, 10.71049967264875491, 39.21067981925356349 ) ) ;
#15148=CARTESIAN_POINT ( 'NONE',  ( 47.05648932407426344, 92.51049967264873430, 31.27175355779120025 ) ) ;
#15150=CARTESIAN_POINT ( 'NONE',  ( 39.92123440845005433, 99.23445800887257917, 38.46393386101375711 ) ) ;
#15151=CARTESIAN_POINT ( 'NONE',  ( 38.58424406990784661, 90.52977050742731535, 35.64915139335016647 ) ) ;
#15155=CARTESIAN_POINT ( 'NONE',  ( 47.43856463449117911, 91.46518717409399812, 35.64915139335015937 ) ) ;
#15156=CYLINDRICAL_SURFACE ( 'NONE', #7261, 4.999999999999997335 ) ;
#15158=DIRECTION ( 'NONE',  ( 0.000000000000000000, 1.000000000000000000, 0.000000000000000000 ) ) ;
#15160=CARTESIAN_POINT ( 'NONE',  ( 47.43856463449117911, 142.7297705074273324, 35.64915139335015937 ) ) ;
#15165=CARTESIAN_POINT ( 'NONE',  ( 41.64333658814960870, 141.9797705074273324, 38.42115945441014446 ) ) ;
#15166=CARTESIAN_POINT ( 'NONE',  ( 44.37947211624943833, 94.27977050742731535, 38.42115945441014446 ) ) ;
#15170=CARTESIAN_POINT ( 'NONE',  ( 44.82204145925543060, 59.16666223754087639, 30.14399968058849666 ) ) ;
#15177=CARTESIAN_POINT ( 'NONE',  ( 38.96631938032478359, 146.4844580088725934, 31.27175355779120025 ) ) ;
#15178=CARTESIAN_POINT ( 'NONE',  ( 47.43856463449117200, 122.0297705074273011, 32.77220824515698183 ) ) ;
#15180=CARTESIAN_POINT ( 'NONE',  ( 44.55648932407425633, 99.68445800887256780, 38.96596240072933170 ) ) ;
#15181=CARTESIAN_POINT ( 'NONE',  ( 47.43856463449117911, 121.4651871740939981, 35.64915139335015937 ) ) ;
#15184=B_SPLINE_CURVE_WITH_KNOTS ( 'NONE', 1,
 ( #16972, #3440 ),
 .UNSPECIFIED., .F., .F.,
 ( 2, 2 ),
 ( 0.000000000000000000, 1.000000000000000000 ),
 .UNSPECIFIED. ) ;
#15189=CARTESIAN_POINT ( 'NONE',  ( 45.74753988029934249, 82.42977050742732104, 37.97664729208901235 ) ) ;
#15190=( BOUNDED_CURVE ( )  B_SPLINE_CURVE ( 2, ( #19003, #7657, #910, #19113, #14241, #5977, #17545, #587, #19321, #14134, #2347, #2242, #20872 ),
 .UNSPECIFIED., .F., .F. ) 
 B_SPLINE_CURVE_WITH_KNOTS ( ( 3, 2, 2, 2, 2, 2, 3 ),
 ( 0.5073529411764705621, 0.5088235294117646745, 0.5117647058823528994, 0.5147058823529411242, 0.5176470588235294601, 0.5205882352941176849, 0.5220588235294117974 ),
 .UNSPECIFIED. ) 
 CURVE ( )  GEOMETRIC_REPRESENTATION_ITEM ( )  RATIONAL_B_SPLINE_CURVE ( ( 0.9755282581475768211, 0.9755282581475768211, 1.000000000000000000, 0.9510565162951535312, 1.000000000000000000, 0.9510565162951535312, 1.000000000000000000, 0.9510565162951535312, 1.000000000000000000, 0.9510565162951535312, 1.000000000000000000, 0.9755282581475768211, 0.9755282581475768211 ) ) 
 REPRESENTATION_ITEM ( '' )  );
#15193=CARTESIAN_POINT ( 'NONE',  ( 38.01140435219952707, 74.78445800887257633, 34.21067981925357060 ) ) ;
#15194=DIRECTION ( 'NONE',  ( 0.000000000000000000, 1.000000000000000000, 0.000000000000000000 ) ) ;
#15195=EDGE_CURVE ( 'NONE', #13122, #3596, #14852, .T. ) ;
#15196=CARTESIAN_POINT ( 'NONE',  ( 47.05648932407426344, 131.5104996726487343, 31.27175355779120025 ) ) ;
#15197=CARTESIAN_POINT ( 'NONE',  ( 39.42975644700377558, 83.81518717409400665, 31.60846029578754468 ) ) ;
#15201=CARTESIAN_POINT ( 'NONE',  ( 43.01140435219951996, 10.71049967264875491, 34.21067981925357060 ) ) ;
#15202=CARTESIAN_POINT ( 'NONE',  ( 46.10157429594899270, 126.8344580088725593, 38.46393386101375711 ) ) ;
#15205=DIRECTION ( 'NONE',  ( 0.000000000000000000, 1.000000000000000000, 0.000000000000000000 ) ) ;
#15207=CARTESIAN_POINT ( 'NONE',  ( 43.01140435219951286, 152.6297705074272812, 29.55568802177586463 ) ) ;
#15208=CARTESIAN_POINT ( 'NONE',  ( 43.01140435219951286, 63.53445800887256922, 39.21067981925356349 ) ) ;
#15210=CARTESIAN_POINT ( 'NONE',  ( 38.58424406990785371, 147.2651871740939669, 35.64915139335015937 ) ) ;
#15214=ORIENTED_EDGE ( 'NONE', *, *, #15104, .T. ) ;
#15215=CARTESIAN_POINT ( 'NONE',  ( 47.43856463449117911, 61.46518717409398391, 35.64915139335015937 ) ) ;
#15218=CARTESIAN_POINT ( 'NONE',  ( 39.42975644700377558, 126.4151871740940010, 36.81289934271958941 ) ) ;
#15219=VERTEX_POINT ( 'NONE', #51 ) ;
#15221=AXIS2_PLACEMENT_3D ( 'NONE', #7928, #7823, #16179 ) ;
#15223=CARTESIAN_POINT ( 'NONE',  ( 38.96631938032478359, 147.0844580088725877, 37.14960608071593384 ) ) ;
#15225=CARTESIAN_POINT ( 'NONE',  ( 46.10157429594899270, 99.83445800887257349, 38.46393386101376421 ) ) ;
#15226=CARTESIAN_POINT ( 'NONE',  ( 41.64333658814960870, 155.7797705074273438, 30.00020018409699318 ) ) ;
#15228=CARTESIAN_POINT ( 'NONE',  ( 41.64333658814960870, 65.77977050742732956, 30.00020018409699318 ) ) ;
#15229=CARTESIAN_POINT ( 'NONE',  ( 43.01140435219951286, 120.8651871740940180, 38.86567161673127657 ) ) ;
#15231=CARTESIAN_POINT ( 'NONE',  ( 46.10157429594899270, 83.66049967264873999, 29.95742577749337343 ) ) ;
#15235=CARTESIAN_POINT ( 'NONE',  ( 45.74753988029933538, 76.16518717409400097, 37.97664729208901946 ) ) ;
#15240=CARTESIAN_POINT ( 'NONE',  ( 38.58424406990784661, 69.52977050742730114, 35.64915139335016647 ) ) ;
#15245=CARTESIAN_POINT ( 'NONE',  ( 47.43856463449118621, 157.6151871740940180, 34.21067981925357060 ) ) ;
#15247=CARTESIAN_POINT ( 'NONE',  ( 45.74753988029934249, 118.4297705074272926, 37.97664729208901235 ) ) ;
#15249=VERTEX_POINT ( 'NONE', #10309 ) ;
#15251=VERTEX_POINT ( 'NONE', #17012 ) ;
#15253=CARTESIAN_POINT ( 'NONE',  ( 46.59305225739526435, 86.17977050742732104, 31.60846029578754468 ) ) ;
#15254=CARTESIAN_POINT ( 'NONE',  ( 38.58424406990784661, 152.9651871740940123, 32.77220824515698183 ) ) ;
#15257=CYLINDRICAL_SURFACE ( 'NONE', #3246, 4.999999999999997335 ) ;
#15258=ADVANCED_FACE ( 'NONE', ( #1919 ), #9300, .T. ) ;
#15263=CARTESIAN_POINT ( 'NONE',  ( 47.05648932407426344, 97.58445800887258770, 31.27175355779120025 ) ) ;
#15264=CARTESIAN_POINT ( 'NONE',  ( 42.21948215057684450, 99.45757658655229250, 39.21067981925355639 ) ) ;
#15265=CARTESIAN_POINT ( 'NONE',  ( 44.37947211624943833, 98.47977050742731819, 30.00020018409699318 ) ) ;
#15268=CARTESIAN_POINT ( 'NONE',  ( 47.43856463449117911, 82.76518717409400949, 32.77220824515697473 ) ) ;
#15270=ORIENTED_EDGE ( 'NONE', *, *, #5441, .F. ) ;
#15271=CARTESIAN_POINT ( 'NONE',  ( 38.01140435219952707, 137.6344580088725706, 32.58608133808903773 ) ) ;
#15276=CARTESIAN_POINT ( 'NONE',  ( 47.43856463449118621, 61.87977050742732388, 34.21067981925357060 ) ) ;
#15278=CARTESIAN_POINT ( 'NONE',  ( 43.01140435219951286, 146.6297705074273381, 29.55568802177586463 ) ) ;
#15282=CARTESIAN_POINT ( 'NONE',  ( 47.43856463449118621, 61.61518717409400381, 34.21067981925357060 ) ) ;
#15286=LINE ( 'NONE', #18806, #5882 ) ;
#15290=CARTESIAN_POINT ( 'NONE',  ( 46.10157429594899270, 139.7344580088725934, 29.95742577749337343 ) ) ;
#15291=CARTESIAN_POINT ( 'NONE',  ( 47.43856463449117200, 119.0297705074273296, 32.77220824515698183 ) ) ;
#15293=PLANE ( 'NONE',  #17663 ) ;
#15294=CARTESIAN_POINT ( 'NONE',  ( 46.59305225739526435, 106.9151871740940152, 31.60846029578754468 ) ) ;
#15295=CARTESIAN_POINT ( 'NONE',  ( 39.92123440845005433, 125.3344580088725735, 29.95742577749336988 ) ) ;
#15299=ADVANCED_FACE ( 'NONE', ( #9195 ), #17762, .T. ) ;
#15300=CARTESIAN_POINT ( 'NONE',  ( 46.59305225739526435, 88.57977050742732672, 36.81289934271958941 ) ) ;
#15301=VECTOR ( 'NONE', #9465, 1000.000000000000000 ) ;
#15302=EDGE_CURVE ( 'NONE', #14339, #7314, #20659, .T. ) ;
#15305=CARTESIAN_POINT ( 'NONE',  ( 39.92123440845004723, 69.23445800887259338, 38.46393386101376421 ) ) ;
#15306=CARTESIAN_POINT ( 'NONE',  ( 39.92123440845005433, 59.33445800887256638, 29.95742577749336988 ) ) ;
#15307=CARTESIAN_POINT ( 'NONE',  ( 39.92123440845004723, 126.2604996726487485, 29.95742577749337343 ) ) ;
#15308=CARTESIAN_POINT ( 'NONE',  ( 46.59305225739526435, 82.91518717409400097, 31.60846029578754468 ) ) ;
#15312=CYLINDRICAL_SURFACE ( 'NONE', #5835, 4.999999999999997335 ) ;
#15314=CARTESIAN_POINT ( 'NONE',  ( 38.01140435219952707, 92.93445800887258201, 35.83527830041809636 ) ) ;
#15316=CARTESIAN_POINT ( 'NONE',  ( 38.58424406990784661, 150.5297705074272869, 35.64915139335016647 ) ) ;
#15318=EDGE_CURVE ( 'NONE', #12255, #7439, #15190, .T. ) ;
#15320=CARTESIAN_POINT ( 'NONE',  ( 45.74753988029934249, 146.0651871740940067, 30.44471234641812174 ) ) ;
#15323=CARTESIAN_POINT ( 'NONE',  ( 47.43856463449117911, 61.76518717409399528, 32.77220824515697473 ) ) ;
#15329=CARTESIAN_POINT ( 'NONE',  ( 46.59305225739526435, 121.9151871740940010, 31.60846029578754468 ) ) ;
#15330=ORIENTED_EDGE ( 'NONE', *, *, #12070, .F. ) ;
#15331=ORIENTED_EDGE ( 'NONE', *, *, #18525, .F. ) ;
#15334=CARTESIAN_POINT ( 'NONE',  ( 44.55648932407425633, 102.6844580088725820, 38.96596240072933170 ) ) ;
#15335=CARTESIAN_POINT ( 'NONE',  ( 43.01140435219951996, 157.4604996726487514, 39.21067981925355639 ) ) ;
#15336=CARTESIAN_POINT ( 'NONE',  ( 38.96631938032478359, 159.4104996726487400, 31.27175355779120025 ) ) ;
#15337=CARTESIAN_POINT ( 'NONE',  ( 40.27526882409969033, 114.5651871740939782, 37.97664729208901946 ) ) ;
#15339=CARTESIAN_POINT ( 'NONE',  ( 48.01140435219951996, 71.36049967264874283, 32.58608133808903773 ) ) ;
#15340=CARTESIAN_POINT ( 'NONE',  ( 46.10157429594899270, 136.7344580088725365, 29.95742577749336988 ) ) ;
#15344=CARTESIAN_POINT ( 'NONE',  ( 38.58424406990784661, 74.96518717409401233, 32.77220824515698183 ) ) ;
#15347=CARTESIAN_POINT ( 'NONE',  ( 38.96631938032478359, 132.4104996726487684, 31.27175355779120025 ) ) ;
#15353=VERTEX_POINT ( 'NONE', #20763 ) ;
#15356=CARTESIAN_POINT ( 'NONE',  ( 41.64333658814960870, 155.5151871740940237, 30.00020018409699318 ) ) ;
#15359=CARTESIAN_POINT ( 'NONE',  ( 38.58424406990785371, 117.5297705074273154, 35.64915139335015937 ) ) ;
#15364=CARTESIAN_POINT ( 'NONE',  ( 46.59305225739526435, 109.5797705074273125, 36.81289934271958941 ) ) ;
#15365=CARTESIAN_POINT ( 'NONE',  ( 41.46631938032478359, 131.1844580088725820, 29.45539723777780239 ) ) ;
#15366=CARTESIAN_POINT ( 'NONE',  ( 39.92123440845005433, 129.2344580088725934, 38.46393386101375711 ) ) ;
#15367=CARTESIAN_POINT ( 'NONE',  ( 46.59305225739526435, 148.3151871740940067, 36.81289934271958941 ) ) ;
#15375=CARTESIAN_POINT ( 'NONE',  ( 48.01140435219951996, 92.06049967264873146, 35.83527830041809636 ) ) ;
#15378=CARTESIAN_POINT ( 'NONE',  ( 45.74753988029933538, 94.42977050742732104, 37.97664729208901946 ) ) ;
#15381=CARTESIAN_POINT ( 'NONE',  ( 40.27526882409969744, 81.56518717409399244, 37.97664729208901235 ) ) ;
#15386=DIRECTION ( 'NONE',  ( 0.000000000000000000, 0.000000000000000000, 1.000000000000000000 ) ) ;
#15388=ORIENTED_EDGE ( 'NONE', *, *, #19160, .T. ) ;
#15390=CARTESIAN_POINT ( 'NONE',  ( 42.21948215057684450, 119.1113394311928460, 29.21067981925356705 ) ) ;
#15393=CARTESIAN_POINT ( 'NONE',  ( 41.64333658814960870, 135.9797705074273324, 38.42115945441014446 ) ) ;
#15399=CARTESIAN_POINT ( 'NONE',  ( 38.96631938032478359, 108.4104996726487400, 31.27175355779120025 ) ) ;
#15401=CARTESIAN_POINT ( 'NONE',  ( 43.01140435219951286, 138.5344580088726048, 39.46799094044489209 ) ) ;
#15402=CARTESIAN_POINT ( 'NONE',  ( 47.43856463449117200, 121.7297705074273040, 35.64915139335016647 ) ) ;
#15404=CARTESIAN_POINT ( 'NONE',  ( 38.01140435219952707, 140.9344580088725820, 35.83527830041809636 ) ) ;
#15406=CARTESIAN_POINT ( 'NONE',  ( 41.64333658814960870, 110.5151871740940095, 30.00020018409699318 ) ) ;
#15409=EDGE_CURVE ( 'NONE', #7314, #3622, #9985, .T. ) ;
#15412=CARTESIAN_POINT ( 'NONE',  ( 38.58424406990785371, 87.22977050742731819, 32.77220824515697473 ) ) ;
#15415=CARTESIAN_POINT ( 'NONE',  ( 46.10157429594899270, 134.6604996726487684, 29.95742577749336988 ) ) ;
#15416=CARTESIAN_POINT ( 'NONE',  ( 48.01140435219951996, 73.43445800887255359, 32.58608133808903773 ) ) ;
#15417=CARTESIAN_POINT ( 'NONE',  ( 42.21948215057684450, 60.45757658655230671, 39.21067981925355639 ) ) ;
#15419=CARTESIAN_POINT ( 'NONE',  ( 48.01140435219951996, 134.0604996726486888, 35.83527830041810347 ) ) ;
#15420=CARTESIAN_POINT ( 'NONE',  ( 46.59305225739526435, 88.91518717409400097, 31.60846029578754468 ) ) ;
#15425=CARTESIAN_POINT ( 'NONE',  ( 43.01140435219951286, 125.9604996726487514, 29.21067981925356705 ) ) ;
#15426=CARTESIAN_POINT ( 'NONE',  ( 42.21948215057687293, 93.45757658655232092, 39.21067981925357060 ) ) ;
#15427=CARTESIAN_POINT ( 'NONE',  ( 43.80332655382220253, 143.8836182503284817, 29.21067981925356705 ) ) ;
#15428=CARTESIAN_POINT ( 'NONE',  ( 38.58424406990786082, 147.3797705074273097, 34.21067981925357060 ) ) ;
#15429=CARTESIAN_POINT ( 'NONE',  ( 39.42975644700377558, 105.0797705074273125, 31.60846029578754468 ) ) ;
#15431=CARTESIAN_POINT ( 'NONE',  ( 44.37947211624943833, 140.2151871740940123, 30.00020018409699318 ) ) ;
#15436=CARTESIAN_POINT ( 'NONE',  ( 38.58424406990784661, 119.9651871740939839, 32.77220824515698183 ) ) ;
#15441=CARTESIAN_POINT ( 'NONE',  ( 46.10157429594899270, 100.7344580088725792, 29.95742577749337343 ) ) ;
#15442=CARTESIAN_POINT ( 'NONE',  ( 40.27526882409969744, 152.9297705074273210, 30.44471234641812174 ) ) ;
#15443=CARTESIAN_POINT ( 'NONE',  ( 48.01140435219951996, 155.0604996726487457, 35.83527830041810347 ) ) ;
#15444=CARTESIAN_POINT ( 'NONE',  ( 47.43856463449117200, 118.7651871740940237, 32.77220824515698183 ) ) ;
#15446=CARTESIAN_POINT ( 'NONE',  ( 46.10157429594899270, 71.66049967264873999, 29.95742577749337343 ) ) ;
#15448=CARTESIAN_POINT ( 'NONE',  ( 41.46631938032478359, 75.38445800887258486, 38.96596240072933170 ) ) ;
#15450=CARTESIAN_POINT ( 'NONE',  ( 38.96631938032478359, 123.4104996726487542, 31.27175355779120025 ) ) ;
#15452=( BOUNDED_CURVE ( )  B_SPLINE_CURVE ( 2, ( #10865, #12090, #17050, #1962, #19336, #8695, #21110, #12506, #4131, #5992, #7558, #12720, #311 ),
 .UNSPECIFIED., .F., .T. ) 
 B_SPLINE_CURVE_WITH_KNOTS ( ( 3, 2, 2, 2, 2, 2, 3 ),
 ( 0.4779411764705882582, 0.4794117647058823706, 0.4823529411764705954, 0.4852941176470588203, 0.4882352941176470451, 0.4911764705882352700, 0.4926470588235293824 ),
 .UNSPECIFIED. ) 
 CURVE ( )  GEOMETRIC_REPRESENTATION_ITEM ( )  RATIONAL_B_SPLINE_CURVE ( ( 0.9755282581475768211, 0.9755282581475772652, 1.000000000000000000, 0.9510565162951535312, 1.000000000000000000, 0.9510565162951535312, 1.000000000000000000, 0.9510565162951535312, 1.000000000000000000, 0.9510565162951535312, 1.000000000000000000, 0.9755282581475772652, 0.9755282581475768211 ) ) 
 REPRESENTATION_ITEM ( '' )  );
#15453=CARTESIAN_POINT ( 'NONE',  ( 45.74753988029933538, 74.06518717409399244, 30.44471234641811819 ) ) ;
#15454=CARTESIAN_POINT ( 'NONE',  ( 47.05648932407426344, 103.9104996726487400, 37.14960608071593384 ) ) ;
#15456=CARTESIAN_POINT ( 'NONE',  ( 38.96631938032478359, 133.0104996726487343, 37.14960608071593384 ) ) ;
#15462=CARTESIAN_POINT ( 'NONE',  ( 46.59305225739526435, 139.9151871740940010, 31.60846029578754468 ) ) ;
#15463=CARTESIAN_POINT ( 'NONE',  ( 38.58424406990786082, 159.1151871740940180, 34.21067981925357060 ) ) ;
#15464=CARTESIAN_POINT ( 'NONE',  ( 45.74753988029934249, 101.3297705074273267, 30.44471234641812174 ) ) ;
#15467=AXIS2_PLACEMENT_3D ( 'NONE', #370, #4282, #14313 ) ;
#15469=CARTESIAN_POINT ( 'NONE',  ( 38.58424406990786082, 111.3797705074273239, 34.21067981925357060 ) ) ;
#15470=CARTESIAN_POINT ( 'NONE',  ( 38.96631938032478359, 158.4844580088725934, 31.27175355779120025 ) ) ;
#15471=CARTESIAN_POINT ( 'NONE',  ( 43.01140435219951286, 125.9604996726487514, 29.21067981925356705 ) ) ;
#15472=CARTESIAN_POINT ( 'NONE',  ( 38.58424406990786082, 141.1151871740939896, 34.21067981925357060 ) ) ;
#15473=CARTESIAN_POINT ( 'NONE',  ( 43.01140435219951286, 101.9604996726487514, 28.95336869806222779 ) ) ;
#15479=CARTESIAN_POINT ( 'NONE',  ( 44.55648932407425633, 76.61049967264874283, 38.96596240072933170 ) ) ;
#15480=CARTESIAN_POINT ( 'NONE',  ( 41.64333658814960870, 81.97977050742731819, 38.42115945441014446 ) ) ;
#15483=CARTESIAN_POINT ( 'NONE',  ( 39.42975644700377558, 74.81518717409399244, 31.60846029578754468 ) ) ;
#15484=LINE ( 'NONE', #17125, #13090 ) ;
#15486=VERTEX_POINT ( 'NONE', #17981 ) ;
#15488=CARTESIAN_POINT ( 'NONE',  ( 47.05648932407426344, 122.5104996726487343, 31.27175355779120025 ) ) ;
#15489=CARTESIAN_POINT ( 'NONE',  ( 41.64333658814960870, 134.7797705074273154, 30.00020018409699318 ) ) ;
#15492=CARTESIAN_POINT ( 'NONE',  ( 44.37947211624943833, 61.27977050742732246, 38.42115945441014446 ) ) ;
#15494=CARTESIAN_POINT ( 'NONE',  ( 43.01140435219951286, 133.1297705074273381, 38.86567161673127657 ) ) ;
#15497=CARTESIAN_POINT ( 'NONE',  ( 38.58424406990784661, 60.26518717409400239, 35.64915139335016647 ) ) ;
#15500=CARTESIAN_POINT ( 'NONE',  ( 41.64333658814960870, 93.71518717409401233, 38.42115945441014446 ) ) ;
#15501=CARTESIAN_POINT ( 'NONE',  ( 38.01140435219952707, 153.8604996726487286, 35.83527830041809636 ) ) ;
#15505=CARTESIAN_POINT ( 'NONE',  ( 38.96631938032478359, 147.0844580088725877, 37.14960608071593384 ) ) ;
#15506=CARTESIAN_POINT ( 'NONE',  ( 40.27526882409969033, 114.8297705074273125, 37.97664729208901946 ) ) ;
#15508=CARTESIAN_POINT ( 'NONE',  ( 48.01140435219951996, 100.4344580088725678, 32.58608133808903773 ) ) ;
#15509=CARTESIAN_POINT ( 'NONE',  ( 43.01140435219951286, 102.8651871740940038, 38.86567161673127657 ) ) ;
#15514=CARTESIAN_POINT ( 'NONE',  ( 39.42975644700377558, 84.67977050742732104, 36.81289934271958941 ) ) ;
#15515=EDGE_CURVE ( 'NONE', #3562, #18986, #18093, .T. ) ;
#15516=CARTESIAN_POINT ( 'NONE',  ( 38.01140435219952707, 77.78445800887259054, 34.21067981925357060 ) ) ;
#15518=CARTESIAN_POINT ( 'NONE',  ( 39.92123440845004723, 133.1604996726487400, 38.46393386101376421 ) ) ;
#15519=CARTESIAN_POINT ( 'NONE',  ( 47.43856463449117200, 82.76518717409400949, 32.77220824515698183 ) ) ;
#15523=DIRECTION ( 'NONE',  ( 0.000000000000000000, 1.000000000000000000, 0.000000000000000000 ) ) ;
#15525=CARTESIAN_POINT ( 'NONE',  ( 43.01140435219951996, 10.71049967264875491, 34.21067981925357060 ) ) ;
#15527=CARTESIAN_POINT ( 'NONE',  ( 40.27526882409969033, 152.9297705074273210, 30.44471234641811819 ) ) ;
#15528=CARTESIAN_POINT ( 'NONE',  ( 45.74753988029933538, 106.4297705074273068, 37.97664729208901946 ) ) ;
#15530=CARTESIAN_POINT ( 'NONE',  ( 46.59305225739526435, 136.3151871740940351, 36.81289934271958941 ) ) ;
#15536=CARTESIAN_POINT ( 'NONE',  ( 39.42975644700377558, 111.4151871740940010, 36.81289934271958941 ) ) ;
#15540=CARTESIAN_POINT ( 'NONE',  ( 48.01140435219951996, 100.4344580088725820, 32.58608133808903773 ) ) ;
#15543=CARTESIAN_POINT ( 'NONE',  ( 41.46631938032478359, 154.3104996726487457, 38.96596240072933170 ) ) ;
#15544=CARTESIAN_POINT ( 'NONE',  ( 46.59305225739526435, 115.9151871740940010, 31.60846029578754468 ) ) ;
#15546=ADVANCED_FACE ( 'NONE', ( #14565 ), #16545, .T. ) ;
#15547=CARTESIAN_POINT ( 'NONE',  ( 41.46631938032478359, 69.11049967264872862, 29.45539723777780239 ) ) ;
#15551=CARTESIAN_POINT ( 'NONE',  ( 39.92123440845005433, 123.2604996726487201, 29.95742577749336988 ) ) ;
#15553=CARTESIAN_POINT ( 'NONE',  ( 45.74753988029933538, 82.16518717409400097, 37.97664729208901946 ) ) ;
#15557=ORIENTED_EDGE ( 'NONE', *, *, #618, .T. ) ;
#15560=CARTESIAN_POINT ( 'NONE',  ( 47.43856463449117200, 145.4651871740939839, 35.64915139335016647 ) ) ;
#15563=CARTESIAN_POINT ( 'NONE',  ( 45.74753988029934249, 103.4297705074273210, 37.97664729208901235 ) ) ;
#15567=ORIENTED_EDGE ( 'NONE', *, *, #12505, .F. ) ;
#15570=CARTESIAN_POINT ( 'NONE',  ( 45.74753988029933538, 149.0651871740940067, 30.44471234641811819 ) ) ;
#15571=( BOUNDED_CURVE ( )  B_SPLINE_CURVE ( 2, ( #17708, #2612, #752, #4479, #9466, #16054, #4370, #5922, #15740, #17494, #14189, #2726, #12758 ),
 .UNSPECIFIED., .F., .F. ) 
 B_SPLINE_CURVE_WITH_KNOTS ( ( 3, 2, 2, 2, 2, 2, 3 ),
 ( 0.08088235294117647467, 0.08235294117647058709, 0.08529411764705882582, 0.08823529411764706454, 0.09117647058823528938, 0.09411764705882352811, 0.09558823529411764053 ),
 .UNSPECIFIED. ) 
 CURVE ( )  GEOMETRIC_REPRESENTATION_ITEM ( )  RATIONAL_B_SPLINE_CURVE ( ( 0.9755282581475767101, 0.9755282581475768211, 1.000000000000000000, 0.9510565162951535312, 1.000000000000000000, 0.9510565162951535312, 1.000000000000000000, 0.9510565162951535312, 1.000000000000000000, 0.9510565162951535312, 1.000000000000000000, 0.9755282581475768211, 0.9755282581475767101 ) ) 
 REPRESENTATION_ITEM ( '' )  );
#15572=CARTESIAN_POINT ( 'NONE',  ( 44.55648932407425633, 97.61049967264874283, 38.96596240072933170 ) ) ;
#15574=CARTESIAN_POINT ( 'NONE',  ( 38.01140435219952707, 60.86049967264873573, 35.83527830041809636 ) ) ;
#15579=CARTESIAN_POINT ( 'NONE',  ( 41.46631938032478359, 99.38445800887258486, 38.96596240072933170 ) ) ;
#15580=CARTESIAN_POINT ( 'NONE',  ( 43.01140435219951286, 83.62977050742730967, 29.55568802177586463 ) ) ;
#15582=CARTESIAN_POINT ( 'NONE',  ( 39.42975644700377558, 77.81518717409399244, 31.60846029578754468 ) ) ;
#15586=CARTESIAN_POINT ( 'NONE',  ( 43.01140435219951286, 84.53445800887256212, 39.21067981925356349 ) ) ;
#15587=CARTESIAN_POINT ( 'NONE',  ( 43.01140435219951996, 2.710499672648754466, 34.21067981925357060 ) ) ;
#15588=CARTESIAN_POINT ( 'NONE',  ( 43.01140435219951286, 130.1297705074273381, 38.86567161673127657 ) ) ;
#15591=CARTESIAN_POINT ( 'NONE',  ( 47.05648932407426344, 73.58445800887257349, 31.27175355779120025 ) ) ;
#15593=CARTESIAN_POINT ( 'NONE',  ( 45.74753988029933538, 139.4297705074272926, 37.97664729208901946 ) ) ;
#15594=CARTESIAN_POINT ( 'NONE',  ( 38.96631938032478359, 100.0104996726487485, 37.14960608071593384 ) ) ;
#15595=CARTESIAN_POINT ( 'NONE',  ( 43.01140435219951286, 122.0344580088725763, 29.21067981925356705 ) ) ;
#15596=CARTESIAN_POINT ( 'NONE',  ( 43.01140435219951996, 150.5344580088725763, 39.21067981925356349 ) ) ;
#15597=CARTESIAN_POINT ( 'NONE',  ( 38.58424406990786082, 102.1151871740940180, 34.21067981925357060 ) ) ;
#15599=CARTESIAN_POINT ( 'NONE',  ( 43.01140435219951286, 122.0344580088725763, 29.21067981925356705 ) ) ;
#15602=CARTESIAN_POINT ( 'NONE',  ( 38.01140435219951996, 146.6344580088725991, 32.58608133808903773 ) ) ;
#15603=CARTESIAN_POINT ( 'NONE',  ( 47.43856463449117200, 116.0297705074273154, 32.77220824515698183 ) ) ;
#15605=CARTESIAN_POINT ( 'NONE',  ( 45.43987506541010646, 59.62854787734439554, 30.00461993086704027 ) ) ;
#15606=CARTESIAN_POINT ( 'NONE',  ( 38.58424406990785371, 111.2651871740939953, 35.64915139335015937 ) ) ;
#15608=CARTESIAN_POINT ( 'NONE',  ( 47.05648932407426344, 156.9844580088725934, 37.14960608071593384 ) ) ;
#15611=EDGE_CURVE ( 'NONE', #19361, #17102, #20408, .T. ) ;
#15613=CARTESIAN_POINT ( 'NONE',  ( 44.37947211624943833, 74.47977050742731819, 30.00020018409699318 ) ) ;
#15615=CARTESIAN_POINT ( 'NONE',  ( 38.01140435219952707, 62.78445800887258343, 34.21067981925357060 ) ) ;
#15616=CARTESIAN_POINT ( 'NONE',  ( 43.01140435219951996, 149.9604996726487798, 29.21067981925357060 ) ) ;
#15617=CARTESIAN_POINT ( 'NONE',  ( 41.46631938032478359, 133.3104996726487457, 38.96596240072933170 ) ) ;
#15618=CARTESIAN_POINT ( 'NONE',  ( 47.43856463449117200, 85.46518717409399812, 35.64915139335016647 ) ) ;
#15627=CARTESIAN_POINT ( 'NONE',  ( 46.59305225739526435, 142.5797705074273267, 36.81289934271958941 ) ) ;
#15628=CARTESIAN_POINT ( 'NONE',  ( 41.64333658814960870, 107.7797705074273154, 30.00020018409699318 ) ) ;
#15630=CARTESIAN_POINT ( 'NONE',  ( 47.43856463449117911, 133.4651871740940123, 35.64915139335015937 ) ) ;
#15638=CARTESIAN_POINT ( 'NONE',  ( 47.43856463449118621, 112.6151871740939896, 34.21067981925357060 ) ) ;
#15643=CARTESIAN_POINT ( 'NONE',  ( 39.92123440845004723, 101.3344580088725735, 29.95742577749337343 ) ) ;
#15644=CARTESIAN_POINT ( 'NONE',  ( 39.42975644700377558, 147.0797705074273267, 31.60846029578754468 ) ) ;
#15645=CARTESIAN_POINT ( 'NONE',  ( 47.05648932407426344, 158.5104996726487343, 31.27175355779120025 ) ) ;
#15646=CARTESIAN_POINT ( 'NONE',  ( 39.42975644700377558, 119.8151871740940067, 31.60846029578754468 ) ) ;
#15649=CARTESIAN_POINT ( 'NONE',  ( 46.10157429594899270, 74.66049967264873999, 29.95742577749337343 ) ) ;
#15650=CARTESIAN_POINT ( 'NONE',  ( 38.96631938032478359, 108.0844580088725877, 37.14960608071593384 ) ) ;
#15651=DIRECTION ( 'NONE',  ( 0.000000000000000000, 1.000000000000000000, 0.000000000000000000 ) ) ;
#15652=CARTESIAN_POINT ( 'NONE',  ( 42.21948215057684450, 72.45757658655230671, 39.21067981925355639 ) ) ;
#15654=CARTESIAN_POINT ( 'NONE',  ( 47.43856463449117200, 70.46518717409401233, 35.64915139335016647 ) ) ;
#15662=CARTESIAN_POINT ( 'NONE',  ( 43.01140435219951286, 146.3651871740939896, 29.55568802177586463 ) ) ;
#15665=CARTESIAN_POINT ( 'NONE',  ( 47.43856463449117911, 110.0297705074273296, 32.77220824515697473 ) ) ;
#15674=CARTESIAN_POINT ( 'NONE',  ( 41.64333658814960870, 147.7151871740940123, 38.42115945441014446 ) ) ;
#15675=CARTESIAN_POINT ( 'NONE',  ( 38.01140435219952707, 96.71049967264875136, 34.21067981925357060 ) ) ;
#15677=CARTESIAN_POINT ( 'NONE',  ( 39.92123440845005433, 60.26049967264872720, 29.95742577749336988 ) ) ;
#15679=CARTESIAN_POINT ( 'NONE',  ( 41.46631938032478359, 153.3844580088725991, 38.96596240072933170 ) ) ;
#15684=CARTESIAN_POINT ( 'NONE',  ( 44.37947211624943833, 83.47977050742731819, 30.00020018409699318 ) ) ;
#15686=CARTESIAN_POINT ( 'NONE',  ( 47.43856463449117911, 82.46518717409398391, 35.64915139335015937 ) ) ;
#15691=CARTESIAN_POINT ( 'NONE',  ( 38.01140435219952707, 117.5604996726487315, 32.58608133808903773 ) ) ;
#15693=DIRECTION ( 'NONE',  ( 0.000000000000000000, 1.000000000000000000, 0.000000000000000000 ) ) ;
#15694=CARTESIAN_POINT ( 'NONE',  ( 43.01140435219951286, 134.6297705074273097, 29.55568802177586107 ) ) ;
#15696=ORIENTED_EDGE ( 'NONE', *, *, #14155, .F. ) ;
#15698=( BOUNDED_CURVE ( )  B_SPLINE_CURVE ( 2, ( #7079, #5407, #19079, #15340, #12240, #17409, #2314, #18970, #12125, #8944, #17085, #554, #18857 ),
 .UNSPECIFIED., .F., .F. ) 
 B_SPLINE_CURVE_WITH_KNOTS ( ( 3, 2, 2, 2, 2, 2, 3 ),
 ( 0.2132352941176470507, 0.2147058823529411631, 0.2176470588235294157, 0.2205882352941176405, 0.2235294117647058931, 0.2264705882352941180, 0.2279411764705882304 ),
 .UNSPECIFIED. ) 
 CURVE ( )  GEOMETRIC_REPRESENTATION_ITEM ( )  RATIONAL_B_SPLINE_CURVE ( ( 0.9755282581475768211, 0.9755282581475768211, 1.000000000000000000, 0.9510565162951535312, 1.000000000000000000, 0.9510565162951535312, 1.000000000000000000, 0.9510565162951535312, 1.000000000000000000, 0.9510565162951535312, 1.000000000000000000, 0.9755282581475768211, 0.9755282581475768211 ) ) 
 REPRESENTATION_ITEM ( '' )  );
#15700=CARTESIAN_POINT ( 'NONE',  ( 47.43856463449117200, 139.7297705074273324, 35.64915139335016647 ) ) ;
#15701=CARTESIAN_POINT ( 'NONE',  ( 40.27526882409969033, 90.82977050742731251, 37.97664729208901946 ) ) ;
#15707=CARTESIAN_POINT ( 'NONE',  ( 40.27526882409969033, 96.56518717409399244, 37.97664729208901946 ) ) ;
#15708=CARTESIAN_POINT ( 'NONE',  ( 43.01140435219951286, 65.96049967264873715, 29.21067981925356705 ) ) ;
#15709=CARTESIAN_POINT ( 'NONE',  ( 48.01140435219951996, 125.3604996726487286, 32.58608133808903773 ) ) ;
#15713=EDGE_CURVE ( 'NONE', #8428, #1193, #12222, .T. ) ;
#15714=CARTESIAN_POINT ( 'NONE',  ( 44.55648932407425633, 70.61049967264872862, 38.96596240072933170 ) ) ;
#15715=CARTESIAN_POINT ( 'NONE',  ( 47.05648932407426344, 129.9844580088725934, 37.14960608071593384 ) ) ;
#15716=CARTESIAN_POINT ( 'NONE',  ( 44.37947211624943833, 116.4797705074273324, 30.00020018409699318 ) ) ;
#15719=CARTESIAN_POINT ( 'NONE',  ( 38.58424406990786082, 105.1151871740940038, 34.21067981925357060 ) ) ;
#15721=EDGE_LOOP ( 'NONE', ( #7637, #6516, #3314, #7927 ) ) ;
#15722=CARTESIAN_POINT ( 'NONE',  ( 48.01140435219951996, 76.43445800887258201, 32.58608133808903773 ) ) ;
#15726=FACE_OUTER_BOUND ( 'NONE', #252, .T. ) ;
#15727=CARTESIAN_POINT ( 'NONE',  ( 39.42975644700377558, 78.07977050742731251, 31.60846029578754468 ) ) ;
#15730=CARTESIAN_POINT ( 'NONE',  ( 48.01140435219951996, 67.28445800887257633, 34.21067981925357060 ) ) ;
#15732=CARTESIAN_POINT ( 'NONE',  ( 41.46631938032478359, 123.1104996726487570, 29.45539723777780239 ) ) ;
#15733=CARTESIAN_POINT ( 'NONE',  ( 46.59305225739526435, 79.91518717409400097, 31.60846029578754468 ) ) ;
#15737=CARTESIAN_POINT ( 'NONE',  ( 46.10157429594899270, 113.6604996726487400, 29.95742577749336988 ) ) ;
#15740=CARTESIAN_POINT ( 'NONE',  ( 38.96631938032478359, 149.4844580088725934, 31.27175355779120025 ) ) ;
#15741=CARTESIAN_POINT ( 'NONE',  ( 41.64333658814960870, 143.7797705074273154, 30.00020018409699318 ) ) ;
#15742=CARTESIAN_POINT ( 'NONE',  ( 38.58424406990784661, 108.5297705074273011, 35.64915139335016647 ) ) ;
#15744=CARTESIAN_POINT ( 'NONE',  ( 44.37947211624943833, 133.0151871740939953, 38.42115945441014446 ) ) ;
#15745=CARTESIAN_POINT ( 'NONE',  ( 48.01140435219951996, 67.13445800887257064, 35.83527830041809636 ) ) ;
#15752=CARTESIAN_POINT ( 'NONE',  ( 46.59305225739526435, 118.9151871740940010, 31.60846029578754468 ) ) ;
#15755=ORIENTED_EDGE ( 'NONE', *, *, #7748, .T. ) ;
#15756=CARTESIAN_POINT ( 'NONE',  ( 44.55648932407425633, 88.88445800887258486, 29.45539723777780239 ) ) ;
#15757=CARTESIAN_POINT ( 'NONE',  ( 46.10157429594899270, 158.6604996726487116, 29.95742577749337343 ) ) ;
#15758=CARTESIAN_POINT ( 'NONE',  ( 39.42975644700377558, 111.4151871740940010, 36.81289934271958941 ) ) ;
#15761=CARTESIAN_POINT ( 'NONE',  ( 43.01140435219951286, 74.96049967264873715, 28.95336869806222779 ) ) ;
#15764=AXIS2_PLACEMENT_3D ( 'NONE', #8225, #1164, #14600 ) ;
#15767=CARTESIAN_POINT ( 'NONE',  ( 47.43856463449118621, 70.61518717409400381, 34.21067981925357060 ) ) ;
#15771=ORIENTED_EDGE ( 'NONE', *, *, #9090, .F. ) ;
#15773=VERTEX_POINT ( 'NONE', #1683 ) ;
#15774=CARTESIAN_POINT ( 'NONE',  ( 38.58424406990784661, 141.2651871740940237, 35.64915139335016647 ) ) ;
#15775=CARTESIAN_POINT ( 'NONE',  ( 38.58424406990785371, 156.2651871740939953, 35.64915139335015937 ) ) ;
#15776=CARTESIAN_POINT ( 'NONE',  ( 38.58424406990785371, 108.2297705074273324, 32.77220824515697473 ) ) ;
#15782=CARTESIAN_POINT ( 'NONE',  ( 48.01140435219951996, 89.36049967264874283, 32.58608133808903773 ) ) ;
#15783=CARTESIAN_POINT ( 'NONE',  ( 47.43856463449117200, 142.7651871740939669, 32.77220824515698183 ) ) ;
#15784=CARTESIAN_POINT ( 'NONE',  ( 48.01140435219951996, 98.06049967264873146, 35.83527830041810347 ) ) ;
#15791=CARTESIAN_POINT ( 'NONE',  ( 38.58424406990784661, 84.52977050742731535, 35.64915139335016647 ) ) ;
#15793=CARTESIAN_POINT ( 'NONE',  ( 47.43856463449117911, 67.46518717409399812, 35.64915139335015937 ) ) ;
#15796=ORIENTED_EDGE ( 'NONE', *, *, #16809, .F. ) ;
#15797=CARTESIAN_POINT ( 'NONE',  ( 43.01140435219951286, 116.9604996726487371, 29.21067981925356705 ) ) ;
#15798=CARTESIAN_POINT ( 'NONE',  ( 48.01140435219951996, 122.0604996726487315, 35.83527830041809636 ) ) ;
#15799=CARTESIAN_POINT ( 'NONE',  ( 38.58424406990785371, 132.5297705074272869, 35.64915139335015937 ) ) ;
#15802=VERTEX_POINT ( 'NONE', #10176 ) ;
#15803=CARTESIAN_POINT ( 'NONE',  ( 45.74753988029933538, 136.4297705074273210, 37.97664729208901946 ) ) ;
#15804=CARTESIAN_POINT ( 'NONE',  ( 48.01140435219951996, 139.1344580088725706, 35.83527830041809636 ) ) ;
#15805=CARTESIAN_POINT ( 'NONE',  ( 48.01140435219951996, 155.3604996726487570, 32.58608133808903773 ) ) ;
#15806=CARTESIAN_POINT ( 'NONE',  ( 38.01140435219952707, 99.56049967264873146, 32.58608133808903773 ) ) ;
#15807=CARTESIAN_POINT ( 'NONE',  ( 43.80332655382220253, 120.6113394311928460, 39.21067981925355639 ) ) ;
#15808=CARTESIAN_POINT ( 'NONE',  ( 43.01140435219951996, 10.71049967264875491, 29.21067981925357060 ) ) ;
#15810=CARTESIAN_POINT ( 'NONE',  ( 44.37947211624943833, 94.01518717409400949, 38.42115945441014446 ) ) ;
#15811=CARTESIAN_POINT ( 'NONE',  ( 43.80332655382221674, 132.6113394311928175, 39.21067981925355639 ) ) ;
#15814=CARTESIAN_POINT ( 'NONE',  ( 43.01140435219951286, 70.46049967264873715, 39.21067981925356349 ) ) ;
#15815=CARTESIAN_POINT ( 'NONE',  ( 39.92123440845004723, 128.3344580088725877, 29.95742577749337343 ) ) ;
#15816=CARTESIAN_POINT ( 'NONE',  ( 47.43856463449118621, 112.8797705074273097, 34.21067981925357060 ) ) ;
#15819=CARTESIAN_POINT ( 'NONE',  ( 46.59305225739526435, 97.31518717409400665, 36.81289934271958941 ) ) ;
#15821=CARTESIAN_POINT ( 'NONE',  ( 43.80332655382220253, 156.6113394311928744, 39.21067981925355639 ) ) ;
#15823=( BOUNDED_CURVE ( )  B_SPLINE_CURVE ( 2, ( #1871, #18736, #3853, #12325, #19060, #5713, #20608, #15745, #6951, #20391, #3963, #12108, #20504 ),
 .UNSPECIFIED., .F., .F. ) 
 B_SPLINE_CURVE_WITH_KNOTS ( ( 3, 2, 2, 2, 2, 2, 3 ),
 ( 0.8897058823529412352, 0.8911764705882353477, 0.8941176470588235725, 0.8970588235294117974, 0.9000000000000000222, 0.9029411764705882470, 0.9044117647058823595 ),
 .UNSPECIFIED. ) 
 CURVE ( )  GEOMETRIC_REPRESENTATION_ITEM ( )  RATIONAL_B_SPLINE_CURVE ( ( 0.9755282581475768211, 0.9755282581475777093, 1.000000000000000000, 0.9510565162951535312, 1.000000000000000000, 0.9510565162951535312, 1.000000000000000000, 0.9510565162951535312, 1.000000000000000000, 0.9510565162951535312, 1.000000000000000000, 0.9755282581475768211, 0.9755282581475768211 ) ) 
 REPRESENTATION_ITEM ( '' )  );
#15827=CARTESIAN_POINT ( 'NONE',  ( 38.58424406990785371, 72.22977050742731819, 32.77220824515697473 ) ) ;
#15833=CARTESIAN_POINT ( 'NONE',  ( 47.05648932407426344, 115.9104996726487400, 37.14960608071593384 ) ) ;
#15834=CARTESIAN_POINT ( 'NONE',  ( 44.37947211624943833, 76.01518717409399528, 38.42115945441014446 ) ) ;
#15839=DIRECTION ( 'NONE',  ( 0.000000000000000000, 1.000000000000000000, 0.000000000000000000 ) ) ;
#15841=CARTESIAN_POINT ( 'NONE',  ( 44.55648932407425633, 157.8844580088725706, 29.45539723777780239 ) ) ;
#15842=CARTESIAN_POINT ( 'NONE',  ( 45.74753988029933538, 143.3297705074272699, 30.44471234641811819 ) ) ;
#15844=CARTESIAN_POINT ( 'NONE',  ( 44.37947211624943833, 139.0151871740939953, 38.42115945441014446 ) ) ;
#15847=DIRECTION ( 'NONE',  ( 0.000000000000000000, 0.000000000000000000, 1.000000000000000000 ) ) ;
#15851=CARTESIAN_POINT ( 'NONE',  ( 47.43856463449117200, 112.4651871740939839, 35.64915139335016647 ) ) ;
#15857=ORIENTED_EDGE ( 'NONE', *, *, #17825, .F. ) ;
#15858=CARTESIAN_POINT ( 'NONE',  ( 47.05648932407426344, 91.58445800887257349, 31.27175355779120025 ) ) ;
#15859=CARTESIAN_POINT ( 'NONE',  ( 39.92123440845004723, 145.1604996726487116, 38.46393386101376421 ) ) ;
#15860=CARTESIAN_POINT ( 'NONE',  ( 41.64333658814960870, 102.7151871740939981, 38.42115945441014446 ) ) ;
#15862=CARTESIAN_POINT ( 'NONE',  ( 44.55648932407425633, 67.61049967264872862, 38.96596240072933170 ) ) ;
#15863=CARTESIAN_POINT ( 'NONE',  ( 43.01140435219951996, 10.71049967264875491, 29.21067981925357060 ) ) ;
#15864=CARTESIAN_POINT ( 'NONE',  ( 43.01140435219951996, 148.4604996726487798, 39.21067981925356349 ) ) ;
#15871=VERTEX_POINT ( 'NONE', #11924 ) ;
#15874=CARTESIAN_POINT ( 'NONE',  ( 39.42975644700377558, 144.4151871740940294, 36.81289934271958941 ) ) ;
#15875=CARTESIAN_POINT ( 'NONE',  ( 41.64333658814960870, 155.5151871740940237, 30.00020018409699318 ) ) ;
#15876=CARTESIAN_POINT ( 'NONE',  ( 45.74753988029934249, 104.3297705074273125, 30.44471234641812174 ) ) ;
#15877=EDGE_LOOP ( 'NONE', ( #3804, #11272, #9009, #9129 ) ) ;
#15880=( BOUNDED_CURVE ( )  B_SPLINE_CURVE ( 2, ( #4708, #14412, #16385, #11426, #6033, #1298, #6366, #2732, #14520, #13091, #9472, #19818, #1083 ),
 .UNSPECIFIED., .F., .F. ) 
 B_SPLINE_CURVE_WITH_KNOTS ( ( 3, 2, 2, 2, 2, 2, 3 ),
 ( 0.08088235294117646079, 0.08235294117647058709, 0.08529411764705882582, 0.08823529411764706454, 0.09117647058823528938, 0.09411764705882352811, 0.09558823529411765441 ),
 .UNSPECIFIED. ) 
 CURVE ( )  GEOMETRIC_REPRESENTATION_ITEM ( )  RATIONAL_B_SPLINE_CURVE ( ( 0.9755282581475767101, 0.9755282581475765991, 1.000000000000000000, 0.9510565162951535312, 1.000000000000000000, 0.9510565162951535312, 1.000000000000000000, 0.9510565162951535312, 1.000000000000000000, 0.9510565162951535312, 1.000000000000000000, 0.9755282581475765991, 0.9755282581475767101 ) ) 
 REPRESENTATION_ITEM ( '' )  );
#15882=CARTESIAN_POINT ( 'NONE',  ( 47.05648932407426344, 115.5844580088725877, 31.27175355779120025 ) ) ;
#15883=CARTESIAN_POINT ( 'NONE',  ( 43.01140435219951286, 89.96049967264873715, 29.21067981925356705 ) ) ;
#15884=CARTESIAN_POINT ( 'NONE',  ( 38.58424406990786082, 75.37977050742732388, 34.21067981925357060 ) ) ;
#15885=CARTESIAN_POINT ( 'NONE',  ( 38.58424406990784661, 135.2651871740939953, 35.64915139335016647 ) ) ;
#15886=CARTESIAN_POINT ( 'NONE',  ( 41.46631938032478359, 102.1104996726487286, 29.45539723777780239 ) ) ;
#15888=CARTESIAN_POINT ( 'NONE',  ( 43.80332655382220253, 119.8836182503284533, 29.21067981925356705 ) ) ;
#15890=CARTESIAN_POINT ( 'NONE',  ( 38.96631938032478359, 153.0844580088725877, 37.14960608071593384 ) ) ;
#15891=CARTESIAN_POINT ( 'NONE',  ( 43.80332655382220253, 63.61133943119283174, 39.21067981925355639 ) ) ;
#15895=CARTESIAN_POINT ( 'NONE',  ( 43.01140435219951286, 86.62977050742730967, 29.55568802177586463 ) ) ;
#15902=DIRECTION ( 'NONE',  ( 0.000000000000000000, 1.000000000000000000, 0.000000000000000000 ) ) ;
#15903=CARTESIAN_POINT ( 'NONE',  ( 41.64333658814960870, 132.9797705074273324, 38.42115945441014446 ) ) ;
#15905=ORIENTED_EDGE ( 'NONE', *, *, #13099, .F. ) ;
#15906=CARTESIAN_POINT ( 'NONE',  ( 44.55648932407425633, 72.68445800887258201, 38.96596240072933170 ) ) ;
#15908=CARTESIAN_POINT ( 'NONE',  ( 38.58424406990784661, 126.2297705074273040, 32.77220824515698183 ) ) ;
#15909=CARTESIAN_POINT ( 'NONE',  ( 47.05648932407426344, 139.5844580088725877, 31.27175355779120025 ) ) ;
#15912=CARTESIAN_POINT ( 'NONE',  ( 46.10157429594899270, 154.7604996726487343, 38.46393386101375711 ) ) ;
#15913=CARTESIAN_POINT ( 'NONE',  ( 43.01140435219954838, 110.0344580088725763, 29.21067981925356705 ) ) ;
#15916=CARTESIAN_POINT ( 'NONE',  ( 43.01140435219951286, 99.86518717409400381, 38.86567161673127657 ) ) ;
#15917=CARTESIAN_POINT ( 'NONE',  ( 43.01140435219951286, 74.96049967264873715, 29.21067981925356705 ) ) ;
#15922=CARTESIAN_POINT ( 'NONE',  ( 48.01140435219951996, 133.2844580088726048, 34.21067981925357060 ) ) ;
#15923=CARTESIAN_POINT ( 'NONE',  ( 40.27526882409969033, 111.8297705074272983, 37.97664729208901946 ) ) ;
#15926=CARTESIAN_POINT ( 'NONE',  ( 43.01140435219951286, 93.86518717409401802, 38.86567161673127657 ) ) ;
#15927=CARTESIAN_POINT ( 'NONE',  ( 39.92123440845005433, 91.16049967264873999, 38.46393386101375711 ) ) ;
#15929=CARTESIAN_POINT ( 'NONE',  ( 43.01140435219951286, 129.5344580088725763, 39.21067981925356349 ) ) ;
#15934=CARTESIAN_POINT ( 'NONE',  ( 40.27526882409969744, 78.82977050742729830, 37.97664729208901235 ) ) ;
#15936=EDGE_CURVE ( 'NONE', #11479, #5662, #9272, .T. ) ;
#15937=ORIENTED_EDGE ( 'NONE', *, *, #19450, .T. ) ;
#15938=CARTESIAN_POINT ( 'NONE',  ( 45.74753988029933538, 157.4297705074273495, 37.97664729208901946 ) ) ;
#15941=CARTESIAN_POINT ( 'NONE',  ( 46.10157429594899270, 121.7604996726487485, 38.46393386101376421 ) ) ;
#15942=CARTESIAN_POINT ( 'NONE',  ( 47.43856463449117200, 73.76518717409399528, 32.77220824515698183 ) ) ;
#15949=CARTESIAN_POINT ( 'NONE',  ( 41.64333658814960870, 141.9797705074273324, 38.42115945441014446 ) ) ;
#15950=( BOUNDED_CURVE ( )  B_SPLINE_CURVE ( 2, ( #2110, #12129, #3769, #14003, #5513, #17521, #4088, #12460, #20737, #5411, #10924, #5626, #20846 ),
 .UNSPECIFIED., .F., .F. ) 
 B_SPLINE_CURVE_WITH_KNOTS ( ( 3, 2, 2, 2, 2, 2, 3 ),
 ( 0.9338235294117647189, 0.9352941176470588314, 0.9382352941176470562, 0.9411764705882352811, 0.9441176470588235059, 0.9470588235294117307, 0.9485294117647058432 ),
 .UNSPECIFIED. ) 
 CURVE ( )  GEOMETRIC_REPRESENTATION_ITEM ( )  RATIONAL_B_SPLINE_CURVE ( ( 0.9755282581475768211, 0.9755282581475768211, 1.000000000000000000, 0.9510565162951535312, 1.000000000000000000, 0.9510565162951535312, 1.000000000000000000, 0.9510565162951535312, 1.000000000000000000, 0.9510565162951535312, 1.000000000000000000, 0.9755282581475768211, 0.9755282581475768211 ) ) 
 REPRESENTATION_ITEM ( '' )  );
#15951=CARTESIAN_POINT ( 'NONE',  ( 45.74753988029934249, 130.1651871740940010, 37.97664729208901235 ) ) ;
#15957=CARTESIAN_POINT ( 'NONE',  ( 43.01140435219951286, 121.4604996726487371, 39.21067981925356349 ) ) ;
#15958=CARTESIAN_POINT ( 'NONE',  ( 43.01140435219951286, 102.8651871740940038, 38.86567161673127657 ) ) ;
#15961=CARTESIAN_POINT ( 'NONE',  ( 47.05648932407426344, 86.51049967264874851, 31.27175355779120025 ) ) ;
#15962=ORIENTED_EDGE ( 'NONE', *, *, #3722, .F. ) ;
#15963=CARTESIAN_POINT ( 'NONE',  ( 38.01140435219951996, 89.93445800887256780, 35.83527830041810347 ) ) ;
#15964=CARTESIAN_POINT ( 'NONE',  ( 47.05648932407426344, 148.9104996726487400, 37.14960608071593384 ) ) ;
#15965=CARTESIAN_POINT ( 'NONE',  ( 44.37947211624943833, 107.2151871740940123, 30.00020018409699318 ) ) ;
#15968=DIRECTION ( 'NONE',  ( 0.000000000000000000, 1.000000000000000000, 0.000000000000000000 ) ) ;
#15971=CARTESIAN_POINT ( 'NONE',  ( 48.01140435219951996, 118.2844580088725763, 34.21067981925357060 ) ) ;
#15974=CARTESIAN_POINT ( 'NONE',  ( 40.27526882409969033, 68.66518717409400097, 30.44471234641811819 ) ) ;
#15976=CARTESIAN_POINT ( 'NONE',  ( 46.10157429594899270, 94.76049967264873430, 38.46393386101375711 ) ) ;
#15982=ORIENTED_EDGE ( 'NONE', *, *, #15195, .T. ) ;
#15983=CARTESIAN_POINT ( 'NONE',  ( 38.58424406990784661, 131.9651871740939555, 32.77220824515698183 ) ) ;
#15984=CARTESIAN_POINT ( 'NONE',  ( 40.27526882409969744, 96.82977050742731251, 37.97664729208901235 ) ) ;
#15985=ORIENTED_EDGE ( 'NONE', *, *, #11809, .T. ) ;
#15988=ORIENTED_EDGE ( 'NONE', *, *, #12026, .T. ) ;
#15989=CARTESIAN_POINT ( 'NONE',  ( 47.05648932407426344, 111.9844580088725792, 37.14960608071593384 ) ) ;
#15991=CARTESIAN_POINT ( 'NONE',  ( 41.46631938032478359, 76.31049967264874567, 38.96596240072933170 ) ) ;
#15992=CARTESIAN_POINT ( 'NONE',  ( 40.27526882409969033, 75.82977050742731251, 37.97664729208901946 ) ) ;
#15993=CARTESIAN_POINT ( 'NONE',  ( 38.58424406990784661, 131.9651871740939555, 32.77220824515698183 ) ) ;
#15994=CARTESIAN_POINT ( 'NONE',  ( 48.01140435219951996, 92.21049967264873715, 34.21067981925357060 ) ) ;
#15999=ADVANCED_FACE ( 'NONE', ( #2947 ), #4375, .T. ) ;
#16000=CARTESIAN_POINT ( 'NONE',  ( 43.01140435219951996, 10.71049967264875491, 29.21067981925357060 ) ) ;
#16002=VERTEX_POINT ( 'NONE', #16060 ) ;
#16003=CARTESIAN_POINT ( 'NONE',  ( 39.42975644700377558, 75.07977050742731251, 31.60846029578754468 ) ) ;
#16006=ORIENTED_EDGE ( 'NONE', *, *, #20810, .F. ) ;
#16008=CARTESIAN_POINT ( 'NONE',  ( 46.10157429594899270, 124.7344580088725934, 29.95742577749336988 ) ) ;
#16009=( BOUNDED_CURVE ( )  B_SPLINE_CURVE ( 2, ( #12833, #19668, #9433, #9649, #9318, #16136, #1259, #19781, #8101, #6441, #7996, #21550, #21223 ),
 .UNSPECIFIED., .F., .F. ) 
 B_SPLINE_CURVE_WITH_KNOTS ( ( 3, 2, 2, 2, 2, 2, 3 ),
 ( 0.6102941176470587648, 0.6117647058823529882, 0.6147058823529412130, 0.6176470588235294379, 0.6205882352941176627, 0.6235294117647058876, 0.6250000000000000000 ),
 .UNSPECIFIED. ) 
 CURVE ( )  GEOMETRIC_REPRESENTATION_ITEM ( )  RATIONAL_B_SPLINE_CURVE ( ( 0.9755282581475768211, 0.9755282581475758219, 1.000000000000000000, 0.9510565162951535312, 1.000000000000000000, 0.9510565162951535312, 1.000000000000000000, 0.9510565162951535312, 1.000000000000000000, 0.9510565162951535312, 1.000000000000000000, 0.9755282581475768211, 0.9755282581475768211 ) ) 
 REPRESENTATION_ITEM ( '' )  );
#16010=CARTESIAN_POINT ( 'NONE',  ( 46.59305225739526435, 127.5797705074273267, 36.81289934271958941 ) ) ;
#16011=EDGE_LOOP ( 'NONE', ( #16474, #8039, #18133, #10608 ) ) ;
#16015=CARTESIAN_POINT ( 'NONE',  ( 40.27526882409969033, 122.9297705074272926, 30.44471234641811819 ) ) ;
#16016=EDGE_CURVE ( 'NONE', #9530, #20615, #15880, .T. ) ;
#16017=CARTESIAN_POINT ( 'NONE',  ( 44.55648932407425633, 144.6844580088725820, 38.96596240072933170 ) ) ;
#16018=CARTESIAN_POINT ( 'NONE',  ( 38.01140435219952707, 99.86049967264871441, 35.83527830041809636 ) ) ;
#16019=CARTESIAN_POINT ( 'NONE',  ( 38.01140435219952707, 129.7104996726487514, 34.21067981925357060 ) ) ;
#16022=CARTESIAN_POINT ( 'NONE',  ( 48.01140435219951996, 74.06049967264874567, 35.83527830041809636 ) ) ;
#16025=CARTESIAN_POINT ( 'NONE',  ( 38.01140435219952707, 128.7844580088725763, 34.21067981925357060 ) ) ;
#16026=CARTESIAN_POINT ( 'NONE',  ( 47.43856463449117200, 104.0297705074273011, 32.77220824515698183 ) ) ;
#16028=DIRECTION ( 'NONE',  ( 0.000000000000000000, 1.000000000000000000, 0.000000000000000000 ) ) ;
#16029=CARTESIAN_POINT ( 'NONE',  ( 46.59305225739526435, 100.9151871740940010, 31.60846029578754468 ) ) ;
#16030=CARTESIAN_POINT ( 'NONE',  ( 43.01140435219951286, 134.9604996726487514, 29.21067981925356705 ) ) ;
#16032=CARTESIAN_POINT ( 'NONE',  ( 48.01140435219951996, 76.13445800887258486, 35.83527830041809636 ) ) ;
#16037=CARTESIAN_POINT ( 'NONE',  ( 46.59305225739526435, 79.57977050742731251, 36.81289934271958941 ) ) ;
#16038=AXIS2_PLACEMENT_3D ( 'NONE', #8111, #14817, #18245 ) ;
#16041=FACE_OUTER_BOUND ( 'NONE', #18158, .T. ) ;
#16045=CARTESIAN_POINT ( 'NONE',  ( 38.01140435219951996, 123.5604996726487315, 32.58608133808903773 ) ) ;
#16047=CARTESIAN_POINT ( 'NONE',  ( 47.43856463449118621, 73.61518717409400381, 34.21067981925357060 ) ) ;
#16051=CARTESIAN_POINT ( 'NONE',  ( 44.55648932407425633, 112.6104996726487428, 38.96596240072933170 ) ) ;
#16054=CARTESIAN_POINT ( 'NONE',  ( 38.01140435219952707, 149.9344580088725820, 35.83527830041809636 ) ) ;
#16055=CARTESIAN_POINT ( 'NONE',  ( 38.58424406990784661, 144.2297705074273324, 32.77220824515698183 ) ) ;
#16058=CARTESIAN_POINT ( 'NONE',  ( 45.74753988029934249, 122.0651871740940209, 30.44471234641812174 ) ) ;
#16060=CARTESIAN_POINT ( 'NONE',  ( 43.01140435219951286, 122.0344580088725763, 29.21067981925356705 ) ) ;
#16062=AXIS2_PLACEMENT_3D ( 'NONE', #21321, #21431, #11385 ) ;
#16065=FACE_OUTER_BOUND ( 'NONE', #10500, .T. ) ;
#16066=CARTESIAN_POINT ( 'NONE',  ( 46.59305225739526435, 106.9151871740940152, 31.60846029578754468 ) ) ;
#16067=ORIENTED_EDGE ( 'NONE', *, *, #21520, .T. ) ;
#16069=EDGE_LOOP ( 'NONE', ( #19128, #15696 ) ) ;
#16070=CARTESIAN_POINT ( 'NONE',  ( 39.92123440845004723, 95.33445800887255928, 29.95742577749337343 ) ) ;
#16074=CARTESIAN_POINT ( 'NONE',  ( 41.46631938032478359, 148.3104996726487457, 38.96596240072933170 ) ) ;
#16075=CARTESIAN_POINT ( 'NONE',  ( 45.74753988029933538, 109.1651871740939868, 37.97664729208901946 ) ) ;
#16077=( BOUNDED_CURVE ( )  B_SPLINE_CURVE ( 2, ( #19810, #1290, #11417, #6468, #21690, #11204, #4476, #16377, #10005, #16709, #15061, #11642, #3273 ),
 .UNSPECIFIED., .F., .F. ) 
 B_SPLINE_CURVE_WITH_KNOTS ( ( 3, 2, 2, 2, 2, 2, 3 ),
 ( 0.02205882352941176960, 0.02352941176470588203, 0.02647058823529411728, 0.02941176470588235253, 0.03235294117647059126, 0.03529411764705882304, 0.03676470588235293546 ),
 .UNSPECIFIED. ) 
 CURVE ( )  GEOMETRIC_REPRESENTATION_ITEM ( )  RATIONAL_B_SPLINE_CURVE ( ( 0.9755282581475767101, 0.9755282581475768211, 1.000000000000000000, 0.9510565162951535312, 1.000000000000000000, 0.9510565162951535312, 1.000000000000000000, 0.9510565162951535312, 1.000000000000000000, 0.9510565162951535312, 1.000000000000000000, 0.9755282581475768211, 0.9755282581475767101 ) ) 
 REPRESENTATION_ITEM ( '' )  );
#16078=CARTESIAN_POINT ( 'NONE',  ( 39.92123440845004723, 67.16049967264873999, 38.46393386101376421 ) ) ;
#16080=CARTESIAN_POINT ( 'NONE',  ( 43.01140435219951286, 60.53445800887258343, 39.21067981925356349 ) ) ;
#16081=CARTESIAN_POINT ( 'NONE',  ( 43.80332655382220253, 117.6113394311928317, 39.21067981925355639 ) ) ;
#16082=CARTESIAN_POINT ( 'NONE',  ( 43.80332655382220253, 78.61133943119283174, 39.21067981925355639 ) ) ;
#16083=DIRECTION ( 'NONE',  ( 0.000000000000000000, 1.000000000000000000, 0.000000000000000000 ) ) ;
#16084=CARTESIAN_POINT ( 'NONE',  ( 47.43856463449118621, 73.61518717409400381, 34.21067981925357060 ) ) ;
#16085=EDGE_CURVE ( 'NONE', #19572, #6509, #15484, .T. ) ;
#16088=CARTESIAN_POINT ( 'NONE',  ( 38.01140435219952707, 114.5604996726487315, 32.58608133808903773 ) ) ;
#16096=CARTESIAN_POINT ( 'NONE',  ( 47.43856463449118621, 133.6151871740940180, 34.21067981925357060 ) ) ;
#16097=CARTESIAN_POINT ( 'NONE',  ( 41.64333658814960870, 92.77977050742731535, 30.00020018409699318 ) ) ;
#16098=ORIENTED_EDGE ( 'NONE', *, *, #10327, .F. ) ;
#16099=VERTEX_POINT ( 'NONE', #8769 ) ;
#16102=CARTESIAN_POINT ( 'NONE',  ( 39.92123440845004723, 116.3344580088725735, 29.95742577749337343 ) ) ;
#16107=VECTOR ( 'NONE', #13066, 1000.000000000000000 ) ;
#16108=CARTESIAN_POINT ( 'NONE',  ( 45.74753988029933538, 80.32977050742731251, 30.44471234641811819 ) ) ;
#16109=CARTESIAN_POINT ( 'NONE',  ( 46.59305225739526435, 133.9151871740940010, 31.60846029578754468 ) ) ;
#16111=CARTESIAN_POINT ( 'NONE',  ( 41.46631938032478359, 96.11049967264874283, 29.45539723777780239 ) ) ;
#16117=CARTESIAN_POINT ( 'NONE',  ( 46.10157429594899270, 106.7604996726487201, 38.46393386101375711 ) ) ;
#16120=CARTESIAN_POINT ( 'NONE',  ( 38.58424406990786082, 72.37977050742732388, 34.21067981925357060 ) ) ;
#16126=CARTESIAN_POINT ( 'NONE',  ( 39.92123440845005433, 105.2344580088725650, 38.46393386101375711 ) ) ;
#16127=CARTESIAN_POINT ( 'NONE',  ( 47.43856463449117911, 127.7297705074272898, 35.64915139335015937 ) ) ;
#16129=ORIENTED_EDGE ( 'NONE', *, *, #8212, .F. ) ;
#16130=CARTESIAN_POINT ( 'NONE',  ( 38.58424406990784661, 129.5297705074273154, 35.64915139335016647 ) ) ;
#16133=CARTESIAN_POINT ( 'NONE',  ( 48.01140435219951996, 64.28445800887257633, 34.21067981925357060 ) ) ;
#16136=CARTESIAN_POINT ( 'NONE',  ( 38.01140435219952707, 96.86049967264871441, 35.83527830041809636 ) ) ;
#16138=CARTESIAN_POINT ( 'NONE',  ( 47.05648932407426344, 74.51049967264873430, 31.27175355779120025 ) ) ;
#16141=CARTESIAN_POINT ( 'NONE',  ( 41.46631938032478359, 137.1844580088725820, 29.45539723777780239 ) ) ;
#16142=CARTESIAN_POINT ( 'NONE',  ( 47.43856463449118621, 103.8797705074273239, 34.21067981925357060 ) ) ;
#16143=( BOUNDED_CURVE ( )  B_SPLINE_CURVE ( 2, ( #11230, #9377, #2751, #14213, #14538, #19726, #21166, #21279, #11339, #16299, #993, #16082, #1207 ),
 .UNSPECIFIED., .F., .F. ) 
 B_SPLINE_CURVE_WITH_KNOTS ( ( 3, 2, 2, 2, 2, 2, 3 ),
 ( 0.7720588235294117974, 0.7735294117647059098, 0.7764705882352941346, 0.7794117647058823595, 0.7823529411764705843, 0.7852941176470588092, 0.7867647058823529216 ),
 .UNSPECIFIED. ) 
 CURVE ( )  GEOMETRIC_REPRESENTATION_ITEM ( )  RATIONAL_B_SPLINE_CURVE ( ( 0.9755282581475768211, 0.9755282581475768211, 1.000000000000000000, 0.9510565162951535312, 1.000000000000000000, 0.9510565162951535312, 1.000000000000000000, 0.9510565162951535312, 1.000000000000000000, 0.9510565162951535312, 1.000000000000000000, 0.9755282581475768211, 0.9755282581475768211 ) ) 
 REPRESENTATION_ITEM ( '' )  );
#16145=CYLINDRICAL_SURFACE ( 'NONE', #9583, 4.999999999999997335 ) ;
#16146=CARTESIAN_POINT ( 'NONE',  ( 41.64333658814960870, 98.51518717409399528, 30.00020018409699318 ) ) ;
#16153=CARTESIAN_POINT ( 'NONE',  ( 47.43856463449117911, 64.72977050742731819, 35.64915139335015937 ) ) ;
#16155=ORIENTED_EDGE ( 'NONE', *, *, #6177, .T. ) ;
#16158=CARTESIAN_POINT ( 'NONE',  ( 41.46631938032478359, 120.1104996726487570, 29.45539723777780239 ) ) ;
#16159=CARTESIAN_POINT ( 'NONE',  ( 41.64333658814960870, 74.51518717409399528, 30.00020018409699318 ) ) ;
#16166=CARTESIAN_POINT ( 'NONE',  ( 43.01140435219951996, 10.71049967264875491, 29.21067981925357060 ) ) ;
#16167=CARTESIAN_POINT ( 'NONE',  ( 47.43856463449117200, 131.0297705074272869, 32.77220824515698183 ) ) ;
#16169=CARTESIAN_POINT ( 'NONE',  ( 38.58424406990785371, 125.9651871740939697, 32.77220824515697473 ) ) ;
#16171=CARTESIAN_POINT ( 'NONE',  ( 43.01140435219951996, 10.71049967264875491, 34.21067981925357060 ) ) ;
#16172=APPLICATION_CONTEXT ( 'automotive_design' ) ;
#16174=CARTESIAN_POINT ( 'NONE',  ( 43.01140435219951996, 10.71049967264875491, 39.21067981925356349 ) ) ;
#16177=CARTESIAN_POINT ( 'NONE',  ( 44.37947211624943833, 107.2151871740940123, 30.00020018409699318 ) ) ;
#16179=DIRECTION ( 'NONE',  ( 0.000000000000000000, 0.000000000000000000, 1.000000000000000000 ) ) ;
#16181=CARTESIAN_POINT ( 'NONE',  ( 38.01140435219951996, 95.63445800887255643, 32.58608133808903773 ) ) ;
#16182=CARTESIAN_POINT ( 'NONE',  ( 43.01140435219951286, 84.53445800887256212, 39.21067981925356349 ) ) ;
#16183=CARTESIAN_POINT ( 'NONE',  ( 48.01140435219951996, 146.2104996726487229, 34.21067981925357060 ) ) ;
#16184=CARTESIAN_POINT ( 'NONE',  ( 41.64333658814960870, 110.5151871740940095, 30.00020018409699318 ) ) ;
#16186=CARTESIAN_POINT ( 'NONE',  ( 45.51148226160370314, 59.71123016864974176, 29.88059778228138086 ) ) ;
#16188=CARTESIAN_POINT ( 'NONE',  ( 43.01140435219951996, 147.5344580088726048, 39.21067981925356349 ) ) ;
#16192=CARTESIAN_POINT ( 'NONE',  ( 41.64333658814960870, 65.51518717409400949, 30.00020018409699318 ) ) ;
#16194=CARTESIAN_POINT ( 'NONE',  ( 44.55648932407425633, 94.61049967264874283, 38.96596240072933170 ) ) ;
#16198=CARTESIAN_POINT ( 'NONE',  ( 38.58424406990785371, 65.96518717409398391, 32.77220824515697473 ) ) ;
#16201=DIRECTION ( 'NONE',  ( 0.000000000000000000, 1.000000000000000000, 0.000000000000000000 ) ) ;
#16202=CARTESIAN_POINT ( 'NONE',  ( 41.64333658814960870, 131.5151871740939953, 30.00020018409699318 ) ) ;
#16203=AXIS2_PLACEMENT_3D ( 'NONE', #2300, #20613, #10691 ) ;
#16208=EDGE_LOOP ( 'NONE', ( #2877, #8016, #5319, #12613, #17932, #8558, #21243, #11985, #5112, #20905, #14799, #8207, #13240, #20137, #11855, #9061, #19327, #4772, #8070, #5270, #16862, #1558, #11716, #11383, #7880, #12356, #4114, #14459, #17312, #14143, #15129, #806, #18766, #20165, #15796, #18423, #21790, #21762, #13684, #6749, #11463, #7790, #3880, #13101, #18048, #17417, #18635, #17902, #11579, #21597, #17633, #5110, #11581, #14030, #1475, #16529, #3992, #13204, #13637, #20990, #20060, #10881, #1986, #8771, #1556, #3493, #14851, #6234, #20582, #3539, #1448 ) ) ;
#16209=( BOUNDED_CURVE ( )  B_SPLINE_CURVE ( 2, ( #9981, #16246, #21553, #9869, #3252, #11506, #14918, #6218, #1155, #6444, #11180, #14591, #14482 ),
 .UNSPECIFIED., .F., .F. ) 
 B_SPLINE_CURVE_WITH_KNOTS ( ( 3, 2, 2, 2, 2, 2, 3 ),
 ( 0.2720588235294117974, 0.2735294117647059098, 0.2764705882352941346, 0.2794117647058823595, 0.2823529411764705843, 0.2852941176470588092, 0.2867647058823529216 ),
 .UNSPECIFIED. ) 
 CURVE ( )  GEOMETRIC_REPRESENTATION_ITEM ( )  RATIONAL_B_SPLINE_CURVE ( ( 0.9755282581475768211, 0.9755282581475772652, 1.000000000000000000, 0.9510565162951535312, 1.000000000000000000, 0.9510565162951535312, 1.000000000000000000, 0.9510565162951535312, 1.000000000000000000, 0.9510565162951535312, 1.000000000000000000, 0.9755282581475768211, 0.9755282581475768211 ) ) 
 REPRESENTATION_ITEM ( '' )  );
#16210=ADVANCED_FACE ( 'NONE', ( #9902 ), #20449, .T. ) ;
#16211=CARTESIAN_POINT ( 'NONE',  ( 41.46631938032478359, 116.1844580088725820, 29.45539723777780239 ) ) ;
#16212=CARTESIAN_POINT ( 'NONE',  ( 45.05633291560663167, 59.76197383743924973, 29.61780626570246966 ) ) ;
#16213=CARTESIAN_POINT ( 'NONE',  ( 38.58424406990786082, 78.37977050742732388, 34.21067981925357060 ) ) ;
#16214=CARTESIAN_POINT ( 'NONE',  ( 40.27526882409969033, 137.6651871740940294, 30.44471234641811819 ) ) ;
#16216=CARTESIAN_POINT ( 'NONE',  ( 47.05648932407426344, 94.91049967264873999, 37.14960608071593384 ) ) ;
#16221=DIRECTION ( 'NONE',  ( 0.000000000000000000, 1.000000000000000000, 0.000000000000000000 ) ) ;
#16223=CARTESIAN_POINT ( 'NONE',  ( 46.59305225739526435, 71.17977050742730682, 31.60846029578754468 ) ) ;
#16230=CARTESIAN_POINT ( 'NONE',  ( 47.43856463449117911, 125.0297705074273011, 32.77220824515697473 ) ) ;
#16232=EDGE_CURVE ( 'NONE', #5984, #7609, #12058, .T. ) ;
#16233=CARTESIAN_POINT ( 'NONE',  ( 43.01140435219951286, 87.53445800887257633, 39.21067981925356349 ) ) ;
#16235=CARTESIAN_POINT ( 'NONE',  ( 41.64333658814960870, 128.7797705074273438, 30.00020018409699318 ) ) ;
#16237=CARTESIAN_POINT ( 'NONE',  ( 38.58424406990784661, 90.52977050742731535, 35.64915139335016647 ) ) ;
#16238=CARTESIAN_POINT ( 'NONE',  ( 38.01140435219951996, 65.63445800887257064, 32.58608133808903773 ) ) ;
#16240=AXIS2_PLACEMENT_3D ( 'NONE', #8535, #2226, #5636 ) ;
#16242=CARTESIAN_POINT ( 'NONE',  ( 38.01140435219952707, 101.6344580088725849, 32.58608133808903773 ) ) ;
#16245=CARTESIAN_POINT ( 'NONE',  ( 38.96631938032478359, 89.48445800887257917, 31.27175355779120025 ) ) ;
#16246=CARTESIAN_POINT ( 'NONE',  ( 43.80332655382221674, 131.8836182503284533, 29.21067981925357060 ) ) ;
#16249=AXIS2_PLACEMENT_3D ( 'NONE', #1942, #3271, #21796 ) ;
#16250=CARTESIAN_POINT ( 'NONE',  ( 44.55648932407425633, 121.8844580088725849, 29.45539723777780239 ) ) ;
#16251=CARTESIAN_POINT ( 'NONE',  ( 40.27526882409969033, 101.9297705074273068, 30.44471234641811819 ) ) ;
#16254=CARTESIAN_POINT ( 'NONE',  ( 39.42975644700377558, 96.41518717409400097, 36.81289934271958941 ) ) ;
#16263=CARTESIAN_POINT ( 'NONE',  ( 47.43856463449117911, 70.72977050742730398, 35.64915139335015937 ) ) ;
#16266=CARTESIAN_POINT ( 'NONE',  ( 38.58424406990784661, 156.2297705074273040, 32.77220824515698183 ) ) ;
#16268=CARTESIAN_POINT ( 'NONE',  ( 46.10157429594899270, 112.7604996726487485, 38.46393386101376421 ) ) ;
#16269=CARTESIAN_POINT ( 'NONE',  ( 47.43856463449117200, 64.76518717409400949, 32.77220824515698183 ) ) ;
#16271=CARTESIAN_POINT ( 'NONE',  ( 41.46631938032478359, 66.38445800887257064, 38.96596240072933170 ) ) ;
#16272=( BOUNDED_CURVE ( )  B_SPLINE_CURVE ( 2, ( #5997, #4449, #9436, #17784, #12835, #12727, #17463, #19451, #9111, #2692, #2805, #12401, #15708 ),
 .UNSPECIFIED., .F., .F. ) 
 B_SPLINE_CURVE_WITH_KNOTS ( ( 3, 2, 2, 2, 2, 2, 3 ),
 ( 0.9044117647058823595, 0.9058823529411764719, 0.9088235294117646967, 0.9117647058823529216, 0.9147058823529411464, 0.9176470588235293713, 0.9191176470588234837 ),
 .UNSPECIFIED. ) 
 CURVE ( )  GEOMETRIC_REPRESENTATION_ITEM ( )  RATIONAL_B_SPLINE_CURVE ( ( 0.9755282581475768211, 0.9755282581475768211, 1.000000000000000000, 0.9510565162951535312, 1.000000000000000000, 0.9510565162951535312, 1.000000000000000000, 0.9510565162951535312, 1.000000000000000000, 0.9510565162951535312, 1.000000000000000000, 0.9755282581475768211, 0.9755282581475768211 ) ) 
 REPRESENTATION_ITEM ( '' )  );
#16277=CARTESIAN_POINT ( 'NONE',  ( 38.96631938032478359, 149.4844580088725934, 31.27175355779120025 ) ) ;
#16278=CARTESIAN_POINT ( 'NONE',  ( 43.01140435219951286, 136.1297705074273381, 38.86567161673127657 ) ) ;
#16280=CARTESIAN_POINT ( 'NONE',  ( 38.58424406990785371, 122.9651871740939981, 32.77220824515697473 ) ) ;
#16281=EDGE_CURVE ( 'NONE', #14006, #12910, #19932, .T. ) ;
#16283=CARTESIAN_POINT ( 'NONE',  ( 43.80332655382218832, 139.5373810949689926, 39.21067981925355639 ) ) ;
#16284=CARTESIAN_POINT ( 'NONE',  ( 43.01140435219951996, 10.71049967264875491, 59.21067981925356349 ) ) ;
#16289=CARTESIAN_POINT ( 'NONE',  ( 44.55648932407425633, 84.68445800887256780, 38.96596240072933170 ) ) ;
#16290=CYLINDRICAL_SURFACE ( 'NONE', #14745, 4.999999999999997335 ) ;
#16292=CARTESIAN_POINT ( 'NONE',  ( 44.55648932407425633, 145.6104996726487570, 38.96596240072933170 ) ) ;
#16293=CARTESIAN_POINT ( 'NONE',  ( 45.74753988029933538, 101.0651871740939924, 30.44471234641811819 ) ) ;
#16296=CARTESIAN_POINT ( 'NONE',  ( 48.01140435219951996, 65.21049967264873715, 34.21067981925357060 ) ) ;
#16299=CARTESIAN_POINT ( 'NONE',  ( 46.10157429594899270, 78.83445800887255928, 38.46393386101375711 ) ) ;
#16301=CARTESIAN_POINT ( 'NONE',  ( 43.01140435219951286, 60.86518717409400381, 38.86567161673127657 ) ) ;
#16303=FACE_OUTER_BOUND ( 'NONE', #11169, .T. ) ;
#16307=CARTESIAN_POINT ( 'NONE',  ( 43.01140435219951286, 69.86518717409400381, 38.86567161673127657 ) ) ;
#16311=CARTESIAN_POINT ( 'NONE',  ( 40.27526882409969033, 138.5651871740939498, 37.97664729208901946 ) ) ;
#16315=ORIENTED_EDGE ( 'NONE', *, *, #20810, .T. ) ;
#16317=VERTEX_POINT ( 'NONE', #8137 ) ;
#16318=CYLINDRICAL_SURFACE ( 'NONE', #7640, 4.999999999999997335 ) ;
#16319=CARTESIAN_POINT ( 'NONE',  ( 44.37947211624943833, 74.47977050742731819, 30.00020018409699318 ) ) ;
#16320=CARTESIAN_POINT ( 'NONE',  ( 45.74753988029933538, 137.0651871740940067, 30.44471234641811819 ) ) ;
#16322=CARTESIAN_POINT ( 'NONE',  ( 41.46631938032478359, 87.11049967264874283, 29.45539723777780239 ) ) ;
#16326=CARTESIAN_POINT ( 'NONE',  ( 43.01140435219951286, 92.36518717409398960, 29.55568802177586463 ) ) ;
#16327=CARTESIAN_POINT ( 'NONE',  ( 47.05648932407426344, 107.5104996726487485, 31.27175355779120025 ) ) ;
#16331=CARTESIAN_POINT ( 'NONE',  ( 47.43856463449118621, 76.87977050742732388, 34.21067981925357060 ) ) ;
#16337=CARTESIAN_POINT ( 'NONE',  ( 38.58424406990784661, 158.9651871740940123, 32.77220824515698183 ) ) ;
#16340=CARTESIAN_POINT ( 'NONE',  ( 39.42975644700377558, 123.0797705074273267, 31.60846029578754468 ) ) ;
#16342=CARTESIAN_POINT ( 'NONE',  ( 43.80332655382221674, 130.9575765865523067, 29.21067981925357060 ) ) ;
#16344=ORIENTED_EDGE ( 'NONE', *, *, #13885, .T. ) ;
#16345=CARTESIAN_POINT ( 'NONE',  ( 40.27526882409969033, 123.8297705074273125, 37.97664729208901946 ) ) ;
#16347=CARTESIAN_POINT ( 'NONE',  ( 39.92123440845004723, 63.23445800887258628, 38.46393386101376421 ) ) ;
#16353=CARTESIAN_POINT ( 'NONE',  ( 38.01140435219952707, 102.8604996726487286, 35.83527830041809636 ) ) ;
#16356=CARTESIAN_POINT ( 'NONE',  ( 39.92123440845004723, 126.2344580088725934, 38.46393386101376421 ) ) ;
#16357=CARTESIAN_POINT ( 'NONE',  ( 38.58424406990784661, 99.52977050742728693, 35.64915139335016647 ) ) ;
#16360=CARTESIAN_POINT ( 'NONE',  ( 41.64333658814960870, 90.71518717409401233, 38.42115945441014446 ) ) ;
#16361=CYLINDRICAL_SURFACE ( 'NONE', #9440, 4.999999999999997335 ) ;
#16363=CARTESIAN_POINT ( 'NONE',  ( 43.01140435219951286, 128.9604996726487229, 29.21067981925356705 ) ) ;
#16365=CARTESIAN_POINT ( 'NONE',  ( 38.58424406990785371, 144.5297705074273154, 35.64915139335015937 ) ) ;
#16367=CARTESIAN_POINT ( 'NONE',  ( 47.43856463449117911, 67.72977050742733240, 35.64915139335015937 ) ) ;
#16370=CARTESIAN_POINT ( 'NONE',  ( 47.43856463449117200, 154.7297705074273040, 35.64915139335016647 ) ) ;
#16373=CARTESIAN_POINT ( 'NONE',  ( 46.10157429594899270, 107.6604996726487116, 29.95742577749337343 ) ) ;
#16374=CARTESIAN_POINT ( 'NONE',  ( 39.42975644700377558, 69.41518717409400097, 36.81289934271958941 ) ) ;
#16377=CARTESIAN_POINT ( 'NONE',  ( 38.01140435219952707, 155.6344580088725706, 32.58608133808903773 ) ) ;
#16380=CARTESIAN_POINT ( 'NONE',  ( 47.05648932407426344, 154.5844580088725877, 31.27175355779120025 ) ) ;
#16381=CARTESIAN_POINT ( 'NONE',  ( 41.64333658814960870, 129.9797705074273040, 38.42115945441014446 ) ) ;
#16383=CARTESIAN_POINT ( 'NONE',  ( 38.58424406990786082, 126.1151871740940038, 34.21067981925357060 ) ) ;
#16385=CARTESIAN_POINT ( 'NONE',  ( 41.46631938032478359, 151.3104996726487457, 38.96596240072933170 ) ) ;
#16386=CARTESIAN_POINT ( 'NONE',  ( 46.10157429594899270, 64.76049967264873430, 38.46393386101375711 ) ) ;
#16387=CARTESIAN_POINT ( 'NONE',  ( 48.01140435219951996, 149.2104996726487514, 34.21067981925357060 ) ) ;
#16389=VECTOR ( 'NONE', #1708, 1000.000000000000000 ) ;
#16390=LINE ( 'NONE', #21482, #18498 ) ;
#16395=CARTESIAN_POINT ( 'NONE',  ( 44.55648932407425633, 78.68445800887258201, 38.96596240072933170 ) ) ;
#16398=CARTESIAN_POINT ( 'NONE',  ( 48.01140435219951996, 140.3604996726487002, 32.58608133808903773 ) ) ;
#16399=CARTESIAN_POINT ( 'NONE',  ( 38.58424406990786082, 93.11518717409400381, 34.21067981925357060 ) ) ;
#16406=CARTESIAN_POINT ( 'NONE',  ( 39.92123440845005433, 105.2604996726487485, 29.95742577749336988 ) ) ;
#16409=CARTESIAN_POINT ( 'NONE',  ( 43.80332655382220253, 145.5373810949689926, 39.21067981925355639 ) ) ;
#16411=CARTESIAN_POINT ( 'NONE',  ( 46.59305225739526435, 61.31518717409399954, 36.81289934271958941 ) ) ;
#16416=CARTESIAN_POINT ( 'NONE',  ( 45.74753988029934249, 74.06518717409399244, 30.44471234641812174 ) ) ;
#16419=SURFACE_SIDE_STYLE ('',( #3095 ) ) ;
#16420=CARTESIAN_POINT ( 'NONE',  ( 43.01140435219951286, 135.8651871740940180, 38.86567161673127657 ) ) ;
#16426=CARTESIAN_POINT ( 'NONE',  ( 48.01140435219951996, 116.0604996726487599, 35.83527830041809636 ) ) ;
#16427=CARTESIAN_POINT ( 'NONE',  ( 40.27526882409969033, 71.92977050742729261, 30.44471234641811819 ) ) ;
#16428=CARTESIAN_POINT ( 'NONE',  ( 44.37947211624943833, 130.0151871740939953, 38.42115945441014446 ) ) ;
#16430=CARTESIAN_POINT ( 'NONE',  ( 46.10157429594899270, 91.76049967264873430, 38.46393386101376421 ) ) ;
#16434=CARTESIAN_POINT ( 'NONE',  ( 40.27526882409969033, 92.66518717409398675, 30.44471234641811819 ) ) ;
#16439=CARTESIAN_POINT ( 'NONE',  ( 39.42975644700377558, 78.67977050742732104, 36.81289934271958941 ) ) ;
#16445=ADVANCED_FACE ( 'NONE', ( #20348 ), #17129, .T. ) ;
#16447=CARTESIAN_POINT ( 'NONE',  ( 44.37947211624943833, 128.4797705074273040, 30.00020018409699318 ) ) ;
#16449=CARTESIAN_POINT ( 'NONE',  ( 48.01140435219951996, 130.1344580088725422, 35.83527830041809636 ) ) ;
#16451=CIRCLE ( 'NONE', #1682, 24.99999999999998934 ) ;
#16452=CARTESIAN_POINT ( 'NONE',  ( 43.01140435219954838, 132.5344580088725763, 39.21067981925356349 ) ) ;
#16453=CARTESIAN_POINT ( 'NONE',  ( 38.58424406990786082, 90.37977050742732388, 34.21067981925357060 ) ) ;
#16454=CARTESIAN_POINT ( 'NONE',  ( 45.51146558786459195, 58.78519036379218221, 29.88058815533641166 ) ) ;
#16459=CARTESIAN_POINT ( 'NONE',  ( 42.21948215057684450, 89.11133943119283174, 29.21067981925356705 ) ) ;
#16463=CARTESIAN_POINT ( 'NONE',  ( 38.01140435219952707, 119.7844580088725763, 34.21067981925357060 ) ) ;
#16464=CARTESIAN_POINT ( 'NONE',  ( 39.42975644700377558, 105.0797705074273125, 31.60846029578754468 ) ) ;
#16467=CARTESIAN_POINT ( 'NONE',  ( 46.59305225739526435, 85.31518717409400665, 36.81289934271958941 ) ) ;
#16468=CYLINDRICAL_SURFACE ( 'NONE', #16038, 4.999999999999997335 ) ;
#16470=DIRECTION ( 'NONE',  ( 0.000000000000000000, 1.000000000000000000, 0.000000000000000000 ) ) ;
#16473=CARTESIAN_POINT ( 'NONE',  ( 41.64333658814960870, 62.77977050742732246, 30.00020018409699318 ) ) ;
#16474=ORIENTED_EDGE ( 'NONE', *, *, #11473, .F. ) ;
#16475=ORIENTED_EDGE ( 'NONE', *, *, #2604, .T. ) ;
#16476=CARTESIAN_POINT ( 'NONE',  ( 39.42975644700377558, 144.0797705074273267, 31.60846029578754468 ) ) ;
#16480=CARTESIAN_POINT ( 'NONE',  ( 46.10157429594899270, 110.6604996726487400, 29.95742577749337343 ) ) ;
#16481=CARTESIAN_POINT ( 'NONE',  ( 47.43856463449117200, 70.46518717409401233, 35.64915139335016647 ) ) ;
#16486=CARTESIAN_POINT ( 'NONE',  ( 47.05648932407426344, 151.5844580088725877, 31.27175355779120025 ) ) ;
#16487=CARTESIAN_POINT ( 'NONE',  ( 38.58424406990784661, 132.5297705074272869, 35.64915139335016647 ) ) ;
#16489=CARTESIAN_POINT ( 'NONE',  ( 46.59305225739526435, 115.3151871740940067, 36.81289934271958941 ) ) ;
#16492=CARTESIAN_POINT ( 'NONE',  ( 46.10157429594899270, 140.6604996726487116, 29.95742577749336988 ) ) ;
#16495=CARTESIAN_POINT ( 'NONE',  ( 43.01140435219951286, 119.9604996726487229, 29.21067981925356705 ) ) ;
#16498=CARTESIAN_POINT ( 'NONE',  ( 44.37947211624943833, 91.27977050742731535, 38.42115945441014446 ) ) ;
#16499=ORIENTED_EDGE ( 'NONE', *, *, #3722, .T. ) ;
#16502=CARTESIAN_POINT ( 'NONE',  ( 38.01140435219951996, 86.93445800887258201, 35.83527830041810347 ) ) ;
#16504=CARTESIAN_POINT ( 'NONE',  ( 46.10157429594899270, 137.6604996726487116, 29.95742577749337343 ) ) ;
#16505=CARTESIAN_POINT ( 'NONE',  ( 43.01140435219951286, 98.36518717409401802, 29.55568802177586463 ) ) ;
#16515=CARTESIAN_POINT ( 'NONE',  ( 38.58424406990784661, 159.2297705074272756, 32.77220824515698183 ) ) ;
#16516=CARTESIAN_POINT ( 'NONE',  ( 44.55648932407425633, 157.6104996726487570, 38.96596240072933170 ) ) ;
#16518=CARTESIAN_POINT ( 'NONE',  ( 44.37947211624943833, 148.0151871740940237, 38.42115945441014446 ) ) ;
#16522=CARTESIAN_POINT ( 'NONE',  ( 47.43856463449118621, 73.61518717409400381, 34.21067981925357060 ) ) ;
#16525=CARTESIAN_POINT ( 'NONE',  ( 44.37947211624943833, 121.0151871740940095, 38.42115945441014446 ) ) ;
#16526=ADVANCED_FACE ( 'NONE', ( #18690 ), #492, .T. ) ;
#16529=ORIENTED_EDGE ( 'NONE', *, *, #2728, .F. ) ;
#16530=VERTEX_POINT ( 'NONE', #18899 ) ;
#16532=CARTESIAN_POINT ( 'NONE',  ( 38.01140435219952707, 113.7844580088725763, 34.21067981925357060 ) ) ;
#16534=CARTESIAN_POINT ( 'NONE',  ( 43.01140435219951286, 107.0344580088725905, 28.95336869806222779 ) ) ;
#16536=CARTESIAN_POINT ( 'NONE',  ( 38.58424406990784661, 69.52977050742730114, 35.64915139335016647 ) ) ;
#16537=CARTESIAN_POINT ( 'NONE',  ( 38.58424406990784661, 126.2651871740940237, 35.64915139335016647 ) ) ;
#16539=CARTESIAN_POINT ( 'NONE',  ( 48.01140435219951996, 80.21049967264875136, 34.21067981925357060 ) ) ;
#16541=CARTESIAN_POINT ( 'NONE',  ( 43.01140435219951286, 145.4604996726487229, 39.21067981925356349 ) ) ;
#16543=CARTESIAN_POINT ( 'NONE',  ( 47.43856463449118621, 91.61518717409400381, 34.21067981925357060 ) ) ;
#16544=CARTESIAN_POINT ( 'NONE',  ( 43.80332655382220253, 150.6113394311928460, 39.21067981925355639 ) ) ;
#16545=CYLINDRICAL_SURFACE ( 'NONE', #21183, 4.999999999999997335 ) ;
#16548=CARTESIAN_POINT ( 'NONE',  ( 45.74753988029933538, 62.32977050742730540, 30.44471234641811819 ) ) ;
#16554=CARTESIAN_POINT ( 'NONE',  ( 39.42975644700377558, 156.4151871740940010, 36.81289934271958941 ) ) ;
#16555=DIRECTION ( 'NONE',  ( 0.000000000000000000, 1.000000000000000000, 0.000000000000000000 ) ) ;
#16556=CARTESIAN_POINT ( 'NONE',  ( 44.37947211624943833, 113.4797705074273324, 30.00020018409699318 ) ) ;
#16560=CARTESIAN_POINT ( 'NONE',  ( 47.43856463449117200, 115.7297705074273324, 35.64915139335016647 ) ) ;
#16562=CARTESIAN_POINT ( 'NONE',  ( 45.05632365893699642, 58.83593307231945602, 29.61780325802818226 ) ) ;
#16564=CARTESIAN_POINT ( 'NONE',  ( 41.46631938032478359, 83.18445800887258201, 29.45539723777780239 ) ) ;
#16567=CARTESIAN_POINT ( 'NONE',  ( 39.92123440845005433, 157.1604996726487400, 38.46393386101375711 ) ) ;
#16568=CARTESIAN_POINT ( 'NONE',  ( 48.01140435219951996, 94.13445800887258486, 35.83527830041809636 ) ) ;
#16571=CARTESIAN_POINT ( 'NONE',  ( 47.05648932407426344, 127.5844580088725877, 31.27175355779120025 ) ) ;
#16572=CARTESIAN_POINT ( 'NONE',  ( 39.42975644700377558, 93.07977050742731251, 31.60846029578754468 ) ) ;
#16575=CARTESIAN_POINT ( 'NONE',  ( 44.37947211624943833, 88.01518717409399528, 38.42115945441014446 ) ) ;
#16576=CARTESIAN_POINT ( 'NONE',  ( 38.96631938032478359, 85.01049967264874851, 37.14960608071593384 ) ) ;
#16578=CYLINDRICAL_SURFACE ( 'NONE', #17158, 4.999999999999997335 ) ;
#16581=CARTESIAN_POINT ( 'NONE',  ( 40.27526882409969033, 104.6651871740939868, 30.44471234641811819 ) ) ;
#16582=ADVANCED_FACE ( 'NONE', ( #8664 ), #11959, .T. ) ;
#16583=CARTESIAN_POINT ( 'NONE',  ( 40.27526882409969744, 68.92977050742732104, 30.44471234641812174 ) ) ;
#16585=CARTESIAN_POINT ( 'NONE',  ( 43.01140435219951286, 143.6297705074272812, 29.55568802177586463 ) ) ;
#16587=CARTESIAN_POINT ( 'NONE',  ( 39.42975644700377558, 99.07977050742732672, 31.60846029578754468 ) ) ;
#16590=CARTESIAN_POINT ( 'NONE',  ( 41.46631938032478359, 106.3104996726487457, 38.96596240072933170 ) ) ;
#16591=CARTESIAN_POINT ( 'NONE',  ( 47.43856463449118621, 70.61518717409400381, 34.21067981925357060 ) ) ;
#16599=CARTESIAN_POINT ( 'NONE',  ( 38.01140435219951996, 152.9344580088725536, 35.83527830041810347 ) ) ;
#16600=CARTESIAN_POINT ( 'NONE',  ( 45.74753988029933538, 133.4297705074273210, 37.97664729208901946 ) ) ;
#16603=CARTESIAN_POINT ( 'NONE',  ( 47.43856463449117911, 118.7651871740940237, 32.77220824515697473 ) ) ;
#16607=CARTESIAN_POINT ( 'NONE',  ( 43.80332655382220253, 65.88361825032846752, 29.21067981925356705 ) ) ;
#16613=CARTESIAN_POINT ( 'NONE',  ( 47.43856463449117911, 94.72977050742733240, 35.64915139335015937 ) ) ;
#16617=CARTESIAN_POINT ( 'NONE',  ( 48.01140435219951996, 85.13445800887258486, 35.83527830041810347 ) ) ;
#16620=CARTESIAN_POINT ( 'NONE',  ( 38.96631938032478359, 135.4104996726487400, 31.27175355779120025 ) ) ;
#16621=CARTESIAN_POINT ( 'NONE',  ( 38.58424406990784661, 98.96518717409398391, 32.77220824515698183 ) ) ;
#16623=DIRECTION ( 'NONE',  ( 0.000000000000000000, 1.000000000000000000, 0.000000000000000000 ) ) ;
#16629=CARTESIAN_POINT ( 'NONE',  ( 39.92123440845005433, 148.1604996726487400, 38.46393386101375711 ) ) ;
#16630=CARTESIAN_POINT ( 'NONE',  ( 47.05648932407426344, 145.9104996726487400, 37.14960608071593384 ) ) ;
#16631=CARTESIAN_POINT ( 'NONE',  ( 39.42975644700377558, 62.81518717409399954, 31.60846029578754468 ) ) ;
#16632=LINE ( 'NONE', #8384, #12593 ) ;
#16634=CARTESIAN_POINT ( 'NONE',  ( 41.64333658814960870, 149.5151871740940237, 30.00020018409699318 ) ) ;
#16637=ADVANCED_FACE ( 'NONE', ( #20453 ), #3592, .T. ) ;
#16638=ORIENTED_EDGE ( 'NONE', *, *, #13631, .T. ) ;
#16639=CARTESIAN_POINT ( 'NONE',  ( 43.01140435219951286, 77.03445800887257633, 29.21067981925356705 ) ) ;
#16642=CARTESIAN_POINT ( 'NONE',  ( 48.01140435219951996, 112.4344580088725536, 32.58608133808903773 ) ) ;
#16643=CARTESIAN_POINT ( 'NONE',  ( 44.37947211624943833, 122.2151871740940123, 30.00020018409699318 ) ) ;
#16649=CARTESIAN_POINT ( 'NONE',  ( 44.37947211624943833, 157.2797705074273438, 38.42115945441014446 ) ) ;
#16650=CARTESIAN_POINT ( 'NONE',  ( 44.37947211624943833, 64.27977050742731535, 38.42115945441014446 ) ) ;
#16651=CARTESIAN_POINT ( 'NONE',  ( 43.01140435219951286, 123.8651871740939896, 38.86567161673127657 ) ) ;
#16653=CARTESIAN_POINT ( 'NONE',  ( 38.01140435219951996, 84.56049967264871725, 32.58608133808903773 ) ) ;
#16655=EDGE_CURVE ( 'NONE', #16987, #6094, #1089, .T. ) ;
#16657=CARTESIAN_POINT ( 'NONE',  ( 38.96631938032478359, 138.4104996726487400, 31.27175355779120025 ) ) ;
#16658=CARTESIAN_POINT ( 'NONE',  ( 40.27526882409969033, 86.66518717409400097, 30.44471234641811819 ) ) ;
#16659=CARTESIAN_POINT ( 'NONE',  ( 38.01140435219952707, 81.71049967264873715, 34.21067981925357060 ) ) ;
#16660=CARTESIAN_POINT ( 'NONE',  ( 42.21948215057684450, 133.3836182503284533, 39.21067981925356349 ) ) ;
#16662=CARTESIAN_POINT ( 'NONE',  ( 45.74753988029933538, 68.32977050742731251, 30.44471234641811819 ) ) ;
#16663=( BOUNDED_CURVE ( )  B_SPLINE_CURVE ( 2, ( #19185, #14321, #21063, #10813, #17516, #12674, #2425, #19394, #4291, #11018, #17729, #2634, #16080 ),
 .UNSPECIFIED., .F., .T. ) 
 B_SPLINE_CURVE_WITH_KNOTS ( ( 3, 2, 2, 2, 2, 2, 3 ),
 ( 0.9485294117647058432, 0.9499999999999999556, 0.9529411764705881804, 0.9558823529411765163, 0.9588235294117647411, 0.9617647058823529660, 0.9632352941176470784 ),
 .UNSPECIFIED. ) 
 CURVE ( )  GEOMETRIC_REPRESENTATION_ITEM ( )  RATIONAL_B_SPLINE_CURVE ( ( 0.9755282581475768211, 0.9755282581475768211, 1.000000000000000000, 0.9510565162951535312, 1.000000000000000000, 0.9510565162951535312, 1.000000000000000000, 0.9510565162951535312, 1.000000000000000000, 0.9510565162951535312, 1.000000000000000000, 0.9755282581475768211, 0.9755282581475768211 ) ) 
 REPRESENTATION_ITEM ( '' )  );
#16667=ORIENTED_EDGE ( 'NONE', *, *, #9958, .T. ) ;
#16668=CARTESIAN_POINT ( 'NONE',  ( 43.01140435219951286, 149.3651871740939612, 29.55568802177586463 ) ) ;
#16670=CARTESIAN_POINT ( 'NONE',  ( 47.43856463449117911, 113.0297705074273154, 32.77220824515697473 ) ) ;
#16674=VERTEX_POINT ( 'NONE', #8880 ) ;
#16675=CARTESIAN_POINT ( 'NONE',  ( 38.58424406990784661, 114.2297705074273040, 32.77220824515698183 ) ) ;
#16677=CARTESIAN_POINT ( 'NONE',  ( 44.37947211624943833, 151.0151871740940237, 38.42115945441014446 ) ) ;
#16686=CARTESIAN_POINT ( 'NONE',  ( 43.80332655382220253, 77.88361825032845331, 29.21067981925356705 ) ) ;
#16688=CARTESIAN_POINT ( 'NONE',  ( 45.74753988029933538, 92.32977050742731251, 30.44471234641811819 ) ) ;
#16691=AXIS2_PLACEMENT_3D ( 'NONE', #14619, #12757, #17493 ) ;
#16693=CARTESIAN_POINT ( 'NONE',  ( 38.01140435219952707, 84.71049967264873715, 34.21067981925357060 ) ) ;
#16697=CARTESIAN_POINT ( 'NONE',  ( 47.43856463449117911, 139.7297705074273324, 35.64915139335015937 ) ) ;
#16700=CARTESIAN_POINT ( 'NONE',  ( 38.58424406990785371, 60.52977050742731535, 35.64915139335015937 ) ) ;
#16702=CARTESIAN_POINT ( 'NONE',  ( 41.64333658814960870, 146.7797705074273154, 30.00020018409699318 ) ) ;
#16703=CARTESIAN_POINT ( 'NONE',  ( 43.01140435219951996, 10.71049967264875491, 29.21067981925357060 ) ) ;
#16705=CARTESIAN_POINT ( 'NONE',  ( 48.01140435219951996, 110.3604996726487570, 32.58608133808903773 ) ) ;
#16706=CARTESIAN_POINT ( 'NONE',  ( 41.64333658814960870, 66.71518717409399812, 38.42115945441014446 ) ) ;
#16709=CARTESIAN_POINT ( 'NONE',  ( 39.92123440845005433, 155.3344580088726161, 29.95742577749336988 ) ) ;
#16711=CARTESIAN_POINT ( 'NONE',  ( 43.01140435219951286, 112.4604996726487514, 39.21067981925356349 ) ) ;
#16712=CARTESIAN_POINT ( 'NONE',  ( 46.10157429594899270, 150.8344580088725593, 38.46393386101376421 ) ) ;
#16713=CARTESIAN_POINT ( 'NONE',  ( 46.59305225739526435, 127.5797705074273267, 36.81289934271958941 ) ) ;
#16715=LINE ( 'NONE', #11023, #9946 ) ;
#16716=CARTESIAN_POINT ( 'NONE',  ( 47.43856463449118621, 112.6151871740939896, 34.21067981925357060 ) ) ;
#16718=CARTESIAN_POINT ( 'NONE',  ( 41.46631938032478359, 126.3844580088725706, 38.96596240072933170 ) ) ;
#16721=CARTESIAN_POINT ( 'NONE',  ( 39.42975644700377558, 99.67977050742732104, 36.81289934271958941 ) ) ;
#16722=( BOUNDED_CURVE ( )  B_SPLINE_CURVE ( 2, ( #16541, #6530, #14891, #4871, #19986, #18541, #10172, #9841, #18319, #3220, #6652, #1568, #15003 ),
 .UNSPECIFIED., .F., .F. ) 
 B_SPLINE_CURVE_WITH_KNOTS ( ( 3, 2, 2, 2, 2, 2, 3 ),
 ( 0.1397058823529411797, 0.1411764705882352922, 0.1441176470588235170, 0.1470588235294117696, 0.1499999999999999944, 0.1529411764705882470, 0.1544117647058823595 ),
 .UNSPECIFIED. ) 
 CURVE ( )  GEOMETRIC_REPRESENTATION_ITEM ( )  RATIONAL_B_SPLINE_CURVE ( ( 0.9755282581475768211, 0.9755282581475768211, 1.000000000000000000, 0.9510565162951535312, 1.000000000000000000, 0.9510565162951535312, 1.000000000000000000, 0.9510565162951535312, 1.000000000000000000, 0.9510565162951535312, 1.000000000000000000, 0.9755282581475768211, 0.9755282581475768211 ) ) 
 REPRESENTATION_ITEM ( '' )  );
#16727=CARTESIAN_POINT ( 'NONE',  ( 48.01140435219951996, 82.28445800887257633, 34.21067981925357060 ) ) ;
#16729=CARTESIAN_POINT ( 'NONE',  ( 46.10157429594899270, 143.6604996726487400, 29.95742577749337343 ) ) ;
#16730=CARTESIAN_POINT ( 'NONE',  ( 44.37947211624943833, 95.21518717409399812, 30.00020018409699318 ) ) ;
#16732=EDGE_CURVE ( 'NONE', #11079, #1056, #7875, .T. ) ;
#16739=CARTESIAN_POINT ( 'NONE',  ( 38.96631938032478359, 78.41049967264873999, 31.27175355779120025 ) ) ;
#16740=CARTESIAN_POINT ( 'NONE',  ( 45.74753988029933538, 155.3297705074273267, 30.44471234641811819 ) ) ;
#16743=CARTESIAN_POINT ( 'NONE',  ( 38.58424406990785371, 140.9651871740939839, 32.77220824515697473 ) ) ;
#16747=ORIENTED_EDGE ( 'NONE', *, *, #15515, .T. ) ;
#16752=CARTESIAN_POINT ( 'NONE',  ( 39.42975644700377558, 128.8151871740940067, 31.60846029578754468 ) ) ;
#16755=CARTESIAN_POINT ( 'NONE',  ( 38.01140435219952707, 146.9344580088725820, 35.83527830041809636 ) ) ;
#16757=CARTESIAN_POINT ( 'NONE',  ( 44.55648932407425633, 108.6844580088725820, 38.96596240072933170 ) ) ;
#16758=CARTESIAN_POINT ( 'NONE',  ( 45.74753988029934249, 158.3297705074273267, 30.44471234641812174 ) ) ;
#16760=CARTESIAN_POINT ( 'NONE',  ( 46.59305225739526435, 67.57977050742732672, 36.81289934271958941 ) ) ;
#16761=CARTESIAN_POINT ( 'NONE',  ( 39.42975644700377558, 126.4151871740940010, 36.81289934271958941 ) ) ;
#16763=CIRCLE ( 'NONE', #4805, 4.999999999999997335 ) ;
#16765=CARTESIAN_POINT ( 'NONE',  ( 41.46631938032478359, 78.11049967264874283, 29.45539723777780239 ) ) ;
#16768=CARTESIAN_POINT ( 'NONE',  ( 42.21948215057684450, 138.0373810949690210, 29.21067981925356705 ) ) ;
#16769=CARTESIAN_POINT ( 'NONE',  ( 44.37947211624943833, 89.21518717409399812, 30.00020018409699318 ) ) ;
#16770=CARTESIAN_POINT ( 'NONE',  ( 41.46631938032478359, 82.31049967264873146, 38.96596240072933170 ) ) ;
#16773=CARTESIAN_POINT ( 'NONE',  ( 43.01140435219951286, 65.62977050742730967, 29.55568802177586463 ) ) ;
#16780=CARTESIAN_POINT ( 'NONE',  ( 46.59305225739526435, 151.9151871740940010, 31.60846029578754468 ) ) ;
#16782=CARTESIAN_POINT ( 'NONE',  ( 38.58424406990785371, 111.2297705074273324, 32.77220824515697473 ) ) ;
#16785=EDGE_CURVE ( 'NONE', #14880, #310, #3082, .T. ) ;
#16788=CARTESIAN_POINT ( 'NONE',  ( 42.21948215057684450, 128.1113394311928175, 29.21067981925356705 ) ) ;
#16789=CARTESIAN_POINT ( 'NONE',  ( 38.58424406990786082, 159.1151871740940180, 34.21067981925357060 ) ) ;
#16797=CARTESIAN_POINT ( 'NONE',  ( 38.01140435219952707, 98.63445800887257064, 32.58608133808903773 ) ) ;
#16798=CARTESIAN_POINT ( 'NONE',  ( 41.64333658814960870, 90.97977050742731819, 38.42115945441014446 ) ) ;
#16801=CARTESIAN_POINT ( 'NONE',  ( 38.58424406990786082, 87.11518717409400381, 34.21067981925357060 ) ) ;
#16803=CARTESIAN_POINT ( 'NONE',  ( 43.01140435219951996, 10.71049967264875491, 34.21067981925357060 ) ) ;
#16805=CARTESIAN_POINT ( 'NONE',  ( 43.01140435219951996, 10.71049967264875491, 34.21067981925357060 ) ) ;
#16807=CARTESIAN_POINT ( 'NONE',  ( 43.01140435219951286, 143.6297705074272812, 29.55568802177586107 ) ) ;
#16809=EDGE_CURVE ( 'NONE', #7439, #5452, #7024, .T. ) ;
#16812=CARTESIAN_POINT ( 'NONE',  ( 39.42975644700377558, 147.0797705074273267, 31.60846029578754468 ) ) ;
#16813=CARTESIAN_POINT ( 'NONE',  ( 47.43856463449117200, 94.72977050742733240, 35.64915139335016647 ) ) ;
#16814=CARTESIAN_POINT ( 'NONE',  ( 38.01140435219952707, 141.8604996726487570, 35.83527830041809636 ) ) ;
#16815=CARTESIAN_POINT ( 'NONE',  ( 48.01140435219951996, 104.0604996726487457, 35.83527830041810347 ) ) ;
#16816=CARTESIAN_POINT ( 'NONE',  ( 38.58424406990786082, 60.11518717409400381, 34.21067981925357060 ) ) ;
#16821=FACE_OUTER_BOUND ( 'NONE', #3890, .T. ) ;
#16822=CARTESIAN_POINT ( 'NONE',  ( 39.92123440845004723, 140.3344580088726161, 29.95742577749337343 ) ) ;
#16823=CARTESIAN_POINT ( 'NONE',  ( 38.58424406990784661, 123.5297705074273438, 35.64915139335016647 ) ) ;
#16825=CARTESIAN_POINT ( 'NONE',  ( 47.05648932407426344, 99.98445800887257917, 37.14960608071593384 ) ) ;
#16826=CARTESIAN_POINT ( 'NONE',  ( 44.37947211624943833, 116.2151871740940123, 30.00020018409699318 ) ) ;
#16830=ADVANCED_FACE ( 'NONE', ( #17555 ), #813, .T. ) ;
#16833=CARTESIAN_POINT ( 'NONE',  ( 45.74753988029934249, 83.32977050742732672, 30.44471234641812174 ) ) ;
#16834=VERTEX_POINT ( 'NONE', #14362 ) ;
#16837=CARTESIAN_POINT ( 'NONE',  ( 38.96631938032478359, 72.08445800887257349, 37.14960608071593384 ) ) ;
#16838=CARTESIAN_POINT ( 'NONE',  ( 43.01140435219951996, 10.71049967264875491, 39.21067981925356349 ) ) ;
#16839=CARTESIAN_POINT ( 'NONE',  ( 48.01140435219951996, 137.2104996726487514, 34.21067981925357060 ) ) ;
#16840=CARTESIAN_POINT ( 'NONE',  ( 44.37947211624943833, 89.21518717409399812, 30.00020018409699318 ) ) ;
#16844=CARTESIAN_POINT ( 'NONE',  ( 38.01140435219952707, 93.71049967264875136, 34.21067981925357060 ) ) ;
#16845=CARTESIAN_POINT ( 'NONE',  ( 43.80332655382220253, 80.88361825032846752, 29.21067981925356705 ) ) ;
#16846=CARTESIAN_POINT ( 'NONE',  ( 44.37947211624943833, 151.2797705074273438, 38.42115945441014446 ) ) ;
#16849=CARTESIAN_POINT ( 'NONE',  ( 38.58424406990786082, 147.1151871740939896, 34.21067981925357060 ) ) ;
#16852=ORIENTED_EDGE ( 'NONE', *, *, #10434, .T. ) ;
#16853=CARTESIAN_POINT ( 'NONE',  ( 45.74753988029934249, 61.16518717409399386, 37.97664729208901235 ) ) ;
#16854=( BOUNDED_CURVE ( )  B_SPLINE_CURVE ( 2, ( #2238, #15888, #3682, #17541, #801, #14238, #5331, #17331, #10410, #17112, #7214, #2028, #5431 ),
 .UNSPECIFIED., .F., .F. ) 
 B_SPLINE_CURVE_WITH_KNOTS ( ( 3, 2, 2, 2, 2, 2, 3 ),
 ( 0.3897058823529411797, 0.3911764705882352922, 0.3941176470588235170, 0.3970588235294117418, 0.4000000000000000222, 0.4029411764705882470, 0.4044117647058823595 ),
 .UNSPECIFIED. ) 
 CURVE ( )  GEOMETRIC_REPRESENTATION_ITEM ( )  RATIONAL_B_SPLINE_CURVE ( ( 0.9755282581475768211, 0.9755282581475768211, 1.000000000000000000, 0.9510565162951535312, 1.000000000000000000, 0.9510565162951535312, 1.000000000000000000, 0.9510565162951535312, 1.000000000000000000, 0.9510565162951535312, 1.000000000000000000, 0.9755282581475768211, 0.9755282581475768211 ) ) 
 REPRESENTATION_ITEM ( '' )  );
#16857=CARTESIAN_POINT ( 'NONE',  ( 39.92123440845005433, 135.2344580088725365, 38.46393386101375711 ) ) ;
#16858=CARTESIAN_POINT ( 'NONE',  ( 39.42975644700377558, 123.4151871740940010, 36.81289934271958941 ) ) ;
#16862=ORIENTED_EDGE ( 'NONE', *, *, #6638, .F. ) ;
#16863=CARTESIAN_POINT ( 'NONE',  ( 44.55648932407425633, 100.8844580088725849, 29.45539723777780239 ) ) ;
#16865=CARTESIAN_POINT ( 'NONE',  ( 46.59305225739526435, 157.5797705074273267, 36.81289934271958941 ) ) ;
#16867=CARTESIAN_POINT ( 'NONE',  ( 41.64333658814960870, 63.97977050742731109, 38.42115945441014446 ) ) ;
#16868=CARTESIAN_POINT ( 'NONE',  ( 47.43856463449118621, 130.6151871740940180, 34.21067981925357060 ) ) ;
#16870=CARTESIAN_POINT ( 'NONE',  ( 47.05648932407426344, 85.91049967264873999, 37.14960608071593384 ) ) ;
#16874=CARTESIAN_POINT ( 'NONE',  ( 43.01140435219951286, 80.36518717409398960, 29.55568802177586463 ) ) ;
#16875=CARTESIAN_POINT ( 'NONE',  ( 43.01140435219951286, 80.96049967264873715, 29.21067981925356705 ) ) ;
#16879=CARTESIAN_POINT ( 'NONE',  ( 41.64333658814960870, 65.77977050742732956, 30.00020018409699318 ) ) ;
#16884=CARTESIAN_POINT ( 'NONE',  ( 46.59305225739526435, 148.9151871740940294, 31.60846029578754468 ) ) ;
#16888=CARTESIAN_POINT ( 'NONE',  ( 46.59305225739526435, 119.1797705074273068, 31.60846029578754468 ) ) ;
#16892=ORIENTED_EDGE ( 'NONE', *, *, #13309, .T. ) ;
#16893=CARTESIAN_POINT ( 'NONE',  ( 46.59305225739526435, 110.1797705074273210, 31.60846029578754468 ) ) ;
#16895=LINE ( 'NONE', #13590, #8692 ) ;
#16896=CARTESIAN_POINT ( 'NONE',  ( 47.43856463449117200, 154.4651871740940123, 35.64915139335016647 ) ) ;
#16900=CARTESIAN_POINT ( 'NONE',  ( 43.01140435219951286, 80.96049967264873715, 29.21067981925356705 ) ) ;
#16902=CARTESIAN_POINT ( 'NONE',  ( 43.80332655382220253, 101.8836182503284675, 29.21067981925356705 ) ) ;
#16904=CARTESIAN_POINT ( 'NONE',  ( 47.05648932407426344, 91.91049967264873999, 37.14960608071593384 ) ) ;
#16907=CARTESIAN_POINT ( 'NONE',  ( 41.64333658814960870, 96.97977050742731819, 38.42115945441014446 ) ) ;
#16910=CARTESIAN_POINT ( 'NONE',  ( 40.27526882409969744, 80.66518717409400097, 30.44471234641812174 ) ) ;
#16912=ORIENTED_EDGE ( 'NONE', *, *, #7465, .T. ) ;
#16918=CARTESIAN_POINT ( 'NONE',  ( 41.46631938032478359, 120.3844580088725849, 38.96596240072933170 ) ) ;
#16920=CARTESIAN_POINT ( 'NONE',  ( 38.58424406990786082, 147.3797705074273097, 34.21067981925357060 ) ) ;
#16921=CARTESIAN_POINT ( 'NONE',  ( 41.64333658814960870, 96.97977050742731819, 38.42115945441014446 ) ) ;
#16925=CARTESIAN_POINT ( 'NONE',  ( 43.01140435219951996, 10.71049967264875491, 29.21067981925357060 ) ) ;
#16928=CARTESIAN_POINT ( 'NONE',  ( 41.46631938032478359, 140.1844580088725820, 29.45539723777780239 ) ) ;
#16929=CARTESIAN_POINT ( 'NONE',  ( 44.37947211624943833, 121.2797705074273296, 38.42115945441014446 ) ) ;
#16931=CARTESIAN_POINT ( 'NONE',  ( 47.05648932407426344, 100.5844580088725877, 31.27175355779120025 ) ) ;
#16932=CARTESIAN_POINT ( 'NONE',  ( 45.74753988029934249, 118.1651871740939868, 37.97664729208901235 ) ) ;
#16937=CARTESIAN_POINT ( 'NONE',  ( 45.74753988029934249, 85.42977050742730682, 37.97664729208901235 ) ) ;
#16940=CARTESIAN_POINT ( 'NONE',  ( 48.01140435219951996, 70.43445800887258201, 32.58608133808903773 ) ) ;
#16942=CARTESIAN_POINT ( 'NONE',  ( 46.10157429594899270, 130.7604996726487343, 38.46393386101376421 ) ) ;
#16943=CARTESIAN_POINT ( 'NONE',  ( 39.42975644700377558, 86.81518717409400665, 31.60846029578754468 ) ) ;
#16948=CARTESIAN_POINT ( 'NONE',  ( 42.21948215057687293, 94.38361825032848174, 39.21067981925357060 ) ) ;
#16951=EDGE_CURVE ( 'NONE', #11189, #13667, #14688, .T. ) ;
#16953=CARTESIAN_POINT ( 'NONE',  ( 48.01140435219951996, 68.21049967264873715, 34.21067981925357060 ) ) ;
#16955=CARTESIAN_POINT ( 'NONE',  ( 45.74753988029933538, 148.4297705074273210, 37.97664729208901946 ) ) ;
#16956=CARTESIAN_POINT ( 'NONE',  ( 46.10157429594899270, 157.7604996726487343, 38.46393386101375711 ) ) ;
#16958=CARTESIAN_POINT ( 'NONE',  ( 40.27526882409969744, 144.5651871740940067, 37.97664729208901235 ) ) ;
#16961=CARTESIAN_POINT ( 'NONE',  ( 38.96631938032478359, 78.08445800887257349, 37.14960608071593384 ) ) ;
#16965=CARTESIAN_POINT ( 'NONE',  ( 40.27526882409969033, 125.6651871740939868, 30.44471234641811819 ) ) ;
#16969=CARTESIAN_POINT ( 'NONE',  ( 43.01140435219951286, 114.5344580088725621, 39.21067981925356349 ) ) ;
#16971=CARTESIAN_POINT ( 'NONE',  ( 46.10157429594899270, 103.7344580088725934, 29.95742577749337343 ) ) ;
#16972=CARTESIAN_POINT ( 'NONE',  ( 38.58424406990786082, 159.1151871740940180, 34.21067981925357060 ) ) ;
#16973=CARTESIAN_POINT ( 'NONE',  ( 38.01140435219951996, 159.5604996726487457, 32.58608133808903773 ) ) ;
#16974=CARTESIAN_POINT ( 'NONE',  ( 38.58424406990786082, 120.1151871740940038, 34.21067981925357060 ) ) ;
#16976=CARTESIAN_POINT ( 'NONE',  ( 38.01140435219951996, 81.86049967264874283, 35.83527830041810347 ) ) ;
#16977=CARTESIAN_POINT ( 'NONE',  ( 47.05648932407426344, 147.9844580088725934, 37.14960608071593384 ) ) ;
#16978=FACE_OUTER_BOUND ( 'NONE', #7337, .T. ) ;
#16981=CARTESIAN_POINT ( 'NONE',  ( 38.58424406990784661, 75.26518717409399528, 35.64915139335016647 ) ) ;
#16984=CARTESIAN_POINT ( 'NONE',  ( 43.01140435219951286, 123.5344580088725621, 39.46799094044489209 ) ) ;
#16987=VERTEX_POINT ( 'NONE', #3123 ) ;
#16992=CARTESIAN_POINT ( 'NONE',  ( 40.27526882409969033, 153.5651871740940067, 37.97664729208901946 ) ) ;
#16993=LINE ( 'NONE', #2119, #14476 ) ;
#16998=CARTESIAN_POINT ( 'NONE',  ( 47.43856463449117200, 113.0297705074273011, 32.77220824515698183 ) ) ;
#16999=FACE_OUTER_BOUND ( 'NONE', #4332, .T. ) ;
#17002=CARTESIAN_POINT ( 'NONE',  ( 38.58424406990784661, 147.2651871740939669, 35.64915139335016647 ) ) ;
#17009=CYLINDRICAL_SURFACE ( 'NONE', #21399, 4.999999999999997335 ) ;
#17012=CARTESIAN_POINT ( 'NONE',  ( 43.01140435219951996, 2.710499672648754466, 9.210679819253577705 ) ) ;
#17013=CARTESIAN_POINT ( 'NONE',  ( 40.27526882409969033, 96.82977050742731251, 37.97664729208901946 ) ) ;
#17016=CARTESIAN_POINT ( 'NONE',  ( 39.42975644700377558, 75.41518717409400097, 36.81289934271958941 ) ) ;
#17018=CYLINDRICAL_SURFACE ( 'NONE', #560, 4.999999999999997335 ) ;
#17021=CARTESIAN_POINT ( 'NONE',  ( 46.10157429594899270, 121.7604996726487343, 38.46393386101375711 ) ) ;
#17026=CARTESIAN_POINT ( 'NONE',  ( 43.01140435219951286, 137.6297705074273381, 29.55568802177586463 ) ) ;
#17028=CARTESIAN_POINT ( 'NONE',  ( 38.58424406990786082, 99.37977050742732388, 34.21067981925357060 ) ) ;
#17029=CARTESIAN_POINT ( 'NONE',  ( 46.10157429594899270, 151.7604996726487059, 38.46393386101375711 ) ) ;
#17033=CARTESIAN_POINT ( 'NONE',  ( 41.46631938032478359, 154.3104996726487457, 38.96596240072933170 ) ) ;
#17037=CARTESIAN_POINT ( 'NONE',  ( 39.92123440845004723, 144.2344580088725934, 38.46393386101376421 ) ) ;
#17038=CARTESIAN_POINT ( 'NONE',  ( 44.37947211624943833, 125.4797705074273182, 30.00020018409699318 ) ) ;
#17040=DIRECTION ( 'NONE',  ( -0.4999508154438193630, 0.000000000000000000, 0.8660537986390106635 ) ) ;
#17041=CARTESIAN_POINT ( 'NONE',  ( 38.58424406990785371, 104.9651871740940123, 32.77220824515697473 ) ) ;
#17046=CARTESIAN_POINT ( 'NONE',  ( 46.59305225739526435, 82.57977050742731251, 36.81289934271958941 ) ) ;
#17049=EDGE_CURVE ( 'NONE', #15871, #9910, #1359, .T. ) ;
#17050=CARTESIAN_POINT ( 'NONE',  ( 44.55648932407425633, 110.8104996726487457, 29.45539723777780239 ) ) ;
#17051=CARTESIAN_POINT ( 'NONE',  ( 39.92123440845004723, 77.33445800887257349, 29.95742577749337343 ) ) ;
#17052=CARTESIAN_POINT ( 'NONE',  ( 42.21948215057684450, 86.11133943119284595, 29.21067981925356705 ) ) ;
#17053=CARTESIAN_POINT ( 'NONE',  ( 47.05648932407426344, 128.5104996726487343, 31.27175355779120025 ) ) ;
#17054=CARTESIAN_POINT ( 'NONE',  ( 40.27526882409969033, 89.66518717409400097, 30.44471234641811819 ) ) ;
#17062=CARTESIAN_POINT ( 'NONE',  ( 40.27526882409969033, 150.8297705074273267, 37.97664729208901946 ) ) ;
#17063=CARTESIAN_POINT ( 'NONE',  ( 45.74753988029933538, 103.4297705074273210, 37.97664729208901946 ) ) ;
#17065=CARTESIAN_POINT ( 'NONE',  ( 38.58424406990785371, 132.2651871740939953, 35.64915139335015937 ) ) ;
#17068=CARTESIAN_POINT ( 'NONE',  ( 46.59305225739526435, 64.31518717409399244, 36.81289934271958941 ) ) ;
#17072=CARTESIAN_POINT ( 'NONE',  ( 43.01140435219951286, 111.8651871740939896, 38.86567161673127657 ) ) ;
#17073=VERTEX_POINT ( 'NONE', #1470 ) ;
#17078=CARTESIAN_POINT ( 'NONE',  ( 47.05648932407426344, 97.58445800887258770, 31.27175355779120025 ) ) ;
#17079=CARTESIAN_POINT ( 'NONE',  ( 47.43856463449117911, 154.7297705074273040, 35.64915139335015937 ) ) ;
#17080=CARTESIAN_POINT ( 'NONE',  ( 43.01140435219951286, 59.62977050742730967, 29.55568802177586463 ) ) ;
#17081=CARTESIAN_POINT ( 'NONE',  ( 40.27526882409969033, 111.5651871740939782, 37.97664729208901946 ) ) ;
#17083=CARTESIAN_POINT ( 'NONE',  ( 46.10157429594899270, 73.76049967264873430, 38.46393386101376421 ) ) ;
#17084=CARTESIAN_POINT ( 'NONE',  ( 38.01140435219952707, 10.71049967264875491, 34.21067981925357060 ) ) ;
#17085=CARTESIAN_POINT ( 'NONE',  ( 44.55648932407425633, 135.6844580088725820, 38.96596240072933170 ) ) ;
#17087=CARTESIAN_POINT ( 'NONE',  ( 41.46631938032478359, 124.3104996726487457, 38.96596240072933170 ) ) ;
#17089=CARTESIAN_POINT ( 'NONE',  ( 43.01140435219951286, 74.36518717409400381, 29.55568802177586463 ) ) ;
#17093=VERTEX_POINT ( 'NONE', #3234 ) ;
#17097=ORIENTED_EDGE ( 'NONE', *, *, #20616, .F. ) ;
#17098=CARTESIAN_POINT ( 'NONE',  ( 47.43856463449117200, 139.7651871740939953, 32.77220824515698183 ) ) ;
#17100=CARTESIAN_POINT ( 'NONE',  ( 41.64333658814960870, 105.9797705074273182, 38.42115945441014446 ) ) ;
#17102=VERTEX_POINT ( 'NONE', #9966 ) ;
#17105=VERTEX_POINT ( 'NONE', #8309 ) ;
#17106=CARTESIAN_POINT ( 'NONE',  ( 43.01140435219951286, 100.4604996726487371, 39.21067981925356349 ) ) ;
#17107=CARTESIAN_POINT ( 'NONE',  ( 43.01140435219957681, 96.53445800887259054, 39.21067981925356349 ) ) ;
#17108=CARTESIAN_POINT ( 'NONE',  ( 47.43856463449117200, 83.02977050742730114, 32.77220824515698183 ) ) ;
#17109=CARTESIAN_POINT ( 'NONE',  ( 44.37947211624943833, 148.0151871740940237, 38.42115945441014446 ) ) ;
#17110=( BOUNDED_CURVE ( )  B_SPLINE_CURVE ( 2, ( #5731, #12343, #13997, #9052, #15650, #5013, #10595, #11721, #20732, #18344, #15031, #3247, #18754 ),
 .UNSPECIFIED., .F., .F. ) 
 B_SPLINE_CURVE_WITH_KNOTS ( ( 3, 2, 2, 2, 2, 2, 3 ),
 ( 0.4926470588235293824, 0.4941176470588235503, 0.4970588235294117752, 0.5000000000000000000, 0.5029411764705882248, 0.5058823529411764497, 0.5073529411764705621 ),
 .UNSPECIFIED. ) 
 CURVE ( )  GEOMETRIC_REPRESENTATION_ITEM ( )  RATIONAL_B_SPLINE_CURVE ( ( 0.9755282581475768211, 0.9755282581475763770, 1.000000000000000000, 0.9510565162951535312, 1.000000000000000000, 0.9510565162951535312, 1.000000000000000000, 0.9510565162951535312, 1.000000000000000000, 0.9510565162951535312, 1.000000000000000000, 0.9755282581475768211, 0.9755282581475768211 ) ) 
 REPRESENTATION_ITEM ( '' )  );
#17112=CARTESIAN_POINT ( 'NONE',  ( 46.10157429594899270, 118.7604996726487201, 38.46393386101375711 ) ) ;
#17121=CARTESIAN_POINT ( 'NONE',  ( 47.43856463449118621, 88.87977050742732388, 34.21067981925357060 ) ) ;
#17124=CARTESIAN_POINT ( 'NONE',  ( 38.58424406990785371, 75.26518717409399528, 35.64915139335015937 ) ) ;
#17125=CARTESIAN_POINT ( 'NONE',  ( 43.01140435219951996, 10.71049967264875491, 39.21067981925356349 ) ) ;
#17127=VERTEX_POINT ( 'NONE', #19096 ) ;
#17129=CYLINDRICAL_SURFACE ( 'NONE', #11318, 4.999999999999997335 ) ;
#17131=EDGE_LOOP ( 'NONE', ( #15331, #1775, #8991, #9714 ) ) ;
#17132=CARTESIAN_POINT ( 'NONE',  ( 47.43856463449117911, 62.02977050742732246, 32.77220824515697473 ) ) ;
#17133=ORIENTED_EDGE ( 'NONE', *, *, #11208, .F. ) ;
#17135=CARTESIAN_POINT ( 'NONE',  ( 45.74753988029933538, 133.4297705074273210, 37.97664729208901946 ) ) ;
#17137=CARTESIAN_POINT ( 'NONE',  ( 38.58424406990784661, 62.96518717409399812, 32.77220824515698183 ) ) ;
#17140=CARTESIAN_POINT ( 'NONE',  ( 38.58424406990784661, 96.26518717409400949, 35.64915139335016647 ) ) ;
#17145=CARTESIAN_POINT ( 'NONE',  ( 43.80332655382221674, 109.9575765865523067, 29.21067981925357060 ) ) ;
#17146=CARTESIAN_POINT ( 'NONE',  ( 38.96631938032478359, 140.4844580088725650, 31.27175355779120025 ) ) ;
#17147=CARTESIAN_POINT ( 'NONE',  ( 44.37947211624943833, 122.4797705074273182, 30.00020018409699318 ) ) ;
#17150=CARTESIAN_POINT ( 'NONE',  ( 44.37947211624943833, 106.0151871740939953, 38.42115945441014446 ) ) ;
#17151=CARTESIAN_POINT ( 'NONE',  ( 39.92123440845005433, 126.2344580088725934, 38.46393386101375711 ) ) ;
#17155=ADVANCED_FACE ( 'NONE', ( #7197 ), #20745, .T. ) ;
#17156=CARTESIAN_POINT ( 'NONE',  ( 40.27526882409969744, 83.92977050742732104, 30.44471234641812174 ) ) ;
#17158=AXIS2_PLACEMENT_3D ( 'NONE', #14928, #8009, #11080 ) ;
#17159=CARTESIAN_POINT ( 'NONE',  ( 41.46631938032478359, 77.18445800887258201, 29.45539723777780239 ) ) ;
#17162=CARTESIAN_POINT ( 'NONE',  ( 38.01140435219952707, 129.7104996726487514, 34.21067981925357060 ) ) ;
#17163=CARTESIAN_POINT ( 'NONE',  ( 43.01140435219951286, 84.86518717409398960, 38.86567161673127657 ) ) ;
#17167=DIRECTION ( 'NONE',  ( 0.000000000000000000, 0.000000000000000000, 1.000000000000000000 ) ) ;
#17169=DIRECTION ( 'NONE',  ( 1.000000000000000000, 0.000000000000000000, 0.000000000000000000 ) ) ;
#17171=CARTESIAN_POINT ( 'NONE',  ( 43.01140435219954838, 110.0344580088725763, 29.21067981925356705 ) ) ;
#17172=CARTESIAN_POINT ( 'NONE',  ( 47.43856463449117200, 148.7297705074273324, 35.64915139335016647 ) ) ;
#17173=CARTESIAN_POINT ( 'NONE',  ( 44.37947211624943833, 101.4797705074273182, 30.00020018409699318 ) ) ;
#17175=CARTESIAN_POINT ( 'NONE',  ( 46.59305225739526435, 136.9151871740940010, 31.60846029578754468 ) ) ;
#17180=CARTESIAN_POINT ( 'NONE',  ( 43.01140435219951996, 10.71049967264875491, 39.21067981925356349 ) ) ;
#17181=CARTESIAN_POINT ( 'NONE',  ( 38.58424406990786082, 114.1151871740939896, 34.21067981925357060 ) ) ;
#17185=CARTESIAN_POINT ( 'NONE',  ( 38.01140435219952707, 101.7844580088725905, 34.21067981925357060 ) ) ;
#17186=CARTESIAN_POINT ( 'NONE',  ( 45.74753988029934249, 152.3297705074272983, 30.44471234641812174 ) ) ;
#17187=CARTESIAN_POINT ( 'NONE',  ( 47.43856463449117200, 61.72977050742730398, 35.64915139335016647 ) ) ;
#17188=CARTESIAN_POINT ( 'NONE',  ( 41.64333658814960870, 111.7151871740940123, 38.42115945441014446 ) ) ;
#17190=CARTESIAN_POINT ( 'NONE',  ( 38.01140435219951996, 69.56049967264873146, 32.58608133808903773 ) ) ;
#17192=CARTESIAN_POINT ( 'NONE',  ( 46.10157429594899270, 148.7344580088725934, 29.95742577749336988 ) ) ;
#17195=CYLINDRICAL_SURFACE ( 'NONE', #1295, 4.999999999999997335 ) ;
#17196=CARTESIAN_POINT ( 'NONE',  ( 39.42975644700377558, 81.41518717409400097, 36.81289934271958941 ) ) ;
#17197=CARTESIAN_POINT ( 'NONE',  ( 48.01140435219951996, 104.0604996726487457, 35.83527830041809636 ) ) ;
#17199=ORIENTED_EDGE ( 'NONE', *, *, #4945, .T. ) ;
#17202=CARTESIAN_POINT ( 'NONE',  ( 38.58424406990786082, 147.1151871740939896, 34.21067981925357060 ) ) ;
#17204=CARTESIAN_POINT ( 'NONE',  ( 41.64333658814960870, 108.9797705074273324, 38.42115945441014446 ) ) ;
#17211=CARTESIAN_POINT ( 'NONE',  ( 44.55648932407425633, 88.61049967264874283, 38.96596240072933170 ) ) ;
#17212=CARTESIAN_POINT ( 'NONE',  ( 38.58424406990786082, 84.37977050742730967, 34.21067981925357060 ) ) ;
#17213=CARTESIAN_POINT ( 'NONE',  ( 47.43856463449118621, 142.6151871740939896, 34.21067981925357060 ) ) ;
#17214=CARTESIAN_POINT ( 'NONE',  ( 41.46631938032478359, 99.11049967264872862, 29.45539723777780239 ) ) ;
#17216=CARTESIAN_POINT ( 'NONE',  ( 43.01140435219951286, 61.46049967264873715, 39.21067981925356349 ) ) ;
#17221=CARTESIAN_POINT ( 'NONE',  ( 43.01140435219951286, 65.03445800887257633, 29.21067981925356705 ) ) ;
#17224=CARTESIAN_POINT ( 'NONE',  ( 47.43856463449117200, 89.02977050742731535, 32.77220824515698183 ) ) ;
#17226=CARTESIAN_POINT ( 'NONE',  ( 38.58424406990786082, 78.11518717409400381, 34.21067981925357060 ) ) ;
#17230=CARTESIAN_POINT ( 'NONE',  ( 41.46631938032478359, 69.38445800887258486, 38.96596240072933170 ) ) ;
#17231=DIRECTION ( 'NONE',  ( 0.000000000000000000, 1.000000000000000000, 0.000000000000000000 ) ) ;
#17232=CARTESIAN_POINT ( 'NONE',  ( 47.43856463449117911, 133.7297705074273324, 35.64915139335015937 ) ) ;
#17236=( BOUNDED_CURVE ( )  B_SPLINE_CURVE ( 2, ( #388, #10956, #7117, #17343, #2250, #20562, #8985, #15691, #597, #17448, #2357, #9096, #15797 ),
 .UNSPECIFIED., .F., .F. ) 
 B_SPLINE_CURVE_WITH_KNOTS ( ( 3, 2, 2, 2, 2, 2, 3 ),
 ( 0.4044117647058823595, 0.4058823529411764719, 0.4088235294117646967, 0.4117647058823529216, 0.4147058823529412019, 0.4176470588235294268, 0.4191176470588235392 ),
 .UNSPECIFIED. ) 
 CURVE ( )  GEOMETRIC_REPRESENTATION_ITEM ( )  RATIONAL_B_SPLINE_CURVE ( ( 0.9755282581475768211, 0.9755282581475768211, 1.000000000000000000, 0.9510565162951535312, 1.000000000000000000, 0.9510565162951535312, 1.000000000000000000, 0.9510565162951535312, 1.000000000000000000, 0.9510565162951535312, 1.000000000000000000, 0.9755282581475768211, 0.9755282581475768211 ) ) 
 REPRESENTATION_ITEM ( '' )  );
#17237=ORIENTED_EDGE ( 'NONE', *, *, #6350, .F. ) ;
#17238=CARTESIAN_POINT ( 'NONE',  ( 41.64333658814960870, 131.7797705074273154, 30.00020018409699318 ) ) ;
#17240=CARTESIAN_POINT ( 'NONE',  ( 43.01140435219951286, 92.62977050742732388, 29.55568802177586463 ) ) ;
#17242=LINE ( 'NONE', #20250, #10104 ) ;
#17245=CARTESIAN_POINT ( 'NONE',  ( 46.59305225739526435, 100.3151871740940067, 36.81289934271958941 ) ) ;
#17246=CARTESIAN_POINT ( 'NONE',  ( 39.92123440845005433, 153.2604996726487343, 29.95742577749336988 ) ) ;
#17250=CARTESIAN_POINT ( 'NONE',  ( 48.01140435219951996, 142.2844580088725763, 34.21067981925357060 ) ) ;
#17251=CARTESIAN_POINT ( 'NONE',  ( 41.64333658814960870, 113.7797705074273296, 30.00020018409699318 ) ) ;
#17253=CARTESIAN_POINT ( 'NONE',  ( 38.96631938032478359, 141.0844580088725877, 37.14960608071593384 ) ) ;
#17254=CARTESIAN_POINT ( 'NONE',  ( 40.27526882409969744, 107.6651871740940152, 30.44471234641812174 ) ) ;
#17260=CARTESIAN_POINT ( 'NONE',  ( 43.01140435219951996, 10.71049967264875491, 39.21067981925356349 ) ) ;
#17261=CARTESIAN_POINT ( 'NONE',  ( 46.59305225739526435, 85.57977050742732672, 36.81289934271958941 ) ) ;
#17264=CARTESIAN_POINT ( 'NONE',  ( 46.10157429594899270, 67.73445800887256496, 29.95742577749337343 ) ) ;
#17266=CARTESIAN_POINT ( 'NONE',  ( 39.92123440845004723, 130.1604996726487400, 38.46393386101376421 ) ) ;
#17268=CARTESIAN_POINT ( 'NONE',  ( 41.64333658814960870, 90.71518717409401233, 38.42115945441014446 ) ) ;
#17272=CARTESIAN_POINT ( 'NONE',  ( 41.46631938032478359, 117.3844580088725849, 38.96596240072933170 ) ) ;
#17274=CARTESIAN_POINT ( 'NONE',  ( 43.80332655382222384, 68.88361825032845331, 29.21067981925357770 ) ) ;
#17276=CARTESIAN_POINT ( 'NONE',  ( 38.58424406990784661, 141.5297705074272869, 35.64915139335016647 ) ) ;
#17277=CARTESIAN_POINT ( 'NONE',  ( 47.43856463449117200, 100.7297705074273040, 35.64915139335016647 ) ) ;
#17280=CARTESIAN_POINT ( 'NONE',  ( 47.43856463449118621, 133.6151871740940180, 34.21067981925357060 ) ) ;
#17283=CARTESIAN_POINT ( 'NONE',  ( 43.01140435219951286, 68.62977050742729546, 29.55568802177586463 ) ) ;
#17288=CARTESIAN_POINT ( 'NONE',  ( 47.43856463449117200, 115.7651871740939811, 32.77220824515698183 ) ) ;
#17292=CARTESIAN_POINT ( 'NONE',  ( 41.46631938032478359, 104.1844580088725820, 29.45539723777780239 ) ) ;
#17296=CARTESIAN_POINT ( 'NONE',  ( 44.55648932407425633, 154.6104996726487570, 38.96596240072933170 ) ) ;
#17297=CARTESIAN_POINT ( 'NONE',  ( 44.37947211624943833, 118.0151871740940095, 38.42115945441014446 ) ) ;
#17299=CARTESIAN_POINT ( 'NONE',  ( 48.01140435219951996, 74.36049967264871441, 32.58608133808903773 ) ) ;
#17301=CARTESIAN_POINT ( 'NONE',  ( 39.92123440845005433, 75.23445800887257917, 38.46393386101375711 ) ) ;
#17305=CARTESIAN_POINT ( 'NONE',  ( 39.42975644700377558, 80.81518717409400665, 31.60846029578754468 ) ) ;
#17306=CARTESIAN_POINT ( 'NONE',  ( 44.55648932407425633, 103.6104996726487428, 38.96596240072933170 ) ) ;
#17312=ORIENTED_EDGE ( 'NONE', *, *, #6100, .F. ) ;
#17314=CARTESIAN_POINT ( 'NONE',  ( 46.59305225739526435, 145.9151871740940294, 31.60846029578754468 ) ) ;
#17317=CARTESIAN_POINT ( 'NONE',  ( 40.27526882409969744, 102.8297705074273125, 37.97664729208901235 ) ) ;
#17323=CARTESIAN_POINT ( 'NONE',  ( 40.27526882409969033, 110.9297705074272926, 30.44471234641811819 ) ) ;
#17325=CARTESIAN_POINT ( 'NONE',  ( 43.01140435219951996, 147.5344580088726048, 39.21067981925356349 ) ) ;
#17327=CARTESIAN_POINT ( 'NONE',  ( 47.43856463449117200, 82.72977050742731819, 35.64915139335016647 ) ) ;
#17328=CARTESIAN_POINT ( 'NONE',  ( 47.43856463449117200, 145.4651871740939839, 35.64915139335016647 ) ) ;
#17329=CARTESIAN_POINT ( 'NONE',  ( 38.01140435219951996, 96.86049967264871441, 35.83527830041810347 ) ) ;
#17331=CARTESIAN_POINT ( 'NONE',  ( 48.01140435219951996, 119.0604996726487315, 35.83527830041809636 ) ) ;
#17335=DIRECTION ( 'NONE',  ( 0.000000000000000000, 1.000000000000000000, 0.000000000000000000 ) ) ;
#17336=ORIENTED_EDGE ( 'NONE', *, *, #3727, .F. ) ;
#17337=CARTESIAN_POINT ( 'NONE',  ( 45.74753988029933538, 80.32977050742731251, 30.44471234641811819 ) ) ;
#17339=CARTESIAN_POINT ( 'NONE',  ( 41.64333658814960870, 77.51518717409399528, 30.00020018409699318 ) ) ;
#17343=CARTESIAN_POINT ( 'NONE',  ( 39.92123440845005433, 118.1604996726487400, 38.46393386101375711 ) ) ;
#17344=CARTESIAN_POINT ( 'NONE',  ( 39.42975644700377558, 129.0797705074273267, 31.60846029578754468 ) ) ;
#17349=CARTESIAN_POINT ( 'NONE',  ( 47.43856463449117200, 134.0297705074273154, 32.77220824515698183 ) ) ;
#17350=EDGE_CURVE ( 'NONE', #15251, #16317, #16993, .T. ) ;
#17351=CARTESIAN_POINT ( 'NONE',  ( 47.43856463449117200, 91.72977050742730398, 35.64915139335016647 ) ) ;
#17356=CARTESIAN_POINT ( 'NONE',  ( 41.64333658814960870, 101.5151871740939953, 30.00020018409699318 ) ) ;
#17361=CARTESIAN_POINT ( 'NONE',  ( 47.05648932407426344, 132.9844580088725934, 37.14960608071593384 ) ) ;
#17362=CARTESIAN_POINT ( 'NONE',  ( 46.59305225739526435, 115.5797705074273267, 36.81289934271958941 ) ) ;
#17365=CARTESIAN_POINT ( 'NONE',  ( 40.27526882409969744, 111.5651871740939782, 37.97664729208901235 ) ) ;
#17369=( BOUNDED_CURVE ( )  B_SPLINE_CURVE ( 2, ( #4394, #12781, #19502, #7620, #20841, #19612, #15971, #14537, #21278, #12891, #5834, #16081, #4506 ),
 .UNSPECIFIED., .F., .F. ) 
 B_SPLINE_CURVE_WITH_KNOTS ( ( 3, 2, 2, 2, 2, 2, 3 ),
 ( 0.3897058823529411797, 0.3911764705882352922, 0.3941176470588235170, 0.3970588235294117418, 0.4000000000000000222, 0.4029411764705882470, 0.4044117647058823595 ),
 .UNSPECIFIED. ) 
 CURVE ( )  GEOMETRIC_REPRESENTATION_ITEM ( )  RATIONAL_B_SPLINE_CURVE ( ( 0.9755282581475768211, 0.9755282581475768211, 1.000000000000000000, 0.9510565162951535312, 1.000000000000000000, 0.9510565162951535312, 1.000000000000000000, 0.9510565162951535312, 1.000000000000000000, 0.9510565162951535312, 1.000000000000000000, 0.9755282581475768211, 0.9755282581475768211 ) ) 
 REPRESENTATION_ITEM ( '' )  );
#17372=CARTESIAN_POINT ( 'NONE',  ( 41.64333658814960870, 72.97977050742731819, 38.42115945441014446 ) ) ;
#17373=VERTEX_POINT ( 'NONE', #18871 ) ;
#17374=CARTESIAN_POINT ( 'NONE',  ( 38.96631938032478359, 65.48445800887257917, 31.27175355779120025 ) ) ;
#17376=CARTESIAN_POINT ( 'NONE',  ( 47.05648932407426344, 127.9104996726487542, 37.14960608071593384 ) ) ;
#17377=CARTESIAN_POINT ( 'NONE',  ( 38.58424406990784661, 80.96518717409399812, 32.77220824515698183 ) ) ;
#17381=CARTESIAN_POINT ( 'NONE',  ( 43.80332655382220253, 113.8836182503284533, 29.21067981925356705 ) ) ;
#17383=CYLINDRICAL_SURFACE ( 'NONE', #8460, 4.999999999999997335 ) ;
#17384=CARTESIAN_POINT ( 'NONE',  ( 38.96631938032478359, 93.08445800887257349, 37.14960608071593384 ) ) ;
#17385=CARTESIAN_POINT ( 'NONE',  ( 47.05648932407426344, 143.5104996726487627, 31.27175355779120025 ) ) ;
#17386=CARTESIAN_POINT ( 'NONE',  ( 38.58424406990784661, 144.5297705074273154, 35.64915139335016647 ) ) ;
#17387=CARTESIAN_POINT ( 'NONE',  ( 43.01140435219951286, 104.6297705074273239, 29.55568802177586463 ) ) ;
#17389=CARTESIAN_POINT ( 'NONE',  ( 43.01140435219951286, 132.8651871740940180, 38.86567161673127657 ) ) ;
#17394=EDGE_CURVE ( 'NONE', #137, #890, #17426, .T. ) ;
#17395=CARTESIAN_POINT ( 'NONE',  ( 38.01140435219952707, 135.7104996726487514, 34.21067981925357060 ) ) ;
#17398=CARTESIAN_POINT ( 'NONE',  ( 38.58424406990784661, 117.2651871740940095, 35.64915139335016647 ) ) ;
#17399=EDGE_CURVE ( 'NONE', #1684, #10985, #19693, .T. ) ;
#17400=ORIENTED_EDGE ( 'NONE', *, *, #16785, .T. ) ;
#17403=CARTESIAN_POINT ( 'NONE',  ( 38.01140435219952707, 89.78445800887257633, 34.21067981925357060 ) ) ;
#17404=CARTESIAN_POINT ( 'NONE',  ( 40.27526882409969033, 60.82977050742731961, 37.97664729208901946 ) ) ;
#17405=CARTESIAN_POINT ( 'NONE',  ( 41.64333658814960870, 117.7151871740939981, 38.42115945441014446 ) ) ;
#17407=CARTESIAN_POINT ( 'NONE',  ( 39.92123440845004723, 70.16049967264873999, 38.46393386101376421 ) ) ;
#17409=CARTESIAN_POINT ( 'NONE',  ( 48.01140435219951996, 136.4344580088725820, 32.58608133808903773 ) ) ;
#17413=CARTESIAN_POINT ( 'NONE',  ( 46.59305225739526435, 67.91518717409400097, 31.60846029578754468 ) ) ;
#17417=ORIENTED_EDGE ( 'NONE', *, *, #6596, .F. ) ;
#17421=CARTESIAN_POINT ( 'NONE',  ( 45.74753988029933538, 148.1651871740940010, 37.97664729208901946 ) ) ;
#17422=CARTESIAN_POINT ( 'NONE',  ( 47.43856463449117911, 106.7297705074273182, 35.64915139335015937 ) ) ;
#17423=VERTEX_POINT ( 'NONE', #5078 ) ;
#17426=( BOUNDED_CURVE ( )  B_SPLINE_CURVE ( 2, ( #15463, #144, #6875, #13582, #6987, #13690, #20425, #20533, #18768, #13796, #5420, #12580, #1007, #6173, #7743, #3994, #21178, #6069, #7633, #15775, #680, #5744, #10829, #17528, #15875, #789, #14337, #4306, #12796, #21077, #5959, #17745, #4409, #17855, #2766, #9382, #6060, #21504, #4623, #11343, #12787, #5949, #18066, #1105, #7840, #13119, #14542, #6162, #12897, #19617, #4512, #1212, #11235, #17955, #2973, #2860, #9603, #7945, #14651, #20284, #3310, #21615, #13225, #5073, #16634, #6625, #18297, #6740, #4847, #110, #698, #15095, #13447, #1545, #16518, #5287, #3427, #8164, #13340, #15210, #16849, #8276, #3531, #18517, #5179, #20182, #11787, #15320, #6506, #10147, #18180, #6842, #1764, #8386, #3086, #14976, #20077, #16958, #4965, #11568, #1434, #14870, #8498, #19963, #6950, #13548, #213, #8600, #11897, #3199, #18626, #13657, #9929, #10256, #20390, #11675, #21722, #1870, #9820, #18410, #10040, #16743, #1654, #755, #13976, #9144, #15431, #13762, #18839, #20502, #2088, #12107, #12324, #7384, #15844, #18734, #7490, #3852, #327, #7057, #5391, #3745, #3962, #10475, #20714, #5597, #12001, #9033, #17175, #8821, #14192, #20607, #15530, #4062, #2194, #10364, #10684, #20932, #8925, #12437, #435, #7166, #10577, #2408, #13869, #19163, #5490, #12217, #19059, #18951, #17280, #15630, #535, #7274, #15744, #17389, #2293, #649, #14085, #17065, #3639, #20821, #5712, #10791, #17497, #1978, #8712, #12981, #6138, #7920, #9470, #21258, #2944, #15951, #14518, #5813, #2835, #12870, #17818, #12544, #17710, #4596, #969, #14299, #10901, #11210, #2730, #14623, #18039, #19589, #4482, #21361, #19272, #4172, #6251, #7710, #12761, #9686, #2511, #11000, #16383, #16169, #19705, #11315, #14410, #1296, #21042, #8030, #17605, #1081, #14737, #21146, #9252, #12653, #17926, #2615, #862, #7599, #9574, #6031, #7812, #16280, #5925, #1186, #19377, #4272, #9353, #16058, #19482, #4373, #11104, #15181, #1738, #1518, #83, #8135, #11872, #21473, #11648, #8473, #14949, #6819, #18267, #8358, #13526, #10011, #14838, #20155, #6595, #16603, #5047, #5152, #11758, #16932, #10120, #18489, #20050, #11423, #1848, #13314, #3395, #6475, #21585, #11540, #13196, #21805, #16826, #3507, #6364, #18603, #4937, #3057, #16489, #1406, #19929, #20260, #10230, #8577, #4818, #18380, #13088, #3171, #9900, #19816, #8248, #21696, #4705, #3281, #18149, #9796, #16716, #1625, #15068, #6713, #13420, #17473, #1953, #17365, #411, #15606, #5262, #2166, #13737, #3719, #15406, #3827, #8683, #19034, #18924, #12189, #10553, #20475, #13629, #2383, #514, #11979, #10448, #12296, #13951, #20367, #8904, #7251, #2271, #17254, #20689, #12410, #3616, #5573, #15294, #3932, #10663, #5467, #187, #5367, #17150, #14061, #2066, #303, #18709, #9008, #15719, #17041, #4040, #623, #19141, #5687, #7358, #7032, #10338, #20795, #10767, #6924, #12084, #18814, #8795, #15509, #7142, #13845, #20581, #2700, #17792, #6007, #9551, #21017, #2813, #11292, #17580, #11187, #16029, #9445, #20903, #14492, #4571, #21123, #21234, #18014, #1163, #7687, #942, #7896, #6225, #7572, #7461, #9121, #16146, #5790, #19351, #6113, #7788, #14170, #1054, #17900, #15819, #12521, #5899, #12843, #19561, #4456, #16254, #14598, #11077, #12736, #733, #12629, #4249, #21338, #10975, #2486, #19247, #12956, #19459, #19679, #4146, #10879, #9228, #15926, #838, #14272, #17688, #2590, #14384, #9330, #4349, #18243, #21449, #14925, #18467, #5024, #4793, #3370, #11400, #15155, #2925, #6569, #11733, #3145, #16360, #9770, #1599, #14816, #55, #18123, #8332, #9875, #19905, #15041, #8449, #21782, #20237, #13396, #6689, #1494, #14713, #5129, #16575, #20130, #6339, #1714, #10094, #21561, #16801, #6797, #13504, #9660, #11848, #8224, #13065, #19792, #4684, #3033, #1271, #8006, #16467, #1381, #11514, #8110, #6451, #13174, #20025, #4910, #18354, #3258, #9988, #10207, #3483, #5544, #20448, #3692, #594, #15268, #1924, #15686, #7333, #5659, #274, #5340, #2142, #15381, #12057, #8875, #3909, #20663, #18789, #16910, #3586, #10528, #8659, #8980, #1823, #18893, #13712, #20558, #6898, #5443, #18576, #13605, #3800, #13924, #12271, #14033, #17226, #10419, #15582, #8556, #17339, #485, #7008, #19007, #7223, #166, #20342, #10635, #5237, #20768, #11954, #18684, #2246, #10315, #17016, #17124, #2036, #8768, #15483, #384, #7113, #13818, #8059, #16416, #14767, #2977, #16522, #6284, #21396, #1440, #11347, #1326, #18070, #12492, #4518, #3091, #1110, #13015, #2353, #9715, #8169, #2865, #21509, #21619, #4736, #11240, #17960, #11455, #9824, #6395, #2760, #16307, #13123, #6168, #19624, #19845, #18184, #10740, #19735, #14874, #12382, #9091, #9501, #19117, #4012, #17442, #4628, #15793, #14656, #702, #7436, #17850, #14139, #20876, #5764, #7845, #19219, #16198, #4117, #10853, #14547, #21290, #12902, #9608, #1217, #7951, #6631, #3431, #17068, #4852, #20394, #1982, #3, #3203, #18522, #217, #8603, #11901, #3315, #6744, #18630, #13660, #13452, #3641, #5290, #15323, #10044, #15215, #6953, #16853, #14981, #5182, #20186, #8390, #3534, #12004, #10259, #13553, #1873, #18738, #8715, #8502, #10367, #9934, #8280 ),
 .UNSPECIFIED., .F., .F. ) 
 B_SPLINE_CURVE_WITH_KNOTS ( ( 3, 2, 2, 2, 2, 2, 2, 2, 2, 2, 2, 2, 2, 2, 2, 2, 2, 2, 2, 2, 2, 2, 2, 2, 2, 2, 2, 2, 2, 2, 2, 2, 2, 2, 2, 2, 2, 2, 2, 2, 2, 2, 2, 2, 2, 2, 2, 2, 2, 2, 2, 2, 2, 2, 2, 2, 2, 2, 2, 2, 2, 2, 2, 2, 2, 2, 2, 2, 2, 2, 2, 2, 2, 2, 2, 2, 2, 2, 2, 2, 2, 2, 2, 2, 2, 2, 2, 2, 2, 2, 2, 2, 2, 2, 2, 2, 2, 2, 2, 2, 2, 2, 2, 2, 2, 2, 2, 2, 2, 2, 2, 2, 2, 2, 2, 2, 2, 2, 2, 2, 2, 2, 2, 2, 2, 2, 2, 2, 2, 2, 2, 2, 2, 2, 2, 2, 2, 2, 2, 2, 2, 2, 2, 2, 2, 2, 2, 2, 2, 2, 2, 2, 2, 2, 2, 2, 2, 2, 2, 2, 2, 2, 2, 2, 2, 2, 2, 2, 2, 2, 2, 2, 2, 2, 2, 2, 2, 2, 2, 2, 2, 2, 2, 2, 2, 2, 2, 2, 2, 2, 2, 2, 2, 2, 2, 2, 2, 2, 2, 2, 2, 2, 2, 2, 2, 2, 2, 2, 2, 2, 2, 2, 2, 2, 2, 2, 2, 2, 2, 2, 2, 2, 2, 2, 2, 2, 2, 2, 2, 2, 2, 2, 2, 2, 2, 2, 2, 2, 2, 2, 2, 2, 2, 2, 2, 2, 2, 2, 2, 2, 2, 2, 2, 2, 2, 2, 2, 2, 2, 2, 2, 2, 2, 2, 2, 2, 2, 2, 2, 2, 2, 2, 2, 2, 2, 2, 2, 2, 2, 2, 2, 2, 2, 2, 2, 2, 2, 2, 2, 2, 2, 2, 2, 2, 2, 2, 2, 2, 2, 2, 2, 2, 2, 2, 2, 2, 2, 2, 2, 2, 2, 2, 2, 2, 2, 2, 2, 2, 2, 2, 2, 2, 2, 2, 2, 2, 2, 2, 2, 2, 2, 2, 2, 2, 3 ),
 ( 0.000000000000000000, 0.002999988802223336245, 0.005999977604446672490, 0.008999966406670010036, 0.01199995520889334498, 0.01499994401111668166, 0.01799993281334002007, 0.02099992161556335502, 0.02399991041778668996, 0.02699989922001002837, 0.02999988802223336332, 0.03299987682445670173, 0.03599986562668004014, 0.03899985442890337856, 0.04199984323112671003, 0.04499983203335004844, 0.04799982083557337992, 0.05099980963779672527, 0.05399979844002005674, 0.05699978724224339516, 0.05999977604446672663, 0.06299976484669006505, 0.06599975364891340346, 0.06899974245113672799, 0.07199973125336008029, 0.07499972005558341870, 0.07799970885780675711, 0.08099969766003008165, 0.08399968646225342006, 0.08699967526447675847, 0.08999966406670009689, 0.09299965286892342142, 0.09599964167114675984, 0.09899963047337011213, 0.1019996192755934505, 0.1049996080778167751, 0.1079995968800401135, 0.1109995856822634519, 0.1139995744844867903, 0.1169995632867101149, 0.1199995520889334533, 0.1229995408911567917, 0.1259995296933801301, 0.1289995184956034546, 0.1319995072978268069, 0.1349994961000501315, 0.1379994849022734560, 0.1409994737044968360, 0.1439994625067201606, 0.1469994513089434851, 0.1499994401111668374, 0.1529994289133901619, 0.1559994177156135142, 0.1589994065178368388, 0.1619993953200601633, 0.1649993841222835156, 0.1679993729245068401, 0.1709993617267301647, 0.1739993505289535169, 0.1769993393311768415, 0.1799993281334001938, 0.1829993169356235183, 0.1859993057378468428, 0.1889992945400701951, 0.1919992833422935197, 0.1949992721445168442, 0.1979992609467402243, 0.2009992497489635488, 0.2039992385511869011, 0.2069992273534102256, 0.2099992161556335502, 0.2129992049578569024, 0.2159991937600802270, 0.2189991825623035515, 0.2219991713645269038, 0.2249991601667502283, 0.2279991489689735806, 0.2309991377711969052, 0.2339991265734202297, 0.2369991153756435820, 0.2399991041778669065, 0.2429990929800902311, 0.2459990817823135834, 0.2489990705845369079, 0.2519990593867602602, 0.2549990481889836125, 0.2579990369912069093, 0.2609990257934302615, 0.2639990145956536138, 0.2669990033978769661, 0.2699989922001002629, 0.2729989810023236152, 0.2759989698045469120, 0.2789989586067703198, 0.2819989474089936721, 0.2849989362112169689, 0.2879989250134403211, 0.2909989138156636179, 0.2939989026178869702, 0.2969988914201103225, 0.2999988802223336748, 0.3029988690245569716, 0.3059988578267803239, 0.3089988466290036206, 0.3119988354312270284, 0.3149988242334503252, 0.3179988130356736775, 0.3209988018378969743, 0.3239987906401203266, 0.3269987794423436789, 0.3299987682445670312, 0.3329987570467903280, 0.3359987458490136802, 0.3389987346512370325, 0.3419987234534603293, 0.3449987122556837371, 0.3479987010579070339, 0.3509986898601303862, 0.3539986786623536830, 0.3569986674645770353, 0.3599986562668003875, 0.3629986450690237398, 0.3659986338712470366, 0.3689986226734703889, 0.3719986114756936857, 0.3749986002779170935, 0.3779985890801403903, 0.3809985778823637426, 0.3839985666845870393, 0.3869985554868103916, 0.3899985442890336884, 0.3929985330912570962, 0.3959985218934804485, 0.3989985106957037453, 0.4019984994979270976, 0.4049984883001503944, 0.4079984771023738022, 0.4109984659045970989, 0.4139984547068204512, 0.4169984435090437480, 0.4199984323112671003, 0.4229984211134904526, 0.4259984099157138049, 0.4289983987179371017, 0.4319983875201604540, 0.4349983763223837507, 0.4379983651246071030, 0.4409983539268304553, 0.4439983427290538076, 0.4469983315312771044, 0.4499983203335004567, 0.4529983091357238090, 0.4559982979379471613, 0.4589982867401705136, 0.4619982755423938103, 0.4649982643446171626, 0.4679982531468404594, 0.4709982419490638672, 0.4739982307512871640, 0.4769982195535105163, 0.4799982083557338131, 0.4829981971579571653, 0.4859981859601804621, 0.4889981747624038699, 0.4919981635646271667, 0.4949981523668505190, 0.4979981411690738158, 0.5009981299712971126, 0.5039981187735205204, 0.5069981075757439282, 0.5099980963779672249, 0.5129980851801905217, 0.5159980739824138185, 0.5189980627846372263, 0.5219980515868605231, 0.5249980403890838199, 0.5279980291913072277, 0.5309980179935306355, 0.5339980067957539323, 0.5369979955979772290, 0.5399979844002005258, 0.5429979732024239336, 0.5459979620046472304, 0.5489979508068705272, 0.5519979396090938240, 0.5549979284113172318, 0.5579979172135406396, 0.5609979060157639363, 0.5639978948179873441, 0.5669978836202106409, 0.5699978724224339377, 0.5729978612246572345, 0.5759978500268806423, 0.5789978388291039391, 0.5819978276313272358, 0.5849978164335505326, 0.5879978052357739404, 0.5909977940379973482, 0.5939977828402206450, 0.5969977716424439418, 0.5999977604446673496, 0.6029977492468906464, 0.6059977380491139431, 0.6089977268513372399, 0.6119977156535606477, 0.6149977044557839445, 0.6179976932580072413, 0.6209976820602306491, 0.6239976708624540569, 0.6269976596646773537, 0.6299976484669006505, 0.6329976372691240583, 0.6359976260713473550, 0.6389976148735706518, 0.6419976036757939486, 0.6449975924780173564, 0.6479975812802406532, 0.6509975700824639500, 0.6539975588846873578, 0.6569975476869107656, 0.6599975364891340623, 0.6629975252913573591, 0.6659975140935806559, 0.6689975028958040637, 0.6719974916980273605, 0.6749974805002506573, 0.6779974693024740651, 0.6809974581046973618, 0.6839974469069206586, 0.6869974357091440664, 0.6899974245113674742, 0.6929974133135907710, 0.6959974021158140678, 0.6989973909180373646, 0.7019973797202607724, 0.7049973685224840692, 0.7079973573247073659, 0.7109973461269306627, 0.7139973349291540705, 0.7169973237313773673, 0.7199973125336007751, 0.7229973013358240719, 0.7259972901380474797, 0.7289972789402707765, 0.7319972677424940732, 0.7349972565447174810, 0.7379972453469407778, 0.7409972341491640746, 0.7439972229513873714, 0.7469972117536107792, 0.7499972005558341870, 0.7529971893580574838, 0.7559971781602807805, 0.7589971669625041883, 0.7619971557647274851, 0.7649971445669507819, 0.7679971333691740787, 0.7709971221713974865, 0.7739971109736207833, 0.7769970997758440800, 0.7799970885780673768, 0.7829970773802908957, 0.7859970661825141924, 0.7889970549847374892, 0.7919970437869608970, 0.7949970325891841938, 0.7979970213914074906, 0.8009970101936307874, 0.8039969989958541952, 0.8069969877980774919, 0.8099969766003007887, 0.8129969654025241965, 0.8159969542047476043, 0.8189969430069709011, 0.8219969318091941979, 0.8249969206114174947, 0.8279969094136409025, 0.8309968982158641992, 0.8339968870180874960, 0.8369968758203107928, 0.8399968646225342006, 0.8429968534247574974, 0.8459968422269809052, 0.8489968310292043130, 0.8519968198314276098, 0.8549968086336509066, 0.8579967974358742033, 0.8609967862380976111, 0.8639967750403209079, 0.8669967638425442047, 0.8699967526447675015, 0.8729967414469909093, 0.8759967302492142061, 0.8789967190514376139, 0.8819967078536609106, 0.8849966966558843184, 0.8879966854581076152, 0.8909966742603309120, 0.8939966630625542088, 0.8969966518647776166, 0.8999966406670009134, 0.9029966294692242101, 0.9059966182714476179, 0.9089966070736710257, 0.9119965958758943225, 0.9149965846781176193, 0.9179965734803410271, 0.9209965622825643239, 0.9239965510847876207, 0.9269965398870109174, 0.9299965286892343252, 0.9329965174914576220, 0.9359965062936809188, 0.9389964950959042156, 0.9419964838981277344, 0.9449964727003510312, 0.9479964615025743280, 0.9509964503047977358, 0.9539964391070210326, 0.9569964279092443293, 0.9599964167114676261, 0.9629964055136910339, 0.9659963943159143307, 0.9689963831181376275, 0.9719963719203609243, 0.9749963607225844431, 0.9779963495248077399, 0.9809963383270310366, 0.9839963271292543334, 0.9869963159314777412, 0.9899963047337010380, 0.9929962935359243348, 0.9959962823381476316, 0.9989962711403710394, 1.000000000000000000 ),
 .UNSPECIFIED. ) 
 CURVE ( )  GEOMETRIC_REPRESENTATION_ITEM ( )  RATIONAL_B_SPLINE_CURVE ( ( 1.000000000000000000, 0.9510565162951535312, 1.000000000000000000, 0.9510565162951535312, 1.000000000000000000, 0.9510565162951535312, 1.000000000000000000, 0.9510565162951535312, 1.000000000000000000, 0.9510565162951535312, 1.000000000000000000, 0.9510565162951535312, 1.000000000000000000, 0.9510565162951535312, 1.000000000000000000, 0.9510565162951535312, 1.000000000000000000, 0.9510565162951535312, 1.000000000000000000, 0.9510565162951535312, 1.000000000000000000, 0.9510565162951535312, 1.000000000000000000, 0.9510565162951535312, 1.000000000000000000, 0.9510565162951535312, 1.000000000000000000, 0.9510565162951535312, 1.000000000000000000, 0.9510565162951535312, 1.000000000000000000, 0.9510565162951535312, 1.000000000000000000, 0.9510565162951535312, 1.000000000000000000, 0.9510565162951535312, 1.000000000000000000, 0.9510565162951535312, 1.000000000000000000, 0.9510565162951535312, 1.000000000000000000, 0.9510565162951535312, 1.000000000000000000, 0.9510565162951535312, 1.000000000000000000, 0.9510565162951535312, 1.000000000000000000, 0.9510565162951535312, 1.000000000000000000, 0.9510565162951535312, 1.000000000000000000, 0.9510565162951535312, 1.000000000000000000, 0.9510565162951535312, 1.000000000000000000, 0.9510565162951535312, 1.000000000000000000, 0.9510565162951535312, 1.000000000000000000, 0.9510565162951535312, 1.000000000000000000, 0.9510565162951535312, 1.000000000000000000, 0.9510565162951535312, 1.000000000000000000, 0.9510565162951535312, 1.000000000000000000, 0.9510565162951535312, 1.000000000000000000, 0.9510565162951535312, 1.000000000000000000, 0.9510565162951535312, 1.000000000000000000, 0.9510565162951535312, 1.000000000000000000, 0.9510565162951535312, 1.000000000000000000, 0.9510565162951535312, 1.000000000000000000, 0.9510565162951535312, 1.000000000000000000, 0.9510565162951535312, 1.000000000000000000, 0.9510565162951535312, 1.000000000000000000, 0.9510565162951535312, 1.000000000000000000, 0.9510565162951535312, 1.000000000000000000, 0.9510565162951535312, 1.000000000000000000, 0.9510565162951535312, 1.000000000000000000, 0.9510565162951535312, 1.000000000000000000, 0.9510565162951535312, 1.000000000000000000, 0.9510565162951535312, 1.000000000000000000, 0.9510565162951535312, 1.000000000000000000, 0.9510565162951535312, 1.000000000000000000, 0.9510565162951535312, 1.000000000000000000, 0.9510565162951535312, 1.000000000000000000, 0.9510565162951535312, 1.000000000000000000, 0.9510565162951535312, 1.000000000000000000, 0.9510565162951535312, 1.000000000000000000, 0.9510565162951535312, 1.000000000000000000, 0.9510565162951535312, 1.000000000000000000, 0.9510565162951535312, 1.000000000000000000, 0.9510565162951535312, 1.000000000000000000, 0.9510565162951535312, 1.000000000000000000, 0.9510565162951535312, 1.000000000000000000, 0.9510565162951535312, 1.000000000000000000, 0.9510565162951535312, 1.000000000000000000, 0.9510565162951535312, 1.000000000000000000, 0.9510565162951535312, 1.000000000000000000, 0.9510565162951535312, 1.000000000000000000, 0.9510565162951535312, 1.000000000000000000, 0.9510565162951535312, 1.000000000000000000, 0.9510565162951535312, 1.000000000000000000, 0.9510565162951535312, 1.000000000000000000, 0.9510565162951535312, 1.000000000000000000, 0.9510565162951535312, 1.000000000000000000, 0.9510565162951535312, 1.000000000000000000, 0.9510565162951535312, 1.000000000000000000, 0.9510565162951535312, 1.000000000000000000, 0.9510565162951535312, 1.000000000000000000, 0.9510565162951535312, 1.000000000000000000, 0.9510565162951535312, 1.000000000000000000, 0.9510565162951535312, 1.000000000000000000, 0.9510565162951535312, 1.000000000000000000, 0.9510565162951535312, 1.000000000000000000, 0.9510565162951535312, 1.000000000000000000, 0.9510565162951535312, 1.000000000000000000, 0.9510565162951535312, 1.000000000000000000, 0.9510565162951535312, 1.000000000000000000, 0.9510565162951535312, 1.000000000000000000, 0.9510565162951535312, 1.000000000000000000, 0.9510565162951535312, 1.000000000000000000, 0.9510565162951535312, 1.000000000000000000, 0.9510565162951535312, 1.000000000000000000, 0.9510565162951535312, 1.000000000000000000, 0.9510565162951535312, 1.000000000000000000, 0.9510565162951535312, 1.000000000000000000, 0.9510565162951535312, 1.000000000000000000, 0.9510565162951535312, 1.000000000000000000, 0.9510565162951535312, 1.000000000000000000, 0.9510565162951535312, 1.000000000000000000, 0.9510565162951535312, 1.000000000000000000, 0.9510565162951535312, 1.000000000000000000, 0.9510565162951535312, 1.000000000000000000, 0.9510565162951535312, 1.000000000000000000, 0.9510565162951535312, 1.000000000000000000, 0.9510565162951535312, 1.000000000000000000, 0.9510565162951535312, 1.000000000000000000, 0.9510565162951535312, 1.000000000000000000, 0.9510565162951535312, 1.000000000000000000, 0.9510565162951535312, 1.000000000000000000, 0.9510565162951535312, 1.000000000000000000, 0.9510565162951535312, 1.000000000000000000, 0.9510565162951535312, 1.000000000000000000, 0.9510565162951535312, 1.000000000000000000, 0.9510565162951535312, 1.000000000000000000, 0.9510565162951535312, 1.000000000000000000, 0.9510565162951535312, 1.000000000000000000, 0.9510565162951535312, 1.000000000000000000, 0.9510565162951535312, 1.000000000000000000, 0.9510565162951535312, 1.000000000000000000, 0.9510565162951535312, 1.000000000000000000, 0.9510565162951535312, 1.000000000000000000, 0.9510565162951535312, 1.000000000000000000, 0.9510565162951535312, 1.000000000000000000, 0.9510565162951535312, 1.000000000000000000, 0.9510565162951535312, 1.000000000000000000, 0.9510565162951535312, 1.000000000000000000, 0.9510565162951535312, 1.000000000000000000, 0.9510565162951535312, 1.000000000000000000, 0.9510565162951535312, 1.000000000000000000, 0.9510565162951535312, 1.000000000000000000, 0.9510565162951535312, 1.000000000000000000, 0.9510565162951535312, 1.000000000000000000, 0.9510565162951535312, 1.000000000000000000, 0.9510565162951535312, 1.000000000000000000, 0.9510565162951535312, 1.000000000000000000, 0.9510565162951535312, 1.000000000000000000, 0.9510565162951535312, 1.000000000000000000, 0.9510565162951535312, 1.000000000000000000, 0.9510565162951535312, 1.000000000000000000, 0.9510565162951535312, 1.000000000000000000, 0.9510565162951535312, 1.000000000000000000, 0.9510565162951535312, 1.000000000000000000, 0.9510565162951535312, 1.000000000000000000, 0.9510565162951535312, 1.000000000000000000, 0.9510565162951535312, 1.000000000000000000, 0.9510565162951535312, 1.000000000000000000, 0.9510565162951535312, 1.000000000000000000, 0.9510565162951535312, 1.000000000000000000, 0.9510565162951535312, 1.000000000000000000, 0.9510565162951535312, 1.000000000000000000, 0.9510565162951535312, 1.000000000000000000, 0.9510565162951535312, 1.000000000000000000, 0.9510565162951535312, 1.000000000000000000, 0.9510565162951535312, 1.000000000000000000, 0.9510565162951535312, 1.000000000000000000, 0.9510565162951535312, 1.000000000000000000, 0.9510565162951535312, 1.000000000000000000, 0.9510565162951535312, 1.000000000000000000, 0.9510565162951535312, 1.000000000000000000, 0.9510565162951535312, 1.000000000000000000, 0.9510565162951535312, 1.000000000000000000, 0.9510565162951535312, 1.000000000000000000, 0.9510565162951535312, 1.000000000000000000, 0.9510565162951535312, 1.000000000000000000, 0.9510565162951535312, 1.000000000000000000, 0.9510565162951535312, 1.000000000000000000, 0.9510565162951535312, 1.000000000000000000, 0.9510565162951535312, 1.000000000000000000, 0.9510565162951535312, 1.000000000000000000, 0.9510565162951535312, 1.000000000000000000, 0.9510565162951535312, 1.000000000000000000, 0.9510565162951535312, 1.000000000000000000, 0.9510565162951535312, 1.000000000000000000, 0.9510565162951535312, 1.000000000000000000, 0.9510565162951535312, 1.000000000000000000, 0.9510565162951535312, 1.000000000000000000, 0.9510565162951535312, 1.000000000000000000, 0.9510565162951535312, 1.000000000000000000, 0.9510565162951535312, 1.000000000000000000, 0.9510565162951535312, 1.000000000000000000, 0.9510565162951535312, 1.000000000000000000, 0.9510565162951535312, 1.000000000000000000, 0.9510565162951535312, 1.000000000000000000, 0.9510565162951535312, 1.000000000000000000, 0.9510565162951535312, 1.000000000000000000, 0.9510565162951535312, 1.000000000000000000, 0.9510565162951535312, 1.000000000000000000, 0.9510565162951535312, 1.000000000000000000, 0.9510565162951535312, 1.000000000000000000, 0.9510565162951535312, 1.000000000000000000, 0.9510565162951535312, 1.000000000000000000, 0.9510565162951535312, 1.000000000000000000, 0.9510565162951535312, 1.000000000000000000, 0.9510565162951535312, 1.000000000000000000, 0.9510565162951535312, 1.000000000000000000, 0.9510565162951535312, 1.000000000000000000, 0.9510565162951535312, 1.000000000000000000, 0.9510565162951535312, 1.000000000000000000, 0.9510565162951535312, 1.000000000000000000, 0.9510565162951535312, 1.000000000000000000, 0.9510565162951535312, 1.000000000000000000, 0.9510565162951535312, 1.000000000000000000, 0.9510565162951535312, 1.000000000000000000, 0.9510565162951535312, 1.000000000000000000, 0.9510565162951535312, 1.000000000000000000, 0.9510565162951535312, 1.000000000000000000, 0.9510565162951535312, 1.000000000000000000, 0.9510565162951535312, 1.000000000000000000, 0.9510565162951535312, 1.000000000000000000, 0.9510565162951535312, 1.000000000000000000, 0.9510565162951535312, 1.000000000000000000, 0.9510565162951535312, 1.000000000000000000, 0.9510565162951535312, 1.000000000000000000, 0.9510565162951535312, 1.000000000000000000, 0.9510565162951535312, 1.000000000000000000, 0.9510565162951535312, 1.000000000000000000, 0.9510565162951535312, 1.000000000000000000, 0.9510565162951535312, 1.000000000000000000, 0.9510565162951535312, 1.000000000000000000, 0.9510565162951535312, 1.000000000000000000, 0.9510565162951535312, 1.000000000000000000, 0.9510565162951535312, 1.000000000000000000, 0.9510565162951535312, 1.000000000000000000, 0.9510565162951535312, 1.000000000000000000, 0.9510565162951535312, 1.000000000000000000, 0.9510565162951535312, 1.000000000000000000, 0.9510565162951535312, 1.000000000000000000, 0.9510565162951535312, 1.000000000000000000, 0.9510565162951535312, 1.000000000000000000, 0.9510565162951535312, 1.000000000000000000, 0.9510565162951535312, 1.000000000000000000, 0.9510565162951535312, 1.000000000000000000, 0.9510565162951535312, 1.000000000000000000, 0.9510565162951535312, 1.000000000000000000, 0.9510565162951535312, 1.000000000000000000, 0.9510565162951535312, 1.000000000000000000, 0.9510565162951535312, 1.000000000000000000, 0.9510565162951535312, 1.000000000000000000, 0.9510565162951535312, 1.000000000000000000, 0.9510565162951535312, 1.000000000000000000, 0.9510565162951535312, 1.000000000000000000, 0.9510565162951535312, 1.000000000000000000, 0.9510565162951535312, 1.000000000000000000, 0.9510565162951535312, 1.000000000000000000, 0.9510565162951535312, 1.000000000000000000, 0.9510565162951535312, 1.000000000000000000, 0.9510565162951535312, 1.000000000000000000, 0.9510565162951535312, 1.000000000000000000, 0.9510565162951535312, 1.000000000000000000, 0.9510565162951535312, 1.000000000000000000, 0.9510565162951535312, 1.000000000000000000, 0.9510565162951535312, 1.000000000000000000, 0.9510565162951535312, 1.000000000000000000, 0.9510565162951535312, 1.000000000000000000, 0.9510565162951535312, 1.000000000000000000, 0.9510565162951535312, 1.000000000000000000, 0.9510565162951535312, 1.000000000000000000, 0.9510565162951535312, 1.000000000000000000, 0.9510565162951535312, 1.000000000000000000, 0.9510565162951535312, 1.000000000000000000, 0.9510565162951535312, 1.000000000000000000, 0.9510565162951535312, 1.000000000000000000, 0.9510565162951535312, 1.000000000000000000, 0.9510565162951535312, 1.000000000000000000, 0.9510565162951535312, 1.000000000000000000, 0.9510565162951535312, 1.000000000000000000, 0.9510565162951535312, 1.000000000000000000, 0.9510565162951535312, 1.000000000000000000, 0.9510565162951535312, 1.000000000000000000, 0.9510565162951535312, 1.000000000000000000, 0.9510565162951535312, 1.000000000000000000, 0.9510565162951535312, 1.000000000000000000, 0.9510565162951535312, 1.000000000000000000, 0.9510565162951535312, 1.000000000000000000, 0.9510565162951535312, 1.000000000000000000, 0.9510565162951535312, 1.000000000000000000, 0.9510565162951535312, 1.000000000000000000, 0.9510565162951535312, 1.000000000000000000, 0.9510565162951535312, 1.000000000000000000, 0.9510565162951535312, 1.000000000000000000, 0.9510565162951535312, 1.000000000000000000, 0.9510565162951535312, 1.000000000000000000, 0.9510565162951535312, 1.000000000000000000, 0.9510565162951535312, 1.000000000000000000, 0.9510565162951535312, 1.000000000000000000, 0.9510565162951535312, 1.000000000000000000, 0.9510565162951535312, 1.000000000000000000, 0.9510565162951535312, 1.000000000000000000, 0.9510565162951535312, 1.000000000000000000, 0.9510565162951535312, 1.000000000000000000, 0.9510565162951535312, 1.000000000000000000, 0.9510565162951535312, 1.000000000000000000, 0.9510565162951535312, 1.000000000000000000, 0.9510565162951535312, 1.000000000000000000, 0.9510565162951535312, 1.000000000000000000, 0.9510565162951535312, 1.000000000000000000, 0.9510565162951535312, 1.000000000000000000, 0.9510565162951535312, 1.000000000000000000, 0.9510565162951535312, 1.000000000000000000, 0.9510565162951535312, 1.000000000000000000, 0.9510565162951535312, 1.000000000000000000, 0.9510565162951535312, 1.000000000000000000, 0.9510565162951535312, 1.000000000000000000, 0.9510565162951535312, 1.000000000000000000, 0.9510565162951535312, 1.000000000000000000, 0.9510565162951535312, 1.000000000000000000, 0.9510565162951535312, 1.000000000000000000, 0.9510565162951535312, 1.000000000000000000, 0.9510565162951535312, 1.000000000000000000, 0.9510565162951535312, 1.000000000000000000, 0.9510565162951535312, 1.000000000000000000, 0.9510565162951535312, 1.000000000000000000, 0.9510565162951535312, 1.000000000000000000, 0.9510565162951535312, 1.000000000000000000, 0.9510565162951535312, 1.000000000000000000, 0.9510565162951535312, 1.000000000000000000, 0.9510565162951535312, 1.000000000000000000, 0.9510565162951535312, 1.000000000000000000, 0.9510565162951535312, 1.000000000000000000, 0.9510565162951535312, 1.000000000000000000, 0.9510565162951535312, 1.000000000000000000, 0.9510565162951535312, 1.000000000000000000, 0.9510565162951535312, 1.000000000000000000, 0.9510565162951535312, 1.000000000000000000, 0.9510565162951535312, 1.000000000000000000, 0.9510565162951535312, 1.000000000000000000, 0.9510565162951535312, 1.000000000000000000, 0.9510565162951535312, 1.000000000000000000, 0.9510565162951535312, 1.000000000000000000, 0.9510565162951535312, 1.000000000000000000, 0.9510565162951535312, 1.000000000000000000, 0.9510565162951535312, 1.000000000000000000, 0.9510565162951535312, 1.000000000000000000, 0.9510565162951535312, 1.000000000000000000, 0.9836246098489007661, 0.9782068950532306628 ) ) 
 REPRESENTATION_ITEM ( '' )  );
#17429=CARTESIAN_POINT ( 'NONE',  ( 39.92123440845005433, 76.16049967264873999, 38.46393386101375711 ) ) ;
#17430=VECTOR ( 'NONE', #14176, 1000.000000000000000 ) ;
#17431=CARTESIAN_POINT ( 'NONE',  ( 43.01140435219951286, 144.8651871740939612, 38.86567161673127657 ) ) ;
#17432=CARTESIAN_POINT ( 'NONE',  ( 39.92123440845004723, 100.1604996726487116, 38.46393386101376421 ) ) ;
#17436=CARTESIAN_POINT ( 'NONE',  ( 43.01140435219951996, 10.71049967264875491, 39.21067981925356349 ) ) ;
#17437=CARTESIAN_POINT ( 'NONE',  ( 41.46631938032478359, 143.1844580088725820, 29.45539723777780239 ) ) ;
#17440=CARTESIAN_POINT ( 'NONE',  ( 43.01140435219951286, 89.62977050742729546, 29.55568802177586463 ) ) ;
#17442=CARTESIAN_POINT ( 'NONE',  ( 47.43856463449117911, 67.76518717409399528, 32.77220824515697473 ) ) ;
#17448=CARTESIAN_POINT ( 'NONE',  ( 39.92123440845005433, 117.2604996726487485, 29.95742577749336988 ) ) ;
#17450=CARTESIAN_POINT ( 'NONE',  ( 44.37947211624943833, 134.4797705074273324, 30.00020018409699318 ) ) ;
#17454=VERTEX_POINT ( 'NONE', #6845 ) ;
#17455=CARTESIAN_POINT ( 'NONE',  ( 47.43856463449117200, 140.0297705074273438, 32.77220824515698183 ) ) ;
#17456=CARTESIAN_POINT ( 'NONE',  ( 48.01140435219951996, 139.2844580088725763, 34.21067981925357060 ) ) ;
#17458=CARTESIAN_POINT ( 'NONE',  ( 38.01140435219952707, 99.71049967264875136, 34.21067981925357060 ) ) ;
#17462=CARTESIAN_POINT ( 'NONE',  ( 43.01140435219951286, 95.36518717409400381, 29.55568802177586463 ) ) ;
#17463=CARTESIAN_POINT ( 'NONE',  ( 38.01140435219952707, 66.71049967264873715, 34.21067981925357060 ) ) ;
#17467=CARTESIAN_POINT ( 'NONE',  ( 47.05648932407426344, 70.91049967264873999, 37.14960608071593384 ) ) ;
#17469=CARTESIAN_POINT ( 'NONE',  ( 41.46631938032478359, 134.1844580088725820, 29.45539723777780239 ) ) ;
#17470=CARTESIAN_POINT ( 'NONE',  ( 38.58424406990784661, 114.5297705074273296, 35.64915139335016647 ) ) ;
#17472=DIRECTION ( 'NONE',  ( 0.000000000000000000, 0.000000000000000000, 1.000000000000000000 ) ) ;
#17473=CARTESIAN_POINT ( 'NONE',  ( 43.01140435219951286, 111.8651871740939896, 38.86567161673127657 ) ) ;
#17477=CARTESIAN_POINT ( 'NONE',  ( 48.01140435219951996, 157.4344580088725820, 32.58608133808903773 ) ) ;
#17481=DIRECTION ( 'NONE',  ( 0.000000000000000000, 0.000000000000000000, 1.000000000000000000 ) ) ;
#17482=CARTESIAN_POINT ( 'NONE',  ( 46.59305225739526435, 73.57977050742732672, 36.81289934271958941 ) ) ;
#17484=ORIENTED_EDGE ( 'NONE', *, *, #14513, .T. ) ;
#17486=CARTESIAN_POINT ( 'NONE',  ( 48.01140435219951996, 119.2104996726487371, 34.21067981925357060 ) ) ;
#17487=CARTESIAN_POINT ( 'NONE',  ( 38.58424406990784661, 81.26518717409398107, 35.64915139335016647 ) ) ;
#17493=DIRECTION ( 'NONE',  ( 0.000000000000000000, 0.000000000000000000, 1.000000000000000000 ) ) ;
#17494=CARTESIAN_POINT ( 'NONE',  ( 39.92123440845005433, 149.3344580088725593, 29.95742577749336988 ) ) ;
#17495=CARTESIAN_POINT ( 'NONE',  ( 43.01140435219951286, 139.1297705074272812, 38.86567161673127657 ) ) ;
#17497=CARTESIAN_POINT ( 'NONE',  ( 41.64333658814960870, 131.5151871740939953, 30.00020018409699318 ) ) ;
#17500=CARTESIAN_POINT ( 'NONE',  ( 48.01140435219951996, 91.43445800887258201, 32.58608133808903773 ) ) ;
#17504=CARTESIAN_POINT ( 'NONE',  ( 46.59305225739526435, 112.9151871740940010, 31.60846029578754468 ) ) ;
#17509=CARTESIAN_POINT ( 'NONE',  ( 43.01140435219951286, 87.53445800887256212, 39.46799094044489209 ) ) ;
#17510=CARTESIAN_POINT ( 'NONE',  ( 43.01140435219951286, 151.1297705074273097, 38.86567161673127657 ) ) ;
#17511=CARTESIAN_POINT ( 'NONE',  ( 39.92123440845004723, 147.2604996726487059, 29.95742577749337343 ) ) ;
#17512=CARTESIAN_POINT ( 'NONE',  ( 41.64333658814960870, 107.5151871740939953, 30.00020018409699318 ) ) ;
#17514=CARTESIAN_POINT ( 'NONE',  ( 48.01140435219951996, 74.21049967264873715, 34.21067981925357060 ) ) ;
#17516=CARTESIAN_POINT ( 'NONE',  ( 47.05648932407426344, 61.58445800887258059, 31.27175355779120025 ) ) ;
#17517=CARTESIAN_POINT ( 'NONE',  ( 43.01140435219951286, 72.53445800887256212, 39.21067981925356349 ) ) ;
#17519=CARTESIAN_POINT ( 'NONE',  ( 41.64333658814960870, 66.71518717409399812, 38.42115945441014446 ) ) ;
#17521=CARTESIAN_POINT ( 'NONE',  ( 38.01140435219952707, 63.86049967264874283, 35.83527830041809636 ) ) ;
#17527=CARTESIAN_POINT ( 'NONE',  ( 41.64333658814960870, 146.5151871740939953, 30.00020018409699318 ) ) ;
#17528=CARTESIAN_POINT ( 'NONE',  ( 40.27526882409969744, 155.6651871740940010, 30.44471234641812174 ) ) ;
#17529=CARTESIAN_POINT ( 'NONE',  ( 38.58424406990785371, 105.2297705074273040, 32.77220824515697473 ) ) ;
#17530=ORIENTED_EDGE ( 'NONE', *, *, #17350, .T. ) ;
#17531=ORIENTED_EDGE ( 'NONE', *, *, #13725, .F. ) ;
#17534=CARTESIAN_POINT ( 'NONE',  ( 43.01140435219951286, 114.5344580088725479, 39.46799094044489209 ) ) ;
#17536=CARTESIAN_POINT ( 'NONE',  ( 46.59305225739526435, 76.57977050742731251, 36.81289934271958941 ) ) ;
#17537=CARTESIAN_POINT ( 'NONE',  ( 47.43856463449117200, 136.4651871740939839, 35.64915139335016647 ) ) ;
#17538=CARTESIAN_POINT ( 'NONE',  ( 48.01140435219951996, 98.21049967264875136, 34.21067981925357060 ) ) ;
#17541=CARTESIAN_POINT ( 'NONE',  ( 46.10157429594899270, 119.6604996726487258, 29.95742577749336988 ) ) ;
#17544=CARTESIAN_POINT ( 'NONE',  ( 43.01140435219951286, 144.5344580088726048, 39.21067981925356349 ) ) ;
#17545=CARTESIAN_POINT ( 'NONE',  ( 48.01140435219951996, 106.2844580088725763, 34.21067981925357060 ) ) ;
#17547=CARTESIAN_POINT ( 'NONE',  ( 46.59305225739526435, 85.57977050742732672, 36.81289934271958941 ) ) ;
#17553=CARTESIAN_POINT ( 'NONE',  ( 43.01140435219957681, 68.03445800887257633, 29.21067981925356705 ) ) ;
#17554=VECTOR ( 'NONE', #1284, 1000.000000000000000 ) ;
#17555=FACE_OUTER_BOUND ( 'NONE', #3040, .T. ) ;
#17557=CARTESIAN_POINT ( 'NONE',  ( 46.59305225739526435, 133.5797705074272983, 36.81289934271958941 ) ) ;
#17560=ORIENTED_EDGE ( 'NONE', *, *, #20616, .T. ) ;
#17563=CARTESIAN_POINT ( 'NONE',  ( 46.59305225739526435, 125.1797705074273210, 31.60846029578754468 ) ) ;
#17564=CARTESIAN_POINT ( 'NONE',  ( 43.01140435219950575, 140.0344580088726332, 29.21067981925357060 ) ) ;
#17565=CARTESIAN_POINT ( 'NONE',  ( 44.55648932407425633, 155.8104996726487741, 29.45539723777780239 ) ) ;
#17568=CARTESIAN_POINT ( 'NONE',  ( 42.21948215057684450, 100.3836182503284533, 39.21067981925355639 ) ) ;
#17569=CARTESIAN_POINT ( 'NONE',  ( 42.21948215057684450, 130.3836182503284533, 39.21067981925355639 ) ) ;
#17570=CARTESIAN_POINT ( 'NONE',  ( 45.74753988029933538, 100.1651871740939868, 37.97664729208901946 ) ) ;
#17571=CARTESIAN_POINT ( 'NONE',  ( 48.01140435219951996, 133.4344580088725820, 32.58608133808903773 ) ) ;
#17576=CARTESIAN_POINT ( 'NONE',  ( 48.01140435219951996, 136.2844580088726048, 34.21067981925357060 ) ) ;
#17577=CARTESIAN_POINT ( 'NONE',  ( 43.01140435219951286, 110.6297705074273097, 29.55568802177586463 ) ) ;
#17580=CARTESIAN_POINT ( 'NONE',  ( 44.37947211624943833, 101.2151871740939981, 30.00020018409699318 ) ) ;
#17583=CARTESIAN_POINT ( 'NONE',  ( 46.10157429594899270, 76.73445800887256496, 29.95742577749336988 ) ) ;
#17588=CARTESIAN_POINT ( 'NONE',  ( 38.58424406990785371, 75.22977050742730398, 32.77220824515697473 ) ) ;
#17591=VERTEX_POINT ( 'NONE', #8824 ) ;
#17592=CARTESIAN_POINT ( 'NONE',  ( 46.59305225739526435, 151.5797705074273267, 36.81289934271958941 ) ) ;
#17594=CARTESIAN_POINT ( 'NONE',  ( 41.46631938032478359, 121.3104996726487457, 38.96596240072933170 ) ) ;
#17595=CARTESIAN_POINT ( 'NONE',  ( 46.59305225739526435, 76.91518717409400097, 31.60846029578754468 ) ) ;
#17602=CARTESIAN_POINT ( 'NONE',  ( 46.10157429594899270, 157.7344580088726218, 29.95742577749337343 ) ) ;
#17603=CARTESIAN_POINT ( 'NONE',  ( 39.42975644700377558, 141.0797705074273267, 31.60846029578754468 ) ) ;
#17605=CARTESIAN_POINT ( 'NONE',  ( 46.59305225739526435, 124.9151871740940010, 31.60846029578754468 ) ) ;
#17611=CARTESIAN_POINT ( 'NONE',  ( 38.96631938032478359, 121.0104996726487343, 37.14960608071593384 ) ) ;
#17612=CARTESIAN_POINT ( 'NONE',  ( 46.59305225739526435, 109.9151871740940010, 31.60846029578754468 ) ) ;
#17617=CARTESIAN_POINT ( 'NONE',  ( 38.01140435219951996, 92.93445800887258201, 35.83527830041810347 ) ) ;
#17619=CARTESIAN_POINT ( 'NONE',  ( 43.01140435219951286, 149.6297705074273097, 29.55568802177586107 ) ) ;
#17620=CARTESIAN_POINT ( 'NONE',  ( 47.05648932407426344, 146.5104996726487627, 31.27175355779120025 ) ) ;
#17621=CARTESIAN_POINT ( 'NONE',  ( 41.64333658814960870, 108.7151871740940123, 38.42115945441014446 ) ) ;
#17623=( BOUNDED_CURVE ( )  B_SPLINE_CURVE ( 2, ( #14770, #1330, #21729, #13233, #21513, #16642, #19628, #2764, #1221, #21400, #8283, #6287, #4521 ),
 .UNSPECIFIED., .F., .F. ) 
 B_SPLINE_CURVE_WITH_KNOTS ( ( 3, 2, 2, 2, 2, 2, 3 ),
 ( 0.4485294117647058987, 0.4500000000000000111, 0.4529411764705882359, 0.4558823529411764608, 0.4588235294117646856, 0.4617647058823529660, 0.4632352941176470784 ),
 .UNSPECIFIED. ) 
 CURVE ( )  GEOMETRIC_REPRESENTATION_ITEM ( )  RATIONAL_B_SPLINE_CURVE ( ( 0.9755282581475768211, 0.9755282581475768211, 1.000000000000000000, 0.9510565162951535312, 1.000000000000000000, 0.9510565162951535312, 1.000000000000000000, 0.9510565162951535312, 1.000000000000000000, 0.9510565162951535312, 1.000000000000000000, 0.9755282581475768211, 0.9755282581475768211 ) ) 
 REPRESENTATION_ITEM ( '' )  );
#17624=CARTESIAN_POINT ( 'NONE',  ( 38.01140435219951996, 63.86049967264874283, 35.83527830041810347 ) ) ;
#17629=CARTESIAN_POINT ( 'NONE',  ( 45.74753988029933538, 73.16518717409400097, 37.97664729208901946 ) ) ;
#17633=ORIENTED_EDGE ( 'NONE', *, *, #13309, .F. ) ;
#17638=CARTESIAN_POINT ( 'NONE',  ( 38.58424406990786082, 135.1151871740940180, 34.21067981925357060 ) ) ;
#17639=CARTESIAN_POINT ( 'NONE',  ( 39.42975644700377558, 99.07977050742732672, 31.60846029578754468 ) ) ;
#17645=CARTESIAN_POINT ( 'NONE',  ( 47.05648932407426344, 112.5844580088725877, 31.27175355779120025 ) ) ;
#17647=CARTESIAN_POINT ( 'NONE',  ( 46.59305225739526435, 77.17977050742732104, 31.60846029578754468 ) ) ;
#17648=CARTESIAN_POINT ( 'NONE',  ( 39.42975644700377558, 132.4151871740940010, 36.81289934271958941 ) ) ;
#17649=CARTESIAN_POINT ( 'NONE',  ( 38.96631938032478359, 94.01049967264873430, 37.14960608071593384 ) ) ;
#17652=EDGE_CURVE ( 'NONE', #7609, #6509, #13062, .T. ) ;
#17655=CARTESIAN_POINT ( 'NONE',  ( 46.10157429594899270, 63.83445800887258059, 38.46393386101375711 ) ) ;
#17656=CARTESIAN_POINT ( 'NONE',  ( 43.01140435219951286, 143.0344580088726048, 29.21067981925356705 ) ) ;
#17657=AXIS2_PLACEMENT_3D ( 'NONE', #7441, #15902, #19225 ) ;
#17658=VERTEX_POINT ( 'NONE', #20610 ) ;
#17659=CARTESIAN_POINT ( 'NONE',  ( 47.43856463449117200, 77.02977050742731535, 32.77220824515698183 ) ) ;
#17663=AXIS2_PLACEMENT_3D ( 'NONE', #15605, #1847, #17040 ) ;
#17664=ORIENTED_EDGE ( 'NONE', *, *, #12750, .T. ) ;
#17665=CARTESIAN_POINT ( 'NONE',  ( 41.46631938032478359, 68.18445800887256780, 29.45539723777780239 ) ) ;
#17667=CARTESIAN_POINT ( 'NONE',  ( 40.27526882409969744, 135.8297705074273267, 37.97664729208901235 ) ) ;
#17668=ORIENTED_EDGE ( 'NONE', *, *, #6100, .T. ) ;
#17671=ORIENTED_EDGE ( 'NONE', *, *, #10183, .F. ) ;
#17672=CARTESIAN_POINT ( 'NONE',  ( 39.42975644700377558, 123.0797705074273267, 31.60846029578754468 ) ) ;
#17673=CARTESIAN_POINT ( 'NONE',  ( 44.55648932407425633, 138.6844580088725820, 38.96596240072933170 ) ) ;
#17676=CARTESIAN_POINT ( 'NONE',  ( 41.46631938032478359, 110.1844580088725820, 29.45539723777780239 ) ) ;
#17677=CARTESIAN_POINT ( 'NONE',  ( 41.46631938032478359, 130.3104996726487457, 38.96596240072933170 ) ) ;
#17679=CARTESIAN_POINT ( 'NONE',  ( 43.01140435219951286, 90.53445800887257633, 39.21067981925356349 ) ) ;
#17683=CARTESIAN_POINT ( 'NONE',  ( 46.10157429594899270, 130.7344580088725934, 29.95742577749337343 ) ) ;
#17684=CARTESIAN_POINT ( 'NONE',  ( 44.37947211624943833, 112.2797705074273296, 38.42115945441014446 ) ) ;
#17685=( BOUNDED_CURVE ( )  B_SPLINE_CURVE ( 2, ( #2772, #7960, #9513, #16212, #21299 ),
 .UNSPECIFIED., .F., .F. ) 
 B_SPLINE_CURVE_WITH_KNOTS ( ( 3, 2, 3 ),
 ( 0.9779411764705882026, 0.9794117647058823151, 0.9803958342062289999 ),
 .UNSPECIFIED. ) 
 CURVE ( )  GEOMETRIC_REPRESENTATION_ITEM ( )  RATIONAL_B_SPLINE_CURVE ( ( 0.9755282581475768211, 0.9755282581475768211, 1.000000000000000000, 0.9836243115514174962, 0.9782066976764471899 ) ) 
 REPRESENTATION_ITEM ( '' )  );
#17688=CARTESIAN_POINT ( 'NONE',  ( 39.42975644700377558, 93.41518717409400097, 36.81289934271958941 ) ) ;
#17691=CARTESIAN_POINT ( 'NONE',  ( 38.96631938032478359, 87.41049967264873999, 31.27175355779120025 ) ) ;
#17695=CARTESIAN_POINT ( 'NONE',  ( 43.01140435219951286, 79.12977050742732388, 38.86567161673127657 ) ) ;
#17697=ORIENTED_EDGE ( 'NONE', *, *, #12686, .F. ) ;
#17698=CARTESIAN_POINT ( 'NONE',  ( 46.59305225739526435, 158.1797705074273210, 31.60846029578754468 ) ) ;
#17700=CARTESIAN_POINT ( 'NONE',  ( 46.10157429594899270, 119.6604996726487400, 29.95742577749337343 ) ) ;
#17701=CARTESIAN_POINT ( 'NONE',  ( 41.64333658814960870, 78.71518717409399812, 38.42115945441014446 ) ) ;
#17708=CARTESIAN_POINT ( 'NONE',  ( 43.01140435219951996, 150.5344580088725763, 39.21067981925356349 ) ) ;
#17710=CARTESIAN_POINT ( 'NONE',  ( 38.58424406990786082, 129.1151871740940180, 34.21067981925357060 ) ) ;
#17711=CARTESIAN_POINT ( 'NONE',  ( 41.46631938032478359, 69.11049967264872862, 29.45539723777780239 ) ) ;
#17716=CARTESIAN_POINT ( 'NONE',  ( 40.27526882409969033, 107.6651871740940152, 30.44471234641811819 ) ) ;
#17717=EDGE_CURVE ( 'NONE', #11079, #8083, #129, .T. ) ;
#17721=CARTESIAN_POINT ( 'NONE',  ( 48.01140435219951996, 88.43445800887258201, 32.58608133808903773 ) ) ;
#17724=CARTESIAN_POINT ( 'NONE',  ( 46.10157429594899270, 149.6604996726486831, 29.95742577749337343 ) ) ;
#17725=CARTESIAN_POINT ( 'NONE',  ( 38.58424406990784661, 102.2651871740939811, 35.64915139335016647 ) ) ;
#17727=CARTESIAN_POINT ( 'NONE',  ( 38.01140435219951996, 66.86049967264874283, 35.83527830041810347 ) ) ;
#17729=CARTESIAN_POINT ( 'NONE',  ( 44.55648932407425633, 60.68445800887258201, 38.96596240072933170 ) ) ;
#17732=CARTESIAN_POINT ( 'NONE',  ( 46.59305225739526435, 73.31518717409400665, 36.81289934271958941 ) ) ;
#17734=AXIS2_PLACEMENT_3D ( 'NONE', #1888, #19868, #13139 ) ;
#17743=CARTESIAN_POINT ( 'NONE',  ( 40.27526882409969033, 135.5651871740939782, 37.97664729208901946 ) ) ;
#17744=EDGE_CURVE ( 'NONE', #20615, #1337, #19709, .T. ) ;
#17745=CARTESIAN_POINT ( 'NONE',  ( 47.43856463449117911, 154.4651871740940123, 35.64915139335015937 ) ) ;
#17746=CARTESIAN_POINT ( 'NONE',  ( 38.58424406990786082, 93.37977050742732388, 34.21067981925357060 ) ) ;
#17751=CARTESIAN_POINT ( 'NONE',  ( 48.01140435219951996, 118.4344580088725820, 32.58608133808903773 ) ) ;
#17754=CARTESIAN_POINT ( 'NONE',  ( 41.64333658814960870, 78.97977050742731819, 38.42115945441014446 ) ) ;
#17755=CARTESIAN_POINT ( 'NONE',  ( 40.27526882409969033, 134.6651871740940294, 30.44471234641811819 ) ) ;
#17756=CARTESIAN_POINT ( 'NONE',  ( 44.55648932407425633, 89.81049967264874567, 29.45539723777780239 ) ) ;
#17762=CYLINDRICAL_SURFACE ( 'NONE', #1480, 24.99999999999998579 ) ;
#17764=CARTESIAN_POINT ( 'NONE',  ( 41.64333658814960870, 72.97977050742731819, 38.42115945441014446 ) ) ;
#17770=CARTESIAN_POINT ( 'NONE',  ( 43.80332655382220253, 124.9575765865522925, 29.21067981925356705 ) ) ;
#17771=CARTESIAN_POINT ( 'NONE',  ( 38.58424406990786082, 120.3797705074273239, 34.21067981925357060 ) ) ;
#17773=VECTOR ( 'NONE', #13081, 1000.000000000000000 ) ;
#17774=CARTESIAN_POINT ( 'NONE',  ( 43.01140435219951286, 89.03445800887257633, 29.21067981925356705 ) ) ;
#17776=CARTESIAN_POINT ( 'NONE',  ( 45.74753988029933538, 127.4297705074273068, 37.97664729208901946 ) ) ;
#17778=CARTESIAN_POINT ( 'NONE',  ( 38.01140435219952707, 59.78445800887258343, 34.21067981925357060 ) ) ;
#17779=CARTESIAN_POINT ( 'NONE',  ( 38.01140435219952707, 110.7844580088725905, 34.21067981925357060 ) ) ;
#17780=CARTESIAN_POINT ( 'NONE',  ( 43.01140435219951286, 83.03445800887257633, 29.21067981925356705 ) ) ;
#17784=CARTESIAN_POINT ( 'NONE',  ( 39.92123440845005433, 67.16049967264873999, 38.46393386101375711 ) ) ;
#17788=CARTESIAN_POINT ( 'NONE',  ( 38.01140435219952707, 137.7844580088726048, 34.21067981925357060 ) ) ;
#17789=CARTESIAN_POINT ( 'NONE',  ( 38.58424406990784661, 105.2297705074273040, 32.77220824515698183 ) ) ;
#17792=CARTESIAN_POINT ( 'NONE',  ( 38.58424406990786082, 102.1151871740940180, 34.21067981925357060 ) ) ;
#17799=CARTESIAN_POINT ( 'NONE',  ( 45.74753988029934249, 79.42977050742732104, 37.97664729208901235 ) ) ;
#17802=CARTESIAN_POINT ( 'NONE',  ( 47.43856463449118621, 154.8797705074273097, 34.21067981925357060 ) ) ;
#17805=CARTESIAN_POINT ( 'NONE',  ( 44.55648932407425633, 122.8104996726487457, 29.45539723777780239 ) ) ;
#17806=CARTESIAN_POINT ( 'NONE',  ( 45.74753988029933538, 79.16518717409398675, 37.97664729208901946 ) ) ;
#17815=CARTESIAN_POINT ( 'NONE',  ( 46.59305225739526435, 133.5797705074272983, 36.81289934271958941 ) ) ;
#17818=CARTESIAN_POINT ( 'NONE',  ( 39.42975644700377558, 129.4151871740940010, 36.81289934271958941 ) ) ;
#17823=AXIS2_PLACEMENT_3D ( 'NONE', #14367, #10537, #7445 ) ;
#17824=CARTESIAN_POINT ( 'NONE',  ( 41.46631938032478359, 135.1104996726487286, 29.45539723777780239 ) ) ;
#17825=EDGE_CURVE ( 'NONE', #20615, #2815, #13892, .T. ) ;
#17827=CARTESIAN_POINT ( 'NONE',  ( 43.01140435219951996, 10.71049967264875491, 29.21067981925357060 ) ) ;
#17828=CARTESIAN_POINT ( 'NONE',  ( 46.59305225739526435, 106.3151871740939924, 36.81289934271958941 ) ) ;
#17830=CARTESIAN_POINT ( 'NONE',  ( 44.55648932407425633, 86.81049967264874567, 29.45539723777780239 ) ) ;
#17831=EDGE_LOOP ( 'NONE', ( #14721, #7607, #20643, #21186 ) ) ;
#17832=CARTESIAN_POINT ( 'NONE',  ( 48.01140435219951996, 91.28445800887257633, 34.21067981925357060 ) ) ;
#17833=DIRECTION ( 'NONE',  ( 0.000000000000000000, 1.000000000000000000, 0.000000000000000000 ) ) ;
#17835=CARTESIAN_POINT ( 'NONE',  ( 43.01140435219951286, 149.9604996726487514, 28.95336869806222779 ) ) ;
#17836=CARTESIAN_POINT ( 'NONE',  ( 38.58424406990784661, 108.2651871740939953, 35.64915139335016647 ) ) ;
#17838=CARTESIAN_POINT ( 'NONE',  ( 41.46631938032478359, 64.31049967264873146, 38.96596240072933170 ) ) ;
#17845=CARTESIAN_POINT ( 'NONE',  ( 40.27526882409969033, 158.9297705074272642, 30.44471234641811819 ) ) ;
#17850=CARTESIAN_POINT ( 'NONE',  ( 43.01140435219951286, 66.86518717409397539, 38.86567161673127657 ) ) ;
#17854=CARTESIAN_POINT ( 'NONE',  ( 44.37947211624943833, 133.0151871740939953, 38.42115945441014446 ) ) ;
#17855=CARTESIAN_POINT ( 'NONE',  ( 45.74753988029934249, 154.1651871740939725, 37.97664729208901235 ) ) ;
#17856=VERTEX_POINT ( 'NONE', #16284 ) ;
#17860=CARTESIAN_POINT ( 'NONE',  ( 48.01140435219951996, 118.1344580088725849, 35.83527830041810347 ) ) ;
#17861=CARTESIAN_POINT ( 'NONE',  ( 47.43856463449117200, 73.72977050742731819, 35.64915139335016647 ) ) ;
#17862=CARTESIAN_POINT ( 'NONE',  ( 44.37947211624943833, 137.2151871740940123, 30.00020018409699318 ) ) ;
#17864=CARTESIAN_POINT ( 'NONE',  ( 43.01140435219951286, 94.46049967264872294, 39.46799094044489209 ) ) ;
#17872=CARTESIAN_POINT ( 'NONE',  ( 38.58424406990784661, 75.22977050742730398, 32.77220824515698183 ) ) ;
#17879=CARTESIAN_POINT ( 'NONE',  ( 46.59305225739526435, 124.5797705074273267, 36.81289934271958941 ) ) ;
#17881=CARTESIAN_POINT ( 'NONE',  ( 47.05648932407426344, 87.98445800887257917, 37.14960608071593384 ) ) ;
#17883=CARTESIAN_POINT ( 'NONE',  ( 41.64333658814960870, 123.9797705074273324, 38.42115945441014446 ) ) ;
#17885=CARTESIAN_POINT ( 'NONE',  ( 44.37947211624943833, 88.27977050742731535, 38.42115945441014446 ) ) ;
#17886=CARTESIAN_POINT ( 'NONE',  ( 47.05648932407426344, 61.58445800887258059, 31.27175355779120025 ) ) ;
#17892=CARTESIAN_POINT ( 'NONE',  ( 44.55648932407425633, 73.61049967264874283, 38.96596240072933170 ) ) ;
#17893=CARTESIAN_POINT ( 'NONE',  ( 38.01140435219952707, 102.5604996726487457, 32.58608133808903773 ) ) ;
#17896=CARTESIAN_POINT ( 'NONE',  ( 41.46631938032478359, 125.1844580088725678, 29.45539723777780239 ) ) ;
#17897=CARTESIAN_POINT ( 'NONE',  ( 47.43856463449117200, 107.0297705074273154, 32.77220824515698183 ) ) ;
#17900=CARTESIAN_POINT ( 'NONE',  ( 47.43856463449117911, 97.46518717409399812, 35.64915139335015937 ) ) ;
#17902=ORIENTED_EDGE ( 'NONE', *, *, #16785, .F. ) ;
#17905=CARTESIAN_POINT ( 'NONE',  ( 40.27526882409969744, 144.8297705074273267, 37.97664729208901235 ) ) ;
#17908=CARTESIAN_POINT ( 'NONE',  ( 39.42975644700377558, 69.67977050742732104, 36.81289934271958941 ) ) ;
#17911=CARTESIAN_POINT ( 'NONE',  ( 40.27526882409969033, 150.8297705074273267, 37.97664729208901946 ) ) ;
#17913=CARTESIAN_POINT ( 'NONE',  ( 43.01140435219951286, 113.9604996726487371, 28.95336869806222779 ) ) ;
#17914=CARTESIAN_POINT ( 'NONE',  ( 45.74753988029933538, 65.06518717409400665, 30.44471234641811819 ) ) ;
#17922=CARTESIAN_POINT ( 'NONE',  ( 43.01140435219951286, 155.0344580088725479, 28.95336869806222779 ) ) ;
#17923=EDGE_CURVE ( 'NONE', #7690, #13353, #21479, .T. ) ;
#17924=CARTESIAN_POINT ( 'NONE',  ( 38.58424406990784661, 129.5297705074273154, 35.64915139335016647 ) ) ;
#17926=CARTESIAN_POINT ( 'NONE',  ( 44.37947211624943833, 124.0151871740939953, 38.42115945441014446 ) ) ;
#17928=CARTESIAN_POINT ( 'NONE',  ( 46.10157429594899270, 65.66049967264873999, 29.95742577749336988 ) ) ;
#17929=CARTESIAN_POINT ( 'NONE',  ( 43.01140435219951996, 10.71049967264875491, 29.21067981925357060 ) ) ;
#17931=CARTESIAN_POINT ( 'NONE',  ( 48.01140435219951996, 83.36049967264872862, 32.58608133808903773 ) ) ;
#17932=ORIENTED_EDGE ( 'NONE', *, *, #20457, .F. ) ;
#17934=CARTESIAN_POINT ( 'NONE',  ( 47.05648932407426344, 85.91049967264873999, 37.14960608071593384 ) ) ;
#17937=CARTESIAN_POINT ( 'NONE',  ( 48.01140435219951996, 82.13445800887255643, 35.83527830041810347 ) ) ;
#17941=CARTESIAN_POINT ( 'NONE',  ( 48.01140435219951996, 146.0604996726487457, 35.83527830041810347 ) ) ;
#17942=CARTESIAN_POINT ( 'NONE',  ( 43.01140435219951286, 93.86518717409400381, 38.86567161673127657 ) ) ;
#17946=CARTESIAN_POINT ( 'NONE',  ( 43.01140435219951286, 67.46049967264873715, 39.46799094044489209 ) ) ;
#17949=CARTESIAN_POINT ( 'NONE',  ( 38.96631938032478359, 106.0104996726487485, 37.14960608071593384 ) ) ;
#17952=CARTESIAN_POINT ( 'NONE',  ( 44.37947211624943833, 64.01518717409400949, 38.42115945441014446 ) ) ;
#17955=CARTESIAN_POINT ( 'NONE',  ( 45.74753988029934249, 151.1651871740940010, 37.97664729208901235 ) ) ;
#17956=CARTESIAN_POINT ( 'NONE',  ( 43.80332655382222384, 94.53738109496902098, 39.21067981925354928 ) ) ;
#17959=ORIENTED_EDGE ( 'NONE', *, *, #88, .T. ) ;
#17960=CARTESIAN_POINT ( 'NONE',  ( 47.43856463449118621, 70.61518717409400381, 34.21067981925357060 ) ) ;
#17964=CARTESIAN_POINT ( 'NONE',  ( 38.58424406990786082, 138.1151871740940180, 34.21067981925357060 ) ) ;
#17967=ORIENTED_EDGE ( 'NONE', *, *, #588, .T. ) ;
#17971=ADVANCED_FACE ( 'NONE', ( #13595 ), #15257, .T. ) ;
#17972=CARTESIAN_POINT ( 'NONE',  ( 43.01140435219951286, 77.62977050742729546, 29.55568802177586463 ) ) ;
#17973=CARTESIAN_POINT ( 'NONE',  ( 45.74753988029933538, 134.0651871740939498, 30.44471234641811819 ) ) ;
#17974=CARTESIAN_POINT ( 'NONE',  ( 47.05648932407426344, 89.51049967264873430, 31.27175355779120025 ) ) ;
#17978=CARTESIAN_POINT ( 'NONE',  ( 39.42975644700377558, 87.41518717409401518, 36.81289934271958941 ) ) ;
#17979=CARTESIAN_POINT ( 'NONE',  ( 48.01140435219951996, 151.2844580088725763, 34.21067981925357060 ) ) ;
#17980=CARTESIAN_POINT ( 'NONE',  ( 48.01140435219951996, 109.2844580088725905, 34.21067981925357060 ) ) ;
#17981=CARTESIAN_POINT ( 'NONE',  ( 43.01140435219951286, 124.4604996726487371, 39.21067981925356349 ) ) ;
#17983=CARTESIAN_POINT ( 'NONE',  ( 41.64333658814960870, 77.77977050742731535, 30.00020018409699318 ) ) ;
#17987=ORIENTED_EDGE ( 'NONE', *, *, #21778, .T. ) ;
#17990=CARTESIAN_POINT ( 'NONE',  ( 47.43856463449118621, 121.8797705074273239, 34.21067981925357060 ) ) ;
#17994=EDGE_LOOP ( 'NONE', ( #3645, #11355, #10427, #18160 ) ) ;
#17995=CARTESIAN_POINT ( 'NONE',  ( 43.01140435219951286, 128.6297705074273097, 29.55568802177586463 ) ) ;
#17996=CARTESIAN_POINT ( 'NONE',  ( 41.46631938032478359, 73.31049967264874567, 38.96596240072933170 ) ) ;
#17997=CARTESIAN_POINT ( 'NONE',  ( 45.74753988029933538, 88.42977050742729261, 37.97664729208901946 ) ) ;
#17998=CARTESIAN_POINT ( 'NONE',  ( 47.05648932407426344, 64.58445800887258770, 31.27175355779120025 ) ) ;
#18002=CARTESIAN_POINT ( 'NONE',  ( 43.01140435219951286, 101.0344580088725621, 29.21067981925356705 ) ) ;
#18006=CARTESIAN_POINT ( 'NONE',  ( 45.22504609509771001, 59.11591859955431971, 30.37668211462113277 ) ) ;
#18010=CARTESIAN_POINT ( 'NONE',  ( 43.01140435219951286, 120.5344580088725763, 39.46799094044489209 ) ) ;
#18011=CARTESIAN_POINT ( 'NONE',  ( 39.42975644700377558, 99.67977050742732104, 36.81289934271958941 ) ) ;
#18014=CARTESIAN_POINT ( 'NONE',  ( 43.01140435219951286, 99.86518717409401802, 38.86567161673127657 ) ) ;
#18016=ORIENTED_EDGE ( 'NONE', *, *, #5675, .T. ) ;
#18017=CARTESIAN_POINT ( 'NONE',  ( 43.01140435219951996, 10.71049967264875491, 34.21067981925357060 ) ) ;
#18019=CARTESIAN_POINT ( 'NONE',  ( 41.64333658814960870, 144.9797705074273324, 38.42115945441014446 ) ) ;
#18024=CARTESIAN_POINT ( 'NONE',  ( 46.59305225739526435, 67.57977050742732672, 36.81289934271958941 ) ) ;
#18027=CARTESIAN_POINT ( 'NONE',  ( 47.43856463449117200, 158.0297705074273438, 32.77220824515698183 ) ) ;
#18030=CARTESIAN_POINT ( 'NONE',  ( 44.55648932407425633, 113.8104996726487457, 29.45539723777780239 ) ) ;
#18031=CARTESIAN_POINT ( 'NONE',  ( 39.42975644700377558, 65.81518717409400665, 31.60846029578754468 ) ) ;
#18036=CARTESIAN_POINT ( 'NONE',  ( 38.01140435219952707, 152.7844580088725763, 34.21067981925357060 ) ) ;
#18037=CARTESIAN_POINT ( 'NONE',  ( 43.01140435219951286, 131.6297705074273381, 29.55568802177586463 ) ) ;
#18039=CARTESIAN_POINT ( 'NONE',  ( 46.59305225739526435, 127.9151871740940010, 31.60846029578754468 ) ) ;
#18043=CARTESIAN_POINT ( 'NONE',  ( 43.80332655382220963, 148.5373810949689926, 39.21067981925356349 ) ) ;
#18048=ORIENTED_EDGE ( 'NONE', *, *, #14083, .F. ) ;
#18049=CARTESIAN_POINT ( 'NONE',  ( 38.01140435219952707, 80.78445800887257633, 34.21067981925357060 ) ) ;
#18051=CARTESIAN_POINT ( 'NONE',  ( 44.55648932407425633, 139.6104996726487286, 38.96596240072933170 ) ) ;
#18052=CARTESIAN_POINT ( 'NONE',  ( 47.43856463449117200, 94.46518717409398391, 35.64915139335016647 ) ) ;
#18057=CARTESIAN_POINT ( 'NONE',  ( 39.92123440845004723, 66.26049967264874851, 29.95742577749337343 ) ) ;
#18060=CARTESIAN_POINT ( 'NONE',  ( 43.01140435219951286, 106.4604996726487371, 39.21067981925356349 ) ) ;
#18062=CARTESIAN_POINT ( 'NONE',  ( 44.55648932407425633, 145.6104996726487570, 38.96596240072933170 ) ) ;
#18064=CARTESIAN_POINT ( 'NONE',  ( 46.59305225739526435, 158.1797705074273210, 31.60846029578754468 ) ) ;
#18066=CARTESIAN_POINT ( 'NONE',  ( 39.42975644700377558, 152.8151871740940067, 31.60846029578754468 ) ) ;
#18070=CARTESIAN_POINT ( 'NONE',  ( 41.64333658814960870, 72.71518717409399812, 38.42115945441014446 ) ) ;
#18074=CARTESIAN_POINT ( 'NONE',  ( 39.42975644700377558, 137.8151871740940067, 31.60846029578754468 ) ) ;
#18078=ORIENTED_EDGE ( 'NONE', *, *, #14083, .T. ) ;
#18082=CARTESIAN_POINT ( 'NONE',  ( 48.01140435219951996, 116.3604996726487286, 32.58608133808903773 ) ) ;
#18083=CARTESIAN_POINT ( 'NONE',  ( 43.01140435219951286, 68.62977050742729546, 29.55568802177586463 ) ) ;
#18084=CARTESIAN_POINT ( 'NONE',  ( 39.42975644700377558, 123.4151871740940010, 36.81289934271958941 ) ) ;
#18087=CARTESIAN_POINT ( 'NONE',  ( 39.92123440845004723, 96.26049967264873430, 29.95742577749337343 ) ) ;
#18089=CARTESIAN_POINT ( 'NONE',  ( 43.01140435219951996, 10.71049967264875491, 34.21067981925357060 ) ) ;
#18091=CARTESIAN_POINT ( 'NONE',  ( 45.74753988029933538, 85.16518717409400097, 37.97664729208901946 ) ) ;
#18093=LINE ( 'NONE', #21420, #2874 ) ;
#18094=ORIENTED_EDGE ( 'NONE', *, *, #3602, .F. ) ;
#18095=CARTESIAN_POINT ( 'NONE',  ( 41.64333658814960870, 74.77977050742731535, 30.00020018409699318 ) ) ;
#18105=CARTESIAN_POINT ( 'NONE',  ( 40.27526882409969744, 120.8297705074273125, 37.97664729208901235 ) ) ;
#18106=ORIENTED_EDGE ( 'NONE', *, *, #5672, .F. ) ;
#18107=CARTESIAN_POINT ( 'NONE',  ( 43.80332655382220253, 88.95757658655229250, 29.21067981925356705 ) ) ;
#18109=CARTESIAN_POINT ( 'NONE',  ( 38.96631938032478359, 72.41049967264873999, 31.27175355779120025 ) ) ;
#18110=CARTESIAN_POINT ( 'NONE',  ( 40.27526882409969033, 152.6651871740940010, 30.44471234641811819 ) ) ;
#18115=CARTESIAN_POINT ( 'NONE',  ( 43.01140435219951286, 73.46049967264872294, 39.21067981925356349 ) ) ;
#18119=CARTESIAN_POINT ( 'NONE',  ( 44.55648932407425633, 118.8844580088725849, 29.45539723777780239 ) ) ;
#18120=CARTESIAN_POINT ( 'NONE',  ( 47.43856463449117200, 103.7297705074273182, 35.64915139335016647 ) ) ;
#18123=CARTESIAN_POINT ( 'NONE',  ( 38.58424406990785371, 89.96518717409399812, 32.77220824515697473 ) ) ;
#18126=VERTEX_POINT ( 'NONE', #16900 ) ;
#18130=CARTESIAN_POINT ( 'NONE',  ( 44.37947211624943833, 68.47977050742731819, 30.00020018409699318 ) ) ;
#18131=B_SPLINE_CURVE_WITH_KNOTS ( 'NONE', 3,
 ( #4709, #11427, #8138, #4820 ),
 .UNSPECIFIED., .F., .F.,
 ( 4, 4 ),
 ( 0.000000000000000000, 1.000000000000000000 ),
 .UNSPECIFIED. ) ;
#18133=ORIENTED_EDGE ( 'NONE', *, *, #20409, .T. ) ;
#18134=CARTESIAN_POINT ( 'NONE',  ( 44.37947211624943833, 146.4797705074273324, 30.00020018409699318 ) ) ;
#18135=( BOUNDED_CURVE ( )  B_SPLINE_CURVE ( 2, ( #17216, #18883, #3792, #2134, #8866, #15574, #13914, #10624, #5536, #15677, #581, #14350, #6303 ),
 .UNSPECIFIED., .F., .F. ) 
 B_SPLINE_CURVE_WITH_KNOTS ( ( 3, 2, 2, 2, 2, 2, 3 ),
 ( 0.9632352941176470784, 0.9647058823529411908, 0.9676470588235294157, 0.9705882352941176405, 0.9735294117647058654, 0.9764705882352940902, 0.9779411764705882026 ),
 .UNSPECIFIED. ) 
 CURVE ( )  GEOMETRIC_REPRESENTATION_ITEM ( )  RATIONAL_B_SPLINE_CURVE ( ( 0.9755282581475768211, 0.9755282581475768211, 1.000000000000000000, 0.9510565162951535312, 1.000000000000000000, 0.9510565162951535312, 1.000000000000000000, 0.9510565162951535312, 1.000000000000000000, 0.9510565162951535312, 1.000000000000000000, 0.9755282581475768211, 0.9755282581475768211 ) ) 
 REPRESENTATION_ITEM ( '' )  );
#18138=CARTESIAN_POINT ( 'NONE',  ( 43.01140435219951286, 109.4604996726487514, 39.46799094044489209 ) ) ;
#18139=CARTESIAN_POINT ( 'NONE',  ( 39.42975644700377558, 68.81518717409400665, 31.60846029578754468 ) ) ;
#18140=CARTESIAN_POINT ( 'NONE',  ( 38.96631938032478359, 65.48445800887257917, 31.27175355779120025 ) ) ;
#18145=CARTESIAN_POINT ( 'NONE',  ( 42.21948215057684450, 112.3836182503284675, 39.21067981925355639 ) ) ;
#18146=CARTESIAN_POINT ( 'NONE',  ( 47.05648932407426344, 147.9844580088725934, 37.14960608071593384 ) ) ;
#18147=CARTESIAN_POINT ( 'NONE',  ( 46.59305225739526435, 128.1797705074273210, 31.60846029578754468 ) ) ;
#18149=CARTESIAN_POINT ( 'NONE',  ( 46.59305225739526435, 112.9151871740940010, 31.60846029578754468 ) ) ;
#18154=CARTESIAN_POINT ( 'NONE',  ( 46.10157429594899270, 148.7604996726487627, 38.46393386101375711 ) ) ;
#18156=CARTESIAN_POINT ( 'NONE',  ( 38.96631938032478359, 120.4104996726487400, 31.27175355779120025 ) ) ;
#18157=CARTESIAN_POINT ( 'NONE',  ( 45.74753988029934249, 98.32977050742731251, 30.44471234641812174 ) ) ;
#18158=EDGE_LOOP ( 'NONE', ( #19353, #16067, #2415, #12420, #57, #20749, #4640, #699, #14118, #15388, #7738, #8751, #5746, #20295, #7581, #10512, #15755, #5581, #1009, #2392, #1439, #19099, #14766, #19600, #19541, #21157, #13899, #17967, #20691, #7528, #20832, #5638, #5822, #4580, #14227, #9455, #11239, #4412, #19010, #4334, #1170, #4634, #18521, #12171, #18016, #4311, #14204, #21406, #16638, #11086, #15214, #2844, #15557, #3454, #19258, #357, #9311, #12931, #8878, #9537, #18278, #9779, #2739, #11142, #12771, #3663, #14502, #7195, #16344, #4309, #18686 ) ) ;
#18160=ORIENTED_EDGE ( 'NONE', *, *, #1837, .F. ) ;
#18161=CARTESIAN_POINT ( 'NONE',  ( 44.55648932407425633, 85.88445800887258486, 29.45539723777780239 ) ) ;
#18163=CARTESIAN_POINT ( 'NONE',  ( 38.01140435219951996, 135.8604996726487002, 35.83527830041810347 ) ) ;
#18164=CARTESIAN_POINT ( 'NONE',  ( 38.58424406990784661, 96.26518717409400949, 35.64915139335016647 ) ) ;
#18175=CARTESIAN_POINT ( 'NONE',  ( 43.80332655382220253, 114.6113394311928317, 39.21067981925355639 ) ) ;
#18177=CARTESIAN_POINT ( 'NONE',  ( 45.74753988029933538, 62.06518717409399244, 30.44471234641811819 ) ) ;
#18178=CARTESIAN_POINT ( 'NONE',  ( 38.01140435219952707, 62.63445800887255643, 32.58608133808903773 ) ) ;
#18180=CARTESIAN_POINT ( 'NONE',  ( 47.43856463449118621, 145.6151871740939896, 34.21067981925357060 ) ) ;
#18184=CARTESIAN_POINT ( 'NONE',  ( 38.58424406990786082, 69.11518717409400381, 34.21067981925357060 ) ) ;
#18188=CARTESIAN_POINT ( 'NONE',  ( 47.43856463449117200, 127.4651871740940123, 35.64915139335016647 ) ) ;
#18194=ORIENTED_EDGE ( 'NONE', *, *, #17717, .F. ) ;
#18195=CARTESIAN_POINT ( 'NONE',  ( 41.46631938032478359, 108.3844580088725849, 38.96596240072933170 ) ) ;
#18196=DIRECTION ( 'NONE',  ( 0.000000000000000000, 1.000000000000000000, 0.000000000000000000 ) ) ;
#18197=CARTESIAN_POINT ( 'NONE',  ( 41.64333658814960870, 62.77977050742732246, 30.00020018409699318 ) ) ;
#18198=CARTESIAN_POINT ( 'NONE',  ( 44.37947211624943833, 122.2151871740940123, 30.00020018409699318 ) ) ;
#18200=CARTESIAN_POINT ( 'NONE',  ( 47.05648932407426344, 83.51049967264874851, 31.27175355779120025 ) ) ;
#18204=CARTESIAN_POINT ( 'NONE',  ( 47.43856463449117200, 85.76518717409398107, 32.77220824515698183 ) ) ;
#18205=CARTESIAN_POINT ( 'NONE',  ( 43.01140435219951286, 106.4604996726487371, 39.21067981925356349 ) ) ;
#18207=CARTESIAN_POINT ( 'NONE',  ( 46.10157429594899270, 142.7344580088725650, 29.95742577749336988 ) ) ;
#18210=CARTESIAN_POINT ( 'NONE',  ( 41.64333658814960870, 68.77977050742731535, 30.00020018409699318 ) ) ;
#18211=( BOUNDED_CURVE ( )  B_SPLINE_CURVE ( 2, ( #20154, #15067, #4399, #21285, #11647, #2756, #887, #16088, #1213, #21170, #21804, #7735, #1106 ),
 .UNSPECIFIED., .F., .F. ) 
 B_SPLINE_CURVE_WITH_KNOTS ( ( 3, 2, 2, 2, 2, 2, 3 ),
 ( 0.4338235294117647189, 0.4352941176470588314, 0.4382352941176470562, 0.4411764705882352811, 0.4441176470588235059, 0.4470588235294117863, 0.4485294117647058987 ),
 .UNSPECIFIED. ) 
 CURVE ( )  GEOMETRIC_REPRESENTATION_ITEM ( )  RATIONAL_B_SPLINE_CURVE ( ( 0.9755282581475768211, 0.9755282581475768211, 1.000000000000000000, 0.9510565162951535312, 1.000000000000000000, 0.9510565162951535312, 1.000000000000000000, 0.9510565162951535312, 1.000000000000000000, 0.9510565162951535312, 1.000000000000000000, 0.9755282581475768211, 0.9755282581475768211 ) ) 
 REPRESENTATION_ITEM ( '' )  );
#18218=CARTESIAN_POINT ( 'NONE',  ( 41.64333658814960870, 114.9797705074273324, 38.42115945441014446 ) ) ;
#18225=CARTESIAN_POINT ( 'NONE',  ( 40.27526882409969033, 116.9297705074273210, 30.44471234641811819 ) ) ;
#18229=CARTESIAN_POINT ( 'NONE',  ( 47.43856463449118621, 85.87977050742730967, 34.21067981925357060 ) ) ;
#18230=CARTESIAN_POINT ( 'NONE',  ( 39.42975644700377558, 150.4151871740940010, 36.81289934271958941 ) ) ;
#18236=CARTESIAN_POINT ( 'NONE',  ( 38.01140435219952707, 89.93445800887256780, 35.83527830041809636 ) ) ;
#18237=CARTESIAN_POINT ( 'NONE',  ( 48.01140435219951996, 94.43445800887256780, 32.58608133808903773 ) ) ;
#18239=CARTESIAN_POINT ( 'NONE',  ( 48.01140435219951996, 124.2844580088725905, 34.21067981925357060 ) ) ;
#18240=CARTESIAN_POINT ( 'NONE',  ( 40.27526882409969033, 93.82977050742731251, 37.97664729208901946 ) ) ;
#18243=CARTESIAN_POINT ( 'NONE',  ( 40.27526882409969744, 92.66518717409400097, 30.44471234641812174 ) ) ;
#18245=DIRECTION ( 'NONE',  ( 0.000000000000000000, 0.000000000000000000, 1.000000000000000000 ) ) ;
#18249=CARTESIAN_POINT ( 'NONE',  ( 46.59305225739526435, 145.5797705074273267, 36.81289934271958941 ) ) ;
#18251=CARTESIAN_POINT ( 'NONE',  ( 47.43856463449117200, 109.4651871740940123, 35.64915139335016647 ) ) ;
#18252=CARTESIAN_POINT ( 'NONE',  ( 41.64333658814960870, 68.77977050742731535, 30.00020018409699318 ) ) ;
#18254=CARTESIAN_POINT ( 'NONE',  ( 40.27526882409969033, 143.9297705074273210, 30.44471234641811819 ) ) ;
#18255=CARTESIAN_POINT ( 'NONE',  ( 45.74753988029933538, 97.42977050742730682, 37.97664729208901946 ) ) ;
#18256=CARTESIAN_POINT ( 'NONE',  ( 41.46631938032478359, 142.3104996726487457, 38.96596240072933170 ) ) ;
#18257=CARTESIAN_POINT ( 'NONE',  ( 41.46631938032478359, 111.1104996726487428, 29.45539723777780239 ) ) ;
#18258=CARTESIAN_POINT ( 'NONE',  ( 47.43856463449117200, 64.46518717409398391, 35.64915139335016647 ) ) ;
#18263=DIRECTION ( 'NONE',  ( 0.000000000000000000, 0.000000000000000000, 1.000000000000000000 ) ) ;
#18264=CARTESIAN_POINT ( 'NONE',  ( 38.96631938032478359, 155.4844580088725934, 31.27175355779120025 ) ) ;
#18265=CARTESIAN_POINT ( 'NONE',  ( 44.37947211624943833, 137.4797705074273324, 30.00020018409699318 ) ) ;
#18267=CARTESIAN_POINT ( 'NONE',  ( 39.42975644700377558, 119.8151871740940067, 31.60846029578754468 ) ) ;
#18270=CARTESIAN_POINT ( 'NONE',  ( 47.05648932407426344, 139.9104996726487400, 37.14960608071593384 ) ) ;
#18276=CARTESIAN_POINT ( 'NONE',  ( 39.42975644700377558, 96.07977050742731251, 31.60846029578754468 ) ) ;
#18277=( BOUNDED_CURVE ( )  B_SPLINE_CURVE ( 2, ( #9027, #18946, #7160, #20709, #12317, #3846, #750, #10786, #12431, #13863, #19053, #19157, #13970 ),
 .UNSPECIFIED., .F., .F. ) 
 B_SPLINE_CURVE_WITH_KNOTS ( ( 3, 2, 2, 2, 2, 2, 3 ),
 ( 0.7573529411764705621, 0.7588235294117646745, 0.7617647058823528994, 0.7647058823529411242, 0.7676470588235294601, 0.7705882352941176849, 0.7720588235294117974 ),
 .UNSPECIFIED. ) 
 CURVE ( )  GEOMETRIC_REPRESENTATION_ITEM ( )  RATIONAL_B_SPLINE_CURVE ( ( 0.9755282581475768211, 0.9755282581475768211, 1.000000000000000000, 0.9510565162951535312, 1.000000000000000000, 0.9510565162951535312, 1.000000000000000000, 0.9510565162951535312, 1.000000000000000000, 0.9510565162951535312, 1.000000000000000000, 0.9755282581475768211, 0.9755282581475768211 ) ) 
 REPRESENTATION_ITEM ( '' )  );
#18278=ORIENTED_EDGE ( 'NONE', *, *, #19879, .T. ) ;
#18281=CARTESIAN_POINT ( 'NONE',  ( 43.01140435219951286, 81.53445800887257633, 39.46799094044489209 ) ) ;
#18282=CARTESIAN_POINT ( 'NONE',  ( 48.01140435219951996, 103.4344580088725678, 32.58608133808903773 ) ) ;
#18283=CARTESIAN_POINT ( 'NONE',  ( 46.10157429594899270, 136.7604996726487627, 38.46393386101376421 ) ) ;
#18284=CARTESIAN_POINT ( 'NONE',  ( 41.64333658814960870, 92.51518717409399528, 30.00020018409699318 ) ) ;
#18292=CARTESIAN_POINT ( 'NONE',  ( 39.92123440845005433, 147.2604996726487343, 29.95742577749336988 ) ) ;
#18293=CARTESIAN_POINT ( 'NONE',  ( 43.01140435219951286, 77.96049967264873715, 29.21067981925356705 ) ) ;
#18294=CARTESIAN_POINT ( 'NONE',  ( 38.58424406990786082, 63.11518717409400381, 34.21067981925357060 ) ) ;
#18295=LINE ( 'NONE', #8274, #13642 ) ;
#18297=CARTESIAN_POINT ( 'NONE',  ( 44.37947211624943833, 149.2151871740940123, 30.00020018409699318 ) ) ;
#18300=ORIENTED_EDGE ( 'NONE', *, *, #17744, .F. ) ;
#18301=CARTESIAN_POINT ( 'NONE',  ( 41.46631938032478359, 77.18445800887258201, 29.45539723777780239 ) ) ;
#18304=CARTESIAN_POINT ( 'NONE',  ( 45.74753988029933538, 125.0651871740940209, 30.44471234641811819 ) ) ;
#18308=EDGE_CURVE ( 'NONE', #10912, #9101, #16854, .T. ) ;
#18310=CARTESIAN_POINT ( 'NONE',  ( 39.92123440845005433, 147.2344580088725934, 38.46393386101375711 ) ) ;
#18312=CARTESIAN_POINT ( 'NONE',  ( 38.96631938032478359, 107.4844580088725792, 31.27175355779120025 ) ) ;
#18313=CARTESIAN_POINT ( 'NONE',  ( 39.42975644700377558, 159.0797705074273267, 31.60846029578754468 ) ) ;
#18314=CARTESIAN_POINT ( 'NONE',  ( 46.59305225739526435, 71.17977050742730682, 31.60846029578754468 ) ) ;
#18315=CARTESIAN_POINT ( 'NONE',  ( 41.64333658814960870, 125.5151871740939953, 30.00020018409699318 ) ) ;
#18317=CARTESIAN_POINT ( 'NONE',  ( 38.01140435219951996, 78.86049967264871441, 35.83527830041810347 ) ) ;
#18319=CARTESIAN_POINT ( 'NONE',  ( 38.96631938032478359, 144.4104996726487400, 31.27175355779120025 ) ) ;
#18321=CARTESIAN_POINT ( 'NONE',  ( 47.43856463449118621, 88.61518717409400381, 34.21067981925357060 ) ) ;
#18324=CARTESIAN_POINT ( 'NONE',  ( 43.01140435219953417, 141.5344580088726048, 39.21067981925356349 ) ) ;
#18325=STYLED_ITEM ( 'NONE', ( #13018 ), #62 ) ;
#18327=CARTESIAN_POINT ( 'NONE',  ( 41.64333658814960870, 62.77977050742732246, 30.00020018409699318 ) ) ;
#18332=CARTESIAN_POINT ( 'NONE',  ( 46.59305225739526435, 157.9151871740940010, 31.60846029578754468 ) ) ;
#18334=CARTESIAN_POINT ( 'NONE',  ( 45.74753988029934249, 115.4297705074273068, 37.97664729208901235 ) ) ;
#18339=CARTESIAN_POINT ( 'NONE',  ( 38.58424406990786082, 120.3797705074273239, 34.21067981925357060 ) ) ;
#18340=DIRECTION ( 'NONE',  ( 0.000000000000000000, 1.000000000000000000, 0.000000000000000000 ) ) ;
#18341=CARTESIAN_POINT ( 'NONE',  ( 40.27526882409969033, 84.82977050742732672, 37.97664729208901946 ) ) ;
#18342=CARTESIAN_POINT ( 'NONE',  ( 47.43856463449117200, 157.4651871740940123, 35.64915139335016647 ) ) ;
#18344=CARTESIAN_POINT ( 'NONE',  ( 39.92123440845005433, 107.3344580088725877, 29.95742577749336988 ) ) ;
#18348=CARTESIAN_POINT ( 'NONE',  ( 41.46631938032478359, 90.38445800887258486, 38.96596240072933170 ) ) ;
#18349=CARTESIAN_POINT ( 'NONE',  ( 43.01140435219951286, 95.03445800887257633, 29.21067981925356705 ) ) ;
#18350=CARTESIAN_POINT ( 'NONE',  ( 43.01140435219951286, 98.03445800887257633, 29.21067981925356705 ) ) ;
#18351=CARTESIAN_POINT ( 'NONE',  ( 43.01140435219951286, 92.62977050742732388, 29.55568802177586463 ) ) ;
#18354=CARTESIAN_POINT ( 'NONE',  ( 38.58424406990786082, 84.11518717409400381, 34.21067981925357060 ) ) ;
#18355=CARTESIAN_POINT ( 'NONE',  ( 39.92123440845005433, 84.26049967264873430, 29.95742577749336988 ) ) ;
#18360=CARTESIAN_POINT ( 'NONE',  ( 47.43856463449118621, 64.87977050742730967, 34.21067981925357060 ) ) ;
#18361=ORIENTED_EDGE ( 'NONE', *, *, #5121, .F. ) ;
#18362=EDGE_CURVE ( 'NONE', #17102, #20293, #18135, .T. ) ;
#18363=CARTESIAN_POINT ( 'NONE',  ( 38.58424406990786082, 141.3797705074273381, 34.21067981925357060 ) ) ;
#18364=AXIS2_PLACEMENT_3D ( 'NONE', #7229, #15693, #2358 ) ;
#18365=CARTESIAN_POINT ( 'NONE',  ( 43.80332655382220963, 151.5373810949689926, 39.21067981925356349 ) ) ;
#18367=CARTESIAN_POINT ( 'NONE',  ( 38.01140435219951996, 111.8604996726487570, 35.83527830041810347 ) ) ;
#18368=CARTESIAN_POINT ( 'NONE',  ( 44.37947211624943833, 67.01518717409399528, 38.42115945441014446 ) ) ;
#18369=CYLINDRICAL_SURFACE ( 'NONE', #16249, 4.999999999999997335 ) ;
#18371=LINE ( 'NONE', #14731, #19206 ) ;
#18375=CARTESIAN_POINT ( 'NONE',  ( 44.55648932407425633, 151.8844580088725991, 29.45539723777780239 ) ) ;
#18376=B_SPLINE_CURVE_WITH_KNOTS ( 'NONE', 1,
 ( #2052, #8785 ),
 .UNSPECIFIED., .F., .F.,
 ( 2, 2 ),
 ( 0.000000000000000000, 1.000000000000000000 ),
 .UNSPECIFIED. ) ;
#18377=CARTESIAN_POINT ( 'NONE',  ( 41.64333658814960870, 119.7797705074273296, 30.00020018409699318 ) ) ;
#18380=CARTESIAN_POINT ( 'NONE',  ( 38.58424406990785371, 114.2651871740940095, 35.64915139335015937 ) ) ;
#18384=CARTESIAN_POINT ( 'NONE',  ( 44.55648932407425633, 65.81049967264873146, 29.45539723777780239 ) ) ;
#18389=CARTESIAN_POINT ( 'NONE',  ( 38.58424406990786082, 96.37977050742732388, 34.21067981925357060 ) ) ;
#18392=CARTESIAN_POINT ( 'NONE',  ( 48.01140435219951996, 145.2844580088725763, 34.21067981925357060 ) ) ;
#18394=CARTESIAN_POINT ( 'NONE',  ( 38.96631938032478359, 87.08445800887258770, 37.14960608071593384 ) ) ;
#18396=CARTESIAN_POINT ( 'NONE',  ( 38.01140435219952707, 141.7104996726487514, 34.21067981925357060 ) ) ;
#18397=CARTESIAN_POINT ( 'NONE',  ( 43.01140435219951286, 95.36518717409400381, 29.55568802177586463 ) ) ;
#18406=CARTESIAN_POINT ( 'NONE',  ( 44.55648932407425633, 79.61049967264874283, 38.96596240072933170 ) ) ;
#18407=CARTESIAN_POINT ( 'NONE',  ( 41.64333658814960870, 152.7797705074273438, 30.00020018409699318 ) ) ;
#18410=CARTESIAN_POINT ( 'NONE',  ( 38.58424406990785371, 141.2651871740939953, 35.64915139335015937 ) ) ;
#18413=ADVANCED_FACE ( 'NONE', ( #14674 ), #14455, .T. ) ;
#18420=CARTESIAN_POINT ( 'NONE',  ( 38.96631938032478359, 134.4844580088725934, 31.27175355779120025 ) ) ;
#18421=CARTESIAN_POINT ( 'NONE',  ( 43.01140435219951286, 120.8651871740940180, 38.86567161673127657 ) ) ;
#18423=ORIENTED_EDGE ( 'NONE', *, *, #15318, .F. ) ;
#18426=CARTESIAN_POINT ( 'NONE',  ( 48.01140435219951996, 109.4344580088725820, 32.58608133808903773 ) ) ;
#18427=CARTESIAN_POINT ( 'NONE',  ( 44.37947211624943833, 70.27977050742731535, 38.42115945441014446 ) ) ;
#18428=CARTESIAN_POINT ( 'NONE',  ( 47.43856463449117200, 130.4651871740939839, 35.64915139335016647 ) ) ;
#18430=CARTESIAN_POINT ( 'NONE',  ( 46.10157429594899270, 77.66049967264871157, 29.95742577749337343 ) ) ;
#18434=CARTESIAN_POINT ( 'NONE',  ( 45.74753988029933538, 86.06518717409400665, 30.44471234641811819 ) ) ;
#18438=ORIENTED_EDGE ( 'NONE', *, *, #18752, .T. ) ;
#18439=CARTESIAN_POINT ( 'NONE',  ( 41.64333658814960870, 63.97977050742731109, 38.42115945441014446 ) ) ;
#18445=CARTESIAN_POINT ( 'NONE',  ( 38.58424406990784661, 153.2651871740940237, 35.64915139335016647 ) ) ;
#18447=CARTESIAN_POINT ( 'NONE',  ( 38.58424406990785371, 111.5297705074273296, 35.64915139335015937 ) ) ;
#18452=CARTESIAN_POINT ( 'NONE',  ( 43.01140435219951286, 116.6297705074273097, 29.55568802177586463 ) ) ;
#18453=CARTESIAN_POINT ( 'NONE',  ( 39.92123440845005433, 128.3344580088725877, 29.95742577749336988 ) ) ;
#18454=CARTESIAN_POINT ( 'NONE',  ( 40.27526882409969033, 156.5651871740939498, 37.97664729208901946 ) ) ;
#18459=CARTESIAN_POINT ( 'NONE',  ( 38.96631938032478359, 157.0104996726487343, 37.14960608071593384 ) ) ;
#18463=CARTESIAN_POINT ( 'NONE',  ( 45.74753988029933538, 91.42977050742732104, 37.97664729208901946 ) ) ;
#18467=CARTESIAN_POINT ( 'NONE',  ( 44.37947211624943833, 92.21518717409401233, 30.00020018409699318 ) ) ;
#18468=CARTESIAN_POINT ( 'NONE',  ( 39.92123440845005433, 85.16049967264873999, 38.46393386101375711 ) ) ;
#18470=CARTESIAN_POINT ( 'NONE',  ( 39.92123440845005433, 137.3344580088725593, 29.95742577749336988 ) ) ;
#18473=CARTESIAN_POINT ( 'NONE',  ( 46.59305225739526435, 62.17977050742732104, 31.60846029578754468 ) ) ;
#18475=CARTESIAN_POINT ( 'NONE',  ( 46.59305225739526435, 142.5797705074273267, 36.81289934271958941 ) ) ;
#18476=CARTESIAN_POINT ( 'NONE',  ( 47.43856463449118621, 94.87977050742732388, 34.21067981925357060 ) ) ;
#18478=CARTESIAN_POINT ( 'NONE',  ( 44.55648932407425633, 100.6104996726487286, 38.96596240072933170 ) ) ;
#18484=( NAMED_UNIT ( * ) SI_UNIT ( $, .STERADIAN. ) SOLID_ANGLE_UNIT ( ) );
#18485=CARTESIAN_POINT ( 'NONE',  ( 38.01140435219951996, 140.9344580088725820, 35.83527830041810347 ) ) ;
#18486=CARTESIAN_POINT ( 'NONE',  ( 39.42975644700377558, 123.6797705074273210, 36.81289934271958941 ) ) ;
#18488=DIRECTION ( 'NONE',  ( 0.000000000000000000, 1.000000000000000000, 0.000000000000000000 ) ) ;
#18489=CARTESIAN_POINT ( 'NONE',  ( 43.01140435219951286, 117.8651871740939896, 38.86567161673127657 ) ) ;
#18491=CARTESIAN_POINT ( 'NONE',  ( 42.21948215057684450, 125.1113394311928460, 29.21067981925356705 ) ) ;
#18496=CARTESIAN_POINT ( 'NONE',  ( 44.37947211624943833, 83.47977050742731819, 30.00020018409699318 ) ) ;
#18498=VECTOR ( 'NONE', #6370, 1000.000000000000000 ) ;
#18500=ORIENTED_EDGE ( 'NONE', *, *, #15713, .F. ) ;
#18501=CARTESIAN_POINT ( 'NONE',  ( 47.05648932407426344, 72.98445800887257917, 37.14960608071593384 ) ) ;
#18502=CARTESIAN_POINT ( 'NONE',  ( 43.01140435219951286, 86.03445800887256212, 29.21067981925356705 ) ) ;
#18503=CARTESIAN_POINT ( 'NONE',  ( 41.46631938032478359, 141.1104996726487286, 29.45539723777780239 ) ) ;
#18504=CARTESIAN_POINT ( 'NONE',  ( 46.59305225739526435, 85.91518717409400097, 31.60846029578754468 ) ) ;
#18511=LINE ( 'NONE', #3421, #12821 ) ;
#18513=CARTESIAN_POINT ( 'NONE',  ( 41.64333658814960870, 155.7797705074273438, 30.00020018409699318 ) ) ;
#18517=CARTESIAN_POINT ( 'NONE',  ( 40.27526882409969744, 146.6651871740940294, 30.44471234641812174 ) ) ;
#18521=ORIENTED_EDGE ( 'NONE', *, *, #18525, .T. ) ;
#18522=CARTESIAN_POINT ( 'NONE',  ( 39.42975644700377558, 63.41518717409400097, 36.81289934271958941 ) ) ;
#18525=EDGE_CURVE ( 'NONE', #3863, #3266, #254, .T. ) ;
#18526=CARTESIAN_POINT ( 'NONE',  ( 38.01140435219952707, 134.6344580088725422, 32.58608133808903773 ) ) ;
#18527=CARTESIAN_POINT ( 'NONE',  ( 46.59305225739526435, 127.3151871740940067, 36.81289934271958941 ) ) ;
#18530=CARTESIAN_POINT ( 'NONE',  ( 43.01140435219951996, 147.5344580088726048, 39.21067981925356349 ) ) ;
#18532=CARTESIAN_POINT ( 'NONE',  ( 39.92123440845004723, 98.33445800887258770, 29.95742577749337343 ) ) ;
#18534=CARTESIAN_POINT ( 'NONE',  ( 45.74753988029933538, 70.42977050742730682, 37.97664729208901946 ) ) ;
#18535=CARTESIAN_POINT ( 'NONE',  ( 43.01140435219951286, 126.8651871740940180, 38.86567161673127657 ) ) ;
#18538=CARTESIAN_POINT ( 'NONE',  ( 44.55648932407425633, 82.61049967264874283, 38.96596240072933170 ) ) ;
#18541=CARTESIAN_POINT ( 'NONE',  ( 38.01140435219952707, 144.8604996726487286, 35.83527830041809636 ) ) ;
#18543=( BOUNDED_SURFACE ( )  B_SPLINE_SURFACE ( 1, 2, ( 
 ( #848, #6123, #5912, #12640, #19362, #11301, #4260, #10987, #17698, #18027, #1172, #19573, #2601, #15938, #4159, #8017, #14724, #9340, #21347, #7905, #6237, #16266, #21459, #7583, #12967, #6349, #14284, #14608, #2822, #953, #17802, #16370, #14395, #2934, #21029, #4581, #19689, #2713, #9456, #7698, #21245, #21134, #9670, #1067, #1281, #12852, #6017, #12748, #13075, #11198, #19469, #10889, #17592, #4359, #11089, #4467, #7798, #17911, #9560, #1393, #10217, #13514, #9781, #13407, #6805, #21791, #176, #11857, #3155, #21571, #3379, #8123, #11524, #11409, #9887, #3042, #10105, #6461, #8564, #20138, #16920, #1832, #16812, #19915, #16702, #15278, #18134, #1504, #14935, #4802, #1726, #9997, #20248, #66, #21684, #5139, #13182, #6909, #19803, #1609, #18587, #13299, #16476, #18254, #11743, #16585, #4693, #14825, #5034, #6580, #6698, #8342, #18475, #8234, #20035, #8459, #15165, #3494, #4920, #11633, #18363, #3267, #15052, #20779, #7124, #8779, #2153, #13935, #8992, #17455, #20353, #15700, #10324, #15593, #11965, #715, #20675, #3597, #5671, #12394, #10646, #606, #7235, #14045, #9104, #17026, #1937, #4023, #19129, #8669, #5558, #10751, #498, #15803, #2365, #18800, #15393, #19019, #288, #5352, #5247, #3702, #18696, #3919, #7019, #13615, #12282, #13723, #20460, #17349, #12069, #10539, #10430, #17135, #2050, #15494, #396, #2257, #3813, #13831, #20569, #5453, #12172, #18907, #17238, #8886, #19442, #9538, #926, #20887, #14254, #21216, #19335, #19663, #12504, #7774, #2575, #9424, #4335, #16130, #19231, #7556, #14472, #2796, #16235, #17995, #1039, #4555, #10864, #9211, #14580, #7671, #9314, #17776, #6096, #1146, #11275, #14151, #7881, #4130, #12826, #15908, #819, #20998, #21324, #4440, #19545, #5883, #17563, #7447, #2910, #9643, #12614, #6209, #11172, #12939, #17883, #16345, #2469, #5775, #4235, #10962, #17672, #16015, #14369, #21109, #5991, #12719, #11061, #2681, #1700, #8429, #14909, #21659, #1364, #11611, #9754, #5007, #6549, #10078, #18339, #13049, #15138, #6435, #3016, #6672, #8095, #14802, #21433, #13159, #6322, #20116, #21543, #11830, #8317, #20220, #13488, #11717, #19888, #20007, #10192, #4776, #11496, #18225, #3129, #18452, #13272, #41, #3352, #9859, #6781, #16560, #5113, #1252, #4891, #7989, #1476, #8208, #3241, #15025, #9972, #16675, #6881, #2125, #2021, #3784, #7098, #10513, #13588, #16998, #13907, #12258, #18991, #5642, #3893, #14018, #20326, #18668, #574, #8752, #15469, #12143, #10616, #17323, #12364, #1808, #7318, #5224, #16893, #3571, #1906, #8642, #15364, #256, #6992, #20432, #5326, #20540, #9031, #15742, #324, #20712, #7272, #13974, #15628, #647, #3637, #5595, #7382, #11999, #12322, #8923, #8710, #15528, #2291, #12105, #19057, #18732, #3959, #10682, #433, #7164, #15429, #20605, #1975, #17387, #8818, #14084, #5488, #10362, #20388, #6948, #2192, #17063, #13654, #5285, #7055, #13760, #20500, #5389, #18837, #13867, #12215, #3743, #10472, #18949, #17173, #2086, #3850, #10576, #533, #17277, #18697, #8566, #13616, #5140, #20354, #4804, #1505, #8235, #17028, #5249, #16587, #11858, #3600, #6807, #11525, #10325, #9998, #6581, #10219, #14937, #3268, #18255, #1611, #9888, #16921, #20036, #3157, #18589, #1938, #4923, #6910, #8343, #1727, #15054, #21792, #6700, #5035, #11744, #18476, #16813, #3380, #8461, #15166, #69, #13515, #821, #3703, #10649, #717, #13936, #8780, #5454, #12397, #17240, #398, #7127, #2367, #499, #607, #17351, #13832, #12173, #2154, #20676, #8993, #15701, #3018, #16237, #16453, #21111, #9427, #6324, #21218, #12828, #12942, #11279, #9645, #14256, #21001, #7991, #19547, #17997, #17885, #2912, #14696, #5885, #5115, #13490, #13274, #19890, #14804, #10299, #11498, #20010, #3469, #11832, #15253, #152, #18229, #3131, #13591, #9861, #8210, #4894, #11613, #18341, #20118, #15027, #17212, #7425, #18776, #2338, #20863, #7208, #18995, #13806, #10619, #17108, #5645, #17327, #10729, #8967, #20544, #259, #10839, #577, #20754, #19104, #2127, #12479, #2656, #7646, #19639, #6184, #14558, #16108, #7531, #19750, #9399, #1124, #14233, #12804, #901, #12915, #17754, #21300, #797, #5861, #16213, #21409, #11251, #4531, #7962, #17972, #19313, #9515, #17647, #2881, #4644, #20973, #17536, #2554, #9291, #14669, #4314, #15992, #9620, #7753, #15884, #2446, #1016, #4418, #12695, #14345, #16319, #9186, #4211, #6297, #14451, #17861, #12591, #21087, #21190, #5968, #19417, #11038, #6078, #19525, #11148, #7857, #2775, #16427, #21522, #14996, #15, #4865, #18314, #4981, #11692, #9836, #13562, #18534, #18427, #13463, #21738, #2989, #4748, #16536, #11803, #11362, #8403, #3325, #1562, #18083, #1452, #21632, #10166, #6523, #19861, #1339, #16760, #6646, #20196, #1781, #10054, #20092, #5089, #9730, #8073, #3441, #13244, #3214, #15228, #19980, #15112, #11468, #9947, #20298, #14886, #11586, #1671, #8185, #16650, #6755, #16867, #13355, #8515, #126, #6855, #14779, #6411, #13134, #18197, #3104, #3545, #8725, #344, #12015, #2208, #17187, #20728, #7293, #7073, #5616, #13672, #17404, #5196, #2099, #13992, #20515, #18643, #18749, #18965, #17080, #2309, #10270, #12234 ),
 ( #8939, #16973, #15336, #3868, #9048, #12339, #549, #15757, #15645, #6966, #10591, #20405, #19074, #14100, #1883, #11913, #5303, #3652, #662, #13776, #10380, #3975, #8837, #8617, #228, #12119, #13882, #5402, #1994, #10700, #7399, #15443, #18852, #3760, #17296, #10487, #15543, #448, #7178, #20621, #7933, #12885, #19389, #12669, #11120, #5939, #4078, #9160, #2629, #9484, #14315, #11013, #14425, #21160, #19287, #1198, #6150, #6049, #1095, #9369, #12451, #14206, #4186, #21272, #20836, #17835, #12775, #17724, #5727, #10914, #9264, #19606, #15964, #7506, #10808, #4388, #16074, #7829, #11222, #19496, #7723, #14531, #19179, #17511, #4499, #876, #7613, #2745, #17620, #985, #16183, #17941, #2847, #9591, #16292, #2420, #2528, #15859, #772, #20945, #5827, #12560, #21601, #9809, #2959, #6490, #4718, #16729, #3296, #11659, #13210, #4609, #10135, #19947, #20064, #11330, #9913, #19828, #10024, #14855, #18396, #19718, #9698, #13328, #18503, #8372, #1639, #5061, #15082, #16398, #6612, #8044, #19037, #1752, #18051, #14637, #14749, #21490, #11774, #1421, #6376, #6727, #4832, #12997, #21378, #11555, #1530, #16504, #11438, #13433, #16839, #1309, #20171, #18283, #14962, #13105, #3412, #3185, #6264, #18163, #3071, #8150, #16620, #8262, #4951, #21709, #13537, #18613, #12093, #18939, #1965, #15419, #2076, #8806, #6937, #10673, #15617, #15518, #10566, #18826, #99, #1858, #13643, #8914, #8487, #5479, #421, #20488, #15196, #20378, #18719, #7262, #3626, #16942, #20272, #13856, #5378, #17266, #20703, #7153, #17162, #2178, #6830, #5163, #525, #10350, #314, #12311, #17053, #12204, #8588, #7043, #17376, #11989, #20593, #3839, #5274, #11885, #13963, #5586, #19047, #3731, #3518, #15307, #8698, #3946, #10244, #199, #13749, #10461, #2281, #14181, #12533, #1070, #19260, #10780, #7372, #7700, #21031, #11093, #14506, #16045, #10990, #4363, #15732, #9021, #17805, #4162, #9242, #6126, #10891, #21136, #2396, #15941, #11200, #5802, #17594, #14398, #20918, #2500, #6020, #9457, #851, #21248, #16158, #2716, #7586, #17700, #7800, #12643, #17486, #957, #14287, #5914, #12424, #19364, #4262, #12856, #12751, #19471, #2605, #14073, #19578, #9343, #4470, #20811, #637, #7479, #5701, #19151, #4052, #9133, #15833, #744, #21794, #11637, #13302, #8346, #14939, #19695, #9890, #11303, #20040, #5037, #14613, #17913, #18030, #2936, #15057, #4695, #9673, #10001, #8125, #16268, #2824, #3047, #4807, #13077, #8021, #18367, #20144, #4583, #4926, #9784, #18257, #7910, #1614, #16480, #3269, #16705, #9563, #6703, #1396, #14828, #8237, #18138, #1174, #6240, #21573, #6584, #11412, #6464, #13410, #3160, #21351, #12969, #21686, #16373, #13185, #1286, #14726, #21462, #19806, #6353, #19918, #11529, #16590, #1508, #13912, #5752, #20546, #2448, #11746, #2236, #14126, #5534, #3382, #18881, #4002, #2129, #9188, #16815, #12367, #7212, #14022, #8970, #20756, #2026, #12149, #19106, #7427, #20865, #799, #5647, #15886, #15473, #13808, #19209, #12262, #20651, #579, #10731, #12482, #7533, #18478, #4106, #8756, #17432, #5429, #3790, #10519, #10842, #9077, #2340, #17214, #373, #10108, #14235, #20975, #8864, #17538, #15784, #7103, #690, #15572, #476, #18997, #3897, #10621, #17329, #15675, #7322, #19527, #18087, #16111, #13029, #9293, #6301, #21412, #4420, #11150, #5970, #16216, #14348, #9623, #17864, #14672, #1126, #17649, #4213, #14782, #12917, #2556, #19753, #4647, #2885, #11366, #21302, #2992, #1343, #15994, #903, #9733, #16430, #7649, #6186, #8076, #7860, #5863, #12594, #11040, #21089, #11253, #12697, #19419, #19315, #17756, #10942, #17974, #4316, #7755, #2658, #9402, #1018, #14453, #2777, #7965, #21192, #6080, #12806, #19641, #9517, #14560, #4533, #16322, #1231, #1677, #11695, #8406, #4752, #21636, #6758, #16870, #1785, #10274, #15115, #18646, #3107, #1455, #6859, #15001, #16653, #10057, #18, #8518, #3548, #6414, #15231, #18200, #13467, #8188, #14889, #6527, #13565, #18538, #20199, #13248, #11471, #21525, #16976, #1886, #19984, #130, #3446, #20302, #11806, #8621, #9839, #5200, #13137, #16539, #10170, #5093, #4868, #13358, #11917, #9950, #19866, #11589, #18317, #3218, #20095, #4985, #1566, #16765, #8293, #21742, #18430, #6649, #3328, #5306, #13675, #2423, #552, #12018, #665, #7402, #12342, #2312, #8942, #9051, #10811, #18753, #3655, #5730, #15761, #10383, #15649, #14103, #17299, #17514, #20839, #20518, #17083, #20731, #1998, #7077, #6970, #5405, #20410, #5619, #8729, #4081, #7297, #12454, #19183, #19077, #15446, #12238, #15339, #347, #18855, #10491, #13779, #3978, #5508, #232, #17407, #18968, #12123, #3763, #17190, #2102, #8840, #15547, #451, #10704, #3871, #7182, #13887, #13996, #2212, #20624, #10594, #15862, #17946, #11016, #16078, #13001, #17727, #6153, #9267, #989, #18057, #12672, #2632, #14534, #5942, #9373, #21275, #16296, #7726, #6270, #1203, #2852, #19392, #17838, #9595, #19499, #17624, #7832, #14428, #4289, #19290, #21163, #21061, #11226, #19609, #12888, #6052, #20948, #4614, #12778, #4503, #5831, #4391, #14319, #7937, #11123, #14641, #14209, #4189, #21383, #19722, #11335, #9163, #775, #7510, #10917 ) ),
 .UNSPECIFIED., .F., .F., .T. ) 
 B_SPLINE_SURFACE_WITH_KNOTS ( ( 2, 2 ),
 ( 3, 2, 2, 2, 2, 2, 2, 2, 2, 2, 2, 2, 2, 2, 2, 2, 2, 2, 2, 2, 2, 2, 2, 2, 2, 2, 2, 2, 2, 2, 2, 2, 2, 2, 2, 2, 2, 2, 2, 2, 2, 2, 2, 2, 2, 2, 2, 2, 2, 2, 2, 2, 2, 2, 2, 2, 2, 2, 2, 2, 2, 2, 2, 2, 2, 2, 2, 2, 2, 2, 2, 2, 2, 2, 2, 2, 2, 2, 2, 2, 2, 2, 2, 2, 2, 2, 2, 2, 2, 2, 2, 2, 2, 2, 2, 2, 2, 2, 2, 2, 2, 2, 2, 2, 2, 2, 2, 2, 2, 2, 2, 2, 2, 2, 2, 2, 2, 2, 2, 2, 2, 2, 2, 2, 2, 2, 2, 2, 2, 2, 2, 2, 2, 2, 2, 2, 2, 2, 2, 2, 2, 2, 2, 2, 2, 2, 2, 2, 2, 2, 2, 2, 2, 2, 2, 2, 2, 2, 2, 2, 2, 2, 2, 2, 2, 2, 2, 2, 2, 2, 2, 2, 2, 2, 2, 2, 2, 2, 2, 2, 2, 2, 2, 2, 2, 2, 2, 2, 2, 2, 2, 2, 2, 2, 2, 2, 2, 2, 2, 2, 2, 2, 2, 2, 2, 2, 2, 2, 2, 2, 2, 2, 2, 2, 2, 2, 2, 2, 2, 2, 2, 2, 2, 2, 2, 2, 2, 2, 2, 2, 2, 2, 2, 2, 2, 2, 2, 2, 2, 2, 2, 2, 2, 2, 2, 2, 2, 2, 2, 2, 2, 2, 2, 2, 2, 2, 2, 2, 2, 2, 2, 2, 2, 2, 2, 2, 2, 2, 2, 2, 2, 2, 2, 2, 2, 2, 2, 2, 2, 2, 2, 2, 2, 2, 2, 2, 2, 2, 2, 2, 2, 2, 2, 2, 2, 2, 2, 2, 2, 2, 2, 2, 2, 2, 2, 2, 2, 2, 2, 2, 2, 2, 2, 2, 2, 2, 2, 2, 2, 2, 2, 2, 2, 2, 2, 2, 2, 2, 2, 2, 2, 2, 2, 2, 3 ),
 ( 0.000000000000000000, 1.000000000000000000 ),
 ( 0.000000000000000000, 0.002941176470588235253, 0.005882352941176470507, 0.008823529411764705760, 0.01176470588235294101, 0.01470588235294117627, 0.01764705882352941152, 0.02058823529411764677, 0.02352941176470588203, 0.02647058823529411728, 0.02941176470588235253, 0.03235294117647059126, 0.03529411764705882304, 0.03823529411764706176, 0.04117647058823529355, 0.04411764705882353227, 0.04705882352941176405, 0.05000000000000000278, 0.05294117647058823456, 0.05588235294117647328, 0.05882352941176470507, 0.06176470588235294379, 0.06470588235294118251, 0.06764705882352940736, 0.07058823529411764608, 0.07352941176470588480, 0.07647058823529412352, 0.07941176470588234837, 0.08235294117647058709, 0.08529411764705882582, 0.08823529411764706454, 0.09117647058823528938, 0.09411764705882352811, 0.09705882352941176683, 0.1000000000000000056, 0.1029411764705882304, 0.1058823529411764691, 0.1088235294117647078, 0.1117647058823529466, 0.1147058823529411714, 0.1176470588235294101, 0.1205882352941176489, 0.1235294117647058876, 0.1264705882352941124, 0.1294117647058823650, 0.1323529411764705899, 0.1352941176470588147, 0.1382352941176470673, 0.1411764705882352922, 0.1441176470588235170, 0.1470588235294117696, 0.1499999999999999944, 0.1529411764705882470, 0.1558823529411764719, 0.1588235294117646967, 0.1617647058823529493, 0.1647058823529411742, 0.1676470588235293990, 0.1705882352941176516, 0.1735294117647058765, 0.1764705882352941291, 0.1794117647058823539, 0.1823529411764705788, 0.1852941176470588314, 0.1882352941176470562, 0.1911764705882352811, 0.1941176470588235337, 0.1970588235294117585, 0.2000000000000000111, 0.2029411764705882359, 0.2058823529411764608, 0.2088235294117647134, 0.2117647058823529382, 0.2147058823529411631, 0.2176470588235294157, 0.2205882352941176405, 0.2235294117647058931, 0.2264705882352941180, 0.2294117647058823428, 0.2323529411764705954, 0.2352941176470588203, 0.2382352941176470451, 0.2411764705882352977, 0.2441176470588235226, 0.2470588235294117752, 0.2500000000000000000, 0.2529411764705882248, 0.2558823529411764497, 0.2588235294117647300, 0.2617647058823529549, 0.2647058823529411797, 0.2676470588235294046, 0.2705882352941176294, 0.2735294117647059098, 0.2764705882352941346, 0.2794117647058823595, 0.2823529411764705843, 0.2852941176470588092, 0.2882352941176470340, 0.2911764705882353144, 0.2941176470588235392, 0.2970588235294117641, 0.2999999999999999889, 0.3029411764705882137, 0.3058823529411764941, 0.3088235294117647189, 0.3117647058823529438, 0.3147058823529411686, 0.3176470588235293935, 0.3205882352941176738, 0.3235294117647058987, 0.3264705882352941235, 0.3294117647058823484, 0.3323529411764705732, 0.3352941176470587981, 0.3382352941176470784, 0.3411764705882353033, 0.3441176470588235281, 0.3470588235294117530, 0.3499999999999999778, 0.3529411764705882582, 0.3558823529411764830, 0.3588235294117647078, 0.3617647058823529327, 0.3647058823529411575, 0.3676470588235294379, 0.3705882352941176627, 0.3735294117647058876, 0.3764705882352941124, 0.3794117647058823373, 0.3823529411764705621, 0.3852941176470588425, 0.3882352941176470673, 0.3911764705882352922, 0.3941176470588235170, 0.3970588235294117418, 0.4000000000000000222, 0.4029411764705882470, 0.4058823529411764719, 0.4088235294117646967, 0.4117647058823529216, 0.4147058823529412019, 0.4176470588235294268, 0.4205882352941176516, 0.4235294117647058765, 0.4264705882352941013, 0.4294117647058823262, 0.4323529411764706065, 0.4352941176470588314, 0.4382352941176470562, 0.4411764705882352811, 0.4441176470588235059, 0.4470588235294117863, 0.4500000000000000111, 0.4529411764705882359, 0.4558823529411764608, 0.4588235294117646856, 0.4617647058823529660, 0.4647058823529411908, 0.4676470588235294157, 0.4705882352941176405, 0.4735294117647058654, 0.4764705882352940902, 0.4794117647058823706, 0.4823529411764705954, 0.4852941176470588203, 0.4882352941176470451, 0.4911764705882352700, 0.4941176470588235503, 0.4970588235294117752, 0.5000000000000000000, 0.5029411764705882248, 0.5058823529411764497, 0.5088235294117646745, 0.5117647058823528994, 0.5147058823529411242, 0.5176470588235294601, 0.5205882352941176849, 0.5235294117647059098, 0.5264705882352941346, 0.5294117647058823595, 0.5323529411764705843, 0.5352941176470588092, 0.5382352941176470340, 0.5411764705882352589, 0.5441176470588234837, 0.5470588235294118196, 0.5500000000000000444, 0.5529411764705882693, 0.5558823529411764941, 0.5588235294117647189, 0.5617647058823529438, 0.5647058823529411686, 0.5676470588235293935, 0.5705882352941176183, 0.5735294117647058432, 0.5764705882352940680, 0.5794117647058824039, 0.5823529411764706287, 0.5852941176470588536, 0.5882352941176470784, 0.5911764705882353033, 0.5941176470588235281, 0.5970588235294117530, 0.5999999999999999778, 0.6029411764705882026, 0.6058823529411764275, 0.6088235294117646523, 0.6117647058823529882, 0.6147058823529412130, 0.6176470588235294379, 0.6205882352941176627, 0.6235294117647058876, 0.6264705882352941124, 0.6294117647058823373, 0.6323529411764705621, 0.6352941176470587870, 0.6382352941176470118, 0.6411764705882353477, 0.6441176470588235725, 0.6470588235294117974, 0.6500000000000000222, 0.6529411764705882470, 0.6558823529411764719, 0.6588235294117646967, 0.6617647058823529216, 0.6647058823529411464, 0.6676470588235293713, 0.6705882352941175961, 0.6735294117647059320, 0.6764705882352941568, 0.6794117647058823817, 0.6823529411764706065, 0.6852941176470588314, 0.6882352941176470562, 0.6911764705882352811, 0.6941176470588235059, 0.6970588235294117307, 0.6999999999999999556, 0.7029411764705881804, 0.7058823529411765163, 0.7088235294117647411, 0.7117647058823529660, 0.7147058823529411908, 0.7176470588235294157, 0.7205882352941176405, 0.7235294117647058654, 0.7264705882352940902, 0.7294117647058823151, 0.7323529411764705399, 0.7352941176470588758, 0.7382352941176471006, 0.7411764705882353255, 0.7441176470588235503, 0.7470588235294117752, 0.7500000000000000000, 0.7529411764705882248, 0.7558823529411764497, 0.7588235294117646745, 0.7617647058823528994, 0.7647058823529411242, 0.7676470588235294601, 0.7705882352941176849, 0.7735294117647059098, 0.7764705882352941346, 0.7794117647058823595, 0.7823529411764705843, 0.7852941176470588092, 0.7882352941176470340, 0.7911764705882352589, 0.7941176470588234837, 0.7970588235294118196, 0.8000000000000000444, 0.8029411764705882693, 0.8058823529411764941, 0.8088235294117647189, 0.8117647058823529438, 0.8147058823529411686, 0.8176470588235293935, 0.8205882352941176183, 0.8235294117647058432, 0.8264705882352940680, 0.8294117647058824039, 0.8323529411764706287, 0.8352941176470588536, 0.8382352941176470784, 0.8411764705882353033, 0.8441176470588235281, 0.8470588235294117530, 0.8499999999999999778, 0.8529411764705882026, 0.8558823529411764275, 0.8588235294117646523, 0.8617647058823529882, 0.8647058823529412130, 0.8676470588235294379, 0.8705882352941176627, 0.8735294117647058876, 0.8764705882352941124, 0.8794117647058823373, 0.8823529411764705621, 0.8852941176470587870, 0.8882352941176470118, 0.8911764705882353477, 0.8941176470588235725, 0.8970588235294117974, 0.9000000000000000222, 0.9029411764705882470, 0.9058823529411764719, 0.9088235294117646967, 0.9117647058823529216, 0.9147058823529411464, 0.9176470588235293713, 0.9205882352941175961, 0.9235294117647059320, 0.9264705882352941568, 0.9294117647058823817, 0.9323529411764706065, 0.9352941176470588314, 0.9382352941176470562, 0.9411764705882352811, 0.9441176470588235059, 0.9470588235294117307, 0.9499999999999999556, 0.9529411764705881804, 0.9558823529411765163, 0.9588235294117647411, 0.9617647058823529660, 0.9647058823529411908, 0.9676470588235294157, 0.9705882352941176405, 0.9735294117647058654, 0.9764705882352940902, 0.9794117647058823151, 0.9803958342062289999 ),
 .UNSPECIFIED. ) 
 GEOMETRIC_REPRESENTATION_ITEM ( )  RATIONAL_B_SPLINE_SURFACE ( (
 ( 1.000000000000000000, 0.9510565162951535312, 1.000000000000000000, 0.9510565162951535312, 1.000000000000000000, 0.9510565162951535312, 1.000000000000000000, 0.9510565162951535312, 1.000000000000000000, 0.9510565162951535312, 1.000000000000000000, 0.9510565162951535312, 1.000000000000000000, 0.9510565162951535312, 1.000000000000000000, 0.9510565162951535312, 1.000000000000000000, 0.9510565162951535312, 1.000000000000000000, 0.9510565162951535312, 1.000000000000000000, 0.9510565162951535312, 1.000000000000000000, 0.9510565162951535312, 1.000000000000000000, 0.9510565162951535312, 1.000000000000000000, 0.9510565162951535312, 1.000000000000000000, 0.9510565162951535312, 1.000000000000000000, 0.9510565162951535312, 1.000000000000000000, 0.9510565162951535312, 1.000000000000000000, 0.9510565162951535312, 1.000000000000000000, 0.9510565162951535312, 1.000000000000000000, 0.9510565162951535312, 1.000000000000000000, 0.9510565162951535312, 1.000000000000000000, 0.9510565162951535312, 1.000000000000000000, 0.9510565162951535312, 1.000000000000000000, 0.9510565162951535312, 1.000000000000000000, 0.9510565162951535312, 1.000000000000000000, 0.9510565162951535312, 1.000000000000000000, 0.9510565162951535312, 1.000000000000000000, 0.9510565162951535312, 1.000000000000000000, 0.9510565162951535312, 1.000000000000000000, 0.9510565162951535312, 1.000000000000000000, 0.9510565162951535312, 1.000000000000000000, 0.9510565162951535312, 1.000000000000000000, 0.9510565162951535312, 1.000000000000000000, 0.9510565162951535312, 1.000000000000000000, 0.9510565162951535312, 1.000000000000000000, 0.9510565162951535312, 1.000000000000000000, 0.9510565162951535312, 1.000000000000000000, 0.9510565162951535312, 1.000000000000000000, 0.9510565162951535312, 1.000000000000000000, 0.9510565162951535312, 1.000000000000000000, 0.9510565162951535312, 1.000000000000000000, 0.9510565162951535312, 1.000000000000000000, 0.9510565162951535312, 1.000000000000000000, 0.9510565162951535312, 1.000000000000000000, 0.9510565162951535312, 1.000000000000000000, 0.9510565162951535312, 1.000000000000000000, 0.9510565162951535312, 1.000000000000000000, 0.9510565162951535312, 1.000000000000000000, 0.9510565162951535312, 1.000000000000000000, 0.9510565162951535312, 1.000000000000000000, 0.9510565162951535312, 1.000000000000000000, 0.9510565162951535312, 1.000000000000000000, 0.9510565162951535312, 1.000000000000000000, 0.9510565162951535312, 1.000000000000000000, 0.9510565162951535312, 1.000000000000000000, 0.9510565162951535312, 1.000000000000000000, 0.9510565162951535312, 1.000000000000000000, 0.9510565162951535312, 1.000000000000000000, 0.9510565162951535312, 1.000000000000000000, 0.9510565162951535312, 1.000000000000000000, 0.9510565162951535312, 1.000000000000000000, 0.9510565162951535312, 1.000000000000000000, 0.9510565162951535312, 1.000000000000000000, 0.9510565162951535312, 1.000000000000000000, 0.9510565162951535312, 1.000000000000000000, 0.9510565162951535312, 1.000000000000000000, 0.9510565162951535312, 1.000000000000000000, 0.9510565162951535312, 1.000000000000000000, 0.9510565162951535312, 1.000000000000000000, 0.9510565162951535312, 1.000000000000000000, 0.9510565162951535312, 1.000000000000000000, 0.9510565162951535312, 1.000000000000000000, 0.9510565162951535312, 1.000000000000000000, 0.9510565162951535312, 1.000000000000000000, 0.9510565162951535312, 1.000000000000000000, 0.9510565162951535312, 1.000000000000000000, 0.9510565162951535312, 1.000000000000000000, 0.9510565162951535312, 1.000000000000000000, 0.9510565162951535312, 1.000000000000000000, 0.9510565162951535312, 1.000000000000000000, 0.9510565162951535312, 1.000000000000000000, 0.9510565162951535312, 1.000000000000000000, 0.9510565162951535312, 1.000000000000000000, 0.9510565162951535312, 1.000000000000000000, 0.9510565162951535312, 1.000000000000000000, 0.9510565162951535312, 1.000000000000000000, 0.9510565162951535312, 1.000000000000000000, 0.9510565162951535312, 1.000000000000000000, 0.9510565162951535312, 1.000000000000000000, 0.9510565162951535312, 1.000000000000000000, 0.9510565162951535312, 1.000000000000000000, 0.9510565162951535312, 1.000000000000000000, 0.9510565162951535312, 1.000000000000000000, 0.9510565162951535312, 1.000000000000000000, 0.9510565162951535312, 1.000000000000000000, 0.9510565162951535312, 1.000000000000000000, 0.9510565162951535312, 1.000000000000000000, 0.9510565162951535312, 1.000000000000000000, 0.9510565162951535312, 1.000000000000000000, 0.9510565162951535312, 1.000000000000000000, 0.9510565162951535312, 1.000000000000000000, 0.9510565162951535312, 1.000000000000000000, 0.9510565162951535312, 1.000000000000000000, 0.9510565162951535312, 1.000000000000000000, 0.9510565162951535312, 1.000000000000000000, 0.9510565162951535312, 1.000000000000000000, 0.9510565162951535312, 1.000000000000000000, 0.9510565162951535312, 1.000000000000000000, 0.9510565162951535312, 1.000000000000000000, 0.9510565162951535312, 1.000000000000000000, 0.9510565162951535312, 1.000000000000000000, 0.9510565162951535312, 1.000000000000000000, 0.9510565162951535312, 1.000000000000000000, 0.9510565162951535312, 1.000000000000000000, 0.9510565162951535312, 1.000000000000000000, 0.9510565162951535312, 1.000000000000000000, 0.9510565162951535312, 1.000000000000000000, 0.9510565162951535312, 1.000000000000000000, 0.9510565162951535312, 1.000000000000000000, 0.9510565162951535312, 1.000000000000000000, 0.9510565162951535312, 1.000000000000000000, 0.9510565162951535312, 1.000000000000000000, 0.9510565162951535312, 1.000000000000000000, 0.9510565162951535312, 1.000000000000000000, 0.9510565162951535312, 1.000000000000000000, 0.9510565162951535312, 1.000000000000000000, 0.9510565162951535312, 1.000000000000000000, 0.9510565162951535312, 1.000000000000000000, 0.9510565162951535312, 1.000000000000000000, 0.9510565162951535312, 1.000000000000000000, 0.9510565162951535312, 1.000000000000000000, 0.9510565162951535312, 1.000000000000000000, 0.9510565162951535312, 1.000000000000000000, 0.9510565162951535312, 1.000000000000000000, 0.9510565162951535312, 1.000000000000000000, 0.9510565162951535312, 1.000000000000000000, 0.9510565162951535312, 1.000000000000000000, 0.9510565162951535312, 1.000000000000000000, 0.9510565162951535312, 1.000000000000000000, 0.9510565162951535312, 1.000000000000000000, 0.9510565162951535312, 1.000000000000000000, 0.9510565162951535312, 1.000000000000000000, 0.9510565162951535312, 1.000000000000000000, 0.9510565162951535312, 1.000000000000000000, 0.9510565162951535312, 1.000000000000000000, 0.9510565162951535312, 1.000000000000000000, 0.9510565162951535312, 1.000000000000000000, 0.9510565162951535312, 1.000000000000000000, 0.9510565162951535312, 1.000000000000000000, 0.9510565162951535312, 1.000000000000000000, 0.9510565162951535312, 1.000000000000000000, 0.9510565162951535312, 1.000000000000000000, 0.9510565162951535312, 1.000000000000000000, 0.9510565162951535312, 1.000000000000000000, 0.9510565162951535312, 1.000000000000000000, 0.9510565162951535312, 1.000000000000000000, 0.9510565162951535312, 1.000000000000000000, 0.9510565162951535312, 1.000000000000000000, 0.9510565162951535312, 1.000000000000000000, 0.9510565162951535312, 1.000000000000000000, 0.9510565162951535312, 1.000000000000000000, 0.9510565162951535312, 1.000000000000000000, 0.9510565162951535312, 1.000000000000000000, 0.9510565162951535312, 1.000000000000000000, 0.9510565162951535312, 1.000000000000000000, 0.9510565162951535312, 1.000000000000000000, 0.9510565162951535312, 1.000000000000000000, 0.9510565162951535312, 1.000000000000000000, 0.9510565162951535312, 1.000000000000000000, 0.9510565162951535312, 1.000000000000000000, 0.9510565162951535312, 1.000000000000000000, 0.9510565162951535312, 1.000000000000000000, 0.9510565162951535312, 1.000000000000000000, 0.9510565162951535312, 1.000000000000000000, 0.9510565162951535312, 1.000000000000000000, 0.9510565162951535312, 1.000000000000000000, 0.9510565162951535312, 1.000000000000000000, 0.9510565162951535312, 1.000000000000000000, 0.9510565162951535312, 1.000000000000000000, 0.9510565162951535312, 1.000000000000000000, 0.9510565162951535312, 1.000000000000000000, 0.9510565162951535312, 1.000000000000000000, 0.9510565162951535312, 1.000000000000000000, 0.9510565162951535312, 1.000000000000000000, 0.9510565162951535312, 1.000000000000000000, 0.9510565162951535312, 1.000000000000000000, 0.9510565162951535312, 1.000000000000000000, 0.9510565162951535312, 1.000000000000000000, 0.9510565162951535312, 1.000000000000000000, 0.9510565162951535312, 1.000000000000000000, 0.9510565162951535312, 1.000000000000000000, 0.9510565162951535312, 1.000000000000000000, 0.9510565162951535312, 1.000000000000000000, 0.9510565162951535312, 1.000000000000000000, 0.9510565162951535312, 1.000000000000000000, 0.9510565162951535312, 1.000000000000000000, 0.9510565162951535312, 1.000000000000000000, 0.9510565162951535312, 1.000000000000000000, 0.9510565162951535312, 1.000000000000000000, 0.9510565162951535312, 1.000000000000000000, 0.9510565162951535312, 1.000000000000000000, 0.9510565162951535312, 1.000000000000000000, 0.9510565162951535312, 1.000000000000000000, 0.9510565162951535312, 1.000000000000000000, 0.9510565162951535312, 1.000000000000000000, 0.9510565162951535312, 1.000000000000000000, 0.9510565162951535312, 1.000000000000000000, 0.9510565162951535312, 1.000000000000000000, 0.9510565162951535312, 1.000000000000000000, 0.9510565162951535312, 1.000000000000000000, 0.9510565162951535312, 1.000000000000000000, 0.9510565162951535312, 1.000000000000000000, 0.9510565162951535312, 1.000000000000000000, 0.9510565162951535312, 1.000000000000000000, 0.9510565162951535312, 1.000000000000000000, 0.9510565162951535312, 1.000000000000000000, 0.9510565162951535312, 1.000000000000000000, 0.9510565162951535312, 1.000000000000000000, 0.9510565162951535312, 1.000000000000000000, 0.9510565162951535312, 1.000000000000000000, 0.9510565162951535312, 1.000000000000000000, 0.9510565162951535312, 1.000000000000000000, 0.9510565162951535312, 1.000000000000000000, 0.9510565162951535312, 1.000000000000000000, 0.9510565162951535312, 1.000000000000000000, 0.9510565162951535312, 1.000000000000000000, 0.9510565162951535312, 1.000000000000000000, 0.9510565162951535312, 1.000000000000000000, 0.9510565162951535312, 1.000000000000000000, 0.9510565162951535312, 1.000000000000000000, 0.9510565162951535312, 1.000000000000000000, 0.9510565162951535312, 1.000000000000000000, 0.9510565162951535312, 1.000000000000000000, 0.9510565162951535312, 1.000000000000000000, 0.9510565162951535312, 1.000000000000000000, 0.9510565162951535312, 1.000000000000000000, 0.9510565162951535312, 1.000000000000000000, 0.9510565162951535312, 1.000000000000000000, 0.9510565162951535312, 1.000000000000000000, 0.9510565162951535312, 1.000000000000000000, 0.9510565162951535312, 1.000000000000000000, 0.9510565162951535312, 1.000000000000000000, 0.9510565162951535312, 1.000000000000000000, 0.9510565162951535312, 1.000000000000000000, 0.9510565162951535312, 1.000000000000000000, 0.9510565162951535312, 1.000000000000000000, 0.9510565162951535312, 1.000000000000000000, 0.9510565162951535312, 1.000000000000000000, 0.9510565162951535312, 1.000000000000000000, 0.9510565162951535312, 1.000000000000000000, 0.9510565162951535312, 1.000000000000000000, 0.9510565162951535312, 1.000000000000000000, 0.9510565162951535312, 1.000000000000000000, 0.9510565162951535312, 1.000000000000000000, 0.9510565162951535312, 1.000000000000000000, 0.9510565162951535312, 1.000000000000000000, 0.9510565162951535312, 1.000000000000000000, 0.9510565162951535312, 1.000000000000000000, 0.9510565162951535312, 1.000000000000000000, 0.9510565162951535312, 1.000000000000000000, 0.9510565162951535312, 1.000000000000000000, 0.9510565162951535312, 1.000000000000000000, 0.9510565162951535312, 1.000000000000000000, 0.9510565162951535312, 1.000000000000000000, 0.9510565162951535312, 1.000000000000000000, 0.9510565162951535312, 1.000000000000000000, 0.9510565162951535312, 1.000000000000000000, 0.9510565162951535312, 1.000000000000000000, 0.9510565162951535312, 1.000000000000000000, 0.9510565162951535312, 1.000000000000000000, 0.9510565162951535312, 1.000000000000000000, 0.9510565162951535312, 1.000000000000000000, 0.9510565162951535312, 1.000000000000000000, 0.9510565162951535312, 1.000000000000000000, 0.9510565162951535312, 1.000000000000000000, 0.9510565162951535312, 1.000000000000000000, 0.9510565162951535312, 1.000000000000000000, 0.9510565162951535312, 1.000000000000000000, 0.9510565162951535312, 1.000000000000000000, 0.9510565162951535312, 1.000000000000000000, 0.9510565162951535312, 1.000000000000000000, 0.9510565162951535312, 1.000000000000000000, 0.9510565162951535312, 1.000000000000000000, 0.9510565162951535312, 1.000000000000000000, 0.9510565162951535312, 1.000000000000000000, 0.9510565162951535312, 1.000000000000000000, 0.9510565162951535312, 1.000000000000000000, 0.9510565162951535312, 1.000000000000000000, 0.9510565162951535312, 1.000000000000000000, 0.9510565162951535312, 1.000000000000000000, 0.9510565162951535312, 1.000000000000000000, 0.9510565162951535312, 1.000000000000000000, 0.9510565162951535312, 1.000000000000000000, 0.9510565162951535312, 1.000000000000000000, 0.9510565162951535312, 1.000000000000000000, 0.9510565162951535312, 1.000000000000000000, 0.9510565162951535312, 1.000000000000000000, 0.9510565162951535312, 1.000000000000000000, 0.9510565162951535312, 1.000000000000000000, 0.9510565162951535312, 1.000000000000000000, 0.9510565162951535312, 1.000000000000000000, 0.9510565162951535312, 1.000000000000000000, 0.9510565162951535312, 1.000000000000000000, 0.9510565162951535312, 1.000000000000000000, 0.9510565162951535312, 1.000000000000000000, 0.9510565162951535312, 1.000000000000000000, 0.9510565162951535312, 1.000000000000000000, 0.9510565162951535312, 1.000000000000000000, 0.9510565162951535312, 1.000000000000000000, 0.9510565162951535312, 1.000000000000000000, 0.9510565162951535312, 1.000000000000000000, 0.9510565162951535312, 1.000000000000000000, 0.9510565162951535312, 1.000000000000000000, 0.9510565162951535312, 1.000000000000000000, 0.9510565162951535312, 1.000000000000000000, 0.9510565162951535312, 1.000000000000000000, 0.9510565162951535312, 1.000000000000000000, 0.9510565162951535312, 1.000000000000000000, 0.9510565162951535312, 1.000000000000000000, 0.9510565162951535312, 1.000000000000000000, 0.9510565162951535312, 1.000000000000000000, 0.9510565162951535312, 1.000000000000000000, 0.9510565162951535312, 1.000000000000000000, 0.9510565162951535312, 1.000000000000000000, 0.9510565162951535312, 1.000000000000000000, 0.9510565162951535312, 1.000000000000000000, 0.9510565162951535312, 1.000000000000000000, 0.9510565162951535312, 1.000000000000000000, 0.9510565162951535312, 1.000000000000000000, 0.9510565162951535312, 1.000000000000000000, 0.9510565162951535312, 1.000000000000000000, 0.9510565162951535312, 1.000000000000000000, 0.9510565162951535312, 1.000000000000000000, 0.9836243115514174962, 0.9782066976764471899),
 ( 1.000000000000000000, 0.9510565162951535312, 1.000000000000000000, 0.9510565162951535312, 1.000000000000000000, 0.9510565162951535312, 1.000000000000000000, 0.9510565162951535312, 1.000000000000000000, 0.9510565162951535312, 1.000000000000000000, 0.9510565162951535312, 1.000000000000000000, 0.9510565162951535312, 1.000000000000000000, 0.9510565162951535312, 1.000000000000000000, 0.9510565162951535312, 1.000000000000000000, 0.9510565162951535312, 1.000000000000000000, 0.9510565162951535312, 1.000000000000000000, 0.9510565162951535312, 1.000000000000000000, 0.9510565162951535312, 1.000000000000000000, 0.9510565162951535312, 1.000000000000000000, 0.9510565162951535312, 1.000000000000000000, 0.9510565162951535312, 1.000000000000000000, 0.9510565162951535312, 1.000000000000000000, 0.9510565162951535312, 1.000000000000000000, 0.9510565162951535312, 1.000000000000000000, 0.9510565162951535312, 1.000000000000000000, 0.9510565162951535312, 1.000000000000000000, 0.9510565162951535312, 1.000000000000000000, 0.9510565162951535312, 1.000000000000000000, 0.9510565162951535312, 1.000000000000000000, 0.9510565162951535312, 1.000000000000000000, 0.9510565162951535312, 1.000000000000000000, 0.9510565162951535312, 1.000000000000000000, 0.9510565162951535312, 1.000000000000000000, 0.9510565162951535312, 1.000000000000000000, 0.9510565162951535312, 1.000000000000000000, 0.9510565162951535312, 1.000000000000000000, 0.9510565162951535312, 1.000000000000000000, 0.9510565162951535312, 1.000000000000000000, 0.9510565162951535312, 1.000000000000000000, 0.9510565162951535312, 1.000000000000000000, 0.9510565162951535312, 1.000000000000000000, 0.9510565162951535312, 1.000000000000000000, 0.9510565162951535312, 1.000000000000000000, 0.9510565162951535312, 1.000000000000000000, 0.9510565162951535312, 1.000000000000000000, 0.9510565162951535312, 1.000000000000000000, 0.9510565162951535312, 1.000000000000000000, 0.9510565162951535312, 1.000000000000000000, 0.9510565162951535312, 1.000000000000000000, 0.9510565162951535312, 1.000000000000000000, 0.9510565162951535312, 1.000000000000000000, 0.9510565162951535312, 1.000000000000000000, 0.9510565162951535312, 1.000000000000000000, 0.9510565162951535312, 1.000000000000000000, 0.9510565162951535312, 1.000000000000000000, 0.9510565162951535312, 1.000000000000000000, 0.9510565162951535312, 1.000000000000000000, 0.9510565162951535312, 1.000000000000000000, 0.9510565162951535312, 1.000000000000000000, 0.9510565162951535312, 1.000000000000000000, 0.9510565162951535312, 1.000000000000000000, 0.9510565162951535312, 1.000000000000000000, 0.9510565162951535312, 1.000000000000000000, 0.9510565162951535312, 1.000000000000000000, 0.9510565162951535312, 1.000000000000000000, 0.9510565162951535312, 1.000000000000000000, 0.9510565162951535312, 1.000000000000000000, 0.9510565162951535312, 1.000000000000000000, 0.9510565162951535312, 1.000000000000000000, 0.9510565162951535312, 1.000000000000000000, 0.9510565162951535312, 1.000000000000000000, 0.9510565162951535312, 1.000000000000000000, 0.9510565162951535312, 1.000000000000000000, 0.9510565162951535312, 1.000000000000000000, 0.9510565162951535312, 1.000000000000000000, 0.9510565162951535312, 1.000000000000000000, 0.9510565162951535312, 1.000000000000000000, 0.9510565162951535312, 1.000000000000000000, 0.9510565162951535312, 1.000000000000000000, 0.9510565162951535312, 1.000000000000000000, 0.9510565162951535312, 1.000000000000000000, 0.9510565162951535312, 1.000000000000000000, 0.9510565162951535312, 1.000000000000000000, 0.9510565162951535312, 1.000000000000000000, 0.9510565162951535312, 1.000000000000000000, 0.9510565162951535312, 1.000000000000000000, 0.9510565162951535312, 1.000000000000000000, 0.9510565162951535312, 1.000000000000000000, 0.9510565162951535312, 1.000000000000000000, 0.9510565162951535312, 1.000000000000000000, 0.9510565162951535312, 1.000000000000000000, 0.9510565162951535312, 1.000000000000000000, 0.9510565162951535312, 1.000000000000000000, 0.9510565162951535312, 1.000000000000000000, 0.9510565162951535312, 1.000000000000000000, 0.9510565162951535312, 1.000000000000000000, 0.9510565162951535312, 1.000000000000000000, 0.9510565162951535312, 1.000000000000000000, 0.9510565162951535312, 1.000000000000000000, 0.9510565162951535312, 1.000000000000000000, 0.9510565162951535312, 1.000000000000000000, 0.9510565162951535312, 1.000000000000000000, 0.9510565162951535312, 1.000000000000000000, 0.9510565162951535312, 1.000000000000000000, 0.9510565162951535312, 1.000000000000000000, 0.9510565162951535312, 1.000000000000000000, 0.9510565162951535312, 1.000000000000000000, 0.9510565162951535312, 1.000000000000000000, 0.9510565162951535312, 1.000000000000000000, 0.9510565162951535312, 1.000000000000000000, 0.9510565162951535312, 1.000000000000000000, 0.9510565162951535312, 1.000000000000000000, 0.9510565162951535312, 1.000000000000000000, 0.9510565162951535312, 1.000000000000000000, 0.9510565162951535312, 1.000000000000000000, 0.9510565162951535312, 1.000000000000000000, 0.9510565162951535312, 1.000000000000000000, 0.9510565162951535312, 1.000000000000000000, 0.9510565162951535312, 1.000000000000000000, 0.9510565162951535312, 1.000000000000000000, 0.9510565162951535312, 1.000000000000000000, 0.9510565162951535312, 1.000000000000000000, 0.9510565162951535312, 1.000000000000000000, 0.9510565162951535312, 1.000000000000000000, 0.9510565162951535312, 1.000000000000000000, 0.9510565162951535312, 1.000000000000000000, 0.9510565162951535312, 1.000000000000000000, 0.9510565162951535312, 1.000000000000000000, 0.9510565162951535312, 1.000000000000000000, 0.9510565162951535312, 1.000000000000000000, 0.9510565162951535312, 1.000000000000000000, 0.9510565162951535312, 1.000000000000000000, 0.9510565162951535312, 1.000000000000000000, 0.9510565162951535312, 1.000000000000000000, 0.9510565162951535312, 1.000000000000000000, 0.9510565162951535312, 1.000000000000000000, 0.9510565162951535312, 1.000000000000000000, 0.9510565162951535312, 1.000000000000000000, 0.9510565162951535312, 1.000000000000000000, 0.9510565162951535312, 1.000000000000000000, 0.9510565162951535312, 1.000000000000000000, 0.9510565162951535312, 1.000000000000000000, 0.9510565162951535312, 1.000000000000000000, 0.9510565162951535312, 1.000000000000000000, 0.9510565162951535312, 1.000000000000000000, 0.9510565162951535312, 1.000000000000000000, 0.9510565162951535312, 1.000000000000000000, 0.9510565162951535312, 1.000000000000000000, 0.9510565162951535312, 1.000000000000000000, 0.9510565162951535312, 1.000000000000000000, 0.9510565162951535312, 1.000000000000000000, 0.9510565162951535312, 1.000000000000000000, 0.9510565162951535312, 1.000000000000000000, 0.9510565162951535312, 1.000000000000000000, 0.9510565162951535312, 1.000000000000000000, 0.9510565162951535312, 1.000000000000000000, 0.9510565162951535312, 1.000000000000000000, 0.9510565162951535312, 1.000000000000000000, 0.9510565162951535312, 1.000000000000000000, 0.9510565162951535312, 1.000000000000000000, 0.9510565162951535312, 1.000000000000000000, 0.9510565162951535312, 1.000000000000000000, 0.9510565162951535312, 1.000000000000000000, 0.9510565162951535312, 1.000000000000000000, 0.9510565162951535312, 1.000000000000000000, 0.9510565162951535312, 1.000000000000000000, 0.9510565162951535312, 1.000000000000000000, 0.9510565162951535312, 1.000000000000000000, 0.9510565162951535312, 1.000000000000000000, 0.9510565162951535312, 1.000000000000000000, 0.9510565162951535312, 1.000000000000000000, 0.9510565162951535312, 1.000000000000000000, 0.9510565162951535312, 1.000000000000000000, 0.9510565162951535312, 1.000000000000000000, 0.9510565162951535312, 1.000000000000000000, 0.9510565162951535312, 1.000000000000000000, 0.9510565162951535312, 1.000000000000000000, 0.9510565162951535312, 1.000000000000000000, 0.9510565162951535312, 1.000000000000000000, 0.9510565162951535312, 1.000000000000000000, 0.9510565162951535312, 1.000000000000000000, 0.9510565162951535312, 1.000000000000000000, 0.9510565162951535312, 1.000000000000000000, 0.9510565162951535312, 1.000000000000000000, 0.9510565162951535312, 1.000000000000000000, 0.9510565162951535312, 1.000000000000000000, 0.9510565162951535312, 1.000000000000000000, 0.9510565162951535312, 1.000000000000000000, 0.9510565162951535312, 1.000000000000000000, 0.9510565162951535312, 1.000000000000000000, 0.9510565162951535312, 1.000000000000000000, 0.9510565162951535312, 1.000000000000000000, 0.9510565162951535312, 1.000000000000000000, 0.9510565162951535312, 1.000000000000000000, 0.9510565162951535312, 1.000000000000000000, 0.9510565162951535312, 1.000000000000000000, 0.9510565162951535312, 1.000000000000000000, 0.9510565162951535312, 1.000000000000000000, 0.9510565162951535312, 1.000000000000000000, 0.9510565162951535312, 1.000000000000000000, 0.9510565162951535312, 1.000000000000000000, 0.9510565162951535312, 1.000000000000000000, 0.9510565162951535312, 1.000000000000000000, 0.9510565162951535312, 1.000000000000000000, 0.9510565162951535312, 1.000000000000000000, 0.9510565162951535312, 1.000000000000000000, 0.9510565162951535312, 1.000000000000000000, 0.9510565162951535312, 1.000000000000000000, 0.9510565162951535312, 1.000000000000000000, 0.9510565162951535312, 1.000000000000000000, 0.9510565162951535312, 1.000000000000000000, 0.9510565162951535312, 1.000000000000000000, 0.9510565162951535312, 1.000000000000000000, 0.9510565162951535312, 1.000000000000000000, 0.9510565162951535312, 1.000000000000000000, 0.9510565162951535312, 1.000000000000000000, 0.9510565162951535312, 1.000000000000000000, 0.9510565162951535312, 1.000000000000000000, 0.9510565162951535312, 1.000000000000000000, 0.9510565162951535312, 1.000000000000000000, 0.9510565162951535312, 1.000000000000000000, 0.9510565162951535312, 1.000000000000000000, 0.9510565162951535312, 1.000000000000000000, 0.9510565162951535312, 1.000000000000000000, 0.9510565162951535312, 1.000000000000000000, 0.9510565162951535312, 1.000000000000000000, 0.9510565162951535312, 1.000000000000000000, 0.9510565162951535312, 1.000000000000000000, 0.9510565162951535312, 1.000000000000000000, 0.9510565162951535312, 1.000000000000000000, 0.9510565162951535312, 1.000000000000000000, 0.9510565162951535312, 1.000000000000000000, 0.9510565162951535312, 1.000000000000000000, 0.9510565162951535312, 1.000000000000000000, 0.9510565162951535312, 1.000000000000000000, 0.9510565162951535312, 1.000000000000000000, 0.9510565162951535312, 1.000000000000000000, 0.9510565162951535312, 1.000000000000000000, 0.9510565162951535312, 1.000000000000000000, 0.9510565162951535312, 1.000000000000000000, 0.9510565162951535312, 1.000000000000000000, 0.9510565162951535312, 1.000000000000000000, 0.9510565162951535312, 1.000000000000000000, 0.9510565162951535312, 1.000000000000000000, 0.9510565162951535312, 1.000000000000000000, 0.9510565162951535312, 1.000000000000000000, 0.9510565162951535312, 1.000000000000000000, 0.9510565162951535312, 1.000000000000000000, 0.9510565162951535312, 1.000000000000000000, 0.9510565162951535312, 1.000000000000000000, 0.9510565162951535312, 1.000000000000000000, 0.9510565162951535312, 1.000000000000000000, 0.9510565162951535312, 1.000000000000000000, 0.9510565162951535312, 1.000000000000000000, 0.9510565162951535312, 1.000000000000000000, 0.9510565162951535312, 1.000000000000000000, 0.9510565162951535312, 1.000000000000000000, 0.9510565162951535312, 1.000000000000000000, 0.9510565162951535312, 1.000000000000000000, 0.9510565162951535312, 1.000000000000000000, 0.9510565162951535312, 1.000000000000000000, 0.9510565162951535312, 1.000000000000000000, 0.9510565162951535312, 1.000000000000000000, 0.9510565162951535312, 1.000000000000000000, 0.9510565162951535312, 1.000000000000000000, 0.9510565162951535312, 1.000000000000000000, 0.9510565162951535312, 1.000000000000000000, 0.9510565162951535312, 1.000000000000000000, 0.9510565162951535312, 1.000000000000000000, 0.9510565162951535312, 1.000000000000000000, 0.9510565162951535312, 1.000000000000000000, 0.9510565162951535312, 1.000000000000000000, 0.9510565162951535312, 1.000000000000000000, 0.9510565162951535312, 1.000000000000000000, 0.9510565162951535312, 1.000000000000000000, 0.9510565162951535312, 1.000000000000000000, 0.9510565162951535312, 1.000000000000000000, 0.9510565162951535312, 1.000000000000000000, 0.9510565162951535312, 1.000000000000000000, 0.9510565162951535312, 1.000000000000000000, 0.9510565162951535312, 1.000000000000000000, 0.9510565162951535312, 1.000000000000000000, 0.9510565162951535312, 1.000000000000000000, 0.9510565162951535312, 1.000000000000000000, 0.9510565162951535312, 1.000000000000000000, 0.9510565162951535312, 1.000000000000000000, 0.9510565162951535312, 1.000000000000000000, 0.9510565162951535312, 1.000000000000000000, 0.9510565162951535312, 1.000000000000000000, 0.9510565162951535312, 1.000000000000000000, 0.9510565162951535312, 1.000000000000000000, 0.9510565162951535312, 1.000000000000000000, 0.9510565162951535312, 1.000000000000000000, 0.9510565162951535312, 1.000000000000000000, 0.9510565162951535312, 1.000000000000000000, 0.9510565162951535312, 1.000000000000000000, 0.9510565162951535312, 1.000000000000000000, 0.9510565162951535312, 1.000000000000000000, 0.9510565162951535312, 1.000000000000000000, 0.9510565162951535312, 1.000000000000000000, 0.9510565162951535312, 1.000000000000000000, 0.9510565162951535312, 1.000000000000000000, 0.9510565162951535312, 1.000000000000000000, 0.9510565162951535312, 1.000000000000000000, 0.9510565162951535312, 1.000000000000000000, 0.9510565162951535312, 1.000000000000000000, 0.9510565162951535312, 1.000000000000000000, 0.9510565162951535312, 1.000000000000000000, 0.9510565162951535312, 1.000000000000000000, 0.9510565162951535312, 1.000000000000000000, 0.9510565162951535312, 1.000000000000000000, 0.9510565162951535312, 1.000000000000000000, 0.9510565162951535312, 1.000000000000000000, 0.9510565162951535312, 1.000000000000000000, 0.9510565162951535312, 1.000000000000000000, 0.9510565162951535312, 1.000000000000000000, 0.9510565162951535312, 1.000000000000000000, 0.9510565162951535312, 1.000000000000000000, 0.9510565162951535312, 1.000000000000000000, 0.9510565162951535312, 1.000000000000000000, 0.9510565162951535312, 1.000000000000000000, 0.9510565162951535312, 1.000000000000000000, 0.9510565162951535312, 1.000000000000000000, 0.9510565162951535312, 1.000000000000000000, 0.9510565162951535312, 1.000000000000000000, 0.9510565162951535312, 1.000000000000000000, 0.9510565162951535312, 1.000000000000000000, 0.9510565162951535312, 1.000000000000000000, 0.9510565162951535312, 1.000000000000000000, 0.9510565162951535312, 1.000000000000000000, 0.9510565162951535312, 1.000000000000000000, 0.9510565162951535312, 1.000000000000000000, 0.9510565162951535312, 1.000000000000000000, 0.9510565162951535312, 1.000000000000000000, 0.9510565162951535312, 1.000000000000000000, 0.9510565162951535312, 1.000000000000000000, 0.9510565162951535312, 1.000000000000000000, 0.9510565162951535312, 1.000000000000000000, 0.9836243115514174962, 0.9782066976764471899) ) ) 
 REPRESENTATION_ITEM ( '' )  SURFACE ( )  );
#18544=CARTESIAN_POINT ( 'NONE',  ( 38.58424406990784661, 77.96518717409396970, 32.77220824515698183 ) ) ;
#18545=CARTESIAN_POINT ( 'NONE',  ( 42.21948215057684450, 81.03738109496902098, 29.21067981925356705 ) ) ;
#18547=ORIENTED_EDGE ( 'NONE', *, *, #2884, .T. ) ;
#18548=CARTESIAN_POINT ( 'NONE',  ( 41.64333658814960870, 60.97977050742731109, 38.42115945441014446 ) ) ;
#18554=CARTESIAN_POINT ( 'NONE',  ( 43.01140435219951286, 156.8651871740940180, 38.86567161673127657 ) ) ;
#18557=CARTESIAN_POINT ( 'NONE',  ( 43.01140435219951286, 115.1297705074272955, 38.86567161673127657 ) ) ;
#18563=CARTESIAN_POINT ( 'NONE',  ( 45.74753988029933538, 158.0651871740940067, 30.44471234641811819 ) ) ;
#18573=CARTESIAN_POINT ( 'NONE',  ( 46.59305225739526435, 94.57977050742731251, 36.81289934271958941 ) ) ;
#18576=CARTESIAN_POINT ( 'NONE',  ( 44.37947211624943833, 79.01518717409400949, 38.42115945441014446 ) ) ;
#18577=AXIS2_PLACEMENT_3D ( 'NONE', #16805, #15158, #7012 ) ;
#18580=CARTESIAN_POINT ( 'NONE',  ( 39.92123440845005433, 138.2344580088725650, 38.46393386101375711 ) ) ;
#18582=CARTESIAN_POINT ( 'NONE',  ( 39.42975644700377558, 138.6797705074273210, 36.81289934271958941 ) ) ;
#18585=CARTESIAN_POINT ( 'NONE',  ( 39.42975644700377558, 60.67977050742731393, 36.81289934271958941 ) ) ;
#18587=CARTESIAN_POINT ( 'NONE',  ( 38.58424406990786082, 144.3797705074273097, 34.21067981925357060 ) ) ;
#18589=CARTESIAN_POINT ( 'NONE',  ( 38.58424406990784661, 96.52977050742730114, 35.64915139335016647 ) ) ;
#18590=CARTESIAN_POINT ( 'NONE',  ( 39.92123440845005433, 142.1604996726487400, 38.46393386101375711 ) ) ;
#18592=DIRECTION ( 'NONE',  ( 0.000000000000000000, 1.000000000000000000, 0.000000000000000000 ) ) ;
#18594=LINE ( 'NONE', #16925, #11519 ) ;
#18599=CARTESIAN_POINT ( 'NONE',  ( 38.96631938032478359, 144.0844580088725877, 37.14960608071593384 ) ) ;
#18600=CARTESIAN_POINT ( 'NONE',  ( 47.43856463449118621, 127.8797705074273239, 34.21067981925357060 ) ) ;
#18602=CARTESIAN_POINT ( 'NONE',  ( 39.92123440845005433, 141.2344580088725365, 38.46393386101375711 ) ) ;
#18603=CARTESIAN_POINT ( 'NONE',  ( 47.43856463449117911, 115.7651871740939953, 32.77220824515697473 ) ) ;
#18604=ADVANCED_FACE ( 'NONE', ( #16978 ), #3109, .T. ) ;
#18605=CARTESIAN_POINT ( 'NONE',  ( 42.21948215057684450, 126.4575765865522925, 39.21067981925355639 ) ) ;
#18608=CARTESIAN_POINT ( 'NONE',  ( 47.43856463449118621, 85.87977050742730967, 34.21067981925357060 ) ) ;
#18611=CARTESIAN_POINT ( 'NONE',  ( 44.55648932407425633, 72.68445800887258201, 38.96596240072933170 ) ) ;
#18613=CARTESIAN_POINT ( 'NONE',  ( 46.10157429594899270, 134.6604996726487684, 29.95742577749337343 ) ) ;
#18614=CARTESIAN_POINT ( 'NONE',  ( 41.64333658814960870, 83.51518717409400949, 30.00020018409699318 ) ) ;
#18616=EDGE_CURVE ( 'NONE', #15249, #10801, #16722, .T. ) ;
#18619=CYLINDRICAL_SURFACE ( 'NONE', #11467, 4.999999999999997335 ) ;
#18621=CARTESIAN_POINT ( 'NONE',  ( 43.01140435219957681, 93.53445800887259054, 39.21067981925356349 ) ) ;
#18622=CARTESIAN_POINT ( 'NONE',  ( 43.80332655382221674, 142.5373810949690210, 39.21067981925356349 ) ) ;
#18623=CARTESIAN_POINT ( 'NONE',  ( 47.43856463449117200, 151.7297705074273324, 35.64915139335016647 ) ) ;
#18626=CARTESIAN_POINT ( 'NONE',  ( 47.43856463449118621, 142.6151871740939896, 34.21067981925357060 ) ) ;
#18630=CARTESIAN_POINT ( 'NONE',  ( 41.64333658814960870, 62.51518717409400239, 30.00020018409699318 ) ) ;
#18634=CARTESIAN_POINT ( 'NONE',  ( 44.37947211624943833, 124.0151871740939953, 38.42115945441014446 ) ) ;
#18635=ORIENTED_EDGE ( 'NONE', *, *, #1438, .F. ) ;
#18637=CARTESIAN_POINT ( 'NONE',  ( 43.01140435219951286, 146.0344580088725479, 29.21067981925356705 ) ) ;
#18639=ADVANCED_FACE ( 'NONE', ( #3448 ), #13360, .T. ) ;
#18640=CARTESIAN_POINT ( 'NONE',  ( 46.10157429594899270, 97.73445800887256496, 29.95742577749337343 ) ) ;
#18641=CARTESIAN_POINT ( 'NONE',  ( 46.59305225739526435, 155.1797705074273210, 31.60846029578754468 ) ) ;
#18643=CARTESIAN_POINT ( 'NONE',  ( 39.42975644700377558, 60.07977050742731251, 31.60846029578754468 ) ) ;
#18644=CARTESIAN_POINT ( 'NONE',  ( 40.27526882409969033, 116.6651871740939868, 30.44471234641811819 ) ) ;
#18646=CARTESIAN_POINT ( 'NONE',  ( 41.46631938032478359, 85.31049967264874567, 38.96596240072933170 ) ) ;
#18647=CARTESIAN_POINT ( 'NONE',  ( 43.80332655382220253, 148.9575765865523067, 29.21067981925356705 ) ) ;
#18648=CARTESIAN_POINT ( 'NONE',  ( 43.01140435219957681, 97.46049967264875136, 39.21067981925356349 ) ) ;
#18650=CARTESIAN_POINT ( 'NONE',  ( 41.64333658814960870, 80.51518717409400949, 30.00020018409699318 ) ) ;
#18651=DIRECTION ( 'NONE',  ( 0.000000000000000000, 0.000000000000000000, 1.000000000000000000 ) ) ;
#18652=CARTESIAN_POINT ( 'NONE',  ( 47.05648932407426344, 126.9844580088725934, 37.14960608071593384 ) ) ;
#18660=CARTESIAN_POINT ( 'NONE',  ( 46.59305225739526435, 157.3151871740940067, 36.81289934271958941 ) ) ;
#18661=CARTESIAN_POINT ( 'NONE',  ( 45.74753988029933538, 100.1651871740939868, 37.97664729208901946 ) ) ;
#18663=CARTESIAN_POINT ( 'NONE',  ( 45.74753988029934249, 116.3297705074273125, 30.44471234641812174 ) ) ;
#18668=CARTESIAN_POINT ( 'NONE',  ( 40.27526882409969033, 111.8297705074272983, 37.97664729208901946 ) ) ;
#18669=CARTESIAN_POINT ( 'NONE',  ( 38.01140435219952707, 158.7844580088725763, 34.21067981925357060 ) ) ;
#18671=CARTESIAN_POINT ( 'NONE',  ( 39.42975644700377558, 141.4151871740940010, 36.81289934271958941 ) ) ;
#18672=( BOUNDED_CURVE ( )  B_SPLINE_CURVE ( 2, ( #21441, #11725, #5017, #16567, #18459, #19898, #8218, #19670, #4564, #13282, #2917, #20017, #13057 ),
 .UNSPECIFIED., .F., .F. ) 
 B_SPLINE_CURVE_WITH_KNOTS ( ( 3, 2, 2, 2, 2, 2, 3 ),
 ( 0.02205882352941176267, 0.02352941176470588203, 0.02647058823529411728, 0.02941176470588235253, 0.03235294117647059126, 0.03529411764705882304, 0.03676470588235294240 ),
 .UNSPECIFIED. ) 
 CURVE ( )  GEOMETRIC_REPRESENTATION_ITEM ( )  RATIONAL_B_SPLINE_CURVE ( ( 0.9755282581475768211, 0.9755282581475768211, 1.000000000000000000, 0.9510565162951535312, 1.000000000000000000, 0.9510565162951535312, 1.000000000000000000, 0.9510565162951535312, 1.000000000000000000, 0.9510565162951535312, 1.000000000000000000, 0.9755282581475768211, 0.9755282581475768211 ) ) 
 REPRESENTATION_ITEM ( '' )  );
#18678=LINE ( 'NONE', #15147, #16389 ) ;
#18679=CARTESIAN_POINT ( 'NONE',  ( 46.10157429594899270, 96.83445800887255928, 38.46393386101375711 ) ) ;
#18680=CARTESIAN_POINT ( 'NONE',  ( 38.01140435219952707, 98.78445800887259054, 34.21067981925357060 ) ) ;
#18681=CARTESIAN_POINT ( 'NONE',  ( 44.37947211624943833, 97.27977050742732956, 38.42115945441014446 ) ) ;
#18684=CARTESIAN_POINT ( 'NONE',  ( 43.01140435219951286, 75.86518717409398960, 38.86567161673127657 ) ) ;
#18686=ORIENTED_EDGE ( 'NONE', *, *, #14025, .F. ) ;
#18690=FACE_OUTER_BOUND ( 'NONE', #10049, .T. ) ;
#18691=CARTESIAN_POINT ( 'NONE',  ( 47.43856463449117911, 143.0297705074273154, 32.77220824515697473 ) ) ;
#18696=CARTESIAN_POINT ( 'NONE',  ( 39.42975644700377558, 135.0797705074272983, 31.60846029578754468 ) ) ;
#18697=CARTESIAN_POINT ( 'NONE',  ( 46.59305225739526435, 100.5797705074273267, 36.81289934271958941 ) ) ;
#18700=FACE_OUTER_BOUND ( 'NONE', #7720, .T. ) ;
#18702=CARTESIAN_POINT ( 'NONE',  ( 41.46631938032478359, 123.3844580088725849, 38.96596240072933170 ) ) ;
#18705=CARTESIAN_POINT ( 'NONE',  ( 46.10157429594899270, 138.8344580088725877, 38.46393386101376421 ) ) ;
#18706=CARTESIAN_POINT ( 'NONE',  ( 45.74753988029933538, 119.3297705074273267, 30.44471234641811819 ) ) ;
#18709=CARTESIAN_POINT ( 'NONE',  ( 39.42975644700377558, 105.4151871740940152, 36.81289934271958941 ) ) ;
#18714=CARTESIAN_POINT ( 'NONE',  ( 40.27526882409969744, 84.82977050742732672, 37.97664729208901235 ) ) ;
#18716=CARTESIAN_POINT ( 'NONE',  ( 43.01140435219951996, 10.71049967264875491, 34.21067981925357060 ) ) ;
#18717=CARTESIAN_POINT ( 'NONE',  ( 38.96631938032478359, 68.48445800887257917, 31.27175355779120025 ) ) ;
#18718=CARTESIAN_POINT ( 'NONE',  ( 43.01140435219951996, 10.71049967264875491, 39.21067981925356349 ) ) ;
#18719=CARTESIAN_POINT ( 'NONE',  ( 48.01140435219951996, 131.2104996726487514, 34.21067981925357060 ) ) ;
#18720=CARTESIAN_POINT ( 'NONE',  ( 45.74753988029933538, 91.16518717409397254, 37.97664729208901946 ) ) ;
#18724=CARTESIAN_POINT ( 'NONE',  ( 38.01140435219952707, 93.86049967264874283, 35.83527830041809636 ) ) ;
#18731=CARTESIAN_POINT ( 'NONE',  ( 47.43856463449117200, 155.0297705074273154, 32.77220824515698183 ) ) ;
#18732=CARTESIAN_POINT ( 'NONE',  ( 40.27526882409969033, 105.8297705074273125, 37.97664729208901946 ) ) ;
#18734=CARTESIAN_POINT ( 'NONE',  ( 43.01140435219951286, 138.8651871740940180, 38.86567161673127657 ) ) ;
#18736=CARTESIAN_POINT ( 'NONE',  ( 43.80332655382222384, 67.95757658655230671, 29.21067981925357770 ) ) ;
#18738=CARTESIAN_POINT ( 'NONE',  ( 40.27526882409969744, 59.66518717409400097, 30.44471234641812174 ) ) ;
#18741=CARTESIAN_POINT ( 'NONE',  ( 45.74753988029933538, 112.1651871740939868, 37.97664729208901946 ) ) ;
#18747=CARTESIAN_POINT ( 'NONE',  ( 41.46631938032478359, 102.3844580088725849, 38.96596240072933170 ) ) ;
#18748=CARTESIAN_POINT ( 'NONE',  ( 43.01140435219951286, 157.1297705074273097, 38.86567161673127657 ) ) ;
#18749=CARTESIAN_POINT ( 'NONE',  ( 40.27526882409969033, 59.92977050742730682, 30.44471234641811819 ) ) ;
#18750=CARTESIAN_POINT ( 'NONE',  ( 44.37947211624943833, 113.2151871740940123, 30.00020018409699318 ) ) ;
#18752=EDGE_CURVE ( 'NONE', #15773, #5761, #19123, .T. ) ;
#18753=CARTESIAN_POINT ( 'NONE',  ( 38.96631938032478359, 75.41049967264873999, 31.27175355779120025 ) ) ;
#18754=CARTESIAN_POINT ( 'NONE',  ( 43.01140435219951286, 107.0344580088725763, 29.21067981925356705 ) ) ;
#18758=CARTESIAN_POINT ( 'NONE',  ( 41.64333658814960870, 81.71518717409399812, 38.42115945441014446 ) ) ;
#18766=ORIENTED_EDGE ( 'NONE', *, *, #6823, .F. ) ;
#18767=CARTESIAN_POINT ( 'NONE',  ( 45.74753988029933538, 155.0651871740940067, 30.44471234641811819 ) ) ;
#18768=CARTESIAN_POINT ( 'NONE',  ( 46.59305225739526435, 157.9151871740940010, 31.60846029578754468 ) ) ;
#18769=CARTESIAN_POINT ( 'NONE',  ( 40.27526882409969744, 104.9297705074273210, 30.44471234641812174 ) ) ;
#18775=CARTESIAN_POINT ( 'NONE',  ( 43.01140435219951286, 128.0344580088725479, 29.21067981925356705 ) ) ;
#18776=CARTESIAN_POINT ( 'NONE',  ( 39.42975644700377558, 84.07977050742732672, 31.60846029578754468 ) ) ;
#18777=CARTESIAN_POINT ( 'NONE',  ( 46.59305225739526435, 142.9151871740940294, 31.60846029578754468 ) ) ;
#18780=CARTESIAN_POINT ( 'NONE',  ( 43.01140435219951286, 107.0344580088725763, 29.21067981925356705 ) ) ;
#18783=CARTESIAN_POINT ( 'NONE',  ( 48.01140435219951996, 77.06049967264874567, 35.83527830041809636 ) ) ;
#18785=CARTESIAN_POINT ( 'NONE',  ( 43.01140435219951286, 82.12977050742730967, 38.86567161673127657 ) ) ;
#18788=EDGE_CURVE ( 'NONE', #15486, #16987, #8570, .T. ) ;
#18789=CARTESIAN_POINT ( 'NONE',  ( 39.42975644700377558, 80.81518717409400665, 31.60846029578754468 ) ) ;
#18797=CARTESIAN_POINT ( 'NONE',  ( 46.59305225739526435, 61.57977050742731251, 36.81289934271958941 ) ) ;
#18800=CARTESIAN_POINT ( 'NONE',  ( 43.01140435219951286, 136.1297705074273381, 38.86567161673127657 ) ) ;
#18801=CARTESIAN_POINT ( 'NONE',  ( 47.43856463449117200, 61.46518717409399102, 35.64915139335016647 ) ) ;
#18805=CARTESIAN_POINT ( 'NONE',  ( 46.59305225739526435, 94.91518717409400097, 31.60846029578754468 ) ) ;
#18806=CARTESIAN_POINT ( 'NONE',  ( 43.01140435219951996, 10.71049967264875491, 29.21067981925357060 ) ) ;
#18810=CARTESIAN_POINT ( 'NONE',  ( 47.05648932407426344, 142.5844580088725877, 31.27175355779120025 ) ) ;
#18811=CARTESIAN_POINT ( 'NONE',  ( 47.43856463449117200, 124.7297705074273182, 35.64915139335016647 ) ) ;
#18814=CARTESIAN_POINT ( 'NONE',  ( 45.74753988029934249, 103.1651871740940152, 37.97664729208901235 ) ) ;
#18815=DIRECTION ( 'NONE',  ( 0.000000000000000000, 1.000000000000000000, 0.000000000000000000 ) ) ;
#18819=CARTESIAN_POINT ( 'NONE',  ( 44.37947211624943833, 86.47977050742731819, 30.00020018409699318 ) ) ;
#18822=CARTESIAN_POINT ( 'NONE',  ( 43.01140435219954838, 133.4604996726487514, 39.21067981925356349 ) ) ;
#18823=CARTESIAN_POINT ( 'NONE',  ( 38.01140435219951996, 71.63445800887258486, 32.58608133808903773 ) ) ;
#18826=CARTESIAN_POINT ( 'NONE',  ( 38.01140435219951996, 132.8604996726487286, 35.83527830041810347 ) ) ;
#18827=CARTESIAN_POINT ( 'NONE',  ( 45.74753988029933538, 88.16518717409397254, 37.97664729208901946 ) ) ;
#18832=LINE ( 'NONE', #427, #9676 ) ;
#18834=CARTESIAN_POINT ( 'NONE',  ( 42.21948215057684450, 92.11133943119284595, 29.21067981925356705 ) ) ;
#18836=CARTESIAN_POINT ( 'NONE',  ( 40.27526882409969033, 153.8297705074273267, 37.97664729208901946 ) ) ;
#18837=CARTESIAN_POINT ( 'NONE',  ( 38.58424406990786082, 102.3797705074273381, 34.21067981925357060 ) ) ;
#18839=CARTESIAN_POINT ( 'NONE',  ( 46.59305225739526435, 139.9151871740940010, 31.60846029578754468 ) ) ;
#18842=CARTESIAN_POINT ( 'NONE',  ( 43.01140435219951286, 90.53445800887257633, 39.21067981925356349 ) ) ;
#18844=CARTESIAN_POINT ( 'NONE',  ( 41.46631938032478359, 135.3844580088725706, 38.96596240072933170 ) ) ;
#18845=CARTESIAN_POINT ( 'NONE',  ( 38.58424406990784661, 114.2651871740940095, 35.64915139335016647 ) ) ;
#18849=CARTESIAN_POINT ( 'NONE',  ( 47.05648932407426344, 102.9844580088725792, 37.14960608071593384 ) ) ;
#18851=CARTESIAN_POINT ( 'NONE',  ( 47.43856463449117911, 152.0297705074273438, 32.77220824515697473 ) ) ;
#18852=CARTESIAN_POINT ( 'NONE',  ( 47.05648932407426344, 154.9104996726487400, 37.14960608071593384 ) ) ;
#18853=CARTESIAN_POINT ( 'NONE',  ( 43.01140435219951286, 114.8651871740939754, 38.86567161673127657 ) ) ;
#18855=CARTESIAN_POINT ( 'NONE',  ( 48.01140435219951996, 71.06049967264871725, 35.83527830041810347 ) ) ;
#18857=CARTESIAN_POINT ( 'NONE',  ( 43.01140435219951286, 135.5344580088725763, 39.21067981925356349 ) ) ;
#18859=CARTESIAN_POINT ( 'NONE',  ( 39.92123440845005433, 72.23445800887256496, 38.46393386101375711 ) ) ;
#18861=CARTESIAN_POINT ( 'NONE',  ( 43.01140435219951286, 77.36518717409400381, 29.55568802177586463 ) ) ;
#18869=CARTESIAN_POINT ( 'NONE',  ( 44.37947211624943833, 148.0151871740940237, 38.42115945441014446 ) ) ;
#18871=CARTESIAN_POINT ( 'NONE',  ( 43.01140435219951286, 91.46049967264873715, 39.21067981925356349 ) ) ;
#18872=CARTESIAN_POINT ( 'NONE',  ( 40.27526882409969744, 101.9297705074273068, 30.44471234641812174 ) ) ;
#18874=ORIENTED_EDGE ( 'NONE', *, *, #16016, .F. ) ;
#18879=CARTESIAN_POINT ( 'NONE',  ( 38.96631938032478359, 127.0104996726487343, 37.14960608071593384 ) ) ;
#18880=CARTESIAN_POINT ( 'NONE',  ( 45.74753988029933538, 148.1651871740940010, 37.97664729208901946 ) ) ;
#18881=CARTESIAN_POINT ( 'NONE',  ( 46.10157429594899270, 104.6604996726487116, 29.95742577749337343 ) ) ;
#18883=CARTESIAN_POINT ( 'NONE',  ( 42.21948215057684450, 61.38361825032846752, 39.21067981925355639 ) ) ;
#18886=DIRECTION ( 'NONE',  ( 0.000000000000000000, 1.000000000000000000, 0.000000000000000000 ) ) ;
#18888=CARTESIAN_POINT ( 'NONE',  ( 43.80332655382220253, 64.95757658655230671, 29.21067981925356705 ) ) ;
#18890=AXIS2_PLACEMENT_3D ( 'NONE', #2679, #7879, #11494 ) ;
#18891=CARTESIAN_POINT ( 'NONE',  ( 39.42975644700377558, 84.67977050742732104, 36.81289934271958941 ) ) ;
#18893=CARTESIAN_POINT ( 'NONE',  ( 47.43856463449117911, 79.76518717409400949, 32.77220824515697473 ) ) ;
#18898=CARTESIAN_POINT ( 'NONE',  ( 42.21948215057684450, 69.45757658655230671, 39.21067981925355639 ) ) ;
#18899=CARTESIAN_POINT ( 'NONE',  ( 43.01140435219951286, 83.96049967264873715, 29.21067981925356705 ) ) ;
#18900=CARTESIAN_POINT ( 'NONE',  ( 46.59305225739526435, 131.1797705074273210, 31.60846029578754468 ) ) ;
#18902=ORIENTED_EDGE ( 'NONE', *, *, #11208, .T. ) ;
#18903=ADVANCED_FACE ( 'NONE', ( #7836 ), #14432, .T. ) ;
#18904=FACE_OUTER_BOUND ( 'NONE', #11850, .T. ) ;
#18907=CARTESIAN_POINT ( 'NONE',  ( 40.27526882409969033, 131.9297705074273210, 30.44471234641811819 ) ) ;
#18909=EDGE_CURVE ( 'NONE', #19332, #1684, #16143, .T. ) ;
#18910=CARTESIAN_POINT ( 'NONE',  ( 43.01140435219951286, 60.86518717409400381, 38.86567161673127657 ) ) ;
#18915=CARTESIAN_POINT ( 'NONE',  ( 38.58424406990786082, 93.11518717409400381, 34.21067981925357060 ) ) ;
#18917=DIRECTION ( 'NONE',  ( 0.000000000000000000, 1.000000000000000000, 0.000000000000000000 ) ) ;
#18920=CARTESIAN_POINT ( 'NONE',  ( 47.05648932407426344, 144.9844580088725934, 37.14960608071593384 ) ) ;
#18921=CARTESIAN_POINT ( 'NONE',  ( 43.01140435219951286, 118.1297705074273097, 38.86567161673127657 ) ) ;
#18923=FACE_OUTER_BOUND ( 'NONE', #17994, .T. ) ;
#18924=CARTESIAN_POINT ( 'NONE',  ( 46.59305225739526435, 109.9151871740940010, 31.60846029578754468 ) ) ;
#18928=CARTESIAN_POINT ( 'NONE',  ( 43.01140435219951286, 156.5344580088725479, 39.21067981925355639 ) ) ;
#18930=( BOUNDED_CURVE ( )  B_SPLINE_CURVE ( 2, ( #17221, #18888, #10735, #20871, #7328, #2241, #12599, #14353, #5540, #17655, #12267, #15891, #19002 ),
 .UNSPECIFIED., .F., .F. ) 
 B_SPLINE_CURVE_WITH_KNOTS ( ( 3, 2, 2, 2, 2, 2, 3 ),
 ( 0.9191176470588234837, 0.9205882352941175961, 0.9235294117647059320, 0.9264705882352941568, 0.9294117647058823817, 0.9323529411764706065, 0.9338235294117647189 ),
 .UNSPECIFIED. ) 
 CURVE ( )  GEOMETRIC_REPRESENTATION_ITEM ( )  RATIONAL_B_SPLINE_CURVE ( ( 0.9755282581475768211, 0.9755282581475768211, 1.000000000000000000, 0.9510565162951535312, 1.000000000000000000, 0.9510565162951535312, 1.000000000000000000, 0.9510565162951535312, 1.000000000000000000, 0.9510565162951535312, 1.000000000000000000, 0.9755282581475768211, 0.9755282581475768211 ) ) 
 REPRESENTATION_ITEM ( '' )  );
#18934=CARTESIAN_POINT ( 'NONE',  ( 45.74753988029934249, 89.32977050742732672, 30.44471234641812174 ) ) ;
#18937=CARTESIAN_POINT ( 'NONE',  ( 43.01140435219951286, 77.03445800887259054, 28.95336869806222779 ) ) ;
#18939=CARTESIAN_POINT ( 'NONE',  ( 48.01140435219951996, 134.3604996726487570, 32.58608133808903773 ) ) ;
#18940=CARTESIAN_POINT ( 'NONE',  ( 41.64333658814960870, 87.71518717409399812, 38.42115945441014446 ) ) ;
#18944=CARTESIAN_POINT ( 'NONE',  ( 42.21948215057684450, 93.03738109496902098, 29.21067981925356705 ) ) ;
#18945=CARTESIAN_POINT ( 'NONE',  ( 43.80332655382220253, 127.9575765865522925, 29.21067981925356705 ) ) ;
#18946=CARTESIAN_POINT ( 'NONE',  ( 42.21948215057684450, 81.45757658655229250, 39.21067981925355639 ) ) ;
#18947=CARTESIAN_POINT ( 'NONE',  ( 44.55648932407425633, 67.61049967264872862, 38.96596240072933170 ) ) ;
#18949=CARTESIAN_POINT ( 'NONE',  ( 43.01140435219951286, 101.6297705074273239, 29.55568802177586463 ) ) ;
#18951=CARTESIAN_POINT ( 'NONE',  ( 47.43856463449117911, 133.7651871740939669, 32.77220824515697473 ) ) ;
#18954=CARTESIAN_POINT ( 'NONE',  ( 40.27526882409969033, 63.82977050742731961, 37.97664729208901946 ) ) ;
#18957=CARTESIAN_POINT ( 'NONE',  ( 43.01140435219951996, 10.71049967264875491, 34.21067981925357060 ) ) ;
#18958=CARTESIAN_POINT ( 'NONE',  ( 39.42975644700377558, 110.8151871740939924, 31.60846029578754468 ) ) ;
#18963=CARTESIAN_POINT ( 'NONE',  ( 46.10157429594899270, 105.8344580088725735, 38.46393386101376421 ) ) ;
#18964=CARTESIAN_POINT ( 'NONE',  ( 45.74753988029934249, 149.3297705074273267, 30.44471234641812174 ) ) ;
#18965=CARTESIAN_POINT ( 'NONE',  ( 41.64333658814960870, 59.77977050742731535, 30.00020018409699318 ) ) ;
#18966=CARTESIAN_POINT ( 'NONE',  ( 43.01140435219951286, 116.3651871740939896, 29.55568802177586463 ) ) ;
#18968=CARTESIAN_POINT ( 'NONE',  ( 38.96631938032478359, 70.01049967264874851, 37.14960608071593384 ) ) ;
#18970=CARTESIAN_POINT ( 'NONE',  ( 48.01140435219951996, 136.1344580088725706, 35.83527830041809636 ) ) ;
#18973=CARTESIAN_POINT ( 'NONE',  ( 46.59305225739526435, 82.91518717409400097, 31.60846029578754468 ) ) ;
#18981=EDGE_LOOP ( 'NONE', ( #21345, #2769, #2771, #15982 ) ) ;
#18982=CARTESIAN_POINT ( 'NONE',  ( 47.43856463449118621, 145.6151871740939896, 34.21067981925357060 ) ) ;
#18984=CARTESIAN_POINT ( 'NONE',  ( 46.59305225739526435, 109.5797705074273125, 36.81289934271958941 ) ) ;
#18986=VERTEX_POINT ( 'NONE', #4193 ) ;
#18989=( BOUNDED_CURVE ( )  B_SPLINE_CURVE ( 2, ( #18621, #15426, #7270, #10251, #17384, #15314, #321, #7052, #13757, #20497, #12102, #18834, #3739 ),
 .UNSPECIFIED., .F., .F. ) 
 B_SPLINE_CURVE_WITH_KNOTS ( ( 3, 2, 2, 2, 2, 2, 3 ),
 ( 0.6397058823529411242, 0.6411764705882353477, 0.6441176470588235725, 0.6470588235294117974, 0.6500000000000000222, 0.6529411764705882470, 0.6544117647058823595 ),
 .UNSPECIFIED. ) 
 CURVE ( )  GEOMETRIC_REPRESENTATION_ITEM ( )  RATIONAL_B_SPLINE_CURVE ( ( 0.9755282581475768211, 0.9755282581475758219, 1.000000000000000000, 0.9510565162951535312, 1.000000000000000000, 0.9510565162951535312, 1.000000000000000000, 0.9510565162951535312, 1.000000000000000000, 0.9510565162951535312, 1.000000000000000000, 0.9755282581475768211, 0.9755282581475768211 ) ) 
 REPRESENTATION_ITEM ( '' )  );
#18991=CARTESIAN_POINT ( 'NONE',  ( 46.59305225739526435, 112.5797705074273125, 36.81289934271958941 ) ) ;
#18992=EDGE_CURVE ( 'NONE', #20113, #6422, #106, .T. ) ;
#18995=CARTESIAN_POINT ( 'NONE',  ( 44.37947211624943833, 83.47977050742731819, 30.00020018409699318 ) ) ;
#18996=CARTESIAN_POINT ( 'NONE',  ( 39.42975644700377558, 144.4151871740940294, 36.81289934271958941 ) ) ;
#18997=CARTESIAN_POINT ( 'NONE',  ( 41.46631938032478359, 97.31049967264873146, 38.96596240072933170 ) ) ;
#19002=CARTESIAN_POINT ( 'NONE',  ( 43.01140435219951286, 63.53445800887256922, 39.21067981925356349 ) ) ;
#19003=CARTESIAN_POINT ( 'NONE',  ( 43.01140435219951286, 107.0344580088725763, 29.21067981925356705 ) ) ;
#19004=VECTOR ( 'NONE', #16623, 1000.000000000000000 ) ;
#19005=CARTESIAN_POINT ( 'NONE',  ( 38.58424406990784661, 81.52977050742732956, 35.64915139335016647 ) ) ;
#19007=CARTESIAN_POINT ( 'NONE',  ( 45.74753988029934249, 77.06518717409399244, 30.44471234641812174 ) ) ;
#19010=ORIENTED_EDGE ( 'NONE', *, *, #5620, .T. ) ;
#19011=CARTESIAN_POINT ( 'NONE',  ( 38.96631938032478359, 69.08445800887258770, 37.14960608071593384 ) ) ;
#19013=CARTESIAN_POINT ( 'NONE',  ( 38.58424406990786082, 129.3797705074273381, 34.21067981925357060 ) ) ;
#19018=VERTEX_POINT ( 'NONE', #4727 ) ;
#19019=CARTESIAN_POINT ( 'NONE',  ( 40.27526882409969033, 135.8297705074273551, 37.97664729208901946 ) ) ;
#19023=CARTESIAN_POINT ( 'NONE',  ( 38.01140435219952707, 129.8604996726487286, 35.83527830041809636 ) ) ;
#19025=CARTESIAN_POINT ( 'NONE',  ( 41.64333658814960870, 96.71518717409399812, 38.42115945441014446 ) ) ;
#19030=CARTESIAN_POINT ( 'NONE',  ( 38.01140435219951996, 134.6344580088725422, 32.58608133808903773 ) ) ;
#19031=CARTESIAN_POINT ( 'NONE',  ( 46.59305225739526435, 109.5797705074273125, 36.81289934271958941 ) ) ;
#19033=FACE_OUTER_BOUND ( 'NONE', #11035, .T. ) ;
#19034=CARTESIAN_POINT ( 'NONE',  ( 45.74753988029934249, 110.0651871740939782, 30.44471234641812174 ) ) ;
#19036=AXIS2_PLACEMENT_3D ( 'NONE', #19382, #14091, #7283 ) ;
#19037=CARTESIAN_POINT ( 'NONE',  ( 47.05648932407426344, 139.9104996726487400, 37.14960608071593384 ) ) ;
#19043=CARTESIAN_POINT ( 'NONE',  ( 40.27526882409969744, 75.82977050742731251, 37.97664729208901235 ) ) ;
#19045=CARTESIAN_POINT ( 'NONE',  ( 39.92123440845004723, 62.33445800887258059, 29.95742577749337343 ) ) ;
#19047=CARTESIAN_POINT ( 'NONE',  ( 38.01140435219952707, 126.7104996726487514, 34.21067981925357060 ) ) ;
#19048=CARTESIAN_POINT ( 'NONE',  ( 47.43856463449118621, 76.61518717409400381, 34.21067981925357060 ) ) ;
#19053=CARTESIAN_POINT ( 'NONE',  ( 41.46631938032478359, 80.18445800887258201, 29.45539723777780239 ) ) ;
#19054=DIRECTION ( 'NONE',  ( 0.000000000000000000, 0.000000000000000000, 1.000000000000000000 ) ) ;
#19056=CARTESIAN_POINT ( 'NONE',  ( 40.27526882409969033, 137.9297705074273210, 30.44471234641811819 ) ) ;
#19057=CARTESIAN_POINT ( 'NONE',  ( 41.64333658814960870, 105.9797705074273182, 38.42115945441014446 ) ) ;
#19059=CARTESIAN_POINT ( 'NONE',  ( 46.59305225739526435, 133.9151871740940010, 31.60846029578754468 ) ) ;
#19060=CARTESIAN_POINT ( 'NONE',  ( 47.05648932407426344, 67.58445800887258770, 31.27175355779120025 ) ) ;
#19063=CARTESIAN_POINT ( 'NONE',  ( 39.92123440845005433, 136.1604996726487400, 38.46393386101375711 ) ) ;
#19067=CARTESIAN_POINT ( 'NONE',  ( 40.27526882409969033, 110.6651871740940010, 30.44471234641811819 ) ) ;
#19069=CYLINDRICAL_SURFACE ( 'NONE', #787, 4.999999999999997335 ) ;
#19071=CARTESIAN_POINT ( 'NONE',  ( 39.92123440845004723, 93.23445800887256496, 38.46393386101376421 ) ) ;
#19074=CARTESIAN_POINT ( 'NONE',  ( 47.05648932407426344, 157.9104996726487400, 37.14960608071593384 ) ) ;
#19075=CARTESIAN_POINT ( 'NONE',  ( 38.58424406990786082, 114.1151871740939896, 34.21067981925357060 ) ) ;
#19077=CARTESIAN_POINT ( 'NONE',  ( 44.55648932407425633, 71.81049967264874567, 29.45539723777780239 ) ) ;
#19078=CARTESIAN_POINT ( 'NONE',  ( 43.01140435219951286, 136.4604996726487514, 39.21067981925356349 ) ) ;
#19079=CARTESIAN_POINT ( 'NONE',  ( 44.55648932407425633, 136.8844580088725706, 29.45539723777780239 ) ) ;
#19080=CARTESIAN_POINT ( 'NONE',  ( 44.55648932407425633, 82.88445800887257064, 29.45539723777780239 ) ) ;
#19083=CARTESIAN_POINT ( 'NONE',  ( 38.96631938032478359, 124.0104996726487343, 37.14960608071593384 ) ) ;
#19085=CARTESIAN_POINT ( 'NONE',  ( 45.74753988029933538, 70.16518717409397254, 37.97664729208901946 ) ) ;
#19094=CARTESIAN_POINT ( 'NONE',  ( 44.37947211624943833, 142.0151871740939953, 38.42115945441014446 ) ) ;
#19096=CARTESIAN_POINT ( 'NONE',  ( 43.01140435219951996, 149.0344580088725763, 29.21067981925357060 ) ) ;
#19097=CARTESIAN_POINT ( 'NONE',  ( 39.42975644700377558, 108.6797705074273352, 36.81289934271958941 ) ) ;
#19099=ORIENTED_EDGE ( 'NONE', *, *, #6520, .T. ) ;
#19100=AXIS2_PLACEMENT_3D ( 'NONE', #9648, #6328, #13054 ) ;
#19104=CARTESIAN_POINT ( 'NONE',  ( 38.58424406990784661, 81.52977050742732956, 35.64915139335016647 ) ) ;
#19105=CARTESIAN_POINT ( 'NONE',  ( 44.37947211624943833, 145.0151871740939953, 38.42115945441014446 ) ) ;
#19106=CARTESIAN_POINT ( 'NONE',  ( 38.01140435219951996, 102.8604996726487286, 35.83527830041810347 ) ) ;
#19108=EDGE_CURVE ( 'NONE', #15802, #2795, #18511, .T. ) ;
#19113=CARTESIAN_POINT ( 'NONE',  ( 46.10157429594899270, 106.7344580088725650, 29.95742577749336988 ) ) ;
#19115=CARTESIAN_POINT ( 'NONE',  ( 38.58424406990786082, 87.37977050742732388, 34.21067981925357060 ) ) ;
#19117=CARTESIAN_POINT ( 'NONE',  ( 45.74753988029934249, 68.06518717409399244, 30.44471234641812174 ) ) ;
#19120=ORIENTED_EDGE ( 'NONE', *, *, #21220, .F. ) ;
#19121=CARTESIAN_POINT ( 'NONE',  ( 38.96631938032478359, 68.48445800887257917, 31.27175355779120025 ) ) ;
#19123=( BOUNDED_CURVE ( )  B_SPLINE_CURVE ( 2, ( #17517, #15652, #20412, #18859, #5624, #7300, #6974, #2215, #20843, #13678, #5308, #20521, #12346 ),
 .UNSPECIFIED., .F., .F. ) 
 B_SPLINE_CURVE_WITH_KNOTS ( ( 3, 2, 2, 2, 2, 2, 3 ),
 ( 0.8455882352941176405, 0.8470588235294117530, 0.8499999999999999778, 0.8529411764705882026, 0.8558823529411764275, 0.8588235294117646523, 0.8602941176470588758 ),
 .UNSPECIFIED. ) 
 CURVE ( )  GEOMETRIC_REPRESENTATION_ITEM ( )  RATIONAL_B_SPLINE_CURVE ( ( 0.9755282581475768211, 0.9755282581475768211, 1.000000000000000000, 0.9510565162951535312, 1.000000000000000000, 0.9510565162951535312, 1.000000000000000000, 0.9510565162951535312, 1.000000000000000000, 0.9510565162951535312, 1.000000000000000000, 0.9755282581475758219, 0.9755282581475768211 ) ) 
 REPRESENTATION_ITEM ( '' )  );
#19124=CARTESIAN_POINT ( 'NONE',  ( 47.43856463449118621, 130.8797705074273381, 34.21067981925357060 ) ) ;
#19126=ORIENTED_EDGE ( 'NONE', *, *, #15302, .T. ) ;
#19128=ORIENTED_EDGE ( 'NONE', *, *, #19182, .F. ) ;
#19129=CARTESIAN_POINT ( 'NONE',  ( 46.59305225739526435, 137.1797705074273210, 31.60846029578754468 ) ) ;
#19132=CARTESIAN_POINT ( 'NONE',  ( 43.01140435219951286, 98.36518717409401802, 29.55568802177586463 ) ) ;
#19133=CARTESIAN_POINT ( 'NONE',  ( 47.05648932407426344, 132.9844580088725934, 37.14960608071593384 ) ) ;
#19137=CARTESIAN_POINT ( 'NONE',  ( 46.10157429594899270, 132.8344580088725593, 38.46393386101376421 ) ) ;
#19138=CARTESIAN_POINT ( 'NONE',  ( 41.64333658814960870, 110.7797705074273154, 30.00020018409699318 ) ) ;
#19141=CARTESIAN_POINT ( 'NONE',  ( 41.64333658814960870, 104.5151871740939953, 30.00020018409699318 ) ) ;
#19142=EDGE_LOOP ( 'NONE', ( #18361, #18500, #9087, #10605 ) ) ;
#19143=CARTESIAN_POINT ( 'NONE',  ( 48.01140435219951996, 76.28445800887257633, 34.21067981925357060 ) ) ;
#19147=CARTESIAN_POINT ( 'NONE',  ( 47.43856463449117911, 73.72977050742731819, 35.64915139335015937 ) ) ;
#19151=CARTESIAN_POINT ( 'NONE',  ( 48.01140435219951996, 116.3604996726487428, 32.58608133808903773 ) ) ;
#19152=CARTESIAN_POINT ( 'NONE',  ( 44.37947211624943833, 77.21518717409399812, 30.00020018409699318 ) ) ;
#19157=CARTESIAN_POINT ( 'NONE',  ( 42.21948215057684450, 80.11133943119284595, 29.21067981925356705 ) ) ;
#19160=EDGE_CURVE ( 'NONE', #2815, #1555, #3217, .T. ) ;
#19161=CARTESIAN_POINT ( 'NONE',  ( 38.58424406990784661, 141.2297705074273040, 32.77220824515698183 ) ) ;
#19163=CARTESIAN_POINT ( 'NONE',  ( 43.01140435219951286, 134.3651871740939612, 29.55568802177586107 ) ) ;
#19164=CARTESIAN_POINT ( 'NONE',  ( 39.92123440845005433, 70.16049967264873999, 38.46393386101375711 ) ) ;
#19166=DIRECTION ( 'NONE',  ( 0.000000000000000000, 1.000000000000000000, 0.000000000000000000 ) ) ;
#19170=FACE_OUTER_BOUND ( 'NONE', #4426, .T. ) ;
#19171=CARTESIAN_POINT ( 'NONE',  ( 44.37947211624943833, 119.2151871740939981, 30.00020018409699318 ) ) ;
#19176=CARTESIAN_POINT ( 'NONE',  ( 44.55648932407425633, 87.68445800887258201, 38.96596240072933170 ) ) ;
#19177=CARTESIAN_POINT ( 'NONE',  ( 46.59305225739526435, 152.1797705074273210, 31.60846029578754468 ) ) ;
#19179=CARTESIAN_POINT ( 'NONE',  ( 38.96631938032478359, 147.4104996726487400, 31.27175355779120025 ) ) ;
#19180=CARTESIAN_POINT ( 'NONE',  ( 44.37947211624943833, 104.2151871740939981, 30.00020018409699318 ) ) ;
#19182=EDGE_CURVE ( 'NONE', #1468, #17073, #8605, .T. ) ;
#19183=CARTESIAN_POINT ( 'NONE',  ( 43.01140435219951286, 71.96049967264873715, 28.95336869806222779 ) ) ;
#19185=CARTESIAN_POINT ( 'NONE',  ( 43.01140435219951286, 62.03445800887256922, 29.21067981925356705 ) ) ;
#19189=CARTESIAN_POINT ( 'NONE',  ( 38.58424406990784661, 68.96518717409398391, 32.77220824515698183 ) ) ;
#19198=CARTESIAN_POINT ( 'NONE',  ( 46.59305225739526435, 145.3151871740940067, 36.81289934271958941 ) ) ;
#19199=CARTESIAN_POINT ( 'NONE',  ( 44.37947211624943833, 109.2797705074273154, 38.42115945441014446 ) ) ;
#19201=EDGE_LOOP ( 'NONE', ( #15962, #4669, #16155, #18438 ) ) ;
#19206=VECTOR ( 'NONE', #1618, 1000.000000000000000 ) ;
#19207=ADVANCED_FACE ( 'NONE', ( #644 ), #2288, .T. ) ;
#19208=CARTESIAN_POINT ( 'NONE',  ( 46.59305225739526435, 133.3151871740940067, 36.81289934271958941 ) ) ;
#19209=CARTESIAN_POINT ( 'NONE',  ( 46.10157429594899270, 101.6604996726487542, 29.95742577749337343 ) ) ;
#19213=CARTESIAN_POINT ( 'NONE',  ( 41.46631938032478359, 152.1844580088725820, 29.45539723777780239 ) ) ;
#19214=CARTESIAN_POINT ( 'NONE',  ( 44.55648932407425633, 151.8844580088725991, 29.45539723777780239 ) ) ;
#19217=CARTESIAN_POINT ( 'NONE',  ( 46.59305225739526435, 82.57977050742731251, 36.81289934271958941 ) ) ;
#19219=CARTESIAN_POINT ( 'NONE',  ( 38.58424406990786082, 66.11518717409398960, 34.21067981925357060 ) ) ;
#19224=CARTESIAN_POINT ( 'NONE',  ( 38.01140435219952707, 68.63445800887258486, 32.58608133808903773 ) ) ;
#19225=DIRECTION ( 'NONE',  ( 0.000000000000000000, 0.000000000000000000, 1.000000000000000000 ) ) ;
#19226=CARTESIAN_POINT ( 'NONE',  ( 38.58424406990786082, 135.3797705074273381, 34.21067981925357060 ) ) ;
#19231=CARTESIAN_POINT ( 'NONE',  ( 38.58424406990786082, 129.3797705074273381, 34.21067981925357060 ) ) ;
#19232=CARTESIAN_POINT ( 'NONE',  ( 48.01140435219951996, 134.2104996726487514, 34.21067981925357060 ) ) ;
#19237=CARTESIAN_POINT ( 'NONE',  ( 38.58424406990784661, 102.2651871740939811, 35.64915139335016647 ) ) ;
#19238=DIRECTION ( 'NONE',  ( 0.000000000000000000, 1.000000000000000000, 0.000000000000000000 ) ) ;
#19239=CARTESIAN_POINT ( 'NONE',  ( 46.10157429594899270, 125.6604996726487542, 29.95742577749336988 ) ) ;
#19241=CARTESIAN_POINT ( 'NONE',  ( 43.01140435219954838, 132.5344580088725763, 39.21067981925356349 ) ) ;
#19242=CARTESIAN_POINT ( 'NONE',  ( 44.55648932407425633, 130.8844580088725706, 29.45539723777780239 ) ) ;
#19243=CARTESIAN_POINT ( 'NONE',  ( 45.74753988029933538, 113.3297705074273125, 30.44471234641811819 ) ) ;
#19244=( BOUNDED_CURVE ( )  B_SPLINE_CURVE ( 2, ( #15883, #12694, #20862, #2234, #796, #15782, #5644, #5531, #688, #576, #17211, #7207, #13909 ),
 .UNSPECIFIED., .F., .F. ) 
 B_SPLINE_CURVE_WITH_KNOTS ( ( 3, 2, 2, 2, 2, 2, 3 ),
 ( 0.6838235294117647189, 0.6852941176470588314, 0.6882352941176470562, 0.6911764705882352811, 0.6941176470588235059, 0.6970588235294117307, 0.6985294117647058432 ),
 .UNSPECIFIED. ) 
 CURVE ( )  GEOMETRIC_REPRESENTATION_ITEM ( )  RATIONAL_B_SPLINE_CURVE ( ( 0.9755282581475768211, 0.9755282581475768211, 1.000000000000000000, 0.9510565162951535312, 1.000000000000000000, 0.9510565162951535312, 1.000000000000000000, 0.9510565162951535312, 1.000000000000000000, 0.9510565162951535312, 1.000000000000000000, 0.9755282581475768211, 0.9755282581475768211 ) ) 
 REPRESENTATION_ITEM ( '' )  );
#19247=CARTESIAN_POINT ( 'NONE',  ( 46.59305225739526435, 94.91518717409400097, 31.60846029578754468 ) ) ;
#19248=DIRECTION ( 'NONE',  ( 0.000000000000000000, 1.000000000000000000, 0.000000000000000000 ) ) ;
#19249=CYLINDRICAL_SURFACE ( 'NONE', #2736, 4.999999999999997335 ) ;
#19253=ADVANCED_FACE ( 'NONE', ( #5386 ), #6945, .T. ) ;
#19255=LINE ( 'NONE', #17260, #17430 ) ;
#19256=CARTESIAN_POINT ( 'NONE',  ( 44.37947211624943833, 77.47977050742731819, 30.00020018409699318 ) ) ;
#19258=ORIENTED_EDGE ( 'NONE', *, *, #9655, .T. ) ;
#19260=CARTESIAN_POINT ( 'NONE',  ( 44.55648932407425633, 124.6104996726487428, 38.96596240072933170 ) ) ;
#19261=CARTESIAN_POINT ( 'NONE',  ( 38.58424406990784661, 75.26518717409399528, 35.64915139335016647 ) ) ;
#19264=EDGE_CURVE ( 'NONE', #5192, #5965, #6895, .T. ) ;
#19270=CARTESIAN_POINT ( 'NONE',  ( 40.27526882409969033, 144.8297705074273267, 37.97664729208901946 ) ) ;
#19272=CARTESIAN_POINT ( 'NONE',  ( 46.59305225739526435, 127.3151871740940067, 36.81289934271958941 ) ) ;
#19273=CARTESIAN_POINT ( 'NONE',  ( 46.10157429594899270, 136.7604996726487627, 38.46393386101375711 ) ) ;
#19279=CARTESIAN_POINT ( 'NONE',  ( 45.74753988029933538, 106.1651871740940152, 37.97664729208901946 ) ) ;
#19280=EDGE_LOOP ( 'NONE', ( #840, #17530, #20456, #10724 ) ) ;
#19282=CARTESIAN_POINT ( 'NONE',  ( 46.10157429594899270, 86.66049967264872578, 29.95742577749336988 ) ) ;
#19283=EDGE_CURVE ( 'NONE', #13772, #7609, #18989, .T. ) ;
#19285=CARTESIAN_POINT ( 'NONE',  ( 46.10157429594899270, 93.83445800887258770, 38.46393386101376421 ) ) ;
#19286=CARTESIAN_POINT ( 'NONE',  ( 47.43856463449118621, 151.8797705074273097, 34.21067981925357060 ) ) ;
#19287=CARTESIAN_POINT ( 'NONE',  ( 44.55648932407425633, 151.6104996726487570, 38.96596240072933170 ) ) ;
#19288=CARTESIAN_POINT ( 'NONE',  ( 45.74753988029933538, 107.0651871740939640, 30.44471234641811819 ) ) ;
#19290=CARTESIAN_POINT ( 'NONE',  ( 39.92123440845004723, 63.26049967264874141, 29.95742577749337343 ) ) ;
#19296=CARTESIAN_POINT ( 'NONE',  ( 40.27526882409969033, 65.66518717409398675, 30.44471234641811819 ) ) ;
#19304=CARTESIAN_POINT ( 'NONE',  ( 44.37947211624943833, 130.0151871740939953, 38.42115945441014446 ) ) ;
#19306=CARTESIAN_POINT ( 'NONE',  ( 39.42975644700377558, 93.67977050742732104, 36.81289934271958941 ) ) ;
#19311=CARTESIAN_POINT ( 'NONE',  ( 39.92123440845004723, 113.3344580088725593, 29.95742577749337343 ) ) ;
#19312=CARTESIAN_POINT ( 'NONE',  ( 38.96631938032478359, 76.01049967264873430, 37.14960608071593384 ) ) ;
#19313=CARTESIAN_POINT ( 'NONE',  ( 44.37947211624943833, 77.47977050742731819, 30.00020018409699318 ) ) ;
#19314=CARTESIAN_POINT ( 'NONE',  ( 39.42975644700377558, 137.8151871740940067, 31.60846029578754468 ) ) ;
#19315=CARTESIAN_POINT ( 'NONE',  ( 43.01140435219951286, 89.96049967264872294, 28.95336869806222779 ) ) ;
#19319=CARTESIAN_POINT ( 'NONE',  ( 48.01140435219951996, 158.2104996726487514, 34.21067981925357060 ) ) ;
#19321=CARTESIAN_POINT ( 'NONE',  ( 47.05648932407426344, 105.9844580088725792, 37.14960608071593384 ) ) ;
#19323=CARTESIAN_POINT ( 'NONE',  ( 39.42975644700377558, 72.67977050742730682, 36.81289934271958941 ) ) ;
#19326=DIRECTION ( 'NONE',  ( 0.000000000000000000, 1.000000000000000000, 0.000000000000000000 ) ) ;
#19327=ORIENTED_EDGE ( 'NONE', *, *, #17399, .F. ) ;
#19330=CARTESIAN_POINT ( 'NONE',  ( 43.01140435219951286, 125.0344580088725905, 29.21067981925356705 ) ) ;
#19331=CARTESIAN_POINT ( 'NONE',  ( 39.42975644700377558, 138.0797705074273267, 31.60846029578754468 ) ) ;
#19332=VERTEX_POINT ( 'NONE', #19478 ) ;
#19335=CARTESIAN_POINT ( 'NONE',  ( 46.59305225739526435, 130.5797705074273267, 36.81289934271958941 ) ) ;
#19336=CARTESIAN_POINT ( 'NONE',  ( 47.05648932407426344, 110.5104996726487343, 31.27175355779120025 ) ) ;
#19337=CARTESIAN_POINT ( 'NONE',  ( 43.01140435219951996, 10.71049967264875491, 29.21067981925357060 ) ) ;
#19341=CARTESIAN_POINT ( 'NONE',  ( 46.10157429594899270, 74.66049967264873999, 29.95742577749336988 ) ) ;
#19344=ADVANCED_FACE ( 'NONE', ( #1182 ), #4058, .T. ) ;
#19346=CARTESIAN_POINT ( 'NONE',  ( 48.01140435219951996, 109.1344580088725849, 35.83527830041809636 ) ) ;
#19347=CARTESIAN_POINT ( 'NONE',  ( 39.92123440845004723, 134.3344580088725877, 29.95742577749337343 ) ) ;
#19348=CARTESIAN_POINT ( 'NONE',  ( 43.01140435219951286, 112.1297705074272812, 38.86567161673127657 ) ) ;
#19351=CARTESIAN_POINT ( 'NONE',  ( 44.37947211624943833, 98.21518717409399812, 30.00020018409699318 ) ) ;
#19352=CARTESIAN_POINT ( 'NONE',  ( 42.21948215057684450, 91.38361825032848174, 39.21067981925355639 ) ) ;
#19353=ORIENTED_EDGE ( 'NONE', *, *, #6350, .T. ) ;
#19354=CARTESIAN_POINT ( 'NONE',  ( 43.01140435219951286, 75.53445800887257633, 39.21067981925356349 ) ) ;
#19359=CARTESIAN_POINT ( 'NONE',  ( 43.01140435219951286, 77.62977050742730967, 29.55568802177586107 ) ) ;
#19361=VERTEX_POINT ( 'NONE', #7594 ) ;
#19362=CARTESIAN_POINT ( 'NONE',  ( 41.64333658814960870, 158.7797705074273438, 30.00020018409699318 ) ) ;
#19364=CARTESIAN_POINT ( 'NONE',  ( 43.01140435219951286, 118.4604996726487514, 39.46799094044489209 ) ) ;
#19365=CARTESIAN_POINT ( 'NONE',  ( 40.27526882409969033, 81.56518717409399244, 37.97664729208901946 ) ) ;
#19369=CARTESIAN_POINT ( 'NONE',  ( 47.05648932407426344, 112.9104996726487400, 37.14960608071593384 ) ) ;
#19373=CARTESIAN_POINT ( 'NONE',  ( 43.01140435219951286, 103.4604996726487371, 39.21067981925356349 ) ) ;
#19375=CARTESIAN_POINT ( 'NONE',  ( 46.59305225739526435, 146.1797705074273495, 31.60846029578754468 ) ) ;
#19377=CARTESIAN_POINT ( 'NONE',  ( 41.64333658814960870, 122.5151871740940095, 30.00020018409699318 ) ) ;
#19382=CARTESIAN_POINT ( 'NONE',  ( 43.01140435219951996, 10.71049967264875491, 34.21067981925357060 ) ) ;
#19383=CARTESIAN_POINT ( 'NONE',  ( 47.43856463449118621, 103.6151871740940038, 34.21067981925357060 ) ) ;
#19387=CARTESIAN_POINT ( 'NONE',  ( 47.05648932407426344, 88.58445800887257349, 31.27175355779120025 ) ) ;
#19388=CARTESIAN_POINT ( 'NONE',  ( 42.21948215057684450, 131.1113394311928175, 29.21067981925355994 ) ) ;
#19389=CARTESIAN_POINT ( 'NONE',  ( 38.96631938032478359, 153.4104996726487400, 31.27175355779120025 ) ) ;
#19390=CARTESIAN_POINT ( 'NONE',  ( 38.58424406990786082, 105.1151871740940038, 34.21067981925357060 ) ) ;
#19392=CARTESIAN_POINT ( 'NONE',  ( 43.01140435219951286, 64.46049967264873715, 39.46799094044489209 ) ) ;
#19394=CARTESIAN_POINT ( 'NONE',  ( 48.01140435219951996, 61.13445800887256354, 35.83527830041809636 ) ) ;
#19397=CARTESIAN_POINT ( 'NONE',  ( 46.10157429594899270, 146.6604996726487400, 29.95742577749336988 ) ) ;
#19398=CARTESIAN_POINT ( 'NONE',  ( 38.58424406990786082, 69.11518717409400381, 34.21067981925357060 ) ) ;
#19407=CARTESIAN_POINT ( 'NONE',  ( 46.59305225739526435, 136.3151871740940351, 36.81289934271958941 ) ) ;
#19408=CARTESIAN_POINT ( 'NONE',  ( 46.59305225739526435, 94.57977050742731251, 36.81289934271958941 ) ) ;
#19414=EDGE_LOOP ( 'NONE', ( #13037, #2434 ) ) ;
#19415=CARTESIAN_POINT ( 'NONE',  ( 43.01140435219951286, 111.5344580088725763, 39.46799094044489209 ) ) ;
#19416=CARTESIAN_POINT ( 'NONE',  ( 38.01140435219952707, 75.71049967264873715, 34.21067981925357060 ) ) ;
#19417=CARTESIAN_POINT ( 'NONE',  ( 41.64333658814960870, 72.97977050742731819, 38.42115945441014446 ) ) ;
#19418=CARTESIAN_POINT ( 'NONE',  ( 47.43856463449118621, 139.6151871740939896, 34.21067981925357060 ) ) ;
#19419=CARTESIAN_POINT ( 'NONE',  ( 41.46631938032478359, 90.11049967264874283, 29.45539723777780239 ) ) ;
#19429=VERTEX_POINT ( 'NONE', #19373 ) ;
#19430=CARTESIAN_POINT ( 'NONE',  ( 38.58424406990786082, 78.37977050742732388, 34.21067981925357060 ) ) ;
#19434=AXIS2_PLACEMENT_3D ( 'NONE', #21392, #6278, #9275 ) ;
#19437=CARTESIAN_POINT ( 'NONE',  ( 43.01140435219951996, 10.71049967264875491, 39.21067981925356349 ) ) ;
#19438=CARTESIAN_POINT ( 'NONE',  ( 38.58424406990785371, 120.5297705074273154, 35.64915139335015937 ) ) ;
#19439=ORIENTED_EDGE ( 'NONE', *, *, #10703, .T. ) ;
#19440=CARTESIAN_POINT ( 'NONE',  ( 46.10157429594899270, 88.73445800887256496, 29.95742577749336988 ) ) ;
#19442=CARTESIAN_POINT ( 'NONE',  ( 44.37947211624943833, 131.4797705074273040, 30.00020018409699318 ) ) ;
#19443=CARTESIAN_POINT ( 'NONE',  ( 47.05648932407426344, 134.5104996726487343, 31.27175355779120025 ) ) ;
#19444=CARTESIAN_POINT ( 'NONE',  ( 39.92123440845004723, 60.23445800887256496, 38.46393386101376421 ) ) ;
#19446=CARTESIAN_POINT ( 'NONE',  ( 41.46631938032478359, 111.3844580088725849, 38.96596240072933170 ) ) ;
#19450=EDGE_CURVE ( 'NONE', #10912, #16002, #12432, .T. ) ;
#19451=CARTESIAN_POINT ( 'NONE',  ( 38.01140435219952707, 66.56049967264871725, 32.58608133808903773 ) ) ;
#19455=CARTESIAN_POINT ( 'NONE',  ( 41.46631938032478359, 131.1844580088725820, 29.45539723777780239 ) ) ;
#19456=CARTESIAN_POINT ( 'NONE',  ( 44.37947211624943833, 101.4797705074273182, 30.00020018409699318 ) ) ;
#19459=CARTESIAN_POINT ( 'NONE',  ( 47.43856463449118621, 94.61518717409400381, 34.21067981925357060 ) ) ;
#19466=CARTESIAN_POINT ( 'NONE',  ( 40.27526882409969744, 74.92977050742732104, 30.44471234641812174 ) ) ;
#19469=CARTESIAN_POINT ( 'NONE',  ( 47.43856463449118621, 151.8797705074273097, 34.21067981925357060 ) ) ;
#19471=CARTESIAN_POINT ( 'NONE',  ( 38.01140435219951996, 117.8604996726487428, 35.83527830041810347 ) ) ;
#19472=CARTESIAN_POINT ( 'NONE',  ( 45.74753988029933538, 77.06518717409399244, 30.44471234641811819 ) ) ;
#19478=CARTESIAN_POINT ( 'NONE',  ( 43.01140435219951286, 80.03445800887257633, 29.21067981925356705 ) ) ;
#19480=CARTESIAN_POINT ( 'NONE',  ( 47.43856463449117200, 136.7297705074272756, 35.64915139335016647 ) ) ;
#19482=CARTESIAN_POINT ( 'NONE',  ( 46.59305225739526435, 121.9151871740940010, 31.60846029578754468 ) ) ;
#19486=CARTESIAN_POINT ( 'NONE',  ( 39.92123440845005433, 135.2604996726487343, 29.95742577749336988 ) ) ;
#19489=CARTESIAN_POINT ( 'NONE',  ( 44.37947211624943833, 106.0151871740939953, 38.42115945441014446 ) ) ;
#19493=( BOUNDED_CURVE ( )  B_SPLINE_CURVE ( 2, ( #2965, #21385, #6618, #13217, #3302, #6733, #8269, #3192, #1647, #7939, #14643, #13113, #13438 ),
 .UNSPECIFIED., .F., .F. ) 
 B_SPLINE_CURVE_WITH_KNOTS ( ( 3, 2, 2, 2, 2, 2, 3 ),
 ( 0.8602941176470588758, 0.8617647058823529882, 0.8647058823529412130, 0.8676470588235294379, 0.8705882352941176627, 0.8735294117647058876, 0.8750000000000000000 ),
 .UNSPECIFIED. ) 
 CURVE ( )  GEOMETRIC_REPRESENTATION_ITEM ( )  RATIONAL_B_SPLINE_CURVE ( ( 0.9755282581475768211, 0.9755282581475777093, 1.000000000000000000, 0.9510565162951535312, 1.000000000000000000, 0.9510565162951535312, 1.000000000000000000, 0.9510565162951535312, 1.000000000000000000, 0.9510565162951535312, 1.000000000000000000, 0.9755282581475768211, 0.9755282581475768211 ) ) 
 REPRESENTATION_ITEM ( '' )  );
#19494=CARTESIAN_POINT ( 'NONE',  ( 46.10157429594899270, 94.73445800887257917, 29.95742577749337343 ) ) ;
#19495=CARTESIAN_POINT ( 'NONE',  ( 46.10157429594899270, 103.7344580088725792, 29.95742577749336988 ) ) ;
#19496=CARTESIAN_POINT ( 'NONE',  ( 38.01140435219951996, 147.8604996726487570, 35.83527830041810347 ) ) ;
#19497=CARTESIAN_POINT ( 'NONE',  ( 39.42975644700377558, 104.8151871740939924, 31.60846029578754468 ) ) ;
#19499=CARTESIAN_POINT ( 'NONE',  ( 38.96631938032478359, 64.01049967264873430, 37.14960608071593384 ) ) ;
#19501=DIRECTION ( 'NONE',  ( 0.000000000000000000, 0.000000000000000000, 1.000000000000000000 ) ) ;
#19502=CARTESIAN_POINT ( 'NONE',  ( 44.55648932407425633, 118.8844580088725849, 29.45539723777780239 ) ) ;
#19504=CARTESIAN_POINT ( 'NONE',  ( 43.01140435219951286, 72.86518717409400381, 38.86567161673127657 ) ) ;
#19507=DIRECTION ( 'NONE',  ( 0.000000000000000000, 0.000000000000000000, 1.000000000000000000 ) ) ;
#19514=CYLINDRICAL_SURFACE ( 'NONE', #3885, 4.999999999999997335 ) ;
#19515=CARTESIAN_POINT ( 'NONE',  ( 41.64333658814960870, 138.7151871740940123, 38.42115945441014446 ) ) ;
#19516=CARTESIAN_POINT ( 'NONE',  ( 47.43856463449118621, 91.87977050742732388, 34.21067981925357060 ) ) ;
#19522=CARTESIAN_POINT ( 'NONE',  ( 44.55648932407425633, 117.6844580088725820, 38.96596240072933170 ) ) ;
#19525=CARTESIAN_POINT ( 'NONE',  ( 38.58424406990784661, 72.52977050742731535, 35.64915139335016647 ) ) ;
#19526=CARTESIAN_POINT ( 'NONE',  ( 45.74753988029933538, 136.1651871740939725, 37.97664729208901946 ) ) ;
#19527=CARTESIAN_POINT ( 'NONE',  ( 38.96631938032478359, 96.41049967264873999, 31.27175355779120025 ) ) ;
#19533=CARTESIAN_POINT ( 'NONE',  ( 45.74753988029933538, 76.42977050742729261, 37.97664729208901946 ) ) ;
#19540=CARTESIAN_POINT ( 'NONE',  ( 45.74753988029934249, 122.3297705074273267, 30.44471234641812174 ) ) ;
#19541=ORIENTED_EDGE ( 'NONE', *, *, #1718, .T. ) ;
#19545=CARTESIAN_POINT ( 'NONE',  ( 44.37947211624943833, 125.4797705074273182, 30.00020018409699318 ) ) ;
#19547=CARTESIAN_POINT ( 'NONE',  ( 46.59305225739526435, 88.57977050742732672, 36.81289934271958941 ) ) ;
#19548=CARTESIAN_POINT ( 'NONE',  ( 41.46631938032478359, 59.18445800887258201, 29.45539723777780239 ) ) ;
#19549=DIRECTION ( 'NONE',  ( 0.000000000000000000, 1.000000000000000000, 0.000000000000000000 ) ) ;
#19554=CARTESIAN_POINT ( 'NONE',  ( 43.01140435219957681, 93.53445800887259054, 39.21067981925356349 ) ) ;
#19557=CARTESIAN_POINT ( 'NONE',  ( 46.10157429594899270, 120.8344580088725593, 38.46393386101376421 ) ) ;
#19558=CARTESIAN_POINT ( 'NONE',  ( 47.43856463449118621, 106.8797705074273239, 34.21067981925357060 ) ) ;
#19561=CARTESIAN_POINT ( 'NONE',  ( 41.64333658814960870, 96.71518717409399812, 38.42115945441014446 ) ) ;
#19565=VECTOR ( 'NONE', #19326, 1000.000000000000000 ) ;
#19569=CARTESIAN_POINT ( 'NONE',  ( 45.74753988029934249, 67.42977050742730682, 37.97664729208901235 ) ) ;
#19572=VERTEX_POINT ( 'NONE', #12540 ) ;
#19573=CARTESIAN_POINT ( 'NONE',  ( 47.43856463449117200, 157.7297705074273040, 35.64915139335016647 ) ) ;
#19578=CARTESIAN_POINT ( 'NONE',  ( 38.96631938032478359, 117.4104996726487400, 31.27175355779120025 ) ) ;
#19580=CARTESIAN_POINT ( 'NONE',  ( 38.01140435219952707, 65.63445800887257064, 32.58608133808903773 ) ) ;
#19587=CARTESIAN_POINT ( 'NONE',  ( 39.42975644700377558, 132.6797705074273210, 36.81289934271958941 ) ) ;
#19589=CARTESIAN_POINT ( 'NONE',  ( 47.43856463449117911, 127.7651871740940237, 32.77220824515697473 ) ) ;
#19593=CARTESIAN_POINT ( 'NONE',  ( 43.01140435219953417, 141.5344580088726048, 39.21067981925356349 ) ) ;
#19595=CARTESIAN_POINT ( 'NONE',  ( 48.01140435219951996, 149.3604996726487286, 32.58608133808903773 ) ) ;
#19598=CARTESIAN_POINT ( 'NONE',  ( 41.64333658814960870, 104.5151871740939953, 30.00020018409699318 ) ) ;
#19600=ORIENTED_EDGE ( 'NONE', *, *, #13389, .T. ) ;
#19601=CARTESIAN_POINT ( 'NONE',  ( 48.01140435219951996, 86.36049967264872862, 32.58608133808903773 ) ) ;
#19603=CARTESIAN_POINT ( 'NONE',  ( 38.01140435219951996, 83.63445800887258486, 32.58608133808903773 ) ) ;
#19606=CARTESIAN_POINT ( 'NONE',  ( 48.01140435219951996, 149.0604996726487173, 35.83527830041810347 ) ) ;
#19607=CARTESIAN_POINT ( 'NONE',  ( 41.64333658814960870, 105.7151871740940123, 38.42115945441014446 ) ) ;
#19609=CARTESIAN_POINT ( 'NONE',  ( 46.10157429594899270, 62.66049967264872578, 29.95742577749337343 ) ) ;
#19612=CARTESIAN_POINT ( 'NONE',  ( 48.01140435219951996, 118.4344580088725962, 32.58608133808903773 ) ) ;
#19615=CARTESIAN_POINT ( 'NONE',  ( 45.22505347682923826, 59.11591767009502263, 30.37668637662395099 ) ) ;
#19617=CARTESIAN_POINT ( 'NONE',  ( 47.43856463449117911, 151.7651871740939953, 32.77220824515697473 ) ) ;
#19624=CARTESIAN_POINT ( 'NONE',  ( 39.42975644700377558, 69.41518717409400097, 36.81289934271958941 ) ) ;
#19627=AXIS2_PLACEMENT_3D ( 'NONE', #11434, #11655, #3066 ) ;
#19628=CARTESIAN_POINT ( 'NONE',  ( 48.01140435219951996, 112.2844580088725763, 34.21067981925357060 ) ) ;
#19629=CARTESIAN_POINT ( 'NONE',  ( 40.27526882409969033, 137.6651871740940294, 30.44471234641811819 ) ) ;
#19631=( BOUNDED_CURVE ( )  B_SPLINE_CURVE ( 2, ( #18060, #20071, #5067, #14644, #17949, #2966, #9706, #15089, #4726, #16406, #10031, #8157, #1206 ),
 .UNSPECIFIED., .F., .F. ) 
 B_SPLINE_CURVE_WITH_KNOTS ( ( 3, 2, 2, 2, 2, 2, 3 ),
 ( 0.5220588235294117974, 0.5235294117647059098, 0.5264705882352941346, 0.5294117647058823595, 0.5323529411764705843, 0.5352941176470588092, 0.5367647058823529216 ),
 .UNSPECIFIED. ) 
 CURVE ( )  GEOMETRIC_REPRESENTATION_ITEM ( )  RATIONAL_B_SPLINE_CURVE ( ( 0.9755282581475768211, 0.9755282581475768211, 1.000000000000000000, 0.9510565162951535312, 1.000000000000000000, 0.9510565162951535312, 1.000000000000000000, 0.9510565162951535312, 1.000000000000000000, 0.9510565162951535312, 1.000000000000000000, 0.9755282581475768211, 0.9755282581475768211 ) ) 
 REPRESENTATION_ITEM ( '' )  );
#19633=EDGE_LOOP ( 'NONE', ( #21658, #10482, #944, #11325 ) ) ;
#19636=CARTESIAN_POINT ( 'NONE',  ( 47.05648932407426344, 118.5844580088725735, 31.27175355779120025 ) ) ;
#19639=CARTESIAN_POINT ( 'NONE',  ( 41.64333658814960870, 80.77977050742732956, 30.00020018409699318 ) ) ;
#19640=CARTESIAN_POINT ( 'NONE',  ( 38.58424406990786082, 135.1151871740940180, 34.21067981925357060 ) ) ;
#19641=CARTESIAN_POINT ( 'NONE',  ( 38.01140435219952707, 87.71049967264873715, 34.21067981925357060 ) ) ;
#19646=CARTESIAN_POINT ( 'NONE',  ( 46.59305225739526435, 85.31518717409400665, 36.81289934271958941 ) ) ;
#19649=CARTESIAN_POINT ( 'NONE',  ( 47.05648932407426344, 61.91049967264873288, 37.14960608071593384 ) ) ;
#19651=CARTESIAN_POINT ( 'NONE',  ( 47.43856463449118621, 73.87977050742732388, 34.21067981925357060 ) ) ;
#19657=DIRECTION ( 'NONE',  ( 0.000000000000000000, 1.000000000000000000, 0.000000000000000000 ) ) ;
#19658=CARTESIAN_POINT ( 'NONE',  ( 44.37947211624943833, 119.4797705074273182, 30.00020018409699318 ) ) ;
#19659=ADVANCED_FACE ( 'NONE', ( #19812 ), #19701, .T. ) ;
#19663=CARTESIAN_POINT ( 'NONE',  ( 45.74753988029933538, 130.4297705074273210, 37.97664729208901946 ) ) ;
#19664=CARTESIAN_POINT ( 'NONE',  ( 42.21948215057684450, 73.38361825032846752, 39.21067981925355639 ) ) ;
#19665=CARTESIAN_POINT ( 'NONE',  ( 46.10157429594899270, 66.83445800887257349, 38.46393386101376421 ) ) ;
#19668=CARTESIAN_POINT ( 'NONE',  ( 42.21948215057687293, 97.38361825032846752, 39.21067981925357060 ) ) ;
#19670=CARTESIAN_POINT ( 'NONE',  ( 38.01140435219952707, 156.5604996726487457, 32.58608133808903773 ) ) ;
#19671=CARTESIAN_POINT ( 'NONE',  ( 47.05648932407426344, 94.58445800887257349, 31.27175355779120025 ) ) ;
#19675=CARTESIAN_POINT ( 'NONE',  ( 39.92123440845004723, 123.2344580088725650, 38.46393386101376421 ) ) ;
#19676=CARTESIAN_POINT ( 'NONE',  ( 40.27526882409969033, 99.82977050742729830, 37.97664729208901946 ) ) ;
#19679=CARTESIAN_POINT ( 'NONE',  ( 47.43856463449117911, 94.46518717409399812, 35.64915139335015937 ) ) ;
#19683=ADVANCED_FACE ( 'NONE', ( #16821 ), #9791, .T. ) ;
#19686=CARTESIAN_POINT ( 'NONE',  ( 44.37947211624943833, 65.47977050742731819, 30.00020018409699318 ) ) ;
#19687=ORIENTED_EDGE ( 'NONE', *, *, #4893, .F. ) ;
#19689=CARTESIAN_POINT ( 'NONE',  ( 41.64333658814960870, 153.9797705074273324, 38.42115945441014446 ) ) ;
#19693=( BOUNDED_CURVE ( )  B_SPLINE_CURVE ( 2, ( #1549, #21726, #13344, #6510, #16961, #13230, #20081, #10153, #19967, #11572, #18301, #4968, #16639 ),
 .UNSPECIFIED., .F., .F. ) 
 B_SPLINE_CURVE_WITH_KNOTS ( ( 3, 2, 2, 2, 2, 2, 3 ),
 ( 0.7867647058823529216, 0.7882352941176470340, 0.7911764705882352589, 0.7941176470588234837, 0.7970588235294118196, 0.8000000000000000444, 0.8014705882352941568 ),
 .UNSPECIFIED. ) 
 CURVE ( )  GEOMETRIC_REPRESENTATION_ITEM ( )  RATIONAL_B_SPLINE_CURVE ( ( 0.9755282581475768211, 0.9755282581475768211, 1.000000000000000000, 0.9510565162951535312, 1.000000000000000000, 0.9510565162951535312, 1.000000000000000000, 0.9510565162951535312, 1.000000000000000000, 0.9510565162951535312, 1.000000000000000000, 0.9755282581475768211, 0.9755282581475768211 ) ) 
 REPRESENTATION_ITEM ( '' )  );
#19695=CARTESIAN_POINT ( 'NONE',  ( 38.01140435219951996, 114.8604996726487570, 35.83527830041810347 ) ) ;
#19696=CARTESIAN_POINT ( 'NONE',  ( 38.58424406990786082, 72.11518717409400381, 34.21067981925357060 ) ) ;
#19697=CARTESIAN_POINT ( 'NONE',  ( 42.21948215057684450, 66.45757658655229250, 39.21067981925355639 ) ) ;
#19701=CYLINDRICAL_SURFACE ( 'NONE', #12122, 4.999999999999997335 ) ;
#19702=CARTESIAN_POINT ( 'NONE',  ( 39.92123440845004723, 156.2344580088725934, 38.46393386101376421 ) ) ;
#19703=CARTESIAN_POINT ( 'NONE',  ( 39.42975644700377558, 132.0797705074273267, 31.60846029578754468 ) ) ;
#19705=CARTESIAN_POINT ( 'NONE',  ( 39.42975644700377558, 125.8151871740940067, 31.60846029578754468 ) ) ;
#19708=LINE ( 'NONE', #9689, #20698 ) ;
#19709=LINE ( 'NONE', #17929, #3955 ) ;
#19713=CARTESIAN_POINT ( 'NONE',  ( 43.01140435219951286, 85.46049967264872294, 39.21067981925356349 ) ) ;
#19715=CARTESIAN_POINT ( 'NONE',  ( 46.10157429594899270, 79.73445800887257917, 29.95742577749337343 ) ) ;
#19716=CARTESIAN_POINT ( 'NONE',  ( 48.01140435219951996, 103.2844580088725763, 34.21067981925357060 ) ) ;
#19718=CARTESIAN_POINT ( 'NONE',  ( 38.01140435219951996, 141.5604996726487457, 32.58608133808903773 ) ) ;
#19719=CARTESIAN_POINT ( 'NONE',  ( 47.43856463449117200, 94.76518717409398107, 32.77220824515698183 ) ) ;
#19722=CARTESIAN_POINT ( 'NONE',  ( 39.92123440845004723, 60.26049967264872720, 29.95742577749337343 ) ) ;
#19726=CARTESIAN_POINT ( 'NONE',  ( 48.01140435219951996, 79.43445800887258201, 32.58608133808903773 ) ) ;
#19727=CARTESIAN_POINT ( 'NONE',  ( 46.10157429594899270, 115.7344580088725650, 29.95742577749336988 ) ) ;
#19728=CARTESIAN_POINT ( 'NONE',  ( 46.59305225739526435, 61.91518717409400097, 31.60846029578754468 ) ) ;
#19729=EDGE_CURVE ( 'NONE', #21725, #15219, #6300, .T. ) ;
#19735=CARTESIAN_POINT ( 'NONE',  ( 39.42975644700377558, 68.81518717409400665, 31.60846029578754468 ) ) ;
#19738=FACE_OUTER_BOUND ( 'NONE', #7286, .T. ) ;
#19739=CARTESIAN_POINT ( 'NONE',  ( 41.64333658814960870, 132.7151871740940123, 38.42115945441014446 ) ) ;
#19740=AXIS2_PLACEMENT_3D ( 'NONE', #18957, #3859, #5820 ) ;
#19745=EDGE_LOOP ( 'NONE', ( #19687, #8634, #14988, #1038 ) ) ;
#19746=CARTESIAN_POINT ( 'NONE',  ( 39.92123440845004723, 110.3344580088725877, 29.95742577749337343 ) ) ;
#19747=CARTESIAN_POINT ( 'NONE',  ( 47.05648932407426344, 116.5104996726487485, 31.27175355779120025 ) ) ;
#19750=CARTESIAN_POINT ( 'NONE',  ( 47.43856463449117200, 80.02977050742732956, 32.77220824515698183 ) ) ;
#19751=CARTESIAN_POINT ( 'NONE',  ( 38.58424406990786082, 129.1151871740940180, 34.21067981925357060 ) ) ;
#19753=CARTESIAN_POINT ( 'NONE',  ( 39.92123440845004723, 93.26049967264872009, 29.95742577749337343 ) ) ;
#19757=CARTESIAN_POINT ( 'NONE',  ( 47.43856463449117200, 88.76518717409399528, 32.77220824515698183 ) ) ;
#19762=CARTESIAN_POINT ( 'NONE',  ( 40.27526882409969033, 75.82977050742731251, 37.97664729208901946 ) ) ;
#19769=CARTESIAN_POINT ( 'NONE',  ( 44.37947211624943833, 121.2797705074273296, 38.42115945441014446 ) ) ;
#19771=CARTESIAN_POINT ( 'NONE',  ( 47.05648932407426344, 88.58445800887257349, 31.27175355779120025 ) ) ;
#19776=CARTESIAN_POINT ( 'NONE',  ( 38.96631938032478359, 66.08445800887258770, 37.14960608071593384 ) ) ;
#19778=VECTOR ( 'NONE', #19657, 1000.000000000000000 ) ;
#19779=CARTESIAN_POINT ( 'NONE',  ( 43.01140435219951996, 153.5344580088726048, 39.21067981925357060 ) ) ;
#19781=CARTESIAN_POINT ( 'NONE',  ( 38.01140435219952707, 96.56049967264871725, 32.58608133808903773 ) ) ;
#19784=CARTESIAN_POINT ( 'NONE',  ( 42.21948215057684450, 102.0373810949690210, 29.21067981925356705 ) ) ;
#19788=CARTESIAN_POINT ( 'NONE',  ( 39.92123440845004723, 120.2344580088725650, 38.46393386101376421 ) ) ;
#19789=CARTESIAN_POINT ( 'NONE',  ( 38.58424406990784661, 108.2297705074273182, 32.77220824515698183 ) ) ;
#19792=CARTESIAN_POINT ( 'NONE',  ( 45.74753988029934249, 86.06518717409402086, 30.44471234641812174 ) ) ;
#19793=DIRECTION ( 'NONE',  ( 0.000000000000000000, 0.000000000000000000, 1.000000000000000000 ) ) ;
#19797=CARTESIAN_POINT ( 'NONE',  ( 47.43856463449117911, 145.7297705074273040, 35.64915139335015937 ) ) ;
#19800=CARTESIAN_POINT ( 'NONE',  ( 46.59305225739526435, 68.17977050742732104, 31.60846029578754468 ) ) ;
#19803=CARTESIAN_POINT ( 'NONE',  ( 39.42975644700377558, 144.6797705074273495, 36.81289934271958941 ) ) ;
#19804=EDGE_CURVE ( 'NONE', #9910, #1013, #1674, .T. ) ;
#19806=CARTESIAN_POINT ( 'NONE',  ( 47.05648932407426344, 106.9104996726487400, 37.14960608071593384 ) ) ;
#19807=CARTESIAN_POINT ( 'NONE',  ( 44.37947211624943833, 65.21518717409399812, 30.00020018409699318 ) ) ;
#19810=CARTESIAN_POINT ( 'NONE',  ( 43.01140435219951286, 156.5344580088725479, 39.21067981925355639 ) ) ;
#19812=FACE_OUTER_BOUND ( 'NONE', #4232, .T. ) ;
#19813=CARTESIAN_POINT ( 'NONE',  ( 48.01140435219951996, 148.4344580088725536, 32.58608133808903773 ) ) ;
#19814=CARTESIAN_POINT ( 'NONE',  ( 39.42975644700377558, 129.0797705074273267, 31.60846029578754468 ) ) ;
#19816=CARTESIAN_POINT ( 'NONE',  ( 40.27526882409969744, 113.6651871740939868, 30.44471234641812174 ) ) ;
#19818=CARTESIAN_POINT ( 'NONE',  ( 42.21948215057683740, 150.0373810949690210, 29.21067981925356705 ) ) ;
#19820=CARTESIAN_POINT ( 'NONE',  ( 47.05648932407426344, 149.5104996726487343, 31.27175355779120025 ) ) ;
#19822=( BOUNDED_CURVE ( )  B_SPLINE_CURVE ( 2, ( #2370, #21005, #12618, #20892, #2158, #20784, #4239 ),
 .UNSPECIFIED., .F., .F. ) 
 B_SPLINE_CURVE_WITH_KNOTS ( ( 3, 2, 2, 3 ),
 ( 0.000000000000000000, 0.002941176470588235253, 0.005882352941176470507, 0.007352941176470590735 ),
 .UNSPECIFIED. ) 
 CURVE ( )  GEOMETRIC_REPRESENTATION_ITEM ( )  RATIONAL_B_SPLINE_CURVE ( ( 1.000000000000000000, 0.9510565162951535312, 1.000000000000000000, 0.9510565162951535312, 1.000000000000000000, 0.9755282581475767101, 0.9755282581475768211 ) ) 
 REPRESENTATION_ITEM ( '' )  );
#19823=ORIENTED_EDGE ( 'NONE', *, *, #11878, .T. ) ;
#19826=CARTESIAN_POINT ( 'NONE',  ( 48.01140435219951996, 79.13445800887258486, 35.83527830041810347 ) ) ;
#19828=CARTESIAN_POINT ( 'NONE',  ( 39.92123440845004723, 142.1604996726487400, 38.46393386101376421 ) ) ;
#19829=CARTESIAN_POINT ( 'NONE',  ( 40.27526882409969033, 98.66518717409400097, 30.44471234641811819 ) ) ;
#19838=CARTESIAN_POINT ( 'NONE',  ( 38.01140435219952707, 78.56049967264873146, 32.58608133808903773 ) ) ;
#19839=CARTESIAN_POINT ( 'NONE',  ( 45.74753988029933538, 157.4297705074273495, 37.97664729208901946 ) ) ;
#19845=CARTESIAN_POINT ( 'NONE',  ( 38.58424406990785371, 69.26518717409399528, 35.64915139335015937 ) ) ;
#19849=CARTESIAN_POINT ( 'NONE',  ( 38.58424406990786082, 126.1151871740940038, 34.21067981925357060 ) ) ;
#19857=VERTEX_POINT ( 'NONE', #14679 ) ;
#19859=CARTESIAN_POINT ( 'NONE',  ( 46.10157429594899270, 108.8344580088725735, 38.46393386101376421 ) ) ;
#19861=CARTESIAN_POINT ( 'NONE',  ( 47.43856463449118621, 67.87977050742730967, 34.21067981925357060 ) ) ;
#19862=CARTESIAN_POINT ( 'NONE',  ( 45.74753988029933538, 130.1651871740940010, 37.97664729208901946 ) ) ;
#19866=CARTESIAN_POINT ( 'NONE',  ( 39.92123440845004723, 79.16049967264873999, 38.46393386101376421 ) ) ;
#19868=DIRECTION ( 'NONE',  ( 0.000000000000000000, 1.000000000000000000, 0.000000000000000000 ) ) ;
#19870=CARTESIAN_POINT ( 'NONE',  ( 41.64333658814960870, 87.71518717409399812, 38.42115945441014446 ) ) ;
#19871=CARTESIAN_POINT ( 'NONE',  ( 43.01140435219951286, 107.9604996726487229, 29.21067981925356705 ) ) ;
#19873=ORIENTED_EDGE ( 'NONE', *, *, #13459, .F. ) ;
#19874=CARTESIAN_POINT ( 'NONE',  ( 39.42975644700377558, 63.07977050742731251, 31.60846029578754468 ) ) ;
#19879=EDGE_CURVE ( 'NONE', #9411, #17454, #3922, .T. ) ;
#19882=CARTESIAN_POINT ( 'NONE',  ( 38.58424406990785371, 123.5297705074273438, 35.64915139335015937 ) ) ;
#19885=EDGE_CURVE ( 'NONE', #13022, #10776, #6159, .T. ) ;
#19888=CARTESIAN_POINT ( 'NONE',  ( 39.42975644700377558, 117.6797705074273210, 36.81289934271958941 ) ) ;
#19889=CARTESIAN_POINT ( 'NONE',  ( 43.01140435219957681, 71.96049967264872294, 29.21067981925356705 ) ) ;
#19890=CARTESIAN_POINT ( 'NONE',  ( 38.58424406990784661, 87.22977050742731819, 32.77220824515698183 ) ) ;
#19891=CARTESIAN_POINT ( 'NONE',  ( 40.27526882409969033, 158.6651871740939725, 30.44471234641811819 ) ) ;
#19893=CARTESIAN_POINT ( 'NONE',  ( 43.01140435219951286, 102.5344580088725763, 39.21067981925356349 ) ) ;
#19896=( BOUNDED_CURVE ( )  B_SPLINE_CURVE ( 2, ( #4971, #8717, #18844, #16857, #6747, #10370, #5081, #18526, #18420, #1771, #11683, #3318, #11795 ),
 .UNSPECIFIED., .F., .T. ) 
 B_SPLINE_CURVE_WITH_KNOTS ( ( 3, 2, 2, 2, 2, 2, 3 ),
 ( 0.2279411764705882304, 0.2294117647058823428, 0.2323529411764705954, 0.2352941176470588203, 0.2382352941176470451, 0.2411764705882352977, 0.2426470588235294101 ),
 .UNSPECIFIED. ) 
 CURVE ( )  GEOMETRIC_REPRESENTATION_ITEM ( )  RATIONAL_B_SPLINE_CURVE ( ( 0.9755282581475768211, 0.9755282581475768211, 1.000000000000000000, 0.9510565162951535312, 1.000000000000000000, 0.9510565162951535312, 1.000000000000000000, 0.9510565162951535312, 1.000000000000000000, 0.9510565162951535312, 1.000000000000000000, 0.9755282581475768211, 0.9755282581475768211 ) ) 
 REPRESENTATION_ITEM ( '' )  );
#19898=CARTESIAN_POINT ( 'NONE',  ( 38.01140435219952707, 156.8604996726487855, 35.83527830041809636 ) ) ;
#19899=CARTESIAN_POINT ( 'NONE',  ( 47.05648932407426344, 93.98445800887257917, 37.14960608071593384 ) ) ;
#19901=CARTESIAN_POINT ( 'NONE',  ( 47.05648932407426344, 121.5844580088725735, 31.27175355779120025 ) ) ;
#19902=CARTESIAN_POINT ( 'NONE',  ( 41.64333658814960870, 104.7797705074273154, 30.00020018409699318 ) ) ;
#19905=CARTESIAN_POINT ( 'NONE',  ( 41.64333658814960870, 89.51518717409399528, 30.00020018409699318 ) ) ;
#19906=CARTESIAN_POINT ( 'NONE',  ( 43.01140435219951286, 85.46049967264872294, 39.21067981925356349 ) ) ;
#19909=CARTESIAN_POINT ( 'NONE',  ( 48.01140435219951996, 128.0604996726487457, 35.83527830041809636 ) ) ;
#19911=CARTESIAN_POINT ( 'NONE',  ( 40.27526882409969744, 143.9297705074273210, 30.44471234641812174 ) ) ;
#19913=CARTESIAN_POINT ( 'NONE',  ( 40.27526882409969744, 66.82977050742731251, 37.97664729208901235 ) ) ;
#19915=CARTESIAN_POINT ( 'NONE',  ( 40.27526882409969033, 146.9297705074273210, 30.44471234641811819 ) ) ;
#19916=CARTESIAN_POINT ( 'NONE',  ( 48.01140435219951996, 152.3604996726487570, 32.58608133808903773 ) ) ;
#19918=CARTESIAN_POINT ( 'NONE',  ( 44.55648932407425633, 106.6104996726487428, 38.96596240072933170 ) ) ;
#19919=CARTESIAN_POINT ( 'NONE',  ( 40.27526882409969033, 65.66518717409398675, 30.44471234641811819 ) ) ;
#19924=( NAMED_UNIT ( * ) PLANE_ANGLE_UNIT ( ) SI_UNIT ( $, .RADIAN. ) );
#19926=CARTESIAN_POINT ( 'NONE',  ( 41.46631938032478359, 156.3844580088725706, 38.96596240072933170 ) ) ;
#19927=CARTESIAN_POINT ( 'NONE',  ( 47.43856463449117200, 134.0297705074273154, 32.77220824515698183 ) ) ;
#19929=CARTESIAN_POINT ( 'NONE',  ( 44.37947211624943833, 115.0151871740940095, 38.42115945441014446 ) ) ;
#19932=LINE ( 'NONE', #8250, #21198 ) ;
#19934=CARTESIAN_POINT ( 'NONE',  ( 43.01140435219951996, 170.7104996726487514, 29.21067981925357060 ) ) ;
#19939=CARTESIAN_POINT ( 'NONE',  ( 47.43856463449117911, 97.72977050742730398, 35.64915139335015937 ) ) ;
#19944=CARTESIAN_POINT ( 'NONE',  ( 48.01140435219951996, 82.43445800887258201, 32.58608133808903773 ) ) ;
#19946=ADVANCED_FACE ( 'NONE', ( #257, #16999 ), #8861, .F. ) ;
#19947=CARTESIAN_POINT ( 'NONE',  ( 46.10157429594899270, 142.7604996726487343, 38.46393386101376421 ) ) ;
#19948=CARTESIAN_POINT ( 'NONE',  ( 40.27526882409969033, 92.66518717409398675, 30.44471234641811819 ) ) ;
#19953=CARTESIAN_POINT ( 'NONE',  ( 43.01140435219951286, 62.03445800887256922, 29.21067981925356705 ) ) ;
#19957=CARTESIAN_POINT ( 'NONE',  ( 38.01140435219952707, 147.5604996726487173, 32.58608133808903773 ) ) ;
#19958=CARTESIAN_POINT ( 'NONE',  ( 43.01140435219951286, 79.46049967264875136, 39.21067981925356349 ) ) ;
#19960=CARTESIAN_POINT ( 'NONE',  ( 38.58424406990784661, 60.26518717409400239, 35.64915139335016647 ) ) ;
#19961=CARTESIAN_POINT ( 'NONE',  ( 39.92123440845005433, 63.23445800887257917, 38.46393386101375711 ) ) ;
#19963=CARTESIAN_POINT ( 'NONE',  ( 40.27526882409969744, 143.6651871740940294, 30.44471234641812174 ) ) ;
#19967=CARTESIAN_POINT ( 'NONE',  ( 38.96631938032478359, 77.48445800887257917, 31.27175355779120025 ) ) ;
#19972=CARTESIAN_POINT ( 'NONE',  ( 38.58424406990784661, 122.9651871740939981, 32.77220824515698183 ) ) ;
#19974=AXIS2_PLACEMENT_3D ( 'NONE', #14585, #12944, #1482 ) ;
#19975=VERTEX_POINT ( 'NONE', #7611 ) ;
#19977=CARTESIAN_POINT ( 'NONE',  ( 38.01140435219952707, 146.6344580088725991, 32.58608133808903773 ) ) ;
#19979=CARTESIAN_POINT ( 'NONE',  ( 45.74753988029934249, 155.3297705074273267, 30.44471234641812174 ) ) ;
#19980=CARTESIAN_POINT ( 'NONE',  ( 43.01140435219951286, 65.62977050742730967, 29.55568802177586463 ) ) ;
#19981=CARTESIAN_POINT ( 'NONE',  ( 45.74753988029933538, 121.1651871740939725, 37.97664729208901946 ) ) ;
#19984=CARTESIAN_POINT ( 'NONE',  ( 38.01140435219951996, 81.56049967264873146, 32.58608133808903773 ) ) ;
#19986=CARTESIAN_POINT ( 'NONE',  ( 38.96631938032478359, 145.0104996726487627, 37.14960608071593384 ) ) ;
#19987=CARTESIAN_POINT ( 'NONE',  ( 38.01140435219952707, 138.7104996726487514, 34.21067981925357060 ) ) ;
#19988=CARTESIAN_POINT ( 'NONE',  ( 38.58424406990784661, 84.26518717409399528, 35.64915139335016647 ) ) ;
#19992=ORIENTED_EDGE ( 'NONE', *, *, #7368, .T. ) ;
#19993=CARTESIAN_POINT ( 'NONE',  ( 44.37947211624943833, 67.27977050742731535, 38.42115945441014446 ) ) ;
#19995=EDGE_CURVE ( 'NONE', #3266, #13122, #5327, .T. ) ;
#19999=CARTESIAN_POINT ( 'NONE',  ( 45.74753988029933538, 152.0651871740939782, 30.44471234641811819 ) ) ;
#20001=CARTESIAN_POINT ( 'NONE',  ( 44.37947211624943833, 118.2797705074273296, 38.42115945441014446 ) ) ;
#20007=CARTESIAN_POINT ( 'NONE',  ( 38.58424406990784661, 117.5297705074273011, 35.64915139335016647 ) ) ;
#20008=AXIS2_PLACEMENT_3D ( 'NONE', #3425, #20282, #13338 ) ;
#20010=CARTESIAN_POINT ( 'NONE',  ( 43.01140435219951286, 86.62977050742730967, 29.55568802177586463 ) ) ;
#20011=CARTESIAN_POINT ( 'NONE',  ( 43.01140435219951286, 152.3651871740940180, 29.55568802177586463 ) ) ;
#20017=CARTESIAN_POINT ( 'NONE',  ( 42.21948215057684450, 156.0373810949690210, 29.21067981925356705 ) ) ;
#20021=CARTESIAN_POINT ( 'NONE',  ( 39.42975644700377558, 96.07977050742731251, 31.60846029578754468 ) ) ;
#20025=CARTESIAN_POINT ( 'NONE',  ( 39.42975644700377558, 84.41518717409400097, 36.81289934271958941 ) ) ;
#20031=CARTESIAN_POINT ( 'NONE',  ( 41.64333658814960870, 140.7797705074273154, 30.00020018409699318 ) ) ;
#20033=CARTESIAN_POINT ( 'NONE',  ( 45.74753988029934249, 71.32977050742732672, 30.44471234641812174 ) ) ;
#20035=CARTESIAN_POINT ( 'NONE',  ( 44.37947211624943833, 142.2797705074273154, 38.42115945441014446 ) ) ;
#20036=CARTESIAN_POINT ( 'NONE',  ( 40.27526882409969033, 96.82977050742731251, 37.97664729208901946 ) ) ;
#20037=CARTESIAN_POINT ( 'NONE',  ( 44.55648932407425633, 152.8104996726487457, 29.45539723777780239 ) ) ;
#20038=EDGE_CURVE ( 'NONE', #16317, #17856, #2091, .T. ) ;
#20040=CARTESIAN_POINT ( 'NONE',  ( 38.96631938032478359, 114.4104996726487400, 31.27175355779120025 ) ) ;
#20041=CARTESIAN_POINT ( 'NONE',  ( 40.27526882409969033, 69.56518717409400665, 37.97664729208901946 ) ) ;
#20042=CARTESIAN_POINT ( 'NONE',  ( 42.21948215057684450, 95.11133943119284595, 29.21067981925356705 ) ) ;
#20046=CARTESIAN_POINT ( 'NONE',  ( 43.01140435219951996, 10.71049967264875491, 34.21067981925357060 ) ) ;
#20047=CARTESIAN_POINT ( 'NONE',  ( 48.01140435219951996, 154.1344580088725991, 35.83527830041810347 ) ) ;
#20048=CARTESIAN_POINT ( 'NONE',  ( 38.58424406990784661, 126.5297705074272727, 35.64915139335016647 ) ) ;
#20050=CARTESIAN_POINT ( 'NONE',  ( 41.64333658814960870, 117.7151871740939981, 38.42115945441014446 ) ) ;
#20052=CARTESIAN_POINT ( 'NONE',  ( 47.05648932407426344, 140.5104996726487627, 31.27175355779120025 ) ) ;
#20055=CARTESIAN_POINT ( 'NONE',  ( 43.01140435219951996, 2.710499672648754466, 59.21067981925356349 ) ) ;
#20057=CARTESIAN_POINT ( 'NONE',  ( 45.74753988029934249, 94.42977050742733525, 37.97664729208901235 ) ) ;
#20058=EDGE_LOOP ( 'NONE', ( #14934, #5957, #11656, #12600 ) ) ;
#20059=CARTESIAN_POINT ( 'NONE',  ( 47.05648932407426344, 145.5844580088725877, 31.27175355779120025 ) ) ;
#20060=ORIENTED_EDGE ( 'NONE', *, *, #5076, .F. ) ;
#20061=CARTESIAN_POINT ( 'NONE',  ( 38.01140435219951996, 80.93445800887256780, 35.83527830041810347 ) ) ;
#20064=CARTESIAN_POINT ( 'NONE',  ( 44.55648932407425633, 142.6104996726487570, 38.96596240072933170 ) ) ;
#20065=CARTESIAN_POINT ( 'NONE',  ( 45.74753988029933538, 98.06518717409397823, 30.44471234641811819 ) ) ;
#20071=CARTESIAN_POINT ( 'NONE',  ( 42.21948215057684450, 106.3836182503284533, 39.21067981925355639 ) ) ;
#20074=CARTESIAN_POINT ( 'NONE',  ( 38.96631938032478359, 79.01049967264873430, 37.14960608071593384 ) ) ;
#20075=CARTESIAN_POINT ( 'NONE',  ( 47.43856463449117200, 64.46518717409398391, 35.64915139335016647 ) ) ;
#20077=CARTESIAN_POINT ( 'NONE',  ( 41.64333658814960870, 144.7151871740940123, 38.42115945441014446 ) ) ;
#20081=CARTESIAN_POINT ( 'NONE',  ( 38.01140435219952707, 77.78445800887259054, 34.21067981925357060 ) ) ;
#20085=CARTESIAN_POINT ( 'NONE',  ( 40.27526882409969033, 122.6651871740939725, 30.44471234641811819 ) ) ;
#20091=CARTESIAN_POINT ( 'NONE',  ( 47.43856463449118621, 157.8797705074273381, 34.21067981925357060 ) ) ;
#20092=CARTESIAN_POINT ( 'NONE',  ( 40.27526882409969033, 66.82977050742732672, 37.97664729208901946 ) ) ;
#20093=CARTESIAN_POINT ( 'NONE',  ( 43.01140435219951286, 129.8651871740940180, 38.86567161673127657 ) ) ;
#20095=CARTESIAN_POINT ( 'NONE',  ( 38.01140435219951996, 78.56049967264873146, 32.58608133808903773 ) ) ;
#20097=CARTESIAN_POINT ( 'NONE',  ( 43.01140435219951996, 10.71049967264875491, 34.21067981925357060 ) ) ;
#20098=CARTESIAN_POINT ( 'NONE',  ( 43.01140435219951286, 118.4604996726487371, 39.21067981925356349 ) ) ;
#20099=( BOUNDED_CURVE ( )  B_SPLINE_CURVE ( 2, ( #15917, #5677, #4031, #19341, #16138, #9219, #830, #16022, #934, #14161, #17892, #1047, #7781 ),
 .UNSPECIFIED., .F., .F. ) 
 B_SPLINE_CURVE_WITH_KNOTS ( ( 3, 2, 2, 2, 2, 2, 3 ),
 ( 0.8308823529411765163, 0.8323529411764706287, 0.8352941176470588536, 0.8382352941176470784, 0.8411764705882353033, 0.8441176470588235281, 0.8455882352941176405 ),
 .UNSPECIFIED. ) 
 CURVE ( )  GEOMETRIC_REPRESENTATION_ITEM ( )  RATIONAL_B_SPLINE_CURVE ( ( 0.9755282581475768211, 0.9755282581475768211, 1.000000000000000000, 0.9510565162951535312, 1.000000000000000000, 0.9510565162951535312, 1.000000000000000000, 0.9510565162951535312, 1.000000000000000000, 0.9510565162951535312, 1.000000000000000000, 0.9755282581475768211, 0.9755282581475768211 ) ) 
 REPRESENTATION_ITEM ( '' )  );
#20100=CARTESIAN_POINT ( 'NONE',  ( 46.59305225739526435, 88.91518717409400097, 31.60846029578754468 ) ) ;
#20104=CARTESIAN_POINT ( 'NONE',  ( 45.74753988029933538, 61.42977050742732104, 37.97664729208901946 ) ) ;
#20109=CARTESIAN_POINT ( 'NONE',  ( 43.01140435219951286, 158.3651871740939612, 29.55568802177586463 ) ) ;
#20111=CARTESIAN_POINT ( 'NONE',  ( 41.64333658814960870, 111.9797705074273324, 38.42115945441014446 ) ) ;
#20112=CARTESIAN_POINT ( 'NONE',  ( 48.01140435219951996, 154.2844580088725763, 34.21067981925357060 ) ) ;
#20113=VERTEX_POINT ( 'NONE', #17106 ) ;
#20116=CARTESIAN_POINT ( 'NONE',  ( 47.43856463449117200, 118.7297705074272898, 35.64915139335016647 ) ) ;
#20117=CARTESIAN_POINT ( 'NONE',  ( 41.46631938032478359, 127.3104996726487315, 38.96596240072933170 ) ) ;
#20118=CARTESIAN_POINT ( 'NONE',  ( 39.42975644700377558, 84.67977050742732104, 36.81289934271958941 ) ) ;
#20119=CARTESIAN_POINT ( 'NONE',  ( 38.58424406990786082, 153.1151871740939896, 34.21067981925357060 ) ) ;
#20127=CARTESIAN_POINT ( 'NONE',  ( 47.43856463449118621, 91.87977050742732388, 34.21067981925357060 ) ) ;
#20130=CARTESIAN_POINT ( 'NONE',  ( 43.01140435219951286, 87.86518717409398960, 38.86567161673127657 ) ) ;
#20137=ORIENTED_EDGE ( 'NONE', *, *, #14198, .F. ) ;
#20138=CARTESIAN_POINT ( 'NONE',  ( 38.58424406990784661, 147.5297705074273154, 35.64915139335016647 ) ) ;
#20139=EDGE_CURVE ( 'NONE', #4691, #14439, #20668, .T. ) ;
#20142=EDGE_CURVE ( 'NONE', #495, #5452, #5426, .T. ) ;
#20144=CARTESIAN_POINT ( 'NONE',  ( 38.01140435219952707, 111.7104996726487514, 34.21067981925357060 ) ) ;
#20145=CARTESIAN_POINT ( 'NONE',  ( 46.59305225739526435, 61.31518717409399954, 36.81289934271958941 ) ) ;
#20148=CARTESIAN_POINT ( 'NONE',  ( 38.96631938032478359, 122.4844580088725934, 31.27175355779120025 ) ) ;
#20150=CARTESIAN_POINT ( 'NONE',  ( 43.01140435219951996, 10.71049967264875491, 34.21067981925357060 ) ) ;
#20151=CARTESIAN_POINT ( 'NONE',  ( 46.10157429594899270, 153.8344580088725877, 38.46393386101376421 ) ) ;
#20152=CARTESIAN_POINT ( 'NONE',  ( 38.58424406990784661, 123.2297705074273040, 32.77220824515698183 ) ) ;
#20154=CARTESIAN_POINT ( 'NONE',  ( 43.01140435219951286, 115.4604996726487229, 39.21067981925356349 ) ) ;
#20155=CARTESIAN_POINT ( 'NONE',  ( 45.74753988029934249, 119.0651871740939924, 30.44471234641812174 ) ) ;
#20159=DIRECTION ( 'NONE',  ( 0.000000000000000000, 1.000000000000000000, 0.000000000000000000 ) ) ;
#20164=CARTESIAN_POINT ( 'NONE',  ( 38.58424406990785371, 90.52977050742731535, 35.64915139335015937 ) ) ;
#20165=ORIENTED_EDGE ( 'NONE', *, *, #20255, .F. ) ;
#20169=CARTESIAN_POINT ( 'NONE',  ( 44.55648932407425633, 76.88445800887257064, 29.45539723777780239 ) ) ;
#20170=LINE ( 'NONE', #16838, #2427 ) ;
#20171=CARTESIAN_POINT ( 'NONE',  ( 47.05648932407426344, 136.9104996726487400, 37.14960608071593384 ) ) ;
#20172=CARTESIAN_POINT ( 'NONE',  ( 46.59305225739526435, 94.31518717409399244, 36.81289934271958941 ) ) ;
#20179=CARTESIAN_POINT ( 'NONE',  ( 47.43856463449117200, 152.0297705074273438, 32.77220824515698183 ) ) ;
#20182=CARTESIAN_POINT ( 'NONE',  ( 43.01140435219951286, 146.3651871740939896, 29.55568802177586107 ) ) ;
#20186=CARTESIAN_POINT ( 'NONE',  ( 41.64333658814960870, 60.71518717409399102, 38.42115945441014446 ) ) ;
#20189=CARTESIAN_POINT ( 'NONE',  ( 39.42975644700377558, 120.4151871740940010, 36.81289934271958941 ) ) ;
#20191=ORIENTED_EDGE ( 'NONE', *, *, #14609, .T. ) ;
#20192=CARTESIAN_POINT ( 'NONE',  ( 41.46631938032478359, 147.3844580088725991, 38.96596240072933170 ) ) ;
#20194=CARTESIAN_POINT ( 'NONE',  ( 38.96631938032478359, 99.08445800887258770, 37.14960608071593384 ) ) ;
#20195=CARTESIAN_POINT ( 'NONE',  ( 46.59305225739526435, 154.5797705074273267, 36.81289934271958941 ) ) ;
#20196=CARTESIAN_POINT ( 'NONE',  ( 44.37947211624943833, 67.27977050742731535, 38.42115945441014446 ) ) ;
#20197=CARTESIAN_POINT ( 'NONE',  ( 39.42975644700377558, 125.8151871740940067, 31.60846029578754468 ) ) ;
#20199=CARTESIAN_POINT ( 'NONE',  ( 43.01140435219951286, 82.46049967264873715, 39.46799094044489209 ) ) ;
#20201=CARTESIAN_POINT ( 'NONE',  ( 43.80332655382222384, 97.53738109496902098, 39.21067981925354928 ) ) ;
#20203=CARTESIAN_POINT ( 'NONE',  ( 41.64333658814960870, 77.51518717409399528, 30.00020018409699318 ) ) ;
#20205=CARTESIAN_POINT ( 'NONE',  ( 39.92123440845005433, 133.1604996726487684, 38.46393386101375711 ) ) ;
#20207=CARTESIAN_POINT ( 'NONE',  ( 38.58424406990784661, 63.52977050742730825, 35.64915139335016647 ) ) ;
#20212=VERTEX_POINT ( 'NONE', #12884 ) ;
#20213=CARTESIAN_POINT ( 'NONE',  ( 39.42975644700377558, 152.8151871740940067, 31.60846029578754468 ) ) ;
#20215=CARTESIAN_POINT ( 'NONE',  ( 40.27526882409969744, 117.8297705074273551, 37.97664729208901235 ) ) ;
#20220=CARTESIAN_POINT ( 'NONE',  ( 43.01140435219951286, 118.1297705074273097, 38.86567161673127657 ) ) ;
#20221=CARTESIAN_POINT ( 'NONE',  ( 38.96631938032478359, 126.4104996726487542, 31.27175355779120025 ) ) ;
#20222=CARTESIAN_POINT ( 'NONE',  ( 46.59305225739526435, 157.9151871740940010, 31.60846029578754468 ) ) ;
#20223=( BOUNDED_CURVE ( )  B_SPLINE_CURVE ( 2, ( #3036, #9774, #20452, #18580, #4914, #13291, #13507, #15271, #1719, #18470, #279, #8772, #15046 ),
 .UNSPECIFIED., .F., .F. ) 
 B_SPLINE_CURVE_WITH_KNOTS ( ( 3, 2, 2, 2, 2, 2, 3 ),
 ( 0.1985294117647058709, 0.2000000000000000111, 0.2029411764705882359, 0.2058823529411764608, 0.2088235294117647134, 0.2117647058823529382, 0.2132352941176470507 ),
 .UNSPECIFIED. ) 
 CURVE ( )  GEOMETRIC_REPRESENTATION_ITEM ( )  RATIONAL_B_SPLINE_CURVE ( ( 0.9755282581475765991, 0.9755282581475764880, 1.000000000000000000, 0.9510565162951535312, 1.000000000000000000, 0.9510565162951535312, 1.000000000000000000, 0.9510565162951535312, 1.000000000000000000, 0.9510565162951535312, 1.000000000000000000, 0.9755282581475768211, 0.9755282581475768211 ) ) 
 REPRESENTATION_ITEM ( '' )  );
#20230=CARTESIAN_POINT ( 'NONE',  ( 46.10157429594899270, 76.76049967264872009, 38.46393386101375711 ) ) ;
#20232=CARTESIAN_POINT ( 'NONE',  ( 41.46631938032478359, 98.18445800887256780, 29.45539723777780239 ) ) ;
#20233=CARTESIAN_POINT ( 'NONE',  ( 40.27526882409969033, 89.92977050742730682, 30.44471234641811819 ) ) ;
#20237=CARTESIAN_POINT ( 'NONE',  ( 46.59305225739526435, 88.91518717409400097, 31.60846029578754468 ) ) ;
#20238=FACE_OUTER_BOUND ( 'NONE', #13074, .T. ) ;
#20243=CARTESIAN_POINT ( 'NONE',  ( 40.27526882409969744, 138.8297705074272983, 37.97664729208901235 ) ) ;
#20246=CARTESIAN_POINT ( 'NONE',  ( 44.82204965540741171, 59.43124467221783647, 30.14400234367970910 ) ) ;
#20247=VERTEX_POINT ( 'NONE', #16182 ) ;
#20248=CARTESIAN_POINT ( 'NONE',  ( 46.59305225739526435, 145.5797705074273267, 36.81289934271958941 ) ) ;
#20249=CARTESIAN_POINT ( 'NONE',  ( 47.05648932407426344, 152.5104996726487343, 31.27175355779120025 ) ) ;
#20250=CARTESIAN_POINT ( 'NONE',  ( 43.01140435219951996, 10.71049967264875491, 29.21067981925357060 ) ) ;
#20255=EDGE_CURVE ( 'NONE', #5452, #6422, #5583, .T. ) ;
#20256=CARTESIAN_POINT ( 'NONE',  ( 38.01140435219952707, 143.7844580088725763, 34.21067981925357060 ) ) ;
#20257=CARTESIAN_POINT ( 'NONE',  ( 40.27526882409969033, 119.9297705074272926, 30.44471234641811819 ) ) ;
#20259=CARTESIAN_POINT ( 'NONE',  ( 48.01140435219951996, 100.2844580088725905, 34.21067981925357060 ) ) ;
#20260=CARTESIAN_POINT ( 'NONE',  ( 43.01140435219951286, 114.8651871740939896, 38.86567161673127657 ) ) ;
#20261=CARTESIAN_POINT ( 'NONE',  ( 43.01140435219951286, 126.5344580088725621, 39.21067981925356349 ) ) ;
#20266=CARTESIAN_POINT ( 'NONE',  ( 41.64333658814960870, 81.97977050742731819, 38.42115945441014446 ) ) ;
#20270=CARTESIAN_POINT ( 'NONE',  ( 48.01140435219951996, 73.28445800887257633, 34.21067981925357060 ) ) ;
#20271=CARTESIAN_POINT ( 'NONE',  ( 38.01140435219952707, 59.78445800887258343, 34.21067981925357060 ) ) ;
#20272=CARTESIAN_POINT ( 'NONE',  ( 44.55648932407425633, 130.6104996726487286, 38.96596240072933170 ) ) ;
#20273=CARTESIAN_POINT ( 'NONE',  ( 47.43856463449117200, 91.46518717409398391, 35.64915139335016647 ) ) ;
#20277=CARTESIAN_POINT ( 'NONE',  ( 43.01140435219951996, 10.71049967264875491, 34.21067981925357060 ) ) ;
#20281=CARTESIAN_POINT ( 'NONE',  ( 47.43856463449118621, 148.8797705074273097, 34.21067981925357060 ) ) ;
#20282=DIRECTION ( 'NONE',  ( 0.000000000000000000, 1.000000000000000000, 0.000000000000000000 ) ) ;
#20284=CARTESIAN_POINT ( 'NONE',  ( 38.58424406990785371, 150.2651871740940237, 35.64915139335015937 ) ) ;
#20291=CARTESIAN_POINT ( 'NONE',  ( 40.27526882409969033, 128.6651871740940010, 30.44471234641811819 ) ) ;
#20293=VERTEX_POINT ( 'NONE', #11437 ) ;
#20295=ORIENTED_EDGE ( 'NONE', *, *, #21194, .T. ) ;
#20296=CARTESIAN_POINT ( 'NONE',  ( 38.96631938032478359, 98.48445800887257917, 31.27175355779120025 ) ) ;
#20297=CARTESIAN_POINT ( 'NONE',  ( 43.80332655382220253, 115.5373810949689926, 39.21067981925355639 ) ) ;
#20298=CARTESIAN_POINT ( 'NONE',  ( 47.43856463449117200, 65.02977050742732956, 32.77220824515698183 ) ) ;
#20299=CARTESIAN_POINT ( 'NONE',  ( 47.43856463449117200, 118.4651871740939981, 35.64915139335016647 ) ) ;
#20302=CARTESIAN_POINT ( 'NONE',  ( 41.46631938032478359, 81.11049967264874283, 29.45539723777780239 ) ) ;
#20303=CARTESIAN_POINT ( 'NONE',  ( 44.55648932407425633, 148.8844580088725991, 29.45539723777780239 ) ) ;
#20305=CARTESIAN_POINT ( 'NONE',  ( 48.01140435219951996, 98.36049967264872862, 32.58608133808903773 ) ) ;
#20307=CARTESIAN_POINT ( 'NONE',  ( 40.27526882409969033, 75.56518717409399244, 37.97664729208901946 ) ) ;
#20308=CYLINDRICAL_SURFACE ( 'NONE', #13638, 4.999999999999997335 ) ;
#20309=CARTESIAN_POINT ( 'NONE',  ( 38.01140435219952707, 122.7844580088725763, 34.21067981925357060 ) ) ;
#20312=CARTESIAN_POINT ( 'NONE',  ( 38.58424406990784661, 69.22977050742731819, 32.77220824515698183 ) ) ;
#20318=CARTESIAN_POINT ( 'NONE',  ( 47.43856463449117200, 151.4651871740939839, 35.64915139335016647 ) ) ;
#20320=CARTESIAN_POINT ( 'NONE',  ( 46.59305225739526435, 116.1797705074273210, 31.60846029578754468 ) ) ;
#20326=CARTESIAN_POINT ( 'NONE',  ( 41.64333658814960870, 111.9797705074273324, 38.42115945441014446 ) ) ;
#20327=DIRECTION ( 'NONE',  ( 0.000000000000000000, 1.000000000000000000, 0.000000000000000000 ) ) ;
#20329=CARTESIAN_POINT ( 'NONE',  ( 46.59305225739526435, 151.9151871740940010, 31.60846029578754468 ) ) ;
#20332=CARTESIAN_POINT ( 'NONE',  ( 38.58424406990786082, 159.1151871740940180, 34.21067981925357060 ) ) ;
#20338=CARTESIAN_POINT ( 'NONE',  ( 48.01140435219951996, 97.13445800887257064, 35.83527830041809636 ) ) ;
#20339=CARTESIAN_POINT ( 'NONE',  ( 46.59305225739526435, 92.17977050742732104, 31.60846029578754468 ) ) ;
#20342=CARTESIAN_POINT ( 'NONE',  ( 47.43856463449118621, 76.61518717409400381, 34.21067981925357060 ) ) ;
#20345=FACE_OUTER_BOUND ( 'NONE', #12556, .T. ) ;
#20348=FACE_OUTER_BOUND ( 'NONE', #13149, .T. ) ;
#20350=DIRECTION ( 'NONE',  ( 0.000000000000000000, 1.000000000000000000, 0.000000000000000000 ) ) ;
#20351=( BOUNDED_CURVE ( )  B_SPLINE_CURVE ( 2, ( #4483, #9354, #10793, #19164, #756, #11001, #21043, #12871, #1082, #9471, #17711, #9145, #14624 ),
 .UNSPECIFIED., .F., .F. ) 
 B_SPLINE_CURVE_WITH_KNOTS ( ( 3, 2, 2, 2, 2, 2, 3 ),
 ( 0.8750000000000000000, 0.8764705882352941124, 0.8794117647058823373, 0.8823529411764705621, 0.8852941176470587870, 0.8882352941176470118, 0.8897058823529412352 ),
 .UNSPECIFIED. ) 
 CURVE ( )  GEOMETRIC_REPRESENTATION_ITEM ( )  RATIONAL_B_SPLINE_CURVE ( ( 0.9755282581475768211, 0.9755282581475768211, 1.000000000000000000, 0.9510565162951535312, 1.000000000000000000, 0.9510565162951535312, 1.000000000000000000, 0.9510565162951535312, 1.000000000000000000, 0.9510565162951535312, 1.000000000000000000, 0.9755282581475758219, 0.9755282581475768211 ) ) 
 REPRESENTATION_ITEM ( '' )  );
#20353=CARTESIAN_POINT ( 'NONE',  ( 47.43856463449118621, 139.8797705074273381, 34.21067981925357060 ) ) ;
#20354=CARTESIAN_POINT ( 'NONE',  ( 41.64333658814960870, 99.97977050742731819, 38.42115945441014446 ) ) ;
#20355=CARTESIAN_POINT ( 'NONE',  ( 38.01140435219952707, 141.7104996726487514, 34.21067981925357060 ) ) ;
#20356=CARTESIAN_POINT ( 'NONE',  ( 45.74753988029933538, 62.06518717409399244, 30.44471234641811819 ) ) ;
#20359=LINE ( 'NONE', #8898, #13205 ) ;
#20363=CARTESIAN_POINT ( 'NONE',  ( 48.01140435219951996, 139.2844580088725763, 34.21067981925357060 ) ) ;
#20364=CARTESIAN_POINT ( 'NONE',  ( 38.58424406990786082, 126.3797705074273239, 34.21067981925357060 ) ) ;
#20367=CARTESIAN_POINT ( 'NONE',  ( 38.58424406990785371, 108.2651871740939811, 35.64915139335015937 ) ) ;
#20368=CARTESIAN_POINT ( 'NONE',  ( 41.46631938032478359, 125.1844580088725678, 29.45539723777780239 ) ) ;
#20371=ADVANCED_FACE ( 'NONE', ( #11119 ), #16290, .T. ) ;
#20372=CARTESIAN_POINT ( 'NONE',  ( 41.64333658814960870, 89.77977050742731535, 30.00020018409699318 ) ) ;
#20375=CARTESIAN_POINT ( 'NONE',  ( 46.10157429594899270, 133.7604996726487059, 38.46393386101375711 ) ) ;
#20376=CARTESIAN_POINT ( 'NONE',  ( 38.01140435219952707, 68.78445800887257633, 34.21067981925357060 ) ) ;
#20378=CARTESIAN_POINT ( 'NONE',  ( 48.01140435219951996, 131.3604996726487002, 32.58608133808903773 ) ) ;
#20379=CARTESIAN_POINT ( 'NONE',  ( 43.01140435219951286, 83.36518717409397539, 29.55568802177586463 ) ) ;
#20387=CARTESIAN_POINT ( 'NONE',  ( 44.37947211624943833, 155.4797705074273324, 30.00020018409699318 ) ) ;
#20388=CARTESIAN_POINT ( 'NONE',  ( 47.43856463449118621, 103.8797705074273239, 34.21067981925357060 ) ) ;
#20390=CARTESIAN_POINT ( 'NONE',  ( 44.37947211624943833, 142.0151871740939953, 38.42115945441014446 ) ) ;
#20391=CARTESIAN_POINT ( 'NONE',  ( 46.10157429594899270, 66.83445800887258770, 38.46393386101375711 ) ) ;
#20394=CARTESIAN_POINT ( 'NONE',  ( 44.37947211624943833, 64.01518717409400949, 38.42115945441014446 ) ) ;
#20398=CARTESIAN_POINT ( 'NONE',  ( 47.43856463449118621, 115.6151871740940038, 34.21067981925357060 ) ) ;
#20402=CARTESIAN_POINT ( 'NONE',  ( 48.01140435219951996, 100.2844580088725905, 34.21067981925357060 ) ) ;
#20403=CARTESIAN_POINT ( 'NONE',  ( 46.59305225739526435, 158.1797705074273210, 31.60846029578754468 ) ) ;
#20405=CARTESIAN_POINT ( 'NONE',  ( 48.01140435219951996, 158.0604996726486888, 35.83527830041810347 ) ) ;
#20406=CARTESIAN_POINT ( 'NONE',  ( 43.01140435219951286, 113.3651871740939754, 29.55568802177586463 ) ) ;
#20408=( BOUNDED_CURVE ( )  B_SPLINE_CURVE ( 2, ( #14895, #3002, #1024, #21643, #21308, #9522, #7760, #12924, #19649, #14458, #4540, #11260, #2894 ),
 .UNSPECIFIED., .F., .F. ) 
 B_SPLINE_CURVE_WITH_KNOTS ( ( 3, 2, 2, 2, 2, 2, 3 ),
 ( 0.9485294117647058432, 0.9499999999999999556, 0.9529411764705881804, 0.9558823529411765163, 0.9588235294117647411, 0.9617647058823529660, 0.9632352941176470784 ),
 .UNSPECIFIED. ) 
 CURVE ( )  GEOMETRIC_REPRESENTATION_ITEM ( )  RATIONAL_B_SPLINE_CURVE ( ( 0.9755282581475768211, 0.9755282581475768211, 1.000000000000000000, 0.9510565162951535312, 1.000000000000000000, 0.9510565162951535312, 1.000000000000000000, 0.9510565162951535312, 1.000000000000000000, 0.9510565162951535312, 1.000000000000000000, 0.9755282581475768211, 0.9755282581475768211 ) ) 
 REPRESENTATION_ITEM ( '' )  );
#20409=EDGE_CURVE ( 'NONE', #5965, #1030, #7042, .T. ) ;
#20410=CARTESIAN_POINT ( 'NONE',  ( 38.01140435219951996, 72.86049967264872862, 35.83527830041810347 ) ) ;
#20411=CARTESIAN_POINT ( 'NONE',  ( 42.21948215057684450, 74.11133943119283174, 29.21067981925356705 ) ) ;
#20412=CARTESIAN_POINT ( 'NONE',  ( 41.46631938032478359, 72.38445800887258486, 38.96596240072933170 ) ) ;
#20414=CARTESIAN_POINT ( 'NONE',  ( 41.64333658814960870, 75.71518717409401233, 38.42115945441014446 ) ) ;
#20423=CARTESIAN_POINT ( 'NONE',  ( 43.01140435219951286, 155.3651871740939896, 29.55568802177586463 ) ) ;
#20425=CARTESIAN_POINT ( 'NONE',  ( 44.37947211624943833, 158.2151871740939839, 30.00020018409699318 ) ) ;
#20426=CARTESIAN_POINT ( 'NONE',  ( 38.58424406990786082, 114.3797705074273097, 34.21067981925357060 ) ) ;
#20428=ORIENTED_EDGE ( 'NONE', *, *, #20142, .T. ) ;
#20429=EDGE_CURVE ( 'NONE', #13745, #19857, #7732, .T. ) ;
#20432=CARTESIAN_POINT ( 'NONE',  ( 43.01140435219951286, 109.1297705074273239, 38.86567161673127657 ) ) ;
#20433=DIRECTION ( 'NONE',  ( 0.000000000000000000, 1.000000000000000000, 0.000000000000000000 ) ) ;
#20434=CARTESIAN_POINT ( 'NONE',  ( 38.96631938032478359, 128.4844580088725934, 31.27175355779120025 ) ) ;
#20435=CARTESIAN_POINT ( 'NONE',  ( 38.58424406990784661, 144.2651871740940237, 35.64915139335016647 ) ) ;
#20441=CARTESIAN_POINT ( 'NONE',  ( 46.10157429594899270, 100.7604996726487485, 38.46393386101375711 ) ) ;
#20443=CARTESIAN_POINT ( 'NONE',  ( 48.01140435219951996, 92.36049967264872862, 32.58608133808903773 ) ) ;
#20444=CARTESIAN_POINT ( 'NONE',  ( 42.21948215057684450, 98.11133943119283174, 29.21067981925356705 ) ) ;
#20445=CARTESIAN_POINT ( 'NONE',  ( 39.42975644700377558, 96.67977050742732104, 36.81289934271958941 ) ) ;
#20448=CARTESIAN_POINT ( 'NONE',  ( 44.37947211624943833, 83.21518717409399812, 30.00020018409699318 ) ) ;
#20449=CYLINDRICAL_SURFACE ( 'NONE', #3245, 4.999999999999997335 ) ;
#20452=CARTESIAN_POINT ( 'NONE',  ( 41.46631938032478359, 138.3844580088725991, 38.96596240072933170 ) ) ;
#20453=FACE_OUTER_BOUND ( 'NONE', #20860, .T. ) ;
#20454=CARTESIAN_POINT ( 'NONE',  ( 38.58424406990786082, 141.3797705074273381, 34.21067981925357060 ) ) ;
#20456=ORIENTED_EDGE ( 'NONE', *, *, #20038, .T. ) ;
#20457=EDGE_CURVE ( 'NONE', #11797, #9338, #8446, .T. ) ;
#20460=CARTESIAN_POINT ( 'NONE',  ( 46.59305225739526435, 134.1797705074273210, 31.60846029578754468 ) ) ;
#20462=CARTESIAN_POINT ( 'NONE',  ( 46.59305225739526435, 61.91518717409400097, 31.60846029578754468 ) ) ;
#20464=CARTESIAN_POINT ( 'NONE',  ( 43.01140435219951996, 10.71049967264875491, 39.21067981925356349 ) ) ;
#20465=CARTESIAN_POINT ( 'NONE',  ( 40.27526882409969033, 95.66518717409398675, 30.44471234641811819 ) ) ;
#20471=CARTESIAN_POINT ( 'NONE',  ( 39.92123440845004723, 138.2344580088725650, 38.46393386101376421 ) ) ;
#20472=CARTESIAN_POINT ( 'NONE',  ( 44.37947211624943833, 124.2797705074273154, 38.42115945441014446 ) ) ;
#20475=CARTESIAN_POINT ( 'NONE',  ( 47.43856463449117911, 109.4651871740940123, 35.64915139335015937 ) ) ;
#20483=CARTESIAN_POINT ( 'NONE',  ( 45.74753988029934249, 86.32977050742731251, 30.44471234641812174 ) ) ;
#20485=CARTESIAN_POINT ( 'NONE',  ( 48.01140435219951996, 139.4344580088725536, 32.58608133808903773 ) ) ;
#20486=CARTESIAN_POINT ( 'NONE',  ( 38.01140435219951996, 77.63445800887255643, 32.58608133808903773 ) ) ;
#20487=CARTESIAN_POINT ( 'NONE',  ( 38.96631938032478359, 59.48445800887257207, 31.27175355779120025 ) ) ;
#20488=CARTESIAN_POINT ( 'NONE',  ( 46.10157429594899270, 131.6604996726487116, 29.95742577749337343 ) ) ;
#20489=CARTESIAN_POINT ( 'NONE',  ( 44.37947211624943833, 92.21518717409401233, 30.00020018409699318 ) ) ;
#20497=CARTESIAN_POINT ( 'NONE',  ( 39.92123440845005433, 92.33445800887255928, 29.95742577749336988 ) ) ;
#20499=CARTESIAN_POINT ( 'NONE',  ( 39.42975644700377558, 153.0797705074273267, 31.60846029578754468 ) ) ;
#20500=CARTESIAN_POINT ( 'NONE',  ( 39.42975644700377558, 102.6797705074273210, 36.81289934271958941 ) ) ;
#20502=CARTESIAN_POINT ( 'NONE',  ( 47.43856463449117911, 139.7651871740939953, 32.77220824515697473 ) ) ;
#20504=CARTESIAN_POINT ( 'NONE',  ( 43.01140435219951286, 66.53445800887257633, 39.21067981925356349 ) ) ;
#20508=LINE ( 'NONE', #17180, #14789 ) ;
#20509=CARTESIAN_POINT ( 'NONE',  ( 40.27526882409969033, 113.6651871740939868, 30.44471234641811819 ) ) ;
#20514=CARTESIAN_POINT ( 'NONE',  ( 48.01140435219951996, 97.13445800887258486, 35.83527830041810347 ) ) ;
#20515=CARTESIAN_POINT ( 'NONE',  ( 38.58424406990784661, 60.22977050742731109, 32.77220824515698183 ) ) ;
#20516=CARTESIAN_POINT ( 'NONE',  ( 45.74753988029933538, 116.0651871740939924, 30.44471234641811819 ) ) ;
#20518=CARTESIAN_POINT ( 'NONE',  ( 47.05648932407426344, 73.91049967264873999, 37.14960608071593384 ) ) ;
#20521=CARTESIAN_POINT ( 'NONE',  ( 42.21948215057687293, 71.11133943119284595, 29.21067981925355994 ) ) ;
#20523=CARTESIAN_POINT ( 'NONE',  ( 38.58424406990784661, 78.26518717409400949, 35.64915139335016647 ) ) ;
#20532=CARTESIAN_POINT ( 'NONE',  ( 46.59305225739526435, 139.3151871740940067, 36.81289934271958941 ) ) ;
#20533=CARTESIAN_POINT ( 'NONE',  ( 45.74753988029934249, 158.0651871740940067, 30.44471234641812174 ) ) ;
#20535=CARTESIAN_POINT ( 'NONE',  ( 39.42975644700377558, 105.6797705074273352, 36.81289934271958941 ) ) ;
#20540=CARTESIAN_POINT ( 'NONE',  ( 40.27526882409969033, 108.8297705074272983, 37.97664729208901946 ) ) ;
#20544=CARTESIAN_POINT ( 'NONE',  ( 44.37947211624943833, 82.27977050742732956, 38.42115945441014446 ) ) ;
#20545=CARTESIAN_POINT ( 'NONE',  ( 40.27526882409969033, 140.6651871740939725, 30.44471234641811819 ) ) ;
#20546=CARTESIAN_POINT ( 'NONE',  ( 38.01140435219952707, 105.7104996726487371, 34.21067981925357060 ) ) ;
#20553=CARTESIAN_POINT ( 'NONE',  ( 47.05648932407426344, 76.91049967264873999, 37.14960608071593384 ) ) ;
#20555=CARTESIAN_POINT ( 'NONE',  ( 40.27526882409969033, 81.82977050742729830, 37.97664729208901946 ) ) ;
#20558=CARTESIAN_POINT ( 'NONE',  ( 47.43856463449117911, 79.46518717409399812, 35.64915139335015937 ) ) ;
#20562=CARTESIAN_POINT ( 'NONE',  ( 38.01140435219952707, 117.8604996726487428, 35.83527830041809636 ) ) ;
#20565=CARTESIAN_POINT ( 'NONE',  ( 43.01140435219951286, 133.1297705074273381, 38.86567161673127657 ) ) ;
#20567=ORIENTED_EDGE ( 'NONE', *, *, #12477, .F. ) ;
#20569=CARTESIAN_POINT ( 'NONE',  ( 38.58424406990786082, 132.3797705074273381, 34.21067981925357060 ) ) ;
#20572=CARTESIAN_POINT ( 'NONE',  ( 39.42975644700377558, 96.41518717409400097, 36.81289934271958941 ) ) ;
#20577=CARTESIAN_POINT ( 'NONE',  ( 39.92123440845004723, 146.3344580088725593, 29.95742577749337343 ) ) ;
#20578=CARTESIAN_POINT ( 'NONE',  ( 47.43856463449117200, 109.7297705074273040, 35.64915139335016647 ) ) ;
#20581=CARTESIAN_POINT ( 'NONE',  ( 39.42975644700377558, 102.4151871740940010, 36.81289934271958941 ) ) ;
#20582=ORIENTED_EDGE ( 'NONE', *, *, #1254, .F. ) ;
#20588=CARTESIAN_POINT ( 'NONE',  ( 40.27526882409969744, 89.92977050742732104, 30.44471234641812174 ) ) ;
#20591=CARTESIAN_POINT ( 'NONE',  ( 48.01140435219951996, 73.13445800887258486, 35.83527830041810347 ) ) ;
#20593=CARTESIAN_POINT ( 'NONE',  ( 44.55648932407425633, 127.6104996726487570, 38.96596240072933170 ) ) ;
#20594=CARTESIAN_POINT ( 'NONE',  ( 39.42975644700377558, 90.41518717409400097, 36.81289934271958941 ) ) ;
#20597=EDGE_CURVE ( 'NONE', #11299, #4102, #20170, .T. ) ;
#20599=CARTESIAN_POINT ( 'NONE',  ( 43.01140435219951286, 86.96049967264872294, 29.21067981925356705 ) ) ;
#20600=CARTESIAN_POINT ( 'NONE',  ( 47.05648932407426344, 127.5844580088725877, 31.27175355779120025 ) ) ;
#20601=DIRECTION ( 'NONE',  ( 0.000000000000000000, 1.000000000000000000, 0.000000000000000000 ) ) ;
#20602=CARTESIAN_POINT ( 'NONE',  ( 47.05648932407426344, 142.9104996726487400, 37.14960608071593384 ) ) ;
#20603=CARTESIAN_POINT ( 'NONE',  ( 44.37947211624943833, 152.4797705074273324, 30.00020018409699318 ) ) ;
#20604=( BOUNDED_CURVE ( )  B_SPLINE_CURVE ( 2, ( #725, #9323, #14162, #19239, #11070, #15709, #12621, #9437, #5998, #14263, #4139, #4242, #614 ),
 .UNSPECIFIED., .F., .T. ) 
 B_SPLINE_CURVE_WITH_KNOTS ( ( 3, 2, 2, 2, 2, 2, 3 ),
 ( 0.3308823529411764608, 0.3323529411764705732, 0.3352941176470587981, 0.3382352941176470784, 0.3411764705882353033, 0.3441176470588235281, 0.3455882352941176405 ),
 .UNSPECIFIED. ) 
 CURVE ( )  GEOMETRIC_REPRESENTATION_ITEM ( )  RATIONAL_B_SPLINE_CURVE ( ( 0.9755282581475768211, 0.9755282581475768211, 1.000000000000000000, 0.9510565162951535312, 1.000000000000000000, 0.9510565162951535312, 1.000000000000000000, 0.9510565162951535312, 1.000000000000000000, 0.9510565162951535312, 1.000000000000000000, 0.9755282581475768211, 0.9755282581475768211 ) ) 
 REPRESENTATION_ITEM ( '' )  );
#20605=CARTESIAN_POINT ( 'NONE',  ( 40.27526882409969033, 104.9297705074273210, 30.44471234641811819 ) ) ;
#20607=CARTESIAN_POINT ( 'NONE',  ( 47.43856463449117911, 136.4651871740939839, 35.64915139335015937 ) ) ;
#20608=CARTESIAN_POINT ( 'NONE',  ( 48.01140435219951996, 67.28445800887257633, 34.21067981925357060 ) ) ;
#20610=CARTESIAN_POINT ( 'NONE',  ( 43.01140435219951286, 117.5344580088725763, 39.21067981925356349 ) ) ;
#20613=DIRECTION ( 'NONE',  ( -0.000000000000000000, 1.000000000000000000, -0.000000000000000000 ) ) ;
#20614=CARTESIAN_POINT ( 'NONE',  ( 38.58424406990784661, 116.9651871740939839, 32.77220824515698183 ) ) ;
#20615=VERTEX_POINT ( 'NONE', #15616 ) ;
#20616=EDGE_CURVE ( 'NONE', #13985, #9753, #14286, .T. ) ;
#20617=CARTESIAN_POINT ( 'NONE',  ( 43.01140435219951286, 114.5344580088725621, 39.21067981925356349 ) ) ;
#20619=CARTESIAN_POINT ( 'NONE',  ( 44.55648932407425633, 99.68445800887256780, 38.96596240072933170 ) ) ;
#20620=CARTESIAN_POINT ( 'NONE',  ( 44.37947211624943833, 148.2797705074273154, 38.42115945441014446 ) ) ;
#20621=CARTESIAN_POINT ( 'NONE',  ( 38.01140435219951996, 153.8604996726487002, 35.83527830041810347 ) ) ;
#20622=CARTESIAN_POINT ( 'NONE',  ( 38.58424406990786082, 117.1151871740940038, 34.21067981925357060 ) ) ;
#20624=CARTESIAN_POINT ( 'NONE',  ( 47.05648932407426344, 67.91049967264873999, 37.14960608071593384 ) ) ;
#20626=FACE_OUTER_BOUND ( 'NONE', #19745, .T. ) ;
#20628=DIRECTION ( 'NONE',  ( 0.000000000000000000, 0.000000000000000000, 1.000000000000000000 ) ) ;
#20630=CARTESIAN_POINT ( 'NONE',  ( 40.27526882409969033, 80.66518717409400097, 30.44471234641811819 ) ) ;
#20631=CARTESIAN_POINT ( 'NONE',  ( 44.55648932407425633, 104.8104996726487457, 29.45539723777780239 ) ) ;
#20639=CARTESIAN_POINT ( 'NONE',  ( 43.01140435219951286, 147.8651871740940180, 38.86567161673127657 ) ) ;
#20641=CARTESIAN_POINT ( 'NONE',  ( 46.59305225739526435, 104.1797705074273210, 31.60846029578754468 ) ) ;
#20643=ORIENTED_EDGE ( 'NONE', *, *, #6973, .T. ) ;
#20646=ORIENTED_EDGE ( 'NONE', *, *, #19160, .F. ) ;
#20649=CARTESIAN_POINT ( 'NONE',  ( 44.37947211624943833, 142.0151871740939953, 38.42115945441014446 ) ) ;
#20651=CARTESIAN_POINT ( 'NONE',  ( 48.01140435219951996, 101.3604996726487286, 32.58608133808903773 ) ) ;
#20659=LINE ( 'NONE', #12268, #4285 ) ;
#20661=CARTESIAN_POINT ( 'NONE',  ( 47.43856463449117200, 86.02977050742731535, 32.77220824515698183 ) ) ;
#20663=CARTESIAN_POINT ( 'NONE',  ( 38.58424406990785371, 80.96518717409399812, 32.77220824515697473 ) ) ;
#20665=DIRECTION ( 'NONE',  ( 0.000000000000000000, 0.000000000000000000, 1.000000000000000000 ) ) ;
#20666=EDGE_LOOP ( 'NONE', ( #7064, #12994, #13877, #10019 ) ) ;
#20667=DIRECTION ( 'NONE',  ( 0.000000000000000000, 1.000000000000000000, 0.000000000000000000 ) ) ;
#20668=( BOUNDED_CURVE ( )  B_SPLINE_CURVE ( 2, ( #18669, #3572, #15470, #7099, #8643, #2126, #6994 ),
 .UNSPECIFIED., .F., .F. ) 
 B_SPLINE_CURVE_WITH_KNOTS ( ( 3, 2, 2, 3 ),
 ( 0.000000000000000000, 0.002941176470588235253, 0.005882352941176470507, 0.007352941176470595072 ),
 .UNSPECIFIED. ) 
 CURVE ( )  GEOMETRIC_REPRESENTATION_ITEM ( )  RATIONAL_B_SPLINE_CURVE ( ( 1.000000000000000000, 0.9510565162951535312, 1.000000000000000000, 0.9510565162951535312, 1.000000000000000000, 0.9755282581475765991, 0.9755282581475767101 ) ) 
 REPRESENTATION_ITEM ( '' )  );
#20669=CARTESIAN_POINT ( 'NONE',  ( 46.59305225739526435, 134.1797705074273210, 31.60846029578754468 ) ) ;
#20671=ORIENTED_EDGE ( 'NONE', *, *, #12070, .T. ) ;
#20672=CARTESIAN_POINT ( 'NONE',  ( 48.01140435219951996, 73.28445800887257633, 34.21067981925357060 ) ) ;
#20675=CARTESIAN_POINT ( 'NONE',  ( 41.64333658814960870, 138.9797705074273324, 38.42115945441014446 ) ) ;
#20676=CARTESIAN_POINT ( 'NONE',  ( 43.01140435219951286, 91.12977050742732388, 38.86567161673127657 ) ) ;
#20678=CARTESIAN_POINT ( 'NONE',  ( 44.55648932407425633, 121.8844580088725849, 29.45539723777780239 ) ) ;
#20680=CARTESIAN_POINT ( 'NONE',  ( 39.42975644700377558, 95.81518717409399244, 31.60846029578754468 ) ) ;
#20685=CARTESIAN_POINT ( 'NONE',  ( 46.10157429594899270, 142.7344580088725934, 29.95742577749337343 ) ) ;
#20686=CARTESIAN_POINT ( 'NONE',  ( 38.58424406990784661, 114.2297705074273040, 32.77220824515698183 ) ) ;
#20689=CARTESIAN_POINT ( 'NONE',  ( 41.64333658814960870, 107.5151871740939953, 30.00020018409699318 ) ) ;
#20691=ORIENTED_EDGE ( 'NONE', *, *, #18308, .T. ) ;
#20692=CARTESIAN_POINT ( 'NONE',  ( 43.01140435219951996, 10.71049967264875491, 34.21067981925357060 ) ) ;
#20696=CARTESIAN_POINT ( 'NONE',  ( 38.58424406990786082, 78.37977050742732388, 34.21067981925357060 ) ) ;
#20698=VECTOR ( 'NONE', #8033, 1000.000000000000000 ) ;
#20701=CARTESIAN_POINT ( 'NONE',  ( 41.46631938032478359, 66.38445800887257064, 38.96596240072933170 ) ) ;
#20703=CARTESIAN_POINT ( 'NONE',  ( 38.96631938032478359, 130.0104996726487343, 37.14960608071593384 ) ) ;
#20704=CARTESIAN_POINT ( 'NONE',  ( 38.58424406990786082, 90.11518717409400381, 34.21067981925357060 ) ) ;
#20707=CARTESIAN_POINT ( 'NONE',  ( 38.96631938032478359, 116.4844580088725792, 31.27175355779120025 ) ) ;
#20709=CARTESIAN_POINT ( 'NONE',  ( 39.92123440845005433, 81.23445800887256496, 38.46393386101375711 ) ) ;
#20710=CARTESIAN_POINT ( 'NONE',  ( 48.01140435219951996, 143.3604996726487570, 32.58608133808903773 ) ) ;
#20711=CARTESIAN_POINT ( 'NONE',  ( 47.43856463449118621, 142.8797705074273381, 34.21067981925357060 ) ) ;
#20712=CARTESIAN_POINT ( 'NONE',  ( 38.58424406990784661, 108.2297705074273182, 32.77220824515698183 ) ) ;
#20714=CARTESIAN_POINT ( 'NONE',  ( 41.64333658814960870, 137.5151871740939953, 30.00020018409699318 ) ) ;
#20718=CARTESIAN_POINT ( 'NONE',  ( 48.01140435219951996, 91.13445800887257064, 35.83527830041809636 ) ) ;
#20720=DIRECTION ( 'NONE',  ( 0.000000000000000000, 0.000000000000000000, 1.000000000000000000 ) ) ;
#20721=CARTESIAN_POINT ( 'NONE',  ( 45.74753988029933538, 116.0651871740939924, 30.44471234641811819 ) ) ;
#20726=CARTESIAN_POINT ( 'NONE',  ( 43.01140435219951286, 96.53445800887257633, 39.46799094044489209 ) ) ;
#20727=CARTESIAN_POINT ( 'NONE',  ( 40.27526882409969744, 149.9297705074273210, 30.44471234641812174 ) ) ;
#20728=CARTESIAN_POINT ( 'NONE',  ( 46.59305225739526435, 61.57977050742731251, 36.81289934271958941 ) ) ;
#20729=CARTESIAN_POINT ( 'NONE',  ( 44.37947211624943833, 115.0151871740940095, 38.42115945441014446 ) ) ;
#20731=CARTESIAN_POINT ( 'NONE',  ( 44.55648932407425633, 73.61049967264874283, 38.96596240072933170 ) ) ;
#20732=CARTESIAN_POINT ( 'NONE',  ( 38.96631938032478359, 107.4844580088725792, 31.27175355779120025 ) ) ;
#20733=CARTESIAN_POINT ( 'NONE',  ( 43.01140435219951996, 10.71049967264875491, 34.21067981925357060 ) ) ;
#20736=CARTESIAN_POINT ( 'NONE',  ( 41.64333658814960870, 72.71518717409399812, 38.42115945441014446 ) ) ;
#20737=CARTESIAN_POINT ( 'NONE',  ( 38.96631938032478359, 63.41049967264873999, 31.27175355779120025 ) ) ;
#20740=ORIENTED_EDGE ( 'NONE', *, *, #19729, .F. ) ;
#20743=VERTEX_POINT ( 'NONE', #12642 ) ;
#20744=CARTESIAN_POINT ( 'NONE',  ( 40.27526882409969033, 141.5651871740940067, 37.97664729208901946 ) ) ;
#20745=CYLINDRICAL_SURFACE ( 'NONE', #16240, 4.999999999999997335 ) ;
#20746=CARTESIAN_POINT ( 'NONE',  ( 47.43856463449118621, 100.8797705074273239, 34.21067981925357060 ) ) ;
#20749=ORIENTED_EDGE ( 'NONE', *, *, #11554, .T. ) ;
#20752=ORIENTED_EDGE ( 'NONE', *, *, #21284, .F. ) ;
#20754=CARTESIAN_POINT ( 'NONE',  ( 39.42975644700377558, 81.67977050742732104, 36.81289934271958941 ) ) ;
#20755=CARTESIAN_POINT ( 'NONE',  ( 44.37947211624943833, 149.2151871740940123, 30.00020018409699318 ) ) ;
#20756=CARTESIAN_POINT ( 'NONE',  ( 41.46631938032478359, 103.3104996726487457, 38.96596240072933170 ) ) ;
#20760=CARTESIAN_POINT ( 'NONE',  ( 43.01140435219951286, 152.0344580088725763, 29.21067981925356705 ) ) ;
#20762=CARTESIAN_POINT ( 'NONE',  ( 38.96631938032478359, 144.0844580088725877, 37.14960608071593384 ) ) ;
#20763=CARTESIAN_POINT ( 'NONE',  ( 43.01140435219951286, 113.9604996726487371, 29.21067981925356705 ) ) ;
#20766=CARTESIAN_POINT ( 'NONE',  ( 45.74753988029933538, 83.32977050742732672, 30.44471234641811819 ) ) ;
#20768=CARTESIAN_POINT ( 'NONE',  ( 45.74753988029934249, 76.16518717409400097, 37.97664729208901235 ) ) ;
#20770=LINE ( 'NONE', #9415, #19565 ) ;
#20774=CARTESIAN_POINT ( 'NONE',  ( 44.37947211624943833, 136.2797705074273154, 38.42115945441014446 ) ) ;
#20776=ORIENTED_EDGE ( 'NONE', *, *, #9681, .T. ) ;
#20778=ORIENTED_EDGE ( 'NONE', *, *, #15409, .T. ) ;
#20779=CARTESIAN_POINT ( 'NONE',  ( 40.27526882409969033, 140.9297705074273210, 30.44471234641811819 ) ) ;
#20783=CARTESIAN_POINT ( 'NONE',  ( 44.55648932407425633, 120.6844580088725962, 38.96596240072933170 ) ) ;
#20784=CARTESIAN_POINT ( 'NONE',  ( 42.21948215057683740, 159.0373810949690494, 29.21067981925356705 ) ) ;
#20785=CARTESIAN_POINT ( 'NONE',  ( 43.01140435219951286, 93.86518717409400381, 38.86567161673127657 ) ) ;
#20789=CARTESIAN_POINT ( 'NONE',  ( 47.05648932407426344, 109.5844580088725735, 31.27175355779120025 ) ) ;
#20790=CARTESIAN_POINT ( 'NONE',  ( 38.01140435219951996, 128.9344580088726104, 35.83527830041810347 ) ) ;
#20791=CARTESIAN_POINT ( 'NONE',  ( 43.01140435219951286, 115.1297705074272955, 38.86567161673127657 ) ) ;
#20792=( BOUNDED_CURVE ( )  B_SPLINE_CURVE ( 2, ( #10199, #16902, #1815, #8549, #11947, #3579, #266, #7001, #13706, #20441, #5333, #10412, #8760 ),
 .UNSPECIFIED., .F., .F. ) 
 B_SPLINE_CURVE_WITH_KNOTS ( ( 3, 2, 2, 2, 2, 2, 3 ),
 ( 0.5661764705882352811, 0.5676470588235293935, 0.5705882352941176183, 0.5735294117647058432, 0.5764705882352940680, 0.5794117647058824039, 0.5808823529411765163 ),
 .UNSPECIFIED. ) 
 CURVE ( )  GEOMETRIC_REPRESENTATION_ITEM ( )  RATIONAL_B_SPLINE_CURVE ( ( 0.9755282581475768211, 0.9755282581475768211, 1.000000000000000000, 0.9510565162951535312, 1.000000000000000000, 0.9510565162951535312, 1.000000000000000000, 0.9510565162951535312, 1.000000000000000000, 0.9510565162951535312, 1.000000000000000000, 0.9755282581475768211, 0.9755282581475768211 ) ) 
 REPRESENTATION_ITEM ( '' )  );
#20795=CARTESIAN_POINT ( 'NONE',  ( 47.43856463449117911, 103.7651871740939669, 32.77220824515697473 ) ) ;
#20798=CARTESIAN_POINT ( 'NONE',  ( 39.92123440845005433, 88.16049967264873999, 38.46393386101375711 ) ) ;
#20802=CARTESIAN_POINT ( 'NONE',  ( 43.01140435219951996, 10.71049967264875491, 34.21067981925357060 ) ) ;
#20804=CARTESIAN_POINT ( 'NONE',  ( 38.58424406990785371, 72.52977050742731535, 35.64915139335015937 ) ) ;
#20807=ORIENTED_EDGE ( 'NONE', *, *, #20038, .F. ) ;
#20808=CARTESIAN_POINT ( 'NONE',  ( 44.55648932407425633, 60.68445800887258201, 38.96596240072933170 ) ) ;
#20810=EDGE_CURVE ( 'NONE', #21725, #14883, #2602, .T. ) ;
#20811=CARTESIAN_POINT ( 'NONE',  ( 43.01140435219951286, 116.9604996726487514, 28.95336869806222779 ) ) ;
#20812=CARTESIAN_POINT ( 'NONE',  ( 40.27526882409969033, 78.56518717409399244, 37.97664729208901946 ) ) ;
#20815=CARTESIAN_POINT ( 'NONE',  ( 48.01140435219951996, 113.3604996726487286, 32.58608133808903773 ) ) ;
#20817=CARTESIAN_POINT ( 'NONE',  ( 43.80332655382220253, 67.53738109496899256, 39.21067981925355639 ) ) ;
#20819=CARTESIAN_POINT ( 'NONE',  ( 38.58424406990786082, 144.3797705074273097, 34.21067981925357060 ) ) ;
#20821=CARTESIAN_POINT ( 'NONE',  ( 38.58424406990785371, 131.9651871740939839, 32.77220824515697473 ) ) ;
#20828=CARTESIAN_POINT ( 'NONE',  ( 41.64333658814960870, 114.7151871740940123, 38.42115945441014446 ) ) ;
#20832=ORIENTED_EDGE ( 'NONE', *, *, #13923, .T. ) ;
#20833=CARTESIAN_POINT ( 'NONE',  ( 39.92123440845004723, 89.33445800887257349, 29.95742577749337343 ) ) ;
#20834=CARTESIAN_POINT ( 'NONE',  ( 44.37947211624943833, 149.4797705074273324, 30.00020018409699318 ) ) ;
#20835=AXIS2_PLACEMENT_3D ( 'NONE', #15587, #10745, #5549 ) ;
#20836=CARTESIAN_POINT ( 'NONE',  ( 41.46631938032478359, 150.1104996726487570, 29.45539723777780239 ) ) ;
#20837=CARTESIAN_POINT ( 'NONE',  ( 38.58424406990784661, 105.2651871740939953, 35.64915139335016647 ) ) ;
#20839=CARTESIAN_POINT ( 'NONE',  ( 48.01140435219951996, 74.06049967264874567, 35.83527830041810347 ) ) ;
#20841=CARTESIAN_POINT ( 'NONE',  ( 47.05648932407426344, 118.5844580088725735, 31.27175355779120025 ) ) ;
#20843=CARTESIAN_POINT ( 'NONE',  ( 38.96631938032478359, 71.48445800887257917, 31.27175355779120025 ) ) ;
#20845=CARTESIAN_POINT ( 'NONE',  ( 47.43856463449117200, 67.46518717409399812, 35.64915139335016647 ) ) ;
#20846=CARTESIAN_POINT ( 'NONE',  ( 43.01140435219951286, 62.96049967264873004, 29.21067981925356705 ) ) ;
#20854=CARTESIAN_POINT ( 'NONE',  ( 40.27526882409969033, 140.6651871740939725, 30.44471234641811819 ) ) ;
#20855=CARTESIAN_POINT ( 'NONE',  ( 40.27526882409969744, 107.9297705074273352, 30.44471234641812174 ) ) ;
#20860=EDGE_LOOP ( 'NONE', ( #3231, #13934, #17400, #17697 ) ) ;
#20861=CARTESIAN_POINT ( 'NONE',  ( 38.96631938032478359, 116.4844580088725792, 31.27175355779120025 ) ) ;
#20862=CARTESIAN_POINT ( 'NONE',  ( 44.55648932407425633, 89.81049967264874567, 29.45539723777780239 ) ) ;
#20863=CARTESIAN_POINT ( 'NONE',  ( 41.64333658814960870, 83.77977050742732956, 30.00020018409699318 ) ) ;
#20864=CARTESIAN_POINT ( 'NONE',  ( 38.58424406990784661, 138.2651871740939669, 35.64915139335016647 ) ) ;
#20865=CARTESIAN_POINT ( 'NONE',  ( 38.01140435219951996, 102.5604996726487599, 32.58608133808903773 ) ) ;
#20871=CARTESIAN_POINT ( 'NONE',  ( 46.10157429594899270, 64.73445800887257917, 29.95742577749336988 ) ) ;
#20872=CARTESIAN_POINT ( 'NONE',  ( 43.01140435219951286, 105.5344580088725621, 39.21067981925356349 ) ) ;
#20874=CARTESIAN_POINT ( 'NONE',  ( 43.01140435219951286, 85.12977050742729546, 38.86567161673127657 ) ) ;
#20876=CARTESIAN_POINT ( 'NONE',  ( 40.27526882409969744, 66.56518717409400665, 37.97664729208901235 ) ) ;
#20882=CARTESIAN_POINT ( 'NONE',  ( 41.64333658814960870, 129.9797705074273040, 38.42115945441014446 ) ) ;
#20885=CARTESIAN_POINT ( 'NONE',  ( 48.01140435219951996, 73.43445800887256780, 32.58608133808903773 ) ) ;
#20887=CARTESIAN_POINT ( 'NONE',  ( 47.43856463449117200, 131.0297705074272869, 32.77220824515698183 ) ) ;
#20888=CARTESIAN_POINT ( 'NONE',  ( 48.01140435219951996, 145.1344580088725991, 35.83527830041809636 ) ) ;
#20889=CARTESIAN_POINT ( 'NONE',  ( 43.80332655382220253, 154.5373810949690210, 39.21067981925354218 ) ) ;
#20890=CARTESIAN_POINT ( 'NONE',  ( 38.96631938032478359, 110.4844580088725792, 31.27175355779120025 ) ) ;
#20892=CARTESIAN_POINT ( 'NONE',  ( 39.92123440845005433, 159.2604996726487343, 29.95742577749336988 ) ) ;
#20893=CARTESIAN_POINT ( 'NONE',  ( 44.37947211624943833, 97.01518717409400949, 38.42115945441014446 ) ) ;
#20894=LINE ( 'NONE', #12512, #2024 ) ;
#20895=CARTESIAN_POINT ( 'NONE',  ( 43.01140435219951286, 78.53445800887259054, 39.21067981925356349 ) ) ;
#20899=CARTESIAN_POINT ( 'NONE',  ( 38.01140435219952707, 134.7844580088726048, 34.21067981925357060 ) ) ;
#20900=CARTESIAN_POINT ( 'NONE',  ( 38.58424406990786082, 111.3797705074273239, 34.21067981925357060 ) ) ;
#20902=CARTESIAN_POINT ( 'NONE',  ( 43.01140435219951286, 67.46049967264873715, 39.21067981925356349 ) ) ;
#20903=CARTESIAN_POINT ( 'NONE',  ( 47.43856463449118621, 100.6151871740940180, 34.21067981925357060 ) ) ;
#20905=ORIENTED_EDGE ( 'NONE', *, *, #7540, .F. ) ;
#20912=CARTESIAN_POINT ( 'NONE',  ( 40.27526882409969744, 71.92977050742729261, 30.44471234641812174 ) ) ;
#20917=AXIS2_PLACEMENT_3D ( 'NONE', #10469, #1865, #7379 ) ;
#20918=CARTESIAN_POINT ( 'NONE',  ( 38.96631938032478359, 121.0104996726487343, 37.14960608071593384 ) ) ;
#20920=CARTESIAN_POINT ( 'NONE',  ( 38.58424406990786082, 81.11518717409398960, 34.21067981925357060 ) ) ;
#20929=CARTESIAN_POINT ( 'NONE',  ( 38.58424406990784661, 138.2297705074273324, 32.77220824515698183 ) ) ;
#20932=CARTESIAN_POINT ( 'NONE',  ( 40.27526882409969744, 135.5651871740940067, 37.97664729208901235 ) ) ;
#20933=CARTESIAN_POINT ( 'NONE',  ( 44.55648932407425633, 137.8104996726487457, 29.45539723777780239 ) ) ;
#20937=VECTOR ( 'NONE', #20327, 1000.000000000000000 ) ;
#20939=CARTESIAN_POINT ( 'NONE',  ( 41.64333658814960870, 102.7151871740939981, 38.42115945441014446 ) ) ;
#20942=DIRECTION ( 'NONE',  ( 0.000000000000000000, 1.000000000000000000, 0.000000000000000000 ) ) ;
#20943=ORIENTED_EDGE ( 'NONE', *, *, #712, .T. ) ;
#20944=CARTESIAN_POINT ( 'NONE',  ( 41.46631938032478359, 96.38445800887257064, 38.96596240072933170 ) ) ;
#20945=CARTESIAN_POINT ( 'NONE',  ( 38.01140435219951996, 144.8604996726487002, 35.83527830041810347 ) ) ;
#20946=CARTESIAN_POINT ( 'NONE',  ( 38.58424406990786082, 108.1151871740940038, 34.21067981925357060 ) ) ;
#20948=CARTESIAN_POINT ( 'NONE',  ( 48.01140435219951996, 62.21049967264874425, 34.21067981925357060 ) ) ;
#20951=DIRECTION ( 'NONE',  ( 0.000000000000000000, 1.000000000000000000, 0.000000000000000000 ) ) ;
#20954=CARTESIAN_POINT ( 'NONE',  ( 38.58424406990786082, 66.11518717409398960, 34.21067981925357060 ) ) ;
#20963=DIRECTION ( 'NONE',  ( 0.000000000000000000, 1.000000000000000000, 0.000000000000000000 ) ) ;
#20964=CARTESIAN_POINT ( 'NONE',  ( 44.37947211624943833, 140.2151871740940123, 30.00020018409699318 ) ) ;
#20965=CARTESIAN_POINT ( 'NONE',  ( 46.59305225739526435, 103.5797705074273267, 36.81289934271958941 ) ) ;
#20971=VECTOR ( 'NONE', #8326, 1000.000000000000000 ) ;
#20973=CARTESIAN_POINT ( 'NONE',  ( 47.43856463449117200, 76.72977050742733240, 35.64915139335016647 ) ) ;
#20974=CARTESIAN_POINT ( 'NONE',  ( 44.37947211624943833, 136.0151871740939953, 38.42115945441014446 ) ) ;
#20975=CARTESIAN_POINT ( 'NONE',  ( 47.05648932407426344, 98.51049967264874851, 31.27175355779120025 ) ) ;
#20986=CARTESIAN_POINT ( 'NONE',  ( 41.64333658814960870, 86.77977050742731535, 30.00020018409699318 ) ) ;
#20990=ORIENTED_EDGE ( 'NONE', *, *, #15409, .F. ) ;
#20991=CARTESIAN_POINT ( 'NONE',  ( 44.55648932407425633, 85.88445800887258486, 29.45539723777780239 ) ) ;
#20993=CARTESIAN_POINT ( 'NONE',  ( 43.01140435219951286, 137.6297705074273381, 29.55568802177586107 ) ) ;
#20996=CARTESIAN_POINT ( 'NONE',  ( 46.10157429594899270, 73.73445800887256496, 29.95742577749336988 ) ) ;
#20998=CARTESIAN_POINT ( 'NONE',  ( 40.27526882409969033, 125.9297705074273352, 30.44471234641811819 ) ) ;
#20999=CARTESIAN_POINT ( 'NONE',  ( 43.80332655382221674, 133.5373810949689926, 39.21067981925355639 ) ) ;
#21001=CARTESIAN_POINT ( 'NONE',  ( 47.43856463449118621, 88.87977050742732388, 34.21067981925357060 ) ) ;
#21005=CARTESIAN_POINT ( 'NONE',  ( 38.01140435219952707, 159.5604996726487457, 32.58608133808903773 ) ) ;
#21007=CARTESIAN_POINT ( 'NONE',  ( 38.58424406990786082, 90.11518717409400381, 34.21067981925357060 ) ) ;
#21012=CARTESIAN_POINT ( 'NONE',  ( 38.01140435219952707, 131.7844580088725763, 34.21067981925357060 ) ) ;
#21013=CARTESIAN_POINT ( 'NONE',  ( 38.96631938032478359, 132.0844580088725877, 37.14960608071593384 ) ) ;
#21014=CARTESIAN_POINT ( 'NONE',  ( 43.01140435219951286, 113.6297705074273097, 29.55568802177586463 ) ) ;
#21017=CARTESIAN_POINT ( 'NONE',  ( 40.27526882409969744, 101.6651871740940010, 30.44471234641812174 ) ) ;
#21018=CARTESIAN_POINT ( 'NONE',  ( 38.01140435219952707, 90.71049967264873715, 34.21067981925357060 ) ) ;
#21026=CARTESIAN_POINT ( 'NONE',  ( 39.42975644700377558, 75.07977050742731251, 31.60846029578754468 ) ) ;
#21029=CARTESIAN_POINT ( 'NONE',  ( 44.37947211624943833, 154.2797705074273438, 38.42115945441014446 ) ) ;
#21031=CARTESIAN_POINT ( 'NONE',  ( 38.96631938032478359, 124.0104996726487343, 37.14960608071593384 ) ) ;
#21032=CARTESIAN_POINT ( 'NONE',  ( 46.59305225739526435, 73.31518717409400665, 36.81289934271958941 ) ) ;
#21036=CARTESIAN_POINT ( 'NONE',  ( 43.01140435219951286, 113.9604996726487371, 29.21067981925356705 ) ) ;
#21039=CARTESIAN_POINT ( 'NONE',  ( 43.01140435219951286, 156.5344580088725763, 39.46799094044489209 ) ) ;
#21040=CARTESIAN_POINT ( 'NONE',  ( 44.37947211624943833, 143.4797705074273324, 30.00020018409699318 ) ) ;
#21042=CARTESIAN_POINT ( 'NONE',  ( 44.37947211624943833, 125.2151871740939981, 30.00020018409699318 ) ) ;
#21043=CARTESIAN_POINT ( 'NONE',  ( 38.01140435219952707, 69.71049967264873715, 34.21067981925357060 ) ) ;
#21049=AXIS2_PLACEMENT_3D ( 'NONE', #8113, #16470, #14819 ) ;
#21050=CARTESIAN_POINT ( 'NONE',  ( 38.01140435219952707, 120.5604996726487457, 32.58608133808903773 ) ) ;
#21051=CARTESIAN_POINT ( 'NONE',  ( 44.37947211624943833, 109.0151871740940095, 38.42115945441014446 ) ) ;
#21054=CARTESIAN_POINT ( 'NONE',  ( 43.01140435219951286, 116.9604996726487371, 29.21067981925356705 ) ) ;
#21057=CARTESIAN_POINT ( 'NONE',  ( 46.10157429594899270, 91.73445800887257917, 29.95742577749337343 ) ) ;
#21059=CARTESIAN_POINT ( 'NONE',  ( 40.27526882409969033, 104.6651871740939868, 30.44471234641811819 ) ) ;
#21061=CARTESIAN_POINT ( 'NONE',  ( 43.01140435219951286, 62.96049967264874425, 28.95336869806222779 ) ) ;
#21063=CARTESIAN_POINT ( 'NONE',  ( 44.55648932407425633, 61.88445800887257064, 29.45539723777780239 ) ) ;
#21067=CARTESIAN_POINT ( 'NONE',  ( 47.43856463449117200, 73.46518717409398391, 35.64915139335016647 ) ) ;
#21069=CARTESIAN_POINT ( 'NONE',  ( 43.01140435219957681, 71.03445800887256212, 29.21067981925356705 ) ) ;
#21076=CARTESIAN_POINT ( 'NONE',  ( 44.37947211624943833, 137.2151871740940123, 30.00020018409699318 ) ) ;
#21077=CARTESIAN_POINT ( 'NONE',  ( 47.43856463449117911, 154.7651871740940237, 32.77220824515697473 ) ) ;
#21078=CARTESIAN_POINT ( 'NONE',  ( 43.01140435219951286, 95.62977050742732388, 29.55568802177586107 ) ) ;
#21079=EDGE_LOOP ( 'NONE', ( #15857, #4944, #12746, #14723 ) ) ;
#21085=CARTESIAN_POINT ( 'NONE',  ( 48.01140435219951996, 112.1344580088725706, 35.83527830041810347 ) ) ;
#21087=CARTESIAN_POINT ( 'NONE',  ( 45.74753988029933538, 73.42977050742732104, 37.97664729208901946 ) ) ;
#21088=CARTESIAN_POINT ( 'NONE',  ( 45.74753988029933538, 139.1651871740940010, 37.97664729208901946 ) ) ;
#21089=CARTESIAN_POINT ( 'NONE',  ( 38.01140435219951996, 90.56049967264874567, 32.58608133808903773 ) ) ;
#21097=CARTESIAN_POINT ( 'NONE',  ( 47.43856463449117200, 79.72977050742728977, 35.64915139335016647 ) ) ;
#21105=CARTESIAN_POINT ( 'NONE',  ( 47.43856463449117911, 121.7297705074273040, 35.64915139335015937 ) ) ;
#21106=EDGE_LOOP ( 'NONE', ( #5936, #16499, #18547, #1392 ) ) ;
#21109=CARTESIAN_POINT ( 'NONE',  ( 43.01140435219951286, 122.6297705074273239, 29.55568802177586463 ) ) ;
#21110=CARTESIAN_POINT ( 'NONE',  ( 48.01140435219951996, 110.2104996726487514, 34.21067981925357060 ) ) ;
#21111=CARTESIAN_POINT ( 'NONE',  ( 38.58424406990784661, 90.22977050742731819, 32.77220824515698183 ) ) ;
#21119=CARTESIAN_POINT ( 'NONE',  ( 48.01140435219951996, 136.1344580088725991, 35.83527830041810347 ) ) ;
#21120=CARTESIAN_POINT ( 'NONE',  ( 38.58424406990784661, 102.5297705074273154, 35.64915139335016647 ) ) ;
#21123=CARTESIAN_POINT ( 'NONE',  ( 45.74753988029934249, 100.1651871740939868, 37.97664729208901235 ) ) ;
#21127=CARTESIAN_POINT ( 'NONE',  ( 46.10157429594899270, 157.7344580088725934, 29.95742577749336988 ) ) ;
#21130=CARTESIAN_POINT ( 'NONE',  ( 46.10157429594899270, 153.8344580088725877, 38.46393386101375711 ) ) ;
#21131=CARTESIAN_POINT ( 'NONE',  ( 47.43856463449117911, 74.02977050742730114, 32.77220824515697473 ) ) ;
#21134=CARTESIAN_POINT ( 'NONE',  ( 38.58424406990784661, 153.2297705074273608, 32.77220824515698183 ) ) ;
#21136=CARTESIAN_POINT ( 'NONE',  ( 48.01140435219951996, 122.0604996726487315, 35.83527830041810347 ) ) ;
#21137=CARTESIAN_POINT ( 'NONE',  ( 47.43856463449117200, 79.46518717409399812, 35.64915139335016647 ) ) ;
#21144=CARTESIAN_POINT ( 'NONE',  ( 47.43856463449118621, 130.8797705074273381, 34.21067981925357060 ) ) ;
#21146=CARTESIAN_POINT ( 'NONE',  ( 47.43856463449117911, 124.4651871740940123, 35.64915139335015937 ) ) ;
#21148=CARTESIAN_POINT ( 'NONE',  ( 43.01140435219951286, 137.9604996726487514, 29.21067981925356705 ) ) ;
#21153=CARTESIAN_POINT ( 'NONE',  ( 46.10157429594899270, 83.66049967264873999, 29.95742577749336988 ) ) ;
#21154=CARTESIAN_POINT ( 'NONE',  ( 38.58424406990784661, 108.2651871740939953, 35.64915139335016647 ) ) ;
#21157=ORIENTED_EDGE ( 'NONE', *, *, #18788, .T. ) ;
#21158=CARTESIAN_POINT ( 'NONE',  ( 47.05648932407426344, 90.98445800887257917, 37.14960608071593384 ) ) ;
#21160=CARTESIAN_POINT ( 'NONE',  ( 46.10157429594899270, 151.7604996726487059, 38.46393386101376421 ) ) ;
#21161=CARTESIAN_POINT ( 'NONE',  ( 45.74753988029933538, 106.1651871740940152, 37.97664729208901946 ) ) ;
#21163=CARTESIAN_POINT ( 'NONE',  ( 41.46631938032478359, 63.11049967264874283, 29.45539723777780239 ) ) ;
#21165=CARTESIAN_POINT ( 'NONE',  ( 43.01140435219951996, 10.71049967264875491, 34.21067981925357060 ) ) ;
#21166=CARTESIAN_POINT ( 'NONE',  ( 48.01140435219951996, 79.28445800887259054, 34.21067981925357060 ) ) ;
#21168=CARTESIAN_POINT ( 'NONE',  ( 43.01140435219951286, 71.36518717409397539, 29.55568802177586463 ) ) ;
#21170=CARTESIAN_POINT ( 'NONE',  ( 39.92123440845005433, 114.2604996726487343, 29.95742577749336988 ) ) ;
#21177=CARTESIAN_POINT ( 'NONE',  ( 41.64333658814960870, 137.5151871740939953, 30.00020018409699318 ) ) ;
#21178=CARTESIAN_POINT ( 'NONE',  ( 41.64333658814960870, 156.7151871740939839, 38.42115945441014446 ) ) ;
#21179=( BOUNDED_CURVE ( )  B_SPLINE_CURVE ( 2, ( #6129, #19697, #16271, #3162, #1288, #14728, #12859, #19580, #18140, #6242, #14615, #21353, #21464 ),
 .UNSPECIFIED., .F., .F. ) 
 B_SPLINE_CURVE_WITH_KNOTS ( ( 3, 2, 2, 2, 2, 2, 3 ),
 ( 0.9044117647058823595, 0.9058823529411764719, 0.9088235294117646967, 0.9117647058823529216, 0.9147058823529411464, 0.9176470588235293713, 0.9191176470588234837 ),
 .UNSPECIFIED. ) 
 CURVE ( )  GEOMETRIC_REPRESENTATION_ITEM ( )  RATIONAL_B_SPLINE_CURVE ( ( 0.9755282581475768211, 0.9755282581475768211, 1.000000000000000000, 0.9510565162951535312, 1.000000000000000000, 0.9510565162951535312, 1.000000000000000000, 0.9510565162951535312, 1.000000000000000000, 0.9510565162951535312, 1.000000000000000000, 0.9755282581475768211, 0.9755282581475768211 ) ) 
 REPRESENTATION_ITEM ( '' )  );
#21180=CARTESIAN_POINT ( 'NONE',  ( 45.74753988029934249, 92.32977050742731251, 30.44471234641812174 ) ) ;
#21183=AXIS2_PLACEMENT_3D ( 'NONE', #8194, #9630, #13254 ) ;
#21186=ORIENTED_EDGE ( 'NONE', *, *, #15515, .F. ) ;
#21190=CARTESIAN_POINT ( 'NONE',  ( 44.37947211624943833, 73.27977050742731535, 38.42115945441014446 ) ) ;
#21191=CARTESIAN_POINT ( 'NONE',  ( 45.74753988029933538, 131.0651871740940067, 30.44471234641811819 ) ) ;
#21192=CARTESIAN_POINT ( 'NONE',  ( 39.92123440845004723, 88.16049967264873999, 38.46393386101376421 ) ) ;
#21194=EDGE_CURVE ( 'NONE', #470, #14339, #21371, .T. ) ;
#21198=VECTOR ( 'NONE', #7009, 1000.000000000000000 ) ;
#21202=CARTESIAN_POINT ( 'NONE',  ( 38.58424406990784661, 72.52977050742731535, 35.64915139335016647 ) ) ;
#21210=CARTESIAN_POINT ( 'NONE',  ( 38.96631938032478359, 104.4844580088725650, 31.27175355779120025 ) ) ;
#21211=CARTESIAN_POINT ( 'NONE',  ( 44.37947211624943833, 124.2797705074273154, 38.42115945441014446 ) ) ;
#21212=EDGE_CURVE ( 'NONE', #17591, #9530, #1806, .T. ) ;
#21214=CARTESIAN_POINT ( 'NONE',  ( 43.01140435219954838, 131.0344580088725479, 29.21067981925356705 ) ) ;
#21216=CARTESIAN_POINT ( 'NONE',  ( 47.43856463449117200, 130.7297705074273040, 35.64915139335016647 ) ) ;
#21218=CARTESIAN_POINT ( 'NONE',  ( 41.64333658814960870, 89.77977050742731535, 30.00020018409699318 ) ) ;
#21219=CARTESIAN_POINT ( 'NONE',  ( 39.92123440845004723, 59.33445800887256638, 29.95742577749337343 ) ) ;
#21220=EDGE_CURVE ( 'NONE', #8083, #14631, #8462, .T. ) ;
#21223=CARTESIAN_POINT ( 'NONE',  ( 43.01140435219951286, 95.96049967264873715, 29.21067981925356705 ) ) ;
#21225=CARTESIAN_POINT ( 'NONE',  ( 46.10157429594899270, 133.7344580088725650, 29.95742577749336988 ) ) ;
#21230=CARTESIAN_POINT ( 'NONE',  ( 44.55648932407425633, 123.6844580088725820, 38.96596240072933170 ) ) ;
#21231=CARTESIAN_POINT ( 'NONE',  ( 47.43856463449117200, 101.0297705074273011, 32.77220824515698183 ) ) ;
#21234=CARTESIAN_POINT ( 'NONE',  ( 44.37947211624943833, 100.0151871740939953, 38.42115945441014446 ) ) ;
#21239=CARTESIAN_POINT ( 'NONE',  ( 43.01140435219951286, 145.1297705074273097, 38.86567161673127657 ) ) ;
#21242=CARTESIAN_POINT ( 'NONE',  ( 38.58424406990786082, 66.37977050742730967, 34.21067981925357060 ) ) ;
#21243=ORIENTED_EDGE ( 'NONE', *, *, #12549, .F. ) ;
#21245=CARTESIAN_POINT ( 'NONE',  ( 38.58424406990786082, 153.3797705074273097, 34.21067981925357060 ) ) ;
#21248=CARTESIAN_POINT ( 'NONE',  ( 39.92123440845004723, 120.2604996726487485, 29.95742577749337343 ) ) ;
#21249=CARTESIAN_POINT ( 'NONE',  ( 44.37947211624943833, 70.01518717409399528, 38.42115945441014446 ) ) ;
#21256=CARTESIAN_POINT ( 'NONE',  ( 38.58424406990784661, 135.2297705074273324, 32.77220824515698183 ) ) ;
#21258=CARTESIAN_POINT ( 'NONE',  ( 47.43856463449117911, 130.4651871740939839, 35.64915139335015937 ) ) ;
#21265=CARTESIAN_POINT ( 'NONE',  ( 41.64333658814960870, 108.7151871740940123, 38.42115945441014446 ) ) ;
#21266=ORIENTED_EDGE ( 'NONE', *, *, #4921, .F. ) ;
#21269=CARTESIAN_POINT ( 'NONE',  ( 46.10157429594899270, 81.83445800887258770, 38.46393386101376421 ) ) ;
#21272=CARTESIAN_POINT ( 'NONE',  ( 39.92123440845004723, 150.2604996726487911, 29.95742577749337343 ) ) ;
#21273=CARTESIAN_POINT ( 'NONE',  ( 40.27526882409969033, 108.5651871740939924, 37.97664729208901946 ) ) ;
#21275=CARTESIAN_POINT ( 'NONE',  ( 48.01140435219951996, 65.36049967264874283, 32.58608133808903773 ) ) ;
#21278=CARTESIAN_POINT ( 'NONE',  ( 47.05648932407426344, 117.9844580088725792, 37.14960608071593384 ) ) ;
#21279=CARTESIAN_POINT ( 'NONE',  ( 48.01140435219951996, 79.13445800887257064, 35.83527830041809636 ) ) ;
#21281=CARTESIAN_POINT ( 'NONE',  ( 40.27526882409969033, 62.66518717409400097, 30.44471234641811819 ) ) ;
#21284=EDGE_CURVE ( 'NONE', #11408, #17105, #4050, .T. ) ;
#21285=CARTESIAN_POINT ( 'NONE',  ( 39.92123440845005433, 115.1604996726487400, 38.46393386101375711 ) ) ;
#21290=CARTESIAN_POINT ( 'NONE',  ( 43.01140435219951286, 65.36518717409398960, 29.55568802177586107 ) ) ;
#21293=( NAMED_UNIT ( * ) SI_UNIT ( $, .STERADIAN. ) SOLID_ANGLE_UNIT ( ) );
#21294=CARTESIAN_POINT ( 'NONE',  ( 47.43856463449117200, 136.4651871740939839, 35.64915139335016647 ) ) ;
#21296=ORIENTED_EDGE ( 'NONE', *, *, #13990, .T. ) ;
#21298=CARTESIAN_POINT ( 'NONE',  ( 46.10157429594899270, 115.7344580088725650, 29.95742577749337343 ) ) ;
#21299=CARTESIAN_POINT ( 'NONE',  ( 45.51148226160370314, 59.71123016864974176, 29.88059778228138086 ) ) ;
#21300=CARTESIAN_POINT ( 'NONE',  ( 40.27526882409969033, 78.82977050742731251, 37.97664729208901946 ) ) ;
#21301=CARTESIAN_POINT ( 'NONE',  ( 47.43856463449117200, 136.7651871740939953, 32.77220824515698183 ) ) ;
#21302=CARTESIAN_POINT ( 'NONE',  ( 46.10157429594899270, 92.66049967264873999, 29.95742577749337343 ) ) ;
#21308=CARTESIAN_POINT ( 'NONE',  ( 47.05648932407426344, 62.51049967264874141, 31.27175355779120025 ) ) ;
#21309=ORIENTED_EDGE ( 'NONE', *, *, #12044, .F. ) ;
#21310=CARTESIAN_POINT ( 'NONE',  ( 47.43856463449117200, 70.72977050742730398, 35.64915139335016647 ) ) ;
#21317=CARTESIAN_POINT ( 'NONE',  ( 46.10157429594899270, 123.8344580088725735, 38.46393386101375711 ) ) ;
#21318=CARTESIAN_POINT ( 'NONE',  ( 40.27526882409969744, 119.9297705074272926, 30.44471234641812174 ) ) ;
#21321=CARTESIAN_POINT ( 'NONE',  ( 43.01140435219951996, 2.710499672648754466, 34.21067981925357060 ) ) ;
#21324=CARTESIAN_POINT ( 'NONE',  ( 41.64333658814960870, 125.7797705074273296, 30.00020018409699318 ) ) ;
#21326=CARTESIAN_POINT ( 'NONE',  ( 47.05648932407426344, 66.98445800887257917, 37.14960608071593384 ) ) ;
#21329=CARTESIAN_POINT ( 'NONE',  ( 42.21948215057684450, 102.4575765865523209, 39.21067981925355639 ) ) ;
#21334=CARTESIAN_POINT ( 'NONE',  ( 44.55648932407425633, 127.8844580088725706, 29.45539723777780239 ) ) ;
#21335=CARTESIAN_POINT ( 'NONE',  ( 43.01140435219951286, 100.1297705074273239, 38.86567161673127657 ) ) ;
#21338=CARTESIAN_POINT ( 'NONE',  ( 43.01140435219951286, 95.36518717409400381, 29.55568802177586107 ) ) ;
#21339=CARTESIAN_POINT ( 'NONE',  ( 42.21948215057684450, 85.38361825032846752, 39.21067981925355639 ) ) ;
#21340=ORIENTED_EDGE ( 'NONE', *, *, #7813, .F. ) ;
#21341=CYLINDRICAL_SURFACE ( 'NONE', #2038, 4.999999999999997335 ) ;
#21344=CARTESIAN_POINT ( 'NONE',  ( 43.01140435219951286, 67.12977050742730967, 38.86567161673127657 ) ) ;
#21345=ORIENTED_EDGE ( 'NONE', *, *, #712, .F. ) ;
#21346=EDGE_LOOP ( 'NONE', ( #15330, #18106, #10191, #65 ) ) ;
#21347=CARTESIAN_POINT ( 'NONE',  ( 39.42975644700377558, 156.6797705074273210, 36.81289934271958941 ) ) ;
#21351=CARTESIAN_POINT ( 'NONE',  ( 41.46631938032478359, 108.1104996726487428, 29.45539723777780239 ) ) ;
#21352=CARTESIAN_POINT ( 'NONE',  ( 41.64333658814960870, 65.51518717409400949, 30.00020018409699318 ) ) ;
#21353=CARTESIAN_POINT ( 'NONE',  ( 42.21948215057684450, 65.11133943119283174, 29.21067981925356705 ) ) ;
#21357=CARTESIAN_POINT ( 'NONE',  ( 44.55648932407425633, 153.6844580088725820, 38.96596240072933170 ) ) ;
#21358=CARTESIAN_POINT ( 'NONE',  ( 43.01140435219951286, 130.1297705074273381, 38.86567161673127657 ) ) ;
#21361=CARTESIAN_POINT ( 'NONE',  ( 47.43856463449117911, 127.4651871740939839, 35.64915139335015937 ) ) ;
#21362=CARTESIAN_POINT ( 'NONE',  ( 43.01140435219951286, 92.03445800887257633, 29.21067981925356705 ) ) ;
#21364=CARTESIAN_POINT ( 'NONE',  ( 43.01140435219951286, 65.96049967264873715, 29.21067981925356705 ) ) ;
#21366=CARTESIAN_POINT ( 'NONE',  ( 42.21948215057684450, 135.0373810949689926, 29.21067981925356705 ) ) ;
#21371=( BOUNDED_CURVE ( )  B_SPLINE_CURVE ( 2, ( #11968, #10107, #18256, #18590, #1939, #16814, #20355, #3601, #6808, #290, #11526, #6911, #5036 ),
 .UNSPECIFIED., .F., .F. ) 
 B_SPLINE_CURVE_WITH_KNOTS ( ( 3, 2, 2, 2, 2, 2, 3 ),
 ( 0.1691176470588235115, 0.1705882352941176516, 0.1735294117647058765, 0.1764705882352941291, 0.1794117647058823539, 0.1823529411764705788, 0.1838235294117647189 ),
 .UNSPECIFIED. ) 
 CURVE ( )  GEOMETRIC_REPRESENTATION_ITEM ( )  RATIONAL_B_SPLINE_CURVE ( ( 0.9755282581475765991, 0.9755282581475764880, 1.000000000000000000, 0.9510565162951535312, 1.000000000000000000, 0.9510565162951535312, 1.000000000000000000, 0.9510565162951535312, 1.000000000000000000, 0.9510565162951535312, 1.000000000000000000, 0.9755282581475765991, 0.9755282581475768211 ) ) 
 REPRESENTATION_ITEM ( '' )  );
#21373=CARTESIAN_POINT ( 'NONE',  ( 43.80332655382220253, 85.53738109496900677, 39.21067981925355639 ) ) ;
#21375=CARTESIAN_POINT ( 'NONE',  ( 38.01140435219952707, 83.78445800887257633, 34.21067981925357060 ) ) ;
#21376=CARTESIAN_POINT ( 'NONE',  ( 44.55648932407425633, 102.6844580088725820, 38.96596240072933170 ) ) ;
#21378=CARTESIAN_POINT ( 'NONE',  ( 41.46631938032478359, 138.1104996726487286, 29.45539723777780239 ) ) ;
#21379=CARTESIAN_POINT ( 'NONE',  ( 44.37947211624943833, 94.01518717409400949, 38.42115945441014446 ) ) ;
#21383=CARTESIAN_POINT ( 'NONE',  ( 38.96631938032478359, 60.41049967264873288, 31.27175355779120025 ) ) ;
#21385=CARTESIAN_POINT ( 'NONE',  ( 43.80332655382222384, 70.95757658655230671, 29.21067981925357770 ) ) ;
#21388=CARTESIAN_POINT ( 'NONE',  ( 46.10157429594899270, 79.76049967264873430, 38.46393386101375711 ) ) ;
#21389=CARTESIAN_POINT ( 'NONE',  ( 41.64333658814960870, 156.9797705074273040, 38.42115945441014446 ) ) ;
#21391=VECTOR ( 'NONE', #2431, 1000.000000000000000 ) ;
#21392=CARTESIAN_POINT ( 'NONE',  ( 43.01140435219951996, 10.71049967264875491, 34.21067981925357060 ) ) ;
#21396=CARTESIAN_POINT ( 'NONE',  ( 46.59305225739526435, 73.31518717409400665, 36.81289934271958941 ) ) ;
#21399=AXIS2_PLACEMENT_3D ( 'NONE', #12155, #18886, #10085 ) ;
#21400=CARTESIAN_POINT ( 'NONE',  ( 46.10157429594899270, 111.8344580088725877, 38.46393386101375711 ) ) ;
#21401=CARTESIAN_POINT ( 'NONE',  ( 44.37947211624943833, 131.2151871740940123, 30.00020018409699318 ) ) ;
#21402=EDGE_CURVE ( 'NONE', #17102, #4204, #3606, .T. ) ;
#21406=ORIENTED_EDGE ( 'NONE', *, *, #8181, .T. ) ;
#21408=CARTESIAN_POINT ( 'NONE',  ( 44.55648932407425633, 116.8104996726487599, 29.45539723777780239 ) ) ;
#21409=CARTESIAN_POINT ( 'NONE',  ( 38.58424406990784661, 78.22977050742731819, 32.77220824515698183 ) ) ;
#21410=CARTESIAN_POINT ( 'NONE',  ( 47.43856463449117200, 124.4651871740939839, 35.64915139335016647 ) ) ;
#21412=CARTESIAN_POINT ( 'NONE',  ( 47.05648932407426344, 95.51049967264873430, 31.27175355779120025 ) ) ;
#21417=CARTESIAN_POINT ( 'NONE',  ( 46.59305225739526435, 91.31518717409399244, 36.81289934271958941 ) ) ;
#21419=CARTESIAN_POINT ( 'NONE',  ( 43.80332655382222384, 71.88361825032846752, 29.21067981925357770 ) ) ;
#21420=CARTESIAN_POINT ( 'NONE',  ( 43.01140435219951996, 10.71049967264875491, 39.21067981925356349 ) ) ;
#21421=ORIENTED_EDGE ( 'NONE', *, *, #12984, .F. ) ;
#21422=CARTESIAN_POINT ( 'NONE',  ( 44.37947211624943833, 76.27977050742731535, 38.42115945441014446 ) ) ;
#21429=CARTESIAN_POINT ( 'NONE',  ( 45.74753988029934249, 125.3297705074273409, 30.44471234641812174 ) ) ;
#21431=DIRECTION ( 'NONE',  ( 0.000000000000000000, -1.000000000000000000, 0.000000000000000000 ) ) ;
#21433=CARTESIAN_POINT ( 'NONE',  ( 46.59305225739526435, 119.1797705074273068, 31.60846029578754468 ) ) ;
#21435=CARTESIAN_POINT ( 'NONE',  ( 47.05648932407426344, 67.58445800887258770, 31.27175355779120025 ) ) ;
#21437=CARTESIAN_POINT ( 'NONE',  ( 41.46631938032478359, 84.38445800887258486, 38.96596240072933170 ) ) ;
#21440=( BOUNDED_CURVE ( )  B_SPLINE_CURVE ( 2, ( #7468, #2493, #7579, #9452, #13375, #21760, #20112, #8311, #36, #21130, #5003, #6777, #7694 ),
 .UNSPECIFIED., .F., .F. ) 
 B_SPLINE_CURVE_WITH_KNOTS ( ( 3, 2, 2, 2, 2, 2, 3 ),
 ( 0.03676470588235293546, 0.03823529411764706176, 0.04117647058823529355, 0.04411764705882353227, 0.04705882352941176405, 0.05000000000000000278, 0.05147058823529412214 ),
 .UNSPECIFIED. ) 
 CURVE ( )  GEOMETRIC_REPRESENTATION_ITEM ( )  RATIONAL_B_SPLINE_CURVE ( ( 0.9755282581475767101, 0.9755282581475765991, 1.000000000000000000, 0.9510565162951535312, 1.000000000000000000, 0.9510565162951535312, 1.000000000000000000, 0.9510565162951535312, 1.000000000000000000, 0.9510565162951535312, 1.000000000000000000, 0.9755282581475767101, 0.9755282581475768211 ) ) 
 REPRESENTATION_ITEM ( '' )  );
#21441=CARTESIAN_POINT ( 'NONE',  ( 43.01140435219951996, 157.4604996726487514, 39.21067981925355639 ) ) ;
#21445=CARTESIAN_POINT ( 'NONE',  ( 38.96631938032478359, 119.4844580088725792, 31.27175355779120025 ) ) ;
#21446=CARTESIAN_POINT ( 'NONE',  ( 40.27526882409969033, 104.9297705074273210, 30.44471234641811819 ) ) ;
#21449=CARTESIAN_POINT ( 'NONE',  ( 41.64333658814960870, 92.51518717409399528, 30.00020018409699318 ) ) ;
#21451=VERTEX_POINT ( 'NONE', #12073 ) ;
#21456=CARTESIAN_POINT ( 'NONE',  ( 45.74753988029934249, 70.42977050742730682, 37.97664729208901235 ) ) ;
#21457=EDGE_LOOP ( 'NONE', ( #20567, #9393, #6571, #11571 ) ) ;
#21458=ORIENTED_EDGE ( 'NONE', *, *, #16085, .F. ) ;
#21459=CARTESIAN_POINT ( 'NONE',  ( 39.42975644700377558, 156.0797705074273267, 31.60846029578754468 ) ) ;
#21462=CARTESIAN_POINT ( 'NONE',  ( 48.01140435219951996, 107.0604996726487599, 35.83527830041810347 ) ) ;
#21463=CARTESIAN_POINT ( 'NONE',  ( 43.01140435219951286, 65.36518717409400381, 29.55568802177586463 ) ) ;
#21464=CARTESIAN_POINT ( 'NONE',  ( 43.01140435219951286, 65.03445800887257633, 29.21067981925356705 ) ) ;
#21468=DIRECTION ( 'NONE',  ( 0.000000000000000000, 0.000000000000000000, 1.000000000000000000 ) ) ;
#21470=CARTESIAN_POINT ( 'NONE',  ( 46.10157429594899270, 148.7344580088725934, 29.95742577749337343 ) ) ;
#21471=CARTESIAN_POINT ( 'NONE',  ( 44.37947211624943833, 133.2797705074273154, 38.42115945441014446 ) ) ;
#21473=CARTESIAN_POINT ( 'NONE',  ( 40.27526882409969744, 120.5651871740940209, 37.97664729208901235 ) ) ;
#21475=DIRECTION ( 'NONE',  ( 0.000000000000000000, 0.000000000000000000, 1.000000000000000000 ) ) ;
#21478=CARTESIAN_POINT ( 'NONE',  ( 48.01140435219951996, 140.0604996726487457, 35.83527830041809636 ) ) ;
#21479=LINE ( 'NONE', #16174, #9942 ) ;
#21482=CARTESIAN_POINT ( 'NONE',  ( 43.01140435219951996, 10.71049967264875491, 29.21067981925357060 ) ) ;
#21487=CARTESIAN_POINT ( 'NONE',  ( 38.96631938032478359, 81.08445800887258770, 37.14960608071593384 ) ) ;
#21490=CARTESIAN_POINT ( 'NONE',  ( 39.92123440845004723, 139.1604996726487400, 38.46393386101376421 ) ) ;
#21491=CARTESIAN_POINT ( 'NONE',  ( 44.37947211624943833, 98.21518717409399812, 30.00020018409699318 ) ) ;
#21496=DIRECTION ( 'NONE',  ( 0.000000000000000000, 1.000000000000000000, 0.000000000000000000 ) ) ;
#21500=CARTESIAN_POINT ( 'NONE',  ( 48.01140435219951996, 115.2844580088725763, 34.21067981925357060 ) ) ;
#21501=CARTESIAN_POINT ( 'NONE',  ( 47.43856463449117200, 61.76518717409399528, 32.77220824515698183 ) ) ;
#21504=CARTESIAN_POINT ( 'NONE',  ( 40.27526882409969744, 153.5651871740940067, 37.97664729208901235 ) ) ;
#21509=CARTESIAN_POINT ( 'NONE',  ( 44.37947211624943833, 71.21518717409399812, 30.00020018409699318 ) ) ;
#21513=CARTESIAN_POINT ( 'NONE',  ( 47.05648932407426344, 112.5844580088725877, 31.27175355779120025 ) ) ;
#21514=CARTESIAN_POINT ( 'NONE',  ( 45.74753988029933538, 134.0651871740939498, 30.44471234641811819 ) ) ;
#21520=EDGE_CURVE ( 'NONE', #19975, #4439, #19822, .T. ) ;
#21521=CARTESIAN_POINT ( 'NONE',  ( 43.01140435219951996, 10.71049967264875491, 39.21067981925356349 ) ) ;
#21522=CARTESIAN_POINT ( 'NONE',  ( 41.64333658814960870, 71.77977050742731535, 30.00020018409699318 ) ) ;
#21523=CARTESIAN_POINT ( 'NONE',  ( 46.59305225739526435, 124.9151871740940010, 31.60846029578754468 ) ) ;
#21525=CARTESIAN_POINT ( 'NONE',  ( 38.96631938032478359, 82.01049967264874851, 37.14960608071593384 ) ) ;
#21528=CARTESIAN_POINT ( 'NONE',  ( 47.43856463449117200, 91.76518717409400949, 32.77220824515698183 ) ) ;
#21530=CARTESIAN_POINT ( 'NONE',  ( 48.01140435219951996, 151.1344580088725991, 35.83527830041809636 ) ) ;
#21531=CARTESIAN_POINT ( 'NONE',  ( 44.55648932407425633, 141.6844580088725820, 38.96596240072933170 ) ) ;
#21533=CARTESIAN_POINT ( 'NONE',  ( 46.59305225739526435, 65.17977050742732104, 31.60846029578754468 ) ) ;
#21537=ORIENTED_EDGE ( 'NONE', *, *, #21520, .F. ) ;
#21539=CARTESIAN_POINT ( 'NONE',  ( 38.58424406990785371, 126.5297705074272869, 35.64915139335015937 ) ) ;
#21541=CARTESIAN_POINT ( 'NONE',  ( 43.01140435219951286, 129.5344580088725763, 39.21067981925356349 ) ) ;
#21543=CARTESIAN_POINT ( 'NONE',  ( 46.59305225739526435, 118.5797705074273267, 36.81289934271958941 ) ) ;
#21545=CARTESIAN_POINT ( 'NONE',  ( 46.59305225739526435, 151.3151871740940067, 36.81289934271958941 ) ) ;
#21546=EDGE_CURVE ( 'NONE', #4098, #10985, #12286, .T. ) ;
#21549=CARTESIAN_POINT ( 'NONE',  ( 38.96631938032478359, 84.08445800887258770, 37.14960608071593384 ) ) ;
#21550=CARTESIAN_POINT ( 'NONE',  ( 42.21948215057684450, 96.03738109496902098, 29.21067981925356705 ) ) ;
#21553=CARTESIAN_POINT ( 'NONE',  ( 44.55648932407425633, 131.8104996726487457, 29.45539723777780239 ) ) ;
#21557=CARTESIAN_POINT ( 'NONE',  ( 38.01140435219951996, 125.9344580088725962, 35.83527830041810347 ) ) ;
#21558=CARTESIAN_POINT ( 'NONE',  ( 43.01140435219951286, 107.6297705074272955, 29.55568802177586463 ) ) ;
#21561=CARTESIAN_POINT ( 'NONE',  ( 38.58424406990785371, 87.26518717409399528, 35.64915139335015937 ) ) ;
#21562=CARTESIAN_POINT ( 'NONE',  ( 43.01140435219951996, 10.71049967264875491, 39.21067981925356349 ) ) ;
#21563=ORIENTED_EDGE ( 'NONE', *, *, #10473, .F. ) ;
#21565=CARTESIAN_POINT ( 'NONE',  ( 38.58424406990785371, 144.2297705074273324, 32.77220824515697473 ) ) ;
#21568=CARTESIAN_POINT ( 'NONE',  ( 45.74753988029934249, 62.32977050742730540, 30.44471234641812174 ) ) ;
#21571=CARTESIAN_POINT ( 'NONE',  ( 47.43856463449117200, 149.0297705074273438, 32.77220824515698183 ) ) ;
#21573=CARTESIAN_POINT ( 'NONE',  ( 38.96631938032478359, 109.0104996726487485, 37.14960608071593384 ) ) ;
#21574=CARTESIAN_POINT ( 'NONE',  ( 38.58424406990784661, 72.26518717409398107, 35.64915139335016647 ) ) ;
#21580=CARTESIAN_POINT ( 'NONE',  ( 41.46631938032478359, 112.3104996726487457, 38.96596240072933170 ) ) ;
#21581=CARTESIAN_POINT ( 'NONE',  ( 44.55648932407425633, 147.6844580088725820, 38.96596240072933170 ) ) ;
#21583=CARTESIAN_POINT ( 'NONE',  ( 45.74753988029933538, 134.3297705074273267, 30.44471234641811819 ) ) ;
#21585=CARTESIAN_POINT ( 'NONE',  ( 39.42975644700377558, 116.8151871740940067, 31.60846029578754468 ) ) ;
#21587=DIRECTION ( 'NONE',  ( 0.000000000000000000, 1.000000000000000000, 0.000000000000000000 ) ) ;
#21593=CARTESIAN_POINT ( 'NONE',  ( 46.59305225739526435, 98.17977050742732104, 31.60846029578754468 ) ) ;
#21594=VERTEX_POINT ( 'NONE', #15596 ) ;
#21597=ORIENTED_EDGE ( 'NONE', *, *, #7368, .F. ) ;
#21599=CARTESIAN_POINT ( 'NONE',  ( 46.10157429594899270, 78.83445800887255928, 38.46393386101376421 ) ) ;
#21600=CARTESIAN_POINT ( 'NONE',  ( 43.01140435219951286, 102.5344580088725763, 39.21067981925356349 ) ) ;
#21601=CARTESIAN_POINT ( 'NONE',  ( 38.96631938032478359, 144.4104996726487400, 31.27175355779120025 ) ) ;
#21602=CARTESIAN_POINT ( 'NONE',  ( 39.42975644700377558, 92.81518717409399244, 31.60846029578754468 ) ) ;
#21612=CARTESIAN_POINT ( 'NONE',  ( 43.01140435219951286, 63.86518717409398960, 38.86567161673127657 ) ) ;
#21615=CARTESIAN_POINT ( 'NONE',  ( 38.58424406990785371, 149.9651871740939555, 32.77220824515697473 ) ) ;
#21619=CARTESIAN_POINT ( 'NONE',  ( 45.74753988029934249, 71.06518717409400665, 30.44471234641812174 ) ) ;
#21622=( LENGTH_UNIT ( ) NAMED_UNIT ( * ) SI_UNIT ( .MILLI., .METRE. ) );
#21623=CARTESIAN_POINT ( 'NONE',  ( 47.43856463449118621, 127.6151871740940038, 34.21067981925357060 ) ) ;
#21630=CARTESIAN_POINT ( 'NONE',  ( 44.55648932407425633, 106.8844580088725849, 29.45539723777780239 ) ) ;
#21632=CARTESIAN_POINT ( 'NONE',  ( 45.74753988029933538, 68.32977050742731251, 30.44471234641811819 ) ) ;
#21633=CARTESIAN_POINT ( 'NONE',  ( 47.43856463449117200, 121.7651871740940237, 32.77220824515698183 ) ) ;
#21636=CARTESIAN_POINT ( 'NONE',  ( 48.01140435219951996, 86.21049967264873715, 34.21067981925357060 ) ) ;
#21640=( BOUNDED_CURVE ( )  B_SPLINE_CURVE ( 2, ( #994, #4396, #14324, #19397, #11128, #4293, #10034, #3422, #16630, #11783, #18062, #16409, #5281 ),
 .UNSPECIFIED., .F., .F. ) 
 B_SPLINE_CURVE_WITH_KNOTS ( ( 3, 2, 2, 2, 2, 2, 3 ),
 ( 0.1250000000000000000, 0.1264705882352941124, 0.1294117647058823650, 0.1323529411764705899, 0.1352941176470588147, 0.1382352941176470673, 0.1397058823529411797 ),
 .UNSPECIFIED. ) 
 CURVE ( )  GEOMETRIC_REPRESENTATION_ITEM ( )  RATIONAL_B_SPLINE_CURVE ( ( 0.9755282581475768211, 0.9755282581475768211, 1.000000000000000000, 0.9510565162951535312, 1.000000000000000000, 0.9510565162951535312, 1.000000000000000000, 0.9510565162951535312, 1.000000000000000000, 0.9510565162951535312, 1.000000000000000000, 0.9755282581475768211, 0.9755282581475768211 ) ) 
 REPRESENTATION_ITEM ( '' )  );
#21641=CARTESIAN_POINT ( 'NONE',  ( 43.01140435219951286, 86.36518717409400381, 29.55568802177586463 ) ) ;
#21643=CARTESIAN_POINT ( 'NONE',  ( 46.10157429594899270, 62.66049967264872578, 29.95742577749336988 ) ) ;
#21645=CARTESIAN_POINT ( 'NONE',  ( 45.74753988029933538, 70.42977050742730682, 37.97664729208901946 ) ) ;
#21650=CARTESIAN_POINT ( 'NONE',  ( 44.37947211624943833, 151.0151871740940237, 38.42115945441014446 ) ) ;
#21653=CARTESIAN_POINT ( 'NONE',  ( 43.01140435219951286, 113.6297705074273097, 29.55568802177586107 ) ) ;
#21655=ORIENTED_EDGE ( 'NONE', *, *, #13389, .F. ) ;
#21658=ORIENTED_EDGE ( 'NONE', *, *, #15302, .F. ) ;
#21659=CARTESIAN_POINT ( 'NONE',  ( 45.74753988029933538, 121.4297705074273068, 37.97664729208901946 ) ) ;
#21660=CARTESIAN_POINT ( 'NONE',  ( 39.92123440845005433, 73.16049967264872578, 38.46393386101375711 ) ) ;
#21661=CARTESIAN_POINT ( 'NONE',  ( 47.43856463449117200, 154.7651871740940237, 32.77220824515698183 ) ) ;
#21668=CARTESIAN_POINT ( 'NONE',  ( 45.22505347682923116, 59.38050100342834270, 30.37668637662395099 ) ) ;
#21670=CARTESIAN_POINT ( 'NONE',  ( 38.96631938032478359, 123.0844580088725735, 37.14960608071593384 ) ) ;
#21671=CARTESIAN_POINT ( 'NONE',  ( 46.59305225739526435, 97.57977050742731251, 36.81289934271958941 ) ) ;
#21676=ORIENTED_EDGE ( 'NONE', *, *, #13923, .F. ) ;
#21679=CARTESIAN_POINT ( 'NONE',  ( 45.74753988029934249, 140.3297705074273267, 30.44471234641812174 ) ) ;
#21682=CARTESIAN_POINT ( 'NONE',  ( 38.58424406990785371, 69.52977050742730114, 35.64915139335015937 ) ) ;
#21684=CARTESIAN_POINT ( 'NONE',  ( 44.37947211624943833, 145.2797705074273154, 38.42115945441014446 ) ) ;
#21685=CARTESIAN_POINT ( 'NONE',  ( 43.01140435219951286, 152.9604996726487798, 29.21067981925356705 ) ) ;
#21686=CARTESIAN_POINT ( 'NONE',  ( 44.55648932407425633, 107.8104996726487457, 29.45539723777780239 ) ) ;
#21687=CARTESIAN_POINT ( 'NONE',  ( 47.43856463449117200, 70.76518717409399528, 32.77220824515698183 ) ) ;
#21688=CARTESIAN_POINT ( 'NONE',  ( 38.96631938032478359, 96.08445800887258770, 37.14960608071593384 ) ) ;
#21690=CARTESIAN_POINT ( 'NONE',  ( 38.96631938032478359, 156.0844580088725877, 37.14960608071593384 ) ) ;
#21693=CARTESIAN_POINT ( 'NONE',  ( 48.01140435219951996, 154.2844580088725763, 34.21067981925357060 ) ) ;
#21694=CARTESIAN_POINT ( 'NONE',  ( 46.59305225739526435, 125.1797705074273210, 31.60846029578754468 ) ) ;
#21696=CARTESIAN_POINT ( 'NONE',  ( 43.01140435219951286, 113.3651871740939754, 29.55568802177586107 ) ) ;
#21698=CARTESIAN_POINT ( 'NONE',  ( 47.05648932407426344, 65.51049967264874851, 31.27175355779120025 ) ) ;
#21701=PRODUCT_DEFINITION_SHAPE ( 'NONE', 'NONE',  #8538 ) ;
#21702=CARTESIAN_POINT ( 'NONE',  ( 45.74753988029934249, 97.42977050742730682, 37.97664729208901235 ) ) ;
#21706=CARTESIAN_POINT ( 'NONE',  ( 39.92123440845004723, 84.23445800887256496, 38.46393386101376421 ) ) ;
#21707=CARTESIAN_POINT ( 'NONE',  ( 42.21948215057684450, 87.45757658655232092, 39.21067981925355639 ) ) ;
#21709=CARTESIAN_POINT ( 'NONE',  ( 43.01140435219951286, 134.9604996726487514, 28.95336869806222779 ) ) ;
#21710=CARTESIAN_POINT ( 'NONE',  ( 38.58424406990786082, 96.11518717409400381, 34.21067981925357060 ) ) ;
#21718=EDGE_CURVE ( 'NONE', #3266, #6431, #16009, .T. ) ;
#21719=CARTESIAN_POINT ( 'NONE',  ( 38.58424406990786082, 159.3797705074273381, 34.21067981925357060 ) ) ;
#21722=CARTESIAN_POINT ( 'NONE',  ( 41.64333658814960870, 141.7151871740940123, 38.42115945441014446 ) ) ;
#21725=VERTEX_POINT ( 'NONE', #931 ) ;
#21726=CARTESIAN_POINT ( 'NONE',  ( 42.21948215057684450, 78.45757658655230671, 39.21067981925355639 ) ) ;
#21729=CARTESIAN_POINT ( 'NONE',  ( 44.55648932407425633, 112.8844580088725849, 29.45539723777780239 ) ) ;
#21730=CARTESIAN_POINT ( 'NONE',  ( 39.42975644700377558, 122.8151871740940067, 31.60846029578754468 ) ) ;
#21734=CARTESIAN_POINT ( 'NONE',  ( 39.92123440845005433, 146.3344580088725309, 29.95742577749336988 ) ) ;
#21736=CARTESIAN_POINT ( 'NONE',  ( 47.05648932407426344, 106.5844580088725877, 31.27175355779120025 ) ) ;
#21737=CARTESIAN_POINT ( 'NONE',  ( 43.01140435219951286, 152.6297705074272812, 29.55568802177586107 ) ) ;
#21738=CARTESIAN_POINT ( 'NONE',  ( 41.64333658814960870, 69.97977050742731819, 38.42115945441014446 ) ) ;
#21739=CARTESIAN_POINT ( 'NONE',  ( 46.59305225739526435, 127.3151871740940067, 36.81289934271958941 ) ) ;
#21742=CARTESIAN_POINT ( 'NONE',  ( 44.55648932407425633, 77.81049967264873146, 29.45539723777780239 ) ) ;
#21744=CARTESIAN_POINT ( 'NONE',  ( 46.10157429594899270, 97.76049967264873430, 38.46393386101375711 ) ) ;
#21746=CARTESIAN_POINT ( 'NONE',  ( 39.42975644700377558, 86.81518717409400665, 31.60846029578754468 ) ) ;
#21750=CARTESIAN_POINT ( 'NONE',  ( 46.59305225739526435, 61.57977050742731251, 36.81289934271958941 ) ) ;
#21755=CARTESIAN_POINT ( 'NONE',  ( 44.37947211624943833, 154.0151871740940237, 38.42115945441014446 ) ) ;
#21758=ADVANCED_FACE ( 'NONE', ( #13756 ), #17383, .T. ) ;
#21759=CARTESIAN_POINT ( 'NONE',  ( 38.58424406990786082, 117.3797705074273097, 34.21067981925357060 ) ) ;
#21760=CARTESIAN_POINT ( 'NONE',  ( 48.01140435219951996, 154.4344580088725820, 32.58608133808903773 ) ) ;
#21761=AXIS2_PLACEMENT_3D ( 'NONE', #8360, #188, #6925 ) ;
#21762=ORIENTED_EDGE ( 'NONE', *, *, #19804, .F. ) ;
#21768=CARTESIAN_POINT ( 'NONE',  ( 43.01140435219951286, 155.3651871740939896, 29.55568802177586463 ) ) ;
#21769=( BOUNDED_CURVE ( )  B_SPLINE_CURVE ( 2, ( #21364, #16607, #18384, #17928, #21698, #9579, #13199, #1189, #6598, #16386, #1521, #9473, #14741 ),
 .UNSPECIFIED., .F., .F. ) 
 B_SPLINE_CURVE_WITH_KNOTS ( ( 3, 2, 2, 2, 2, 2, 3 ),
 ( 0.9191176470588234837, 0.9205882352941175961, 0.9235294117647059320, 0.9264705882352941568, 0.9294117647058823817, 0.9323529411764706065, 0.9338235294117647189 ),
 .UNSPECIFIED. ) 
 CURVE ( )  GEOMETRIC_REPRESENTATION_ITEM ( )  RATIONAL_B_SPLINE_CURVE ( ( 0.9755282581475768211, 0.9755282581475768211, 1.000000000000000000, 0.9510565162951535312, 1.000000000000000000, 0.9510565162951535312, 1.000000000000000000, 0.9510565162951535312, 1.000000000000000000, 0.9510565162951535312, 1.000000000000000000, 0.9755282581475768211, 0.9755282581475768211 ) ) 
 REPRESENTATION_ITEM ( '' )  );
#21774=CARTESIAN_POINT ( 'NONE',  ( 39.92123440845005433, 90.23445800887257917, 38.46393386101375711 ) ) ;
#21776=CARTESIAN_POINT ( 'NONE',  ( 46.10157429594899270, 91.76049967264873430, 38.46393386101375711 ) ) ;
#21778=EDGE_CURVE ( 'NONE', #18986, #19332, #18277, .T. ) ;
#21779=CARTESIAN_POINT ( 'NONE',  ( 39.42975644700377558, 93.67977050742732104, 36.81289934271958941 ) ) ;
#21782=CARTESIAN_POINT ( 'NONE',  ( 45.74753988029934249, 89.06518717409399244, 30.44471234641812174 ) ) ;
#21787=CARTESIAN_POINT ( 'NONE',  ( 46.59305225739526435, 139.5797705074273267, 36.81289934271958941 ) ) ;
#21789=CARTESIAN_POINT ( 'NONE',  ( 43.01140435219951996, 10.71049967264875491, 39.21067981925356349 ) ) ;
#21790=ORIENTED_EDGE ( 'NONE', *, *, #10936, .F. ) ;
#21791=CARTESIAN_POINT ( 'NONE',  ( 43.01140435219951286, 149.6297705074273097, 29.55568802177586463 ) ) ;
#21792=CARTESIAN_POINT ( 'NONE',  ( 44.37947211624943833, 95.47977050742731819, 30.00020018409699318 ) ) ;
#21794=CARTESIAN_POINT ( 'NONE',  ( 44.55648932407425633, 115.6104996726487428, 38.96596240072933170 ) ) ;
#21796=DIRECTION ( 'NONE',  ( 0.000000000000000000, 0.000000000000000000, 1.000000000000000000 ) ) ;
#21800=CARTESIAN_POINT ( 'NONE',  ( 42.21948215057684450, 111.0373810949689926, 29.21067981925355994 ) ) ;
#21801=CARTESIAN_POINT ( 'NONE',  ( 44.55648932407425633, 154.8844580088725991, 29.45539723777780239 ) ) ;
#21802=CARTESIAN_POINT ( 'NONE',  ( 46.59305225739526435, 119.1797705074273068, 31.60846029578754468 ) ) ;
#21804=CARTESIAN_POINT ( 'NONE',  ( 41.46631938032478359, 114.1104996726487428, 29.45539723777780239 ) ) ;
#21805=CARTESIAN_POINT ( 'NONE',  ( 43.01140435219951286, 116.3651871740940038, 29.55568802177586107 ) ) ;
#21807=CARTESIAN_POINT ( 'NONE',  ( 43.01140435219951286, 125.0344580088725905, 29.21067981925356705 ) ) ;
#21812=CARTESIAN_POINT ( 'NONE',  ( 43.01140435219951286, 86.62977050742730967, 29.55568802177586107 ) ) ;
#21816=CARTESIAN_POINT ( 'NONE',  ( 47.05648932407426344, 69.98445800887257917, 37.14960608071593384 ) ) ;
ENDSEC;
END-ISO-10303-21;
